ISO-10303-21;
HEADER;
FILE_DESCRIPTION (('STEP AP214'),
    '1' );
FILE_NAME ('Injection Molded Chain Links 14.step',
    '2026-10-08T22:59:04',
    ( '' ),
    ( '' ),
    'SwSTEP 2.0',
    'SolidWorks 2020',
    '' );
FILE_SCHEMA (( 'AUTOMOTIVE_DESIGN' ));
ENDSEC;

DATA;
#2=ADVANCED_FACE ( 'NONE', ( #179969 ), #178383, .T. ) ;
#15=DIRECTION ( 'NONE',  ( 0.000000000000000000, 0.000000000000000000, -1.000000000000000000 ) ) ;
#46=DIRECTION ( 'NONE',  ( 4.408576920032446739E-17, 0.1350103645451945777, -0.9908441862701590219 ) ) ;
#51=LINE ( 'NONE', #18341, #77316 ) ;
#53=CARTESIAN_POINT ( 'NONE',  ( 21.05000000000000071, 76.00000000001172396, -71.52310748452431710 ) ) ;
#71=ORIENTED_EDGE ( 'NONE', *, *, #179559, .T. ) ;
#78=CARTESIAN_POINT ( 'NONE',  ( 22.59999999999999432, 75.89914163091330579, -114.7726746080137161 ) ) ;
#100=EDGE_CURVE ( 'NONE', #48831, #76480, #107799, .T. ) ;
#103=ORIENTED_EDGE ( 'NONE', *, *, #206571, .T. ) ;
#106=CARTESIAN_POINT ( 'NONE',  ( 23.14999999999999858, 76.00000000001170974, -69.52310748452431710 ) ) ;
#153=CARTESIAN_POINT ( 'NONE',  ( 18.59999999999999432, 77.13501884592184865, -61.80613060109197932 ) ) ;
#154=ORIENTED_EDGE ( 'NONE', *, *, #235914, .T. ) ;
#180=CARTESIAN_POINT ( 'NONE',  ( 21.14999999999999858, 76.10000000001194564, -103.0231074845243171 ) ) ;
#217=CARTESIAN_POINT ( 'NONE',  ( 22.49806830649814060, 75.92253568368651884, -114.6729971393633889 ) ) ;
#227=EDGE_CURVE ( 'NONE', #173426, #116632, #172895, .T. ) ;
#239=CARTESIAN_POINT ( 'NONE',  ( -20.64999999999999858, 85.50000000001188027, -93.12913836187179584 ) ) ;
#272=EDGE_CURVE ( 'NONE', #20238, #178566, #58379, .T. ) ;
#278=VERTEX_POINT ( 'NONE', #173282 ) ;
#294=AXIS2_PLACEMENT_3D ( 'NONE', #120251, #5368, #35877 ) ;
#302=ADVANCED_FACE ( 'NONE', ( #14182 ), #214528, .T. ) ;
#355=CIRCLE ( 'NONE', #133630, 0.6000000000000033085 ) ;
#364=CARTESIAN_POINT ( 'NONE',  ( 20.94999999999999929, 85.00000000001179501, -79.41707660717668205 ) ) ;
#379=CARTESIAN_POINT ( 'NONE',  ( 22.47007471830797343, 68.27928934808548433, -103.0231074845243455 ) ) ;
#403=ORIENTED_EDGE ( 'NONE', *, *, #146611, .T. ) ;
#416=VERTEX_POINT ( 'NONE', #243460 ) ;
#435=EDGE_CURVE ( 'NONE', #50141, #155954, #166590, .T. ) ;
#448=ORIENTED_EDGE ( 'NONE', *, *, #174825, .F. ) ;
#507=EDGE_CURVE ( 'NONE', #246385, #131339, #94376, .T. ) ;
#516=CARTESIAN_POINT ( 'NONE',  ( 20.97438252431638972, 67.07457649393589350, -94.55073679551357202 ) ) ;
#518=ORIENTED_EDGE ( 'NONE', *, *, #173023, .F. ) ;
#533=DIRECTION ( 'NONE',  ( 1.000000000000000000, 0.000000000000000000, 0.000000000000000000 ) ) ;
#535=CARTESIAN_POINT ( 'NONE',  ( -23.25000000000000000, 71.75000000001186606, -90.87310748452432563 ) ) ;
#547=FACE_OUTER_BOUND ( 'NONE', #29913, .T. ) ;
#562=CARTESIAN_POINT ( 'NONE',  ( -23.25000000000000000, 76.00000000001165290, -61.62310748452430431 ) ) ;
#582=ADVANCED_FACE ( 'NONE', ( #208207 ), #150784, .T. ) ;
#600=ORIENTED_EDGE ( 'NONE', *, *, #38576, .F. ) ;
#602=ORIENTED_EDGE ( 'NONE', *, *, #47162, .T. ) ;
#603=VERTEX_POINT ( 'NONE', #169105 ) ;
#617=DIRECTION ( 'NONE',  ( 2.557131231893037478E-16, 0.8660254037844420383, -0.4999999999999942824 ) ) ;
#620=CIRCLE ( 'NONE', #221208, 0.2000000000000057288 ) ;
#625=DIRECTION ( 'NONE',  ( 0.000000000000000000, -6.467318590049456648E-15, 1.000000000000000000 ) ) ;
#628=CARTESIAN_POINT ( 'NONE',  ( 20.94999999999999574, 69.65000000001187175, -93.17928539484123007 ) ) ;
#639=VECTOR ( 'NONE', #154118, 1000.000000000000114 ) ;
#713=CARTESIAN_POINT ( 'NONE',  ( -21.14999999999999858, 76.00000000001200817, -109.5637644362255543 ) ) ;
#756=ORIENTED_EDGE ( 'NONE', *, *, #206141, .F. ) ;
#792=ORIENTED_EDGE ( 'NONE', *, *, #7077, .F. ) ;
#799=CARTESIAN_POINT ( 'NONE',  ( 23.14999999999999858, 71.18691588786234092, -91.08158972800052311 ) ) ;
#812=EDGE_CURVE ( 'NONE', #61221, #186482, #97065, .T. ) ;
#820=DIRECTION ( 'NONE',  ( 1.000000000000000000, 0.000000000000000000, 0.000000000000000000 ) ) ;
#830=CARTESIAN_POINT ( 'NONE',  ( 22.37643362114956247, 68.37421000605357335, -103.1221888582057460 ) ) ;
#841=CARTESIAN_POINT ( 'NONE',  ( 23.14999999999999858, 76.00000000001169553, -67.52310748452430289 ) ) ;
#849=EDGE_LOOP ( 'NONE', ( #140911, #103088, #131923, #146660 ) ) ;
#854=ORIENTED_EDGE ( 'NONE', *, *, #85923, .F. ) ;
#861=DIRECTION ( 'NONE',  ( 0.000000000000000000, 0.3738317757009942399, -0.9274965247785252886 ) ) ;
#891=DIRECTION ( 'NONE',  ( 0.000000000000000000, -1.000000000000000000, -6.860497997771532351E-15 ) ) ;
#897=AXIS2_PLACEMENT_3D ( 'NONE', #252922, #212543, #254198 ) ;
#904=CARTESIAN_POINT ( 'NONE',  ( 18.54148534481893762, 65.67467670974396299, -63.95317318268842399 ) ) ;
#919=CARTESIAN_POINT ( 'NONE',  ( -23.25000000000000000, 76.00000000001172396, -71.62310748452431142 ) ) ;
#948=AXIS2_PLACEMENT_3D ( 'NONE', #31250, #130291, #251525 ) ;
#1003=AXIS2_PLACEMENT_3D ( 'NONE', #134817, #155729, #193549 ) ;
#1014=VECTOR ( 'NONE', #215002, 1000.000000000000000 ) ;
#1038=VECTOR ( 'NONE', #250333, 1000.000000000000000 ) ;
#1043=ORIENTED_EDGE ( 'NONE', *, *, #128497, .F. ) ;
#1057=CARTESIAN_POINT ( 'NONE',  ( 21.05000000000000071, 65.52661458509899717, -95.44445302027585853 ) ) ;
#1100=FACE_OUTER_BOUND ( 'NONE', #4489, .T. ) ;
#1112=CIRCLE ( 'NONE', #151177, 0.2000000000000057288 ) ;
#1140=AXIS2_PLACEMENT_3D ( 'NONE', #231171, #127229, #167657 ) ;
#1190=ORIENTED_EDGE ( 'NONE', *, *, #142213, .T. ) ;
#1204=DIRECTION ( 'NONE',  ( 0.000000000000000000, 0.4999999999999689138, 0.8660254037844565822 ) ) ;
#1209=LINE ( 'NONE', #44225, #82841 ) ;
#1223=CARTESIAN_POINT ( 'NONE',  ( -18.59999999999999787, 64.25000000001190870, -96.00830171387039513 ) ) ;
#1235=CARTESIAN_POINT ( 'NONE',  ( 20.95035502843362707, 65.52236167323542304, -95.44680777578801667 ) ) ;
#1238=CARTESIAN_POINT ( 'NONE',  ( -20.94999999999999929, 76.00000000001195133, -103.0231074845243171 ) ) ;
#1246=CARTESIAN_POINT ( 'NONE',  ( -21.05000000000000071, 69.58624026620167058, -102.9374944237203948 ) ) ;
#1256=CARTESIAN_POINT ( 'NONE',  ( 21.14999999999999503, 76.10000000001203091, -114.6726782920691079 ) ) ;
#1276=CARTESIAN_POINT ( 'NONE',  ( 21.05000000000000071, 61.95000000001175522, -75.03680255528533394 ) ) ;
#1295=DIRECTION ( 'NONE',  ( 0.000000000000000000, 7.086529944415894657E-15, -1.000000000000000000 ) ) ;
#1324=DIRECTION ( 'NONE',  ( 1.000000000000000000, 0.000000000000000000, 0.000000000000000000 ) ) ;
#1328=ORIENTED_EDGE ( 'NONE', *, *, #26805, .F. ) ;
#1343=AXIS2_PLACEMENT_3D ( 'NONE', #63673, #119830, #138067 ) ;
#1345=TOROIDAL_SURFACE ( 'NONE', #51387, 0.2000000000000000111, 0.1000000000000000056 ) ;
#1361=AXIS2_PLACEMENT_3D ( 'NONE', #98472, #112958, #18973 ) ;
#1365=ORIENTED_EDGE ( 'NONE', *, *, #203704, .F. ) ;
#1369=ORIENTED_EDGE ( 'NONE', *, *, #215843, .F. ) ;
#1380=ADVANCED_FACE ( 'NONE', ( #14222 ), #167674, .T. ) ;
#1387=TOROIDAL_SURFACE ( 'NONE', #163725, 12.77500000000000036, 0.1000000000000000056 ) ;
#1421=ORIENTED_EDGE ( 'NONE', *, *, #65537, .F. ) ;
#1422=ADVANCED_FACE ( 'NONE', ( #139245 ), #255316, .F. ) ;
#1432=( BOUNDED_SURFACE ( )  B_SPLINE_SURFACE ( 3, 2, ( 
 ( #219285, #241437, #40702 ),
 ( #118927, #101883, #139735 ),
 ( #120236, #257085, #62791 ),
 ( #142312, #181469, #221830 ) ),
 .UNSPECIFIED., .F., .F., .F. ) 
 B_SPLINE_SURFACE_WITH_KNOTS ( ( 4, 4 ),
 ( 3, 3 ),
 ( 0.000000000000000000, 0.001979672783031562362 ),
 ( 0.000000000000000000, 1.000000000000000000 ),
 .UNSPECIFIED. ) 
 GEOMETRIC_REPRESENTATION_ITEM ( )  RATIONAL_B_SPLINE_SURFACE ( (
 ( 1.000000000000000000, 0.7103081912008041288, 1.000000000000000000),
 ( 1.000000000000000000, 0.7104998333558241175, 1.000000000000000000),
 ( 1.000000000000000000, 0.7107238315755781688, 1.000000000000000000),
 ( 1.000000000000000000, 0.7110073749538949883, 1.000000000000000000) ) ) 
 REPRESENTATION_ITEM ( '' )  SURFACE ( )  );
#1434=EDGE_CURVE ( 'NONE', #127173, #23304, #130213, .T. ) ;
#1450=CARTESIAN_POINT ( 'NONE',  ( -23.25000000000000000, 76.00000000001165290, -61.62310748452430431 ) ) ;
#1453=CARTESIAN_POINT ( 'NONE',  ( 21.14999999999999858, 76.00000000001200817, -109.5637644362255685 ) ) ;
#1500=CARTESIAN_POINT ( 'NONE',  ( -21.14999999999999858, 87.75000000001192291, -100.1231074845242262 ) ) ;
#1551=FACE_OUTER_BOUND ( 'NONE', #194817, .T. ) ;
#1554=ORIENTED_EDGE ( 'NONE', *, *, #6296, .T. ) ;
#1560=CARTESIAN_POINT ( 'NONE',  ( 21.93340585898353723, 76.00000000001200817, -110.3472545066553181 ) ) ;
#1580=CARTESIAN_POINT ( 'NONE',  ( 20.95512820512820440, 67.12384868372369340, -81.77310748452437394 ) ) ;
#1591=VECTOR ( 'NONE', #148746, 1000.000000000000000 ) ;
#1634=ADVANCED_FACE ( 'NONE', ( #186106 ), #7459, .T. ) ;
#1640=VERTEX_POINT ( 'NONE', #167851 ) ;
#1644=CARTESIAN_POINT ( 'NONE',  ( 21.13614978966381841, 76.00000000001197975, -109.5222121863580895 ) ) ;
#1684=DIRECTION ( 'NONE',  ( 0.000000000000000000, -8.717686153663073805E-15, 1.000000000000000000 ) ) ;
#1693=ORIENTED_EDGE ( 'NONE', *, *, #85923, .T. ) ;
#1694=CIRCLE ( 'NONE', #255745, 0.2000000000000057288 ) ;
#1698=ORIENTED_EDGE ( 'NONE', *, *, #98166, .F. ) ;
#1702=ORIENTED_EDGE ( 'NONE', *, *, #11566, .F. ) ;
#1719=VECTOR ( 'NONE', #30914, 1000.000000000000000 ) ;
#1724=ORIENTED_EDGE ( 'NONE', *, *, #184061, .F. ) ;
#1760=DIRECTION ( 'NONE',  ( -1.000000000000000000, 0.000000000000000000, 0.000000000000000000 ) ) ;
#1765=AXIS2_PLACEMENT_3D ( 'NONE', #100012, #208153, #186003 ) ;
#1768=AXIS2_PLACEMENT_3D ( 'NONE', #114364, #193911, #170543 ) ;
#1783=EDGE_CURVE ( 'NONE', #88936, #209005, #230361, .T. ) ;
#1791=DIRECTION ( 'NONE',  ( 0.000000000000000000, 0.8660254037844420383, -0.4999999999999943379 ) ) ;
#1802=ORIENTED_EDGE ( 'NONE', *, *, #250928, .T. ) ;
#1817=CYLINDRICAL_SURFACE ( 'NONE', #87465, 0.1000000000000028644 ) ;
#1822=DIRECTION ( 'NONE',  ( -1.000000000000000000, 0.000000000000000000, 0.000000000000000000 ) ) ;
#1853=EDGE_CURVE ( 'NONE', #237782, #214060, #30480, .T. ) ;
#1857=DIRECTION ( 'NONE',  ( -1.000000000000000000, -0.000000000000000000, -0.000000000000000000 ) ) ;
#1873=CIRCLE ( 'NONE', #172642, 7.800000000000001599 ) ;
#1888=DIRECTION ( 'NONE',  ( -1.000000000000000000, -0.000000000000000000, 0.000000000000000000 ) ) ;
#1890=CARTESIAN_POINT ( 'NONE',  ( -23.15000000000000213, 74.00000000001180922, -82.74772940728641402 ) ) ;
#1894=DIRECTION ( 'NONE',  ( -0.000000000000000000, 0.1298341882520054891, 0.9915357197604850459 ) ) ;
#1906=ORIENTED_EDGE ( 'NONE', *, *, #23559, .F. ) ;
#1910=FACE_OUTER_BOUND ( 'NONE', #11950, .T. ) ;
#1935=ORIENTED_EDGE ( 'NONE', *, *, #53136, .T. ) ;
#1949=ORIENTED_EDGE ( 'NONE', *, *, #196865, .F. ) ;
#1950=AXIS2_PLACEMENT_3D ( 'NONE', #25247, #61782, #125604 ) ;
#1959=AXIS2_PLACEMENT_3D ( 'NONE', #29194, #149112, #90393 ) ;
#1969=DIRECTION ( 'NONE',  ( 0.000000000000000000, -0.008583690987162452199, -0.9999631594459053030 ) ) ;
#1986=DIRECTION ( 'NONE',  ( 0.000000000000000000, -1.000000000000000000, -6.982962677686265922E-15 ) ) ;
#1988=ORIENTED_EDGE ( 'NONE', *, *, #170106, .F. ) ;
#1991=VERTEX_POINT ( 'NONE', #196074 ) ;
#2009=CARTESIAN_POINT ( 'NONE',  ( -21.05000000000000071, 76.02110330807114735, -109.3276238137883354 ) ) ;
#2014=AXIS2_PLACEMENT_3D ( 'NONE', #80731, #238540, #218968 ) ;
#2020=CARTESIAN_POINT ( 'NONE',  ( 21.05000000000000071, 76.00000000001170974, -69.52310748452431710 ) ) ;
#2059=CARTESIAN_POINT ( 'NONE',  ( -20.94999999999999929, 64.35000000001176090, -76.30697314750248950 ) ) ;
#2078=FACE_OUTER_BOUND ( 'NONE', #151851, .T. ) ;
#2093=ORIENTED_EDGE ( 'NONE', *, *, #228679, .T. ) ;
#2098=CARTESIAN_POINT ( 'NONE',  ( 18.59999999999999432, 77.86671491006917734, -91.27043223824227880 ) ) ;
#2105=CARTESIAN_POINT ( 'NONE',  ( 21.04999999999998650, 69.35000000001186038, -90.77310748452435973 ) ) ;
#2139=CIRCLE ( 'NONE', #214521, 0.1000000000000017680 ) ;
#2144=AXIS2_PLACEMENT_3D ( 'NONE', #156264, #93689, #76680 ) ;
#2160=ADVANCED_FACE ( 'NONE', ( #220767 ), #22578, .F. ) ;
#2163=EDGE_LOOP ( 'NONE', ( #167237, #72428, #10118, #32795 ) ) ;
#2197=VERTEX_POINT ( 'NONE', #141229 ) ;
#2223=( BOUNDED_SURFACE ( )  B_SPLINE_SURFACE ( 3, 2, ( 
 ( #73787, #72490, #30806 ),
 ( #54182, #169044, #89454 ),
 ( #133722, #193714, #189852 ),
 ( #129863, #248538, #15076 ),
 ( #52900, #214544, #134989 ),
 ( #213255, #191160, #152035 ),
 ( #75073, #170339, #69929 ),
 ( #34656, #94593, #132446 ),
 ( #33385, #174188, #230253 ),
 ( #154612, #234105, #112885 ) ),
 .UNSPECIFIED., .F., .F., .T. ) 
 B_SPLINE_SURFACE_WITH_KNOTS ( ( 4, 2, 2, 2, 4 ),
 ( 3, 3 ),
 ( 0.0001701955120502373817, 0.0002247052511886151935, 0.0002792149903269930053, 0.0003882344686037486831, 0.0006062734251572600387 ),
 ( 0.000000000000000000, 1.000000000000000000 ),
 .UNSPECIFIED. ) 
 GEOMETRIC_REPRESENTATION_ITEM ( )  RATIONAL_B_SPLINE_SURFACE ( (
 ( 1.000000000000000000, 0.2966190024560606542, 1.000000000000000000),
 ( 1.000000000000000000, 0.2964522492712500235, 1.000000000000000000),
 ( 1.000000000000000000, 0.3059923531882490222, 1.000000000000000000),
 ( 1.000000000000000000, 0.3355751146946277519, 1.000000000000000000),
 ( 1.000000000000000000, 0.3550672384962930139, 1.000000000000000000),
 ( 1.000000000000000000, 0.4157034672182384760, 1.000000000000000000),
 ( 1.000000000000000000, 0.4588031877647695822, 1.000000000000000000),
 ( 1.000000000000000000, 0.5771441759674355021, 1.000000000000000000),
 ( 1.000000000000000000, 0.6469377121761927807, 1.000000000000000000),
 ( 1.000000000000000000, 0.7071067811865870967, 1.000000000000000000) ) ) 
 REPRESENTATION_ITEM ( '' )  SURFACE ( )  );
#2231=CARTESIAN_POINT ( 'NONE',  ( -23.25000000000000000, 76.00000000001195133, -103.0231074845243171 ) ) ;
#2236=TOROIDAL_SURFACE ( 'NONE', #114696, 0.4000000000000015210, 0.1000000000000000056 ) ;
#2247=CYLINDRICAL_SURFACE ( 'NONE', #187824, 7.900000000000003908 ) ;
#2273=ORIENTED_EDGE ( 'NONE', *, *, #239821, .F. ) ;
#2293=AXIS2_PLACEMENT_3D ( 'NONE', #61986, #161089, #24153 ) ;
#2296=CARTESIAN_POINT ( 'NONE',  ( -21.05439746398122836, 64.25000000001189449, -96.03319099703979589 ) ) ;
#2297=ORIENTED_EDGE ( 'NONE', *, *, #84952, .T. ) ;
#2315=VECTOR ( 'NONE', #168034, 999.9999999999998863 ) ;
#2332=CYLINDRICAL_SURFACE ( 'NONE', #72274, 0.09999999999999867328 ) ;
#2376=AXIS2_PLACEMENT_3D ( 'NONE', #62994, #87679, #163395 ) ;
#2425=AXIS2_PLACEMENT_3D ( 'NONE', #153513, #135160, #16531 ) ;
#2474=ORIENTED_EDGE ( 'NONE', *, *, #183247, .F. ) ;
#2491=DIRECTION ( 'NONE',  ( -1.000000000000000000, 0.000000000000000000, -0.000000000000000000 ) ) ;
#2497=DIRECTION ( 'NONE',  ( 1.000000000000000000, 0.000000000000000000, 0.000000000000000000 ) ) ;
#2498=EDGE_CURVE ( 'NONE', #84368, #168899, #30849, .T. ) ;
#2562=EDGE_CURVE ( 'NONE', #68348, #25415, #220338, .T. ) ;
#2567=CARTESIAN_POINT ( 'NONE',  ( -21.05000000000000071, 76.00000000001192291, -98.72310748452436258 ) ) ;
#2575=ORIENTED_EDGE ( 'NONE', *, *, #27769, .F. ) ;
#2578=CYLINDRICAL_SURFACE ( 'NONE', #140824, 0.1000000000000028644 ) ;
#2606=FACE_OUTER_BOUND ( 'NONE', #58765, .T. ) ;
#2613=ORIENTED_EDGE ( 'NONE', *, *, #204326, .F. ) ;
#2646=CARTESIAN_POINT ( 'NONE',  ( 22.40000000000020819, 76.10085836911169110, -114.7726746080140146 ) ) ;
#2674=CARTESIAN_POINT ( 'NONE',  ( 20.94999999999999929, 64.35000000001176090, -76.30697314750248950 ) ) ;
#2675=AXIS2_PLACEMENT_3D ( 'NONE', #151542, #152833, #15885 ) ;
#2690=VERTEX_POINT ( 'NONE', #49234 ) ;
#2703=CARTESIAN_POINT ( 'NONE',  ( -20.54999999999999716, 74.00000000001180922, -82.34772940728642254 ) ) ;
#2709=CARTESIAN_POINT ( 'NONE',  ( -18.59999999999999787, 66.85000000001186038, -90.67310748452436542 ) ) ;
#2710=EDGE_LOOP ( 'NONE', ( #128396, #175451, #183466, #19069 ) ) ;
#2715=CARTESIAN_POINT ( 'NONE',  ( -18.49499033040906326, 85.43814877175658751, -95.82495425860084026 ) ) ;
#2768=CARTESIAN_POINT ( 'NONE',  ( 20.94999999999999929, 77.13501884592184865, -61.80613060109197932 ) ) ;
#2828=CARTESIAN_POINT ( 'NONE',  ( -21.05000000000000071, 74.26374286841446803, -91.45445515550682103 ) ) ;
#2830=LINE ( 'NONE', #21162, #251822 ) ;
#2841=ORIENTED_EDGE ( 'NONE', *, *, #163022, .F. ) ;
#2858=CARTESIAN_POINT ( 'NONE',  ( -20.94999999999999929, 77.85102823015273543, -91.36919421510179973 ) ) ;
#2860=CIRCLE ( 'NONE', #256905, 0.09999999999999939493 ) ;
#2865=CIRCLE ( 'NONE', #215273, 0.1000000000000045158 ) ;
#2887=VERTEX_POINT ( 'NONE', #256355 ) ;
#2902=EDGE_CURVE ( 'NONE', #5347, #22332, #68424, .T. ) ;
#2914=FACE_OUTER_BOUND ( 'NONE', #183063, .T. ) ;
#2947=ORIENTED_EDGE ( 'NONE', *, *, #170366, .F. ) ;
#2963=ORIENTED_EDGE ( 'NONE', *, *, #151337, .F. ) ;
#2969=CARTESIAN_POINT ( 'NONE',  ( -22.48660254037843487, 64.35000000001195986, -103.0731074845243711 ) ) ;
#2992=ORIENTED_EDGE ( 'NONE', *, *, #209729, .T. ) ;
#3003=CARTESIAN_POINT ( 'NONE',  ( -21.05000000000000071, 77.25000000001189449, -95.02310748452430289 ) ) ;
#3008=AXIS2_PLACEMENT_3D ( 'NONE', #180, #202250, #217933 ) ;
#3011=ORIENTED_EDGE ( 'NONE', *, *, #90341, .F. ) ;
#3022=DIRECTION ( 'NONE',  ( 0.000000000000000000, -6.982962677686266711E-15, 1.000000000000000000 ) ) ;
#3039=ORIENTED_EDGE ( 'NONE', *, *, #78493, .T. ) ;
#3062=FACE_OUTER_BOUND ( 'NONE', #169130, .T. ) ;
#3063=DIRECTION ( 'NONE',  ( -1.000000000000000000, 0.000000000000000000, -0.000000000000000000 ) ) ;
#3070=PRESENTATION_STYLE_ASSIGNMENT (( #124332 ) ) ;
#3086=ORIENTED_EDGE ( 'NONE', *, *, #200979, .F. ) ;
#3114=CARTESIAN_POINT ( 'NONE',  ( -23.15000000000000213, 76.00000000001195133, -103.0231074845243171 ) ) ;
#3124=CARTESIAN_POINT ( 'NONE',  ( 21.06277459767449045, 67.12713756174359503, -90.81910829216803904 ) ) ;
#3125=CARTESIAN_POINT ( 'NONE',  ( -22.39999999999999858, 76.00000000001195133, -103.0231074845243171 ) ) ;
#3127=AXIS2_PLACEMENT_3D ( 'NONE', #204024, #189618, #46231 ) ;
#3136=CIRCLE ( 'NONE', #161595, 0.1000000000000052097 ) ;
#3152=DIRECTION ( 'NONE',  ( -1.000000000000000000, 2.952720810173289112E-16, 2.061873921506763405E-30 ) ) ;
#3168=AXIS2_PLACEMENT_3D ( 'NONE', #4861, #204369, #84373 ) ;
#3181=VERTEX_POINT ( 'NONE', #111472 ) ;
#3195=CARTESIAN_POINT ( 'NONE',  ( -23.15000000000000213, 74.07476635515205032, -90.29286395139820343 ) ) ;
#3199=VECTOR ( 'NONE', #91874, 1000.000000000000000 ) ;
#3201=DIRECTION ( 'NONE',  ( 0.000000000000000000, 1.000000000000000000, 6.982962677686266711E-15 ) ) ;
#3224=CARTESIAN_POINT ( 'NONE',  ( -23.25000000000000000, 76.00000000001192291, -98.87310748452431142 ) ) ;
#3248=VERTEX_POINT ( 'NONE', #160888 ) ;
#3292=CARTESIAN_POINT ( 'NONE',  ( -20.93284271247462058, 64.25000000001176659, -76.53791325517833855 ) ) ;
#3307=ORIENTED_EDGE ( 'NONE', *, *, #195812, .F. ) ;
#3319=CARTESIAN_POINT ( 'NONE',  ( 18.41356215285961540, 85.50000000001192291, -95.99103808782463432 ) ) ;
#3321=EDGE_CURVE ( 'NONE', #81803, #120417, #89439, .T. ) ;
#3343=VERTEX_POINT ( 'NONE', #17496 ) ;
#3413=CARTESIAN_POINT ( 'NONE',  ( 21.30740335185485890, 69.44334207798394232, -103.1220420103002056 ) ) ;
#3420=VECTOR ( 'NONE', #7726, 1000.000000000000000 ) ;
#3434=ORIENTED_EDGE ( 'NONE', *, *, #212308, .F. ) ;
#3460=EDGE_CURVE ( 'NONE', #164289, #27688, #85326, .T. ) ;
#3470=AXIS2_PLACEMENT_3D ( 'NONE', #11906, #173578, #195682 ) ;
#3495=CARTESIAN_POINT ( 'NONE',  ( 18.55121869061587958, 65.67252876774509218, -63.94570419949945261 ) ) ;
#3506=AXIS2_PLACEMENT_3D ( 'NONE', #201284, #25239, #22679 ) ;
#3519=ADVANCED_FACE ( 'NONE', ( #52457 ), #189416, .F. ) ;
#3564=CARTESIAN_POINT ( 'NONE',  ( 22.39999999999999503, 68.20922040163857503, -103.1231074845243540 ) ) ;
#3568=TOROIDAL_SURFACE ( 'NONE', #149353, 11.90000000000000391, 0.1000000000000000056 ) ;
#3593=CARTESIAN_POINT ( 'NONE',  ( -20.94684162615585876, 64.25000000176534343, -96.18146348457848660 ) ) ;
#3634=ORIENTED_EDGE ( 'NONE', *, *, #235606, .T. ) ;
#3640=ORIENTED_EDGE ( 'NONE', *, *, #137886, .T. ) ;
#3644=TOROIDAL_SURFACE ( 'NONE', #124480, 0.2000000000000000111, 0.1000000000000000056 ) ;
#3655=LINE ( 'NONE', #165308, #64083 ) ;
#3694=ADVANCED_FACE ( 'NONE', ( #215402 ), #202068, .T. ) ;
#3708=DIRECTION ( 'NONE',  ( 2.952720810173289112E-16, 1.000000000000000000, 6.938893903907222067E-15 ) ) ;
#3769=CARTESIAN_POINT ( 'NONE',  ( 18.57071067811864040, 65.82071067813045318, -81.77310748452437394 ) ) ;
#3771=DIRECTION ( 'NONE',  ( 0.000000000000000000, -0.2605042016806647931, -0.9654727137038724427 ) ) ;
#3820=DIRECTION ( 'NONE',  ( -1.000000000000000000, -0.000000000000000000, -0.000000000000000000 ) ) ;
#3840=CARTESIAN_POINT ( 'NONE',  ( -21.05000000000000071, 69.74168394267991289, -103.0888090948464111 ) ) ;
#3846=ORIENTED_EDGE ( 'NONE', *, *, #68339, .T. ) ;
#3911=EDGE_CURVE ( 'NONE', #240371, #242014, #2139, .T. ) ;
#3930=EDGE_CURVE ( 'NONE', #16721, #171947, #116964, .T. ) ;
#3937=CARTESIAN_POINT ( 'NONE',  ( 19.90621891164687440, 64.25000000001176659, -78.19466220664698142 ) ) ;
#3957=VERTEX_POINT ( 'NONE', #154831 ) ;
#3976=DIRECTION ( 'NONE',  ( -1.000000000000000000, 0.000000000000000000, 0.000000000000000000 ) ) ;
#3980=VERTEX_POINT ( 'NONE', #233084 ) ;
#3989=ORIENTED_EDGE ( 'NONE', *, *, #212952, .F. ) ;
#3991=ORIENTED_EDGE ( 'NONE', *, *, #92230, .F. ) ;
#4001=CARTESIAN_POINT ( 'NONE',  ( -20.94999999999999929, 77.36087058720393372, -94.95010955743333625 ) ) ;
#4006=VECTOR ( 'NONE', #114156, 1000.000000000000000 ) ;
#4028=EDGE_CURVE ( 'NONE', #21614, #76960, #152386, .T. ) ;
#4033=AXIS2_PLACEMENT_3D ( 'NONE', #105698, #91313, #28815 ) ;
#4037=EDGE_CURVE ( 'NONE', #98180, #34831, #193791, .T. ) ;
#4047=LINE ( 'NONE', #83558, #118219 ) ;
#4076=EDGE_CURVE ( 'NONE', #96396, #69997, #60755, .T. ) ;
#4090=DIRECTION ( 'NONE',  ( 1.000000000000000000, 0.000000000000000000, 0.000000000000000000 ) ) ;
#4124=AXIS2_PLACEMENT_3D ( 'NONE', #9097, #110753, #115900 ) ;
#4126=CYLINDRICAL_SURFACE ( 'NONE', #182630, 0.1000000000000028644 ) ;
#4151=ADVANCED_FACE ( 'NONE', ( #146760 ), #27513, .T. ) ;
#4172=CARTESIAN_POINT ( 'NONE',  ( -23.15000000000000213, 73.50000000001186606, -89.79848556176223440 ) ) ;
#4199=DIRECTION ( 'NONE',  ( 0.000000000000000000, -6.938893903907222067E-15, 1.000000000000000000 ) ) ;
#4201=CIRCLE ( 'NONE', #229074, 0.09999999999999939493 ) ;
#4226=CARTESIAN_POINT ( 'NONE',  ( -18.37151313414641152, 85.57101412579034161, -62.70644457528530324 ) ) ;
#4281=DIRECTION ( 'NONE',  ( -3.265361837132813093E-16, -1.000000000000000000, 7.445645354460596589E-46 ) ) ;
#4291=ADVANCED_FACE ( 'NONE', ( #154533 ), #56637, .F. ) ;
#4311=LINE ( 'NONE', #83820, #97983 ) ;
#4339=CARTESIAN_POINT ( 'NONE',  ( 21.14999999999999503, 87.75000000001190870, -100.1231074845242262 ) ) ;
#4396=LINE ( 'NONE', #25275, #216752 ) ;
#4408=AXIS2_PLACEMENT_3D ( 'NONE', #61633, #124191, #163311 ) ;
#4410=ORIENTED_EDGE ( 'NONE', *, *, #186572, .F. ) ;
#4418=CARTESIAN_POINT ( 'NONE',  ( 21.04999999999999716, 67.12872031401622053, -90.87310748452436826 ) ) ;
#4425=AXIS2_PLACEMENT_3D ( 'NONE', #251126, #90774, #188601 ) ;
#4431=DIRECTION ( 'NONE',  ( 1.000000000000000000, 7.304098846218134667E-16, 4.639676173203993355E-30 ) ) ;
#4446=CARTESIAN_POINT ( 'NONE',  ( 23.24999999999999645, 76.00000000001170974, -69.52310748452431710 ) ) ;
#4484=EDGE_LOOP ( 'NONE', ( #89886, #139177, #104314, #247561 ) ) ;
#4489=EDGE_LOOP ( 'NONE', ( #43750, #79077, #56309 ) ) ;
#4521=CARTESIAN_POINT ( 'NONE',  ( 23.14999999999999858, 76.00000000001170974, -69.52310748452431710 ) ) ;
#4522=EDGE_LOOP ( 'NONE', ( #199880, #169518, #244690, #47708 ) ) ;
#4525=DIRECTION ( 'NONE',  ( -1.000000000000000000, 2.952720810173289112E-16, 2.061873921506763405E-30 ) ) ;
#4548=VERTEX_POINT ( 'NONE', #49944 ) ;
#4550=ORIENTED_EDGE ( 'NONE', *, *, #190924, .F. ) ;
#4580=CARTESIAN_POINT ( 'NONE',  ( -21.05000000000000071, 76.09999996531153954, -109.5006596670177856 ) ) ;
#4592=ORIENTED_EDGE ( 'NONE', *, *, #8605, .T. ) ;
#4638=CARTESIAN_POINT ( 'NONE',  ( -21.09316766718153247, 75.96073659769731989, -109.3932607969990300 ) ) ;
#4655=CARTESIAN_POINT ( 'NONE',  ( 21.05000000000000071, 76.00000000001195133, -103.0231074845243171 ) ) ;
#4656=DIRECTION ( 'NONE',  ( -0.7071067811865127117, -0.7071067811865821007, 0.000000000000000000 ) ) ;
#4668=ORIENTED_EDGE ( 'NONE', *, *, #81405, .F. ) ;
#4671=DIRECTION ( 'NONE',  ( -0.7071067811865475727, 0.7071067811865475727, 4.937700262164531476E-15 ) ) ;
#4673=EDGE_LOOP ( 'NONE', ( #3086, #81837, #84082, #145393 ) ) ;
#4683=CARTESIAN_POINT ( 'NONE',  ( 20.94999999999999574, 76.00000000001195133, -103.0231074845243171 ) ) ;
#4715=ADVANCED_FACE ( 'NONE', ( #22404 ), #82321, .T. ) ;
#4721=CARTESIAN_POINT ( 'NONE',  ( -20.54999999999999716, 85.00000000001188027, -93.12913836187181005 ) ) ;
#4774=VECTOR ( 'NONE', #46, 1000.000000000000114 ) ;
#4784=FACE_OUTER_BOUND ( 'NONE', #23526, .T. ) ;
#4842=DIRECTION ( 'NONE',  ( 0.000000000000000000, 6.467318590049456648E-15, -1.000000000000000000 ) ) ;
#4858=CARTESIAN_POINT ( 'NONE',  ( 21.14999999999999858, 76.00000000001203659, -114.6726782920691221 ) ) ;
#4861=CARTESIAN_POINT ( 'NONE',  ( -20.94999999999999929, 76.00000000001195133, -103.0231074845243171 ) ) ;
#4870=DIRECTION ( 'NONE',  ( 0.000000000000000000, -1.000000000000000000, -6.982962677686265922E-15 ) ) ;
#4872=CARTESIAN_POINT ( 'NONE',  ( 23.25000000000000000, 84.59626168225477727, -78.97323500167453858 ) ) ;
#4874=VERTEX_POINT ( 'NONE', #131751 ) ;
#4876=ORIENTED_EDGE ( 'NONE', *, *, #63288, .T. ) ;
#4889=DIRECTION ( 'NONE',  ( 0.000000000000000000, -1.000000000000000000, -7.105427357601001859E-15 ) ) ;
#4917=CARTESIAN_POINT ( 'NONE',  ( -20.96428641294179940, 64.25000000001175238, -76.34821430658305985 ) ) ;
#4922=ORIENTED_EDGE ( 'NONE', *, *, #21957, .T. ) ;
#4968=VERTEX_POINT ( 'NONE', #208742 ) ;
#5001=ORIENTED_EDGE ( 'NONE', *, *, #69830, .T. ) ;
#5009=VECTOR ( 'NONE', #50544, 1000.000000000000114 ) ;
#5013=ORIENTED_EDGE ( 'NONE', *, *, #211283, .T. ) ;
#5068=DIRECTION ( 'NONE',  ( -1.000000000000000000, -0.000000000000000000, -0.000000000000000000 ) ) ;
#5096=EDGE_LOOP ( 'NONE', ( #171863, #77285, #145124, #24622 ) ) ;
#5124=TOROIDAL_SURFACE ( 'NONE', #150720, 11.90000000000000213, 0.1000000000000000056 ) ;
#5130=ADVANCED_FACE ( 'NONE', ( #157789 ), #156492, .F. ) ;
#5141=ORIENTED_EDGE ( 'NONE', *, *, #198600, .F. ) ;
#5184=VERTEX_POINT ( 'NONE', #48055 ) ;
#5198=ADVANCED_FACE ( 'NONE', ( #142018 ), #147152, .T. ) ;
#5208=ORIENTED_EDGE ( 'NONE', *, *, #201225, .F. ) ;
#5238=AXIS2_PLACEMENT_3D ( 'NONE', #179155, #96972, #176575 ) ;
#5243=DIRECTION ( 'NONE',  ( 0.000000000000000000, -6.688090509790097607E-15, 1.000000000000000000 ) ) ;
#5248=ORIENTED_EDGE ( 'NONE', *, *, #158209, .T. ) ;
#5292=CYLINDRICAL_SURFACE ( 'NONE', #3008, 0.09999999999999939493 ) ;
#5335=AXIS2_PLACEMENT_3D ( 'NONE', #234878, #56209, #253136 ) ;
#5344=ADVANCED_FACE ( 'NONE', ( #35895 ), #102618, .F. ) ;
#5347=VERTEX_POINT ( 'NONE', #252336 ) ;
#5348=AXIS2_PLACEMENT_3D ( 'NONE', #162640, #84313, #25690 ) ;
#5361=EDGE_LOOP ( 'NONE', ( #211147, #159509, #135371, #128073 ) ) ;
#5368=DIRECTION ( 'NONE',  ( 1.000000000000000000, -0.000000000000000000, 0.000000000000000000 ) ) ;
#5380=CARTESIAN_POINT ( 'NONE',  ( -22.39999999999999503, 68.20922040163854660, -103.1231074845243540 ) ) ;
#5383=CARTESIAN_POINT ( 'NONE',  ( -18.50000000000000711, 64.35000000001190301, -96.00830171387039513 ) ) ;
#5394=DIRECTION ( 'NONE',  ( -1.000000000000000000, 0.000000000000000000, 0.000000000000000000 ) ) ;
#5418=ADVANCED_FACE ( 'NONE', ( #15043 ), #247547, .F. ) ;
#5446=EDGE_CURVE ( 'NONE', #145746, #180772, #223268, .T. ) ;
#5468=CARTESIAN_POINT ( 'NONE',  ( -23.15000000000000213, 74.07476635515199348, -82.25335101765045920 ) ) ;
#5478=DIRECTION ( 'NONE',  ( -1.000000000000000000, -0.000000000000000000, -0.000000000000000000 ) ) ;
#5510=CIRCLE ( 'NONE', #130441, 0.1000000000000045158 ) ;
#5516=ORIENTED_EDGE ( 'NONE', *, *, #237595, .T. ) ;
#5545=VERTEX_POINT ( 'NONE', #257423 ) ;
#5564=PLANE ( 'NONE',  #171594 ) ;
#5566=LINE ( 'NONE', #25180, #35634 ) ;
#5592=AXIS2_PLACEMENT_3D ( 'NONE', #226437, #11275, #47803 ) ;
#5612=DIRECTION ( 'NONE',  ( 0.000000000000000000, -0.1298341882519953860, -0.9915357197604862671 ) ) ;
#5634=ORIENTED_EDGE ( 'NONE', *, *, #24282, .F. ) ;
#5691=CARTESIAN_POINT ( 'NONE',  ( -21.05000000000000071, 76.00000000001195133, -103.0231074845243171 ) ) ;
#5705=ORIENTED_EDGE ( 'NONE', *, *, #138962, .F. ) ;
#5718=AXIS2_PLACEMENT_3D ( 'NONE', #201146, #23829, #241560 ) ;
#5720=DIRECTION ( 'NONE',  ( -1.000000000000000000, 0.000000000000000000, -0.000000000000000000 ) ) ;
#5726=EDGE_CURVE ( 'NONE', #229949, #185034, #136120, .T. ) ;
#5747=ORIENTED_EDGE ( 'NONE', *, *, #122807, .T. ) ;
#5757=CARTESIAN_POINT ( 'NONE',  ( -23.25000000000000000, 71.65000000001180069, -81.87310748452433984 ) ) ;
#5776=AXIS2_PLACEMENT_3D ( 'NONE', #160117, #148227, #105203 ) ;
#5789=LINE ( 'NONE', #211742, #239282 ) ;
#5810=DIRECTION ( 'NONE',  ( -1.000000000000000000, 0.000000000000000000, 0.000000000000000000 ) ) ;
#5814=VERTEX_POINT ( 'NONE', #166973 ) ;
#5817=FACE_OUTER_BOUND ( 'NONE', #229242, .T. ) ;
#5883=DIRECTION ( 'NONE',  ( -1.000000000000000000, 0.000000000000000000, 0.000000000000000000 ) ) ;
#5892=DIRECTION ( 'NONE',  ( 1.000000000000000000, 0.000000000000000000, 0.000000000000000000 ) ) ;
#5894=CARTESIAN_POINT ( 'NONE',  ( 21.05000000000000071, 85.00000000001179501, -79.41707660717668205 ) ) ;
#5982=CARTESIAN_POINT ( 'NONE',  ( 21.07971444708685738, 69.67020791838538685, -103.1109309208422502 ) ) ;
#5999=CARTESIAN_POINT ( 'NONE',  ( -20.85000000000000142, 77.16412189325286874, -61.70825939895269840 ) ) ;
#6025=DIRECTION ( 'NONE',  ( 0.000000000000000000, 0.000000000000000000, -1.000000000000000000 ) ) ;
#6051=ADVANCED_FACE ( 'NONE', ( #1100 ), #83198, .T. ) ;
#6128=ORIENTED_EDGE ( 'NONE', *, *, #53047, .T. ) ;
#6137=CARTESIAN_POINT ( 'NONE',  ( -20.85000000000000142, 77.16412189325286874, -61.60825939895269698 ) ) ;
#6141=FACE_OUTER_BOUND ( 'NONE', #190934, .T. ) ;
#6142=ORIENTED_EDGE ( 'NONE', *, *, #100919, .F. ) ;
#6184=CARTESIAN_POINT ( 'NONE',  ( 20.94999999999999929, 76.00000000001170974, -69.52310748452431710 ) ) ;
#6202=ORIENTED_EDGE ( 'NONE', *, *, #111053, .F. ) ;
#6211=CARTESIAN_POINT ( 'NONE',  ( 20.84999999999999432, 68.97833521811159585, -65.68954208262705663 ) ) ;
#6221=CARTESIAN_POINT ( 'NONE',  ( -20.94999999999999929, 64.36312671090729509, -76.34486669784918433 ) ) ;
#6228=DIRECTION ( 'NONE',  ( -1.000000000000000000, -0.000000000000000000, -0.000000000000000000 ) ) ;
#6243=CARTESIAN_POINT ( 'NONE',  ( -21.45000000000000284, 68.29142135624910281, -81.77310748452435973 ) ) ;
#6250=EDGE_LOOP ( 'NONE', ( #141493, #4410, #237741, #168444 ) ) ;
#6271=EDGE_CURVE ( 'NONE', #127256, #173093, #208661, .T. ) ;
#6296=EDGE_CURVE ( 'NONE', #191619, #130365, #88665, .T. ) ;
#6308=CARTESIAN_POINT ( 'NONE',  ( -20.85000000000000142, 75.83895117929300511, -69.80729732888453043 ) ) ;
#6352=ORIENTED_EDGE ( 'NONE', *, *, #186996, .T. ) ;
#6371=EDGE_CURVE ( 'NONE', #170856, #86374, #27500, .T. ) ;
#6405=VERTEX_POINT ( 'NONE', #251622 ) ;
#6430=ORIENTED_EDGE ( 'NONE', *, *, #165763, .T. ) ;
#6451=AXIS2_PLACEMENT_3D ( 'NONE', #100519, #240077, #138373 ) ;
#6472=EDGE_LOOP ( 'NONE', ( #186807, #107140, #52630, #256998 ) ) ;
#6479=CARTESIAN_POINT ( 'NONE',  ( -20.64999999999999858, 68.85000000001180354, -81.87310748452436826 ) ) ;
#6490=CARTESIAN_POINT ( 'NONE',  ( 20.01093837587850288, 64.25000000001176659, -78.26871004992719350 ) ) ;
#6502=VERTEX_POINT ( 'NONE', #121130 ) ;
#6513=ORIENTED_EDGE ( 'NONE', *, *, #168309, .F. ) ;
#6550=ORIENTED_EDGE ( 'NONE', *, *, #64079, .F. ) ;
#6551=DIRECTION ( 'NONE',  ( -1.000000000000000000, 0.000000000000000000, -0.000000000000000000 ) ) ;
#6552=CARTESIAN_POINT ( 'NONE',  ( 18.49999999999999645, 70.05000000001193428, -92.71740517948948934 ) ) ;
#6555=ORIENTED_EDGE ( 'NONE', *, *, #188635, .F. ) ;
#6568=DIRECTION ( 'NONE',  ( 0.000000000000000000, -0.1350103645451835865, -0.9908441862701605762 ) ) ;
#6600=VECTOR ( 'NONE', #206978, 1000.000000000000000 ) ;
#6609=DIRECTION ( 'NONE',  ( -1.000000000000000000, -0.000000000000000000, -0.000000000000000000 ) ) ;
#6624=CARTESIAN_POINT ( 'NONE',  ( -23.25000000000000000, 74.00000000001180922, -82.74772940728641402 ) ) ;
#6651=ORIENTED_EDGE ( 'NONE', *, *, #208543, .F. ) ;
#6659=CARTESIAN_POINT ( 'NONE',  ( 20.94999999999999929, 85.00000000001188027, -93.12913836187181005 ) ) ;
#6665=EDGE_CURVE ( 'NONE', #113549, #91113, #147059, .T. ) ;
#6678=VECTOR ( 'NONE', #139947, 1000.000000000000000 ) ;
#6698=CARTESIAN_POINT ( 'NONE',  ( 23.24999999999999289, 69.45000000001181206, -81.67310748452436542 ) ) ;
#6730=ORIENTED_EDGE ( 'NONE', *, *, #158461, .T. ) ;
#6769=EDGE_LOOP ( 'NONE', ( #215612, #37892, #40583, #175497 ) ) ;
#6780=AXIS2_PLACEMENT_3D ( 'NONE', #145355, #104911, #28016 ) ;
#6797=AXIS2_PLACEMENT_3D ( 'NONE', #11101, #232729, #136142 ) ;
#6814=ADVANCED_FACE ( 'NONE', ( #176939 ), #116938, .T. ) ;
#6820=TOROIDAL_SURFACE ( 'NONE', #36059, 7.800000000000000711, 0.1000000000000000056 ) ;
#6826=VERTEX_POINT ( 'NONE', #94797 ) ;
#6840=LINE ( 'NONE', #29022, #90510 ) ;
#6896=EDGE_CURVE ( 'NONE', #3980, #208027, #219343, .T. ) ;
#6906=VECTOR ( 'NONE', #211064, 1000.000000000000000 ) ;
#6908=EDGE_CURVE ( 'NONE', #145911, #208704, #244272, .T. ) ;
#6921=CIRCLE ( 'NONE', #161064, 0.5000000000000004441 ) ;
#6928=DIRECTION ( 'NONE',  ( 0.000000000000000000, -7.086529944415894657E-15, 1.000000000000000000 ) ) ;
#6951=CIRCLE ( 'NONE', #152742, 0.1000000000000028644 ) ;
#6992=CARTESIAN_POINT ( 'NONE',  ( 20.97462148592276776, 67.12526242356128137, -90.76846315279371424 ) ) ;
#6993=CYLINDRICAL_SURFACE ( 'NONE', #152394, 0.1000000000000028644 ) ;
#7001=VECTOR ( 'NONE', #150630, 1000.000000000000000 ) ;
#7006=CARTESIAN_POINT ( 'NONE',  ( -20.85000000000000142, 64.35000000001171827, -69.52310748452438816 ) ) ;
#7019=ORIENTED_EDGE ( 'NONE', *, *, #66709, .F. ) ;
#7021=DIRECTION ( 'NONE',  ( 1.000000000000000000, 0.000000000000000000, 0.000000000000000000 ) ) ;
#7035=ORIENTED_EDGE ( 'NONE', *, *, #22250, .F. ) ;
#7050=CYLINDRICAL_SURFACE ( 'NONE', #251725, 0.1000000000000028644 ) ;
#7064=VECTOR ( 'NONE', #156266, 1000.000000000000000 ) ;
#7077=EDGE_CURVE ( 'NONE', #97749, #124985, #252652, .T. ) ;
#7079=ORIENTED_EDGE ( 'NONE', *, *, #220901, .T. ) ;
#7104=CARTESIAN_POINT ( 'NONE',  ( -21.14999999999999858, 64.35000000001195986, -103.0231074845244024 ) ) ;
#7120=ADVANCED_FACE ( 'NONE', ( #51163 ), #132016, .F. ) ;
#7128=CARTESIAN_POINT ( 'NONE',  ( 23.14999999999999858, 76.00000000001195133, -103.0231074845243171 ) ) ;
#7133=ORIENTED_EDGE ( 'NONE', *, *, #245356, .T. ) ;
#7137=ADVANCED_FACE ( 'NONE', ( #49906 ), #86033, .F. ) ;
#7161=FACE_OUTER_BOUND ( 'NONE', #33646, .T. ) ;
#7228=DIRECTION ( 'NONE',  ( 4.336808689942128965E-15, -0.8660254037844367092, 0.5000000000000037748 ) ) ;
#7229=DIRECTION ( 'NONE',  ( -0.000000000000000000, -6.982962677686266711E-15, 1.000000000000000000 ) ) ;
#7335=AXIS2_PLACEMENT_3D ( 'NONE', #132620, #110476, #33562 ) ;
#7336=VERTEX_POINT ( 'NONE', #22367 ) ;
#7350=ORIENTED_EDGE ( 'NONE', *, *, #60333, .F. ) ;
#7356=CARTESIAN_POINT ( 'NONE',  ( 18.59999999999996945, 65.66751761918648356, -63.92826094061123143 ) ) ;
#7371=CARTESIAN_POINT ( 'NONE',  ( -23.25000000000000000, 76.00000000001170974, -69.52310748452431710 ) ) ;
#7409=CARTESIAN_POINT ( 'NONE',  ( 22.39999999999999503, 64.35000000001194564, -102.9231074845243938 ) ) ;
#7410=DIRECTION ( 'NONE',  ( 0.000000000000000000, 0.8777080977375072424, -0.4791956752371691608 ) ) ;
#7419=ORIENTED_EDGE ( 'NONE', *, *, #156101, .F. ) ;
#7437=DIRECTION ( 'NONE',  ( 0.000000000000000000, 0.000000000000000000, 1.000000000000000000 ) ) ;
#7459=CYLINDRICAL_SURFACE ( 'NONE', #21907, 7.900000000000003908 ) ;
#7479=EDGE_CURVE ( 'NONE', #192382, #106895, #229546, .T. ) ;
#7481=VECTOR ( 'NONE', #101192, 1000.000000000000000 ) ;
#7487=ORIENTED_EDGE ( 'NONE', *, *, #1783, .T. ) ;
#7518=CARTESIAN_POINT ( 'NONE',  ( -20.99749315643147440, 64.25000000001175238, -76.53791325328415951 ) ) ;
#7522=CARTESIAN_POINT ( 'NONE',  ( -18.59999999999999787, 77.16270174994990327, -94.92310748452430857 ) ) ;
#7552=ORIENTED_EDGE ( 'NONE', *, *, #134286, .T. ) ;
#7578=ADVANCED_FACE ( 'NONE', ( #91315 ), #49611, .T. ) ;
#7638=DIRECTION ( 'NONE',  ( 0.000000000000000000, -0.1298341882519953860, -0.9915357197604862671 ) ) ;
#7644=CIRCLE ( 'NONE', #32803, 7.900000000000003908 ) ;
#7664=DIRECTION ( 'NONE',  ( -1.000000000000000000, 2.952720810173289112E-16, 2.061873921506763405E-30 ) ) ;
#7674=VERTEX_POINT ( 'NONE', #93869 ) ;
#7682=CARTESIAN_POINT ( 'NONE',  ( -22.50000000000094147, 75.90000000001212754, -114.6726782920691363 ) ) ;
#7711=ORIENTED_EDGE ( 'NONE', *, *, #121237, .T. ) ;
#7712=EDGE_LOOP ( 'NONE', ( #249003, #24636, #213615, #252389, #187638 ) ) ;
#7726=DIRECTION ( 'NONE',  ( 0.000000000000000000, -6.982962677686266711E-15, 1.000000000000000000 ) ) ;
#7734=FACE_OUTER_BOUND ( 'NONE', #89618, .T. ) ;
#7743=LINE ( 'NONE', #115819, #80759 ) ;
#7754=AXIS2_PLACEMENT_3D ( 'NONE', #3125, #226013, #44846 ) ;
#7767=FACE_OUTER_BOUND ( 'NONE', #137380, .T. ) ;
#7775=CARTESIAN_POINT ( 'NONE',  ( -23.25000000000000000, 87.65000000001172964, -72.52310748452423184 ) ) ;
#7814=CARTESIAN_POINT ( 'NONE',  ( 20.94999999999999929, 70.15000000001178648, -79.65560470880228650 ) ) ;
#7823=VERTEX_POINT ( 'NONE', #23355 ) ;
#7827=CIRCLE ( 'NONE', #37067, 4.049999999999998046 ) ;
#7840=AXIS2_PLACEMENT_3D ( 'NONE', #172139, #113407, #14335 ) ;
#7913=ORIENTED_EDGE ( 'NONE', *, *, #211806, .T. ) ;
#7938=EDGE_CURVE ( 'NONE', #152113, #121066, #69897, .T. ) ;
#7941=CARTESIAN_POINT ( 'NONE',  ( -23.25000000000000000, 76.00000000001192291, -98.97310748452431994 ) ) ;
#7962=DIRECTION ( 'NONE',  ( 0.000000000000000000, 1.000000000000000000, 6.938893903907222067E-15 ) ) ;
#7964=DIRECTION ( 'NONE',  ( 0.000000000000000000, -0.6728971962616412394, -0.7397360091703134577 ) ) ;
#7978=CARTESIAN_POINT ( 'NONE',  ( 21.05000000000000071, 67.22371710471941242, -94.53510676294000348 ) ) ;
#8006=ORIENTED_EDGE ( 'NONE', *, *, #197116, .F. ) ;
#8010=DIRECTION ( 'NONE',  ( 1.000000000000000000, 0.000000000000000000, 0.000000000000000000 ) ) ;
#8082=AXIS2_PLACEMENT_3D ( 'NONE', #204972, #45921, #185436 ) ;
#8165=EDGE_CURVE ( 'NONE', #161497, #136482, #32498, .T. ) ;
#8175=VERTEX_POINT ( 'NONE', #200371 ) ;
#8205=VECTOR ( 'NONE', #251093, 1000.000000000000000 ) ;
#8206=AXIS2_PLACEMENT_3D ( 'NONE', #18512, #175064, #58887 ) ;
#8221=CIRCLE ( 'NONE', #220604, 11.80000000000000426 ) ;
#8244=CYLINDRICAL_SURFACE ( 'NONE', #255994, 0.1000000000000028644 ) ;
#8254=ADVANCED_FACE ( 'NONE', ( #187243 ), #53306, .T. ) ;
#8278=ORIENTED_EDGE ( 'NONE', *, *, #165648, .T. ) ;
#8300=CARTESIAN_POINT ( 'NONE',  ( -20.64999999999999858, 74.00000000001180922, -82.74772940728641402 ) ) ;
#8307=EDGE_CURVE ( 'NONE', #190642, #86349, #30744, .T. ) ;
#8311=VERTEX_POINT ( 'NONE', #248482 ) ;
#8317=AXIS2_PLACEMENT_3D ( 'NONE', #58303, #195302, #136562 ) ;
#8333=EDGE_CURVE ( 'NONE', #203922, #78455, #178413, .T. ) ;
#8337=ORIENTED_EDGE ( 'NONE', *, *, #251155, .F. ) ;
#8345=DIRECTION ( 'NONE',  ( 0.000000000000000000, -0.9998779222360104635, -0.01562499999996343723 ) ) ;
#8362=EDGE_LOOP ( 'NONE', ( #69729, #35132, #24417, #47745 ) ) ;
#8371=LINE ( 'NONE', #205258, #143519 ) ;
#8374=VERTEX_POINT ( 'NONE', #5999 ) ;
#8382=ADVANCED_FACE ( 'NONE', ( #155820 ), #112821, .F. ) ;
#8384=VECTOR ( 'NONE', #143993, 999.9999999999998863 ) ;
#8407=DIRECTION ( 'NONE',  ( 0.000000000000000000, -7.026728003956683390E-15, 1.000000000000000000 ) ) ;
#8417=AXIS2_PLACEMENT_3D ( 'NONE', #135443, #54626, #235829 ) ;
#8432=CARTESIAN_POINT ( 'NONE',  ( -1.820710678118657944, 85.92928932189310842, -78.27310748452423184 ) ) ;
#8458=DIRECTION ( 'NONE',  ( 0.000000000000000000, 0.9908441862701605762, 0.1350103645451835310 ) ) ;
#8460=ORIENTED_EDGE ( 'NONE', *, *, #182641, .F. ) ;
#8483=AXIS2_PLACEMENT_3D ( 'NONE', #201322, #59202, #1822 ) ;
#8496=EDGE_CURVE ( 'NONE', #50189, #171936, #157583, .T. ) ;
#8509=CARTESIAN_POINT ( 'NONE',  ( 21.05000000000000071, 70.60000000001186038, -90.61784146561124942 ) ) ;
#8553=ORIENTED_EDGE ( 'NONE', *, *, #144050, .T. ) ;
#8558=ORIENTED_EDGE ( 'NONE', *, *, #58726, .T. ) ;
#8559=ORIENTED_EDGE ( 'NONE', *, *, #126807, .T. ) ;
#8579=CARTESIAN_POINT ( 'NONE',  ( 22.49999999999999645, 64.35012909624776967, -103.1056273753973329 ) ) ;
#8605=EDGE_CURVE ( 'NONE', #232010, #97749, #197477, .T. ) ;
#8625=DIRECTION ( 'NONE',  ( 0.000000000000000000, 0.000000000000000000, 1.000000000000000000 ) ) ;
#8648=CARTESIAN_POINT ( 'NONE',  ( 20.94999999999999929, 69.55000000001187743, -93.00608031408432907 ) ) ;
#8656=VECTOR ( 'NONE', #27563, 1000.000000000000000 ) ;
#8677=CARTESIAN_POINT ( 'NONE',  ( -21.04999999999999716, 76.08574093704538654, -109.4369337733372589 ) ) ;
#8699=DIRECTION ( 'NONE',  ( 0.7071067811865475727, 0.7071067811865475727, 4.937700262164531476E-15 ) ) ;
#8704=CARTESIAN_POINT ( 'NONE',  ( 21.13461538461538325, 67.11458296203740304, -90.67310748452436542 ) ) ;
#8705=DIRECTION ( 'NONE',  ( 0.000000000000000000, 0.000000000000000000, 1.000000000000000000 ) ) ;
#8725=FACE_OUTER_BOUND ( 'NONE', #113130, .T. ) ;
#8800=DIRECTION ( 'NONE',  ( -1.000000000000000000, -0.000000000000000000, -0.000000000000000000 ) ) ;
#8803=PLANE ( 'NONE',  #222166 ) ;
#8810=CARTESIAN_POINT ( 'NONE',  ( -21.04386569057603751, 64.25000000001173817, -76.38027013274417243 ) ) ;
#8812=EDGE_LOOP ( 'NONE', ( #103376, #205042, #31103, #218352 ) ) ;
#8819=CIRCLE ( 'NONE', #162962, 0.09999999999999939493 ) ;
#8821=FACE_OUTER_BOUND ( 'NONE', #119933, .T. ) ;
#8824=ORIENTED_EDGE ( 'NONE', *, *, #9303, .T. ) ;
#8847=DIRECTION ( 'NONE',  ( 0.000000000000000000, -3.469446951953635015E-14, 1.000000000000000000 ) ) ;
#8849=FACE_OUTER_BOUND ( 'NONE', #139835, .T. ) ;
#8864=FACE_OUTER_BOUND ( 'NONE', #77644, .T. ) ;
#8886=DIRECTION ( 'NONE',  ( -1.000000000000000000, 2.952720810173289112E-16, 2.061873921506763405E-30 ) ) ;
#8889=DIRECTION ( 'NONE',  ( -1.000000000000000000, 0.000000000000000000, 0.000000000000000000 ) ) ;
#8901=PLANE ( 'NONE',  #128007 ) ;
#8950=ORIENTED_EDGE ( 'NONE', *, *, #24372, .F. ) ;
#8961=CARTESIAN_POINT ( 'NONE',  ( 20.95462737510932882, 65.44321804836815204, -95.45315742796208269 ) ) ;
#8965=CARTESIAN_POINT ( 'NONE',  ( 21.05000000000000071, 88.41227409416143246, -72.52310748452423184 ) ) ;
#8978=EDGE_CURVE ( 'NONE', #240371, #70373, #1209, .T. ) ;
#8979=ORIENTED_EDGE ( 'NONE', *, *, #57919, .F. ) ;
#8981=VERTEX_POINT ( 'NONE', #160338 ) ;
#9020=CARTESIAN_POINT ( 'NONE',  ( -20.54999999999999716, 76.00000000001195133, -103.0231074845243171 ) ) ;
#9021=DIRECTION ( 'NONE',  ( 3.469446951953635015E-14, 6.982962677686266711E-15, -1.000000000000000000 ) ) ;
#9067=CIRCLE ( 'NONE', #238188, 2.100000000000004530 ) ;
#9068=EDGE_CURVE ( 'NONE', #123180, #143626, #83030, .T. ) ;
#9070=CARTESIAN_POINT ( 'NONE',  ( -20.94999999999999929, 87.48912529308779540, -72.62310748452422615 ) ) ;
#9097=CARTESIAN_POINT ( 'NONE',  ( -18.59999999999999787, 64.35000000001180354, -81.67310748452439384 ) ) ;
#9127=ADVANCED_FACE ( 'NONE', ( #36226 ), #173200, .T. ) ;
#9145=DIRECTION ( 'NONE',  ( 1.000000000000000000, 0.000000000000000000, 0.000000000000000000 ) ) ;
#9146=DIRECTION ( 'NONE',  ( -1.000000000000000000, 0.000000000000000000, 0.000000000000000000 ) ) ;
#9147=CARTESIAN_POINT ( 'NONE',  ( -18.59999999999999787, 64.35000000001180354, -81.77310748452438816 ) ) ;
#9166=DIRECTION ( 'NONE',  ( 0.000000000000000000, 0.000000000000000000, 1.000000000000000000 ) ) ;
#9186=EDGE_LOOP ( 'NONE', ( #86071, #220778, #105308, #152684 ) ) ;
#9196=CARTESIAN_POINT ( 'NONE',  ( 19.75857864376268935, 64.35000000001177511, -78.27310748452438816 ) ) ;
#9197=DIRECTION ( 'NONE',  ( 0.000000000000000000, 0.000000000000000000, 1.000000000000000000 ) ) ;
#9204=CARTESIAN_POINT ( 'NONE',  ( -23.15000000000000213, 74.00000000001180922, -82.74772940728641402 ) ) ;
#9224=AXIS2_PLACEMENT_3D ( 'NONE', #114975, #155429, #234933 ) ;
#9242=CARTESIAN_POINT ( 'NONE',  ( -20.90851465518106167, 65.67467670974397720, -63.95317318268842399 ) ) ;
#9247=ORIENTED_EDGE ( 'NONE', *, *, #23806, .T. ) ;
#9250=DIRECTION ( 'NONE',  ( 0.000000000000000000, -1.000000000000000000, -6.982962677686266711E-15 ) ) ;
#9278=AXIS2_PLACEMENT_3D ( 'NONE', #71171, #171568, #73744 ) ;
#9281=LINE ( 'NONE', #28899, #197521 ) ;
#9284=CARTESIAN_POINT ( 'NONE',  ( -21.11825140030087766, 69.55459243459219465, -103.0303111051572529 ) ) ;
#9303=EDGE_CURVE ( 'NONE', #196167, #30659, #62227, .T. ) ;
#9335=CARTESIAN_POINT ( 'NONE',  ( 21.05000000000000071, 64.40000000001175806, -76.45131071479988805 ) ) ;
#9337=EDGE_CURVE ( 'NONE', #190642, #195198, #232937, .T. ) ;
#9338=DIRECTION ( 'NONE',  ( 1.000000000000000000, 0.000000000000000000, 0.000000000000000000 ) ) ;
#9374=CIRCLE ( 'NONE', #30252, 0.1999999999999987899 ) ;
#9382=ADVANCED_FACE ( 'NONE', ( #148138 ), #146833, .F. ) ;
#9384=ORIENTED_EDGE ( 'NONE', *, *, #144395, .F. ) ;
#9387=VERTEX_POINT ( 'NONE', #86855 ) ;
#9390=CARTESIAN_POINT ( 'NONE',  ( -23.25000000000000000, 85.00000000001179501, -79.41707660717668205 ) ) ;
#9396=ORIENTED_EDGE ( 'NONE', *, *, #184275, .F. ) ;
#9451=FACE_OUTER_BOUND ( 'NONE', #250486, .T. ) ;
#9484=ORIENTED_EDGE ( 'NONE', *, *, #121139, .T. ) ;
#9496=CARTESIAN_POINT ( 'NONE',  ( 18.59999994388910238, 85.36356618708308019, -95.84199024772335918 ) ) ;
#9514=DIRECTION ( 'NONE',  ( -0.7071067811865127117, -0.7071067811865821007, 0.000000000000000000 ) ) ;
#9557=AXIS2_PLACEMENT_3D ( 'NONE', #45932, #167202, #1969 ) ;
#9611=DIRECTION ( 'NONE',  ( 1.000000000000000000, 0.000000000000000000, 0.000000000000000000 ) ) ;
#9655=AXIS2_PLACEMENT_3D ( 'NONE', #229032, #29571, #33429 ) ;
#9679=FACE_OUTER_BOUND ( 'NONE', #185751, .T. ) ;
#9686=VECTOR ( 'NONE', #135382, 1000.000000000000000 ) ;
#9705=CARTESIAN_POINT ( 'NONE',  ( 20.85882249326303040, 65.66751761918648356, -63.92826094061123143 ) ) ;
#9736=PLANE ( 'NONE',  #69833 ) ;
#9799=DIRECTION ( 'NONE',  ( 1.000000000000000000, 0.000000000000000000, 0.000000000000000000 ) ) ;
#9801=AXIS2_PLACEMENT_3D ( 'NONE', #71795, #168355, #7962 ) ;
#9808=CIRCLE ( 'NONE', #47208, 0.1000000000000014488 ) ;
#9828=ADVANCED_FACE ( 'NONE', ( #125697 ), #126985, .T. ) ;
#9831=FACE_OUTER_BOUND ( 'NONE', #34091, .T. ) ;
#9847=DIRECTION ( 'NONE',  ( -1.000000000000000000, 0.000000000000000000, -0.000000000000000000 ) ) ;
#9852=ORIENTED_EDGE ( 'NONE', *, *, #190425, .F. ) ;
#9869=VERTEX_POINT ( 'NONE', #209090 ) ;
#9881=CARTESIAN_POINT ( 'NONE',  ( 23.25000000000000000, 87.65000000001195701, -103.0231074845242318 ) ) ;
#9896=CIRCLE ( 'NONE', #5776, 0.1000000000000009492 ) ;
#9897=ORIENTED_EDGE ( 'NONE', *, *, #168915, .T. ) ;
#9902=LINE ( 'NONE', #89434, #47405 ) ;
#9908=DIRECTION ( 'NONE',  ( 1.000000000000000000, 0.000000000000000000, 0.000000000000000000 ) ) ;
#9918=VERTEX_POINT ( 'NONE', #192120 ) ;
#9920=AXIS2_PLACEMENT_3D ( 'NONE', #86011, #165603, #245125 ) ;
#9929=FACE_OUTER_BOUND ( 'NONE', #64514, .T. ) ;
#9960=AXIS2_PLACEMENT_3D ( 'NONE', #187513, #182368, #3708 ) ;
#10018=DIRECTION ( 'NONE',  ( -1.000000000000000000, -0.000000000000000000, -0.000000000000000000 ) ) ;
#10073=CARTESIAN_POINT ( 'NONE',  ( -23.15000000000000213, 85.00000000001179501, -79.41707660717668205 ) ) ;
#10078=CARTESIAN_POINT ( 'NONE',  ( 23.25000000000000000, 87.65000000001202807, -114.7731074845242318 ) ) ;
#10080=CARTESIAN_POINT ( 'NONE',  ( -18.50000000000000000, 64.25000000001203659, -114.7731074845243882 ) ) ;
#10083=AXIS2_PLACEMENT_3D ( 'NONE', #131895, #196987, #191903 ) ;
#10087=DIRECTION ( 'NONE',  ( 0.000000000000000000, 0.000000000000000000, 1.000000000000000000 ) ) ;
#10090=VERTEX_POINT ( 'NONE', #2768 ) ;
#10104=ORIENTED_EDGE ( 'NONE', *, *, #4028, .T. ) ;
#10118=ORIENTED_EDGE ( 'NONE', *, *, #219431, .F. ) ;
#10141=ORIENTED_EDGE ( 'NONE', *, *, #196865, .T. ) ;
#10153=( BOUNDED_CURVE ( )  B_SPLINE_CURVE ( 3, ( #55628, #137751, #120803, #36124 ),
 .UNSPECIFIED., .F., .T. ) 
 B_SPLINE_CURVE_WITH_KNOTS ( ( 4, 4 ),
 ( 1.570796326794895448, 3.141592653589791784 ),
 .UNSPECIFIED. ) 
 CURVE ( )  GEOMETRIC_REPRESENTATION_ITEM ( )  RATIONAL_B_SPLINE_CURVE ( ( 1.000000000000000000, 0.8047378541243650485, 0.8047378541243650485, 1.000000000000000000 ) ) 
 REPRESENTATION_ITEM ( '' )  );
#10160=VECTOR ( 'NONE', #105027, 1000.000000000000000 ) ;
#10168=ORIENTED_EDGE ( 'NONE', *, *, #253044, .T. ) ;
#10193=CYLINDRICAL_SURFACE ( 'NONE', #82005, 4.000000000000003553 ) ;
#10235=DIRECTION ( 'NONE',  ( 0.000000000000000000, 0.4999999999999689138, -0.8660254037844565822 ) ) ;
#10252=CARTESIAN_POINT ( 'NONE',  ( -21.07928932188134041, 69.67148334361864670, -103.1220026301787414 ) ) ;
#10300=AXIS2_PLACEMENT_3D ( 'NONE', #195355, #80469, #156230 ) ;
#10302=DIRECTION ( 'NONE',  ( -0.000000000000000000, 1.000000000000000000, 6.982962677686266711E-15 ) ) ;
#10349=EDGE_LOOP ( 'NONE', ( #1724, #177786, #186299, #7133 ) ) ;
#10390=ORIENTED_EDGE ( 'NONE', *, *, #120368, .T. ) ;
#10418=ORIENTED_EDGE ( 'NONE', *, *, #159810, .F. ) ;
#10450=CARTESIAN_POINT ( 'NONE',  ( -23.25000000000000000, 64.35000000001195986, -103.0231074845244024 ) ) ;
#10456=DIRECTION ( 'NONE',  ( -0.000000000000000000, 1.000000000000000000, 6.982962677686266711E-15 ) ) ;
#10497=CARTESIAN_POINT ( 'NONE',  ( 23.24999999999999289, 64.35000000001186038, -90.87310748452438247 ) ) ;
#10508=DIRECTION ( 'NONE',  ( 0.000000000000000000, -0.9908441862701605762, 0.1350103645451835310 ) ) ;
#10560=CARTESIAN_POINT ( 'NONE',  ( -22.24259225415828567, 68.50806212944651463, -103.1221733679771972 ) ) ;
#10582=CARTESIAN_POINT ( 'NONE',  ( -21.13435531349793450, 69.50627893641963340, -103.0231074845243597 ) ) ;
#10665=ORIENTED_EDGE ( 'NONE', *, *, #66559, .F. ) ;
#10672=ORIENTED_EDGE ( 'NONE', *, *, #144014, .T. ) ;
#10690=DIRECTION ( 'NONE',  ( 1.000000000000000000, 0.000000000000000000, 0.000000000000000000 ) ) ;
#10696=ORIENTED_EDGE ( 'NONE', *, *, #22250, .T. ) ;
#10701=LINE ( 'NONE', #69403, #173796 ) ;
#10704=VERTEX_POINT ( 'NONE', #66312 ) ;
#10752=DIRECTION ( 'NONE',  ( 0.000000000000000000, -8.267618268485210697E-15, 1.000000000000000000 ) ) ;
#10791=VERTEX_POINT ( 'NONE', #210959 ) ;
#10792=CARTESIAN_POINT ( 'NONE',  ( 21.30000000000002558, 76.00000000001195133, -103.0231074845243171 ) ) ;
#10794=CARTESIAN_POINT ( 'NONE',  ( -18.59999999999999787, 77.63717271298224887, -91.44095411905229298 ) ) ;
#10800=FACE_OUTER_BOUND ( 'NONE', #175281, .T. ) ;
#10823=CARTESIAN_POINT ( 'NONE',  ( -23.15000000000000213, 76.00000000001186606, -90.24810748452431142 ) ) ;
#10824=CIRCLE ( 'NONE', #243857, 4.049999999999998046 ) ;
#10839=VERTEX_POINT ( 'NONE', #75323 ) ;
#10881=CARTESIAN_POINT ( 'NONE',  ( 23.14999999999999503, 64.35000000001186038, -90.87310748452438247 ) ) ;
#11007=DIRECTION ( 'NONE',  ( -1.000000000000000000, 0.000000000000000000, 0.000000000000000000 ) ) ;
#11015=VERTEX_POINT ( 'NONE', #142938 ) ;
#11067=ORIENTED_EDGE ( 'NONE', *, *, #243931, .T. ) ;
#11079=EDGE_CURVE ( 'NONE', #123690, #59708, #213415, .T. ) ;
#11087=CARTESIAN_POINT ( 'NONE',  ( -20.94999999999999929, 61.95000000001191154, -97.50941241376341395 ) ) ;
#11088=VERTEX_POINT ( 'NONE', #251029 ) ;
#11089=EDGE_CURVE ( 'NONE', #184113, #60702, #193651, .T. ) ;
#11099=DIRECTION ( 'NONE',  ( -1.000000000000000000, 0.000000000000000000, -0.000000000000000000 ) ) ;
#11101=CARTESIAN_POINT ( 'NONE',  ( 20.94999999999999929, 71.00000000001180922, -81.92837350343744163 ) ) ;
#11107=CIRCLE ( 'NONE', #177557, 11.70000000000000284 ) ;
#11115=ORIENTED_EDGE ( 'NONE', *, *, #124542, .T. ) ;
#11175=EDGE_CURVE ( 'NONE', #147363, #246499, #76062, .T. ) ;
#11191=DIRECTION ( 'NONE',  ( 0.000000000000000000, 1.000000000000000000, 6.608470384673536824E-15 ) ) ;
#11205=CIRCLE ( 'NONE', #156970, 0.1000000000000028644 ) ;
#11207=FACE_OUTER_BOUND ( 'NONE', #19427, .T. ) ;
#11212=AXIS2_PLACEMENT_3D ( 'NONE', #128138, #109834, #129411 ) ;
#11232=EDGE_LOOP ( 'NONE', ( #219877, #236880, #124474, #208634 ) ) ;
#11233=DIRECTION ( 'NONE',  ( 0.000000000000000000, 1.000000000000000000, 0.000000000000000000 ) ) ;
#11254=LINE ( 'NONE', #90767, #133233 ) ;
#11261=DIRECTION ( 'NONE',  ( 0.7071067811865487940, 4.851104656540973741E-15, -0.7071067811865463515 ) ) ;
#11266=DIRECTION ( 'NONE',  ( 0.000000000000000000, 6.982962677686266711E-15, -1.000000000000000000 ) ) ;
#11269=CYLINDRICAL_SURFACE ( 'NONE', #16345, 0.09999999999999939493 ) ;
#11275=DIRECTION ( 'NONE',  ( -0.000000000000000000, 6.982962677686266711E-15, -1.000000000000000000 ) ) ;
#11301=ADVANCED_FACE ( 'NONE', ( #243993 ), #217035, .F. ) ;
#11310=DIRECTION ( 'NONE',  ( 0.000000000000000000, -1.000000000000000000, -6.982962677686266711E-15 ) ) ;
#11342=ORIENTED_EDGE ( 'NONE', *, *, #132614, .T. ) ;
#11380=CIRCLE ( 'NONE', #115420, 0.09999999999999489853 ) ;
#11388=EDGE_LOOP ( 'NONE', ( #167822, #95945, #183853, #2575 ) ) ;
#11428=CARTESIAN_POINT ( 'NONE',  ( 20.85000000000000142, 68.87972903831409610, -65.86354444268503983 ) ) ;
#11451=VERTEX_POINT ( 'NONE', #131757 ) ;
#11496=ORIENTED_EDGE ( 'NONE', *, *, #221361, .F. ) ;
#11503=LINE ( 'NONE', #144883, #8656 ) ;
#11566=EDGE_CURVE ( 'NONE', #9918, #56583, #22104, .T. ) ;
#11568=EDGE_LOOP ( 'NONE', ( #245553, #102926, #146628, #24602 ) ) ;
#11573=AXIS2_PLACEMENT_3D ( 'NONE', #19546, #3820, #242417 ) ;
#11576=TOROIDAL_SURFACE ( 'NONE', #53253, 4.099999999999999645, 0.1000000000000000056 ) ;
#11582=DIRECTION ( 'NONE',  ( 0.000000000000000000, -6.982962677686266711E-15, 1.000000000000000000 ) ) ;
#11599=AXIS2_PLACEMENT_3D ( 'NONE', #24323, #244621, #86819 ) ;
#11602=FACE_OUTER_BOUND ( 'NONE', #19079, .T. ) ;
#11609=DIRECTION ( 'NONE',  ( 0.000000000000000000, 0.000000000000000000, -1.000000000000000000 ) ) ;
#11618=CIRCLE ( 'NONE', #53101, 0.2000000000000057288 ) ;
#11639=ORIENTED_EDGE ( 'NONE', *, *, #158767, .F. ) ;
#11642=ORIENTED_EDGE ( 'NONE', *, *, #171607, .T. ) ;
#11648=LINE ( 'NONE', #71619, #217742 ) ;
#11664=DIRECTION ( 'NONE',  ( -1.000000000000000000, -0.000000000000000000, -0.000000000000000000 ) ) ;
#11670=EDGE_CURVE ( 'NONE', #201690, #224268, #184558, .T. ) ;
#11679=VERTEX_POINT ( 'NONE', #199461 ) ;
#11730=CARTESIAN_POINT ( 'NONE',  ( 20.94999999999999929, 71.00000000001180922, -81.92837350343744163 ) ) ;
#11739=ORIENTED_EDGE ( 'NONE', *, *, #20313, .F. ) ;
#11804=ORIENTED_EDGE ( 'NONE', *, *, #53149, .T. ) ;
#11817=CARTESIAN_POINT ( 'NONE',  ( 23.25000000000000000, 85.60000000001188880, -93.12913836187179584 ) ) ;
#11836=CARTESIAN_POINT ( 'NONE',  ( -20.00857864376270001, 66.85000000001180354, -81.87310748452438247 ) ) ;
#11839=LINE ( 'NONE', #91359, #225702 ) ;
#11847=CARTESIAN_POINT ( 'NONE',  ( -18.46093223321785359, 85.48068296828637358, -95.93855697059757404 ) ) ;
#11857=CARTESIAN_POINT ( 'NONE',  ( 18.59999999999999076, 64.35000000001177511, -78.17310748452437963 ) ) ;
#11884=ORIENTED_EDGE ( 'NONE', *, *, #54620, .T. ) ;
#11886=CARTESIAN_POINT ( 'NONE',  ( 20.94999999999999574, 74.75000000001189449, -95.02310748452431710 ) ) ;
#11890=FACE_OUTER_BOUND ( 'NONE', #218314, .T. ) ;
#11903=CARTESIAN_POINT ( 'NONE',  ( 20.94999999999999574, 69.45000000001188312, -93.17928539484123007 ) ) ;
#11906=CARTESIAN_POINT ( 'NONE',  ( -23.25000000000000000, 76.10000000001203091, -114.6726782920691079 ) ) ;
#11924=DIRECTION ( 'NONE',  ( 0.000000000000000000, 1.000000000000000000, 6.982962677686266711E-15 ) ) ;
#11928=TOROIDAL_SURFACE ( 'NONE', #57849, 0.4000000000000012990, 0.1000000000000000056 ) ;
#11931=CIRCLE ( 'NONE', #178528, 0.8750000000000007772 ) ;
#11941=DIRECTION ( 'NONE',  ( 0.000000000000000000, 0.000000000000000000, 1.000000000000000000 ) ) ;
#11950=EDGE_LOOP ( 'NONE', ( #231355, #130360, #170042, #70727 ) ) ;
#11952=AXIS2_PLACEMENT_3D ( 'NONE', #236318, #57665, #160670 ) ;
#11992=ORIENTED_EDGE ( 'NONE', *, *, #151471, .T. ) ;
#11996=VERTEX_POINT ( 'NONE', #17911 ) ;
#11998=AXIS2_PLACEMENT_3D ( 'NONE', #41659, #200714, #167706 ) ;
#12005=CARTESIAN_POINT ( 'NONE',  ( 23.14999999999999503, 64.35000000001186038, -90.77310748452438816 ) ) ;
#12008=VERTEX_POINT ( 'NONE', #111910 ) ;
#12014=ORIENTED_EDGE ( 'NONE', *, *, #130601, .T. ) ;
#12015=CARTESIAN_POINT ( 'NONE',  ( 21.05000000000000071, 65.31570632562468859, -95.49643354588684474 ) ) ;
#12073=EDGE_LOOP ( 'NONE', ( #30455, #46079, #213745, #154993 ) ) ;
#12074=ORIENTED_EDGE ( 'NONE', *, *, #243016, .T. ) ;
#12085=LINE ( 'NONE', #171182, #37493 ) ;
#12087=LINE ( 'NONE', #172467, #141427 ) ;
#12149=ORIENTED_EDGE ( 'NONE', *, *, #181360, .F. ) ;
#12166=PLANE ( 'NONE',  #52983 ) ;
#12200=ORIENTED_EDGE ( 'NONE', *, *, #47264, .T. ) ;
#12221=CARTESIAN_POINT ( 'NONE',  ( -20.64999999999999858, 76.00000000001172396, -71.42310748452430857 ) ) ;
#12258=ORIENTED_EDGE ( 'NONE', *, *, #204317, .T. ) ;
#12287=VECTOR ( 'NONE', #254620, 1000.000000000000000 ) ;
#12289=VERTEX_POINT ( 'NONE', #169028 ) ;
#12301=CARTESIAN_POINT ( 'NONE',  ( -20.94999999999999929, 76.00000000001170974, -69.52310748452431710 ) ) ;
#12359=CARTESIAN_POINT ( 'NONE',  ( 23.14999999999999503, 69.35000000001180354, -81.77310748452435973 ) ) ;
#12373=AXIS2_PLACEMENT_3D ( 'NONE', #26817, #185855, #178517 ) ;
#12384=AXIS2_PLACEMENT_3D ( 'NONE', #47793, #84315, #62248 ) ;
#12404=CARTESIAN_POINT ( 'NONE',  ( 23.25000000000000000, 84.59626168225486254, -93.57297996737396772 ) ) ;
#12473=CARTESIAN_POINT ( 'NONE',  ( 20.94999999999999929, 76.00000000001170974, -69.52310748452431710 ) ) ;
#12482=CARTESIAN_POINT ( 'NONE',  ( -21.05000000000000071, 70.15000000001192859, -92.89061026024637613 ) ) ;
#12484=VECTOR ( 'NONE', #250475, 1000.000000000000000 ) ;
#12517=CARTESIAN_POINT ( 'NONE',  ( 23.14999999999999858, 76.00000000001195133, -103.0231074845243171 ) ) ;
#12580=DIRECTION ( 'NONE',  ( 1.000000000000000000, 0.000000000000000000, 0.000000000000000000 ) ) ;
#12592=VECTOR ( 'NONE', #15316, 1000.000000000000000 ) ;
#12610=ORIENTED_EDGE ( 'NONE', *, *, #209729, .F. ) ;
#12651=ORIENTED_EDGE ( 'NONE', *, *, #122018, .T. ) ;
#12653=AXIS2_PLACEMENT_3D ( 'NONE', #251437, #187632, #231896 ) ;
#12678=CIRCLE ( 'NONE', #37623, 0.1000000000000028644 ) ;
#12692=ORIENTED_EDGE ( 'NONE', *, *, #49968, .F. ) ;
#12694=CARTESIAN_POINT ( 'NONE',  ( 21.05000000000000071, 85.40000000001178648, -79.41707660717668205 ) ) ;
#12738=FACE_OUTER_BOUND ( 'NONE', #51082, .T. ) ;
#12781=CARTESIAN_POINT ( 'NONE',  ( -21.05000000000000071, 87.75000000001173817, -72.52310748452423184 ) ) ;
#12789=AXIS2_PLACEMENT_3D ( 'NONE', #64739, #33055, #13449 ) ;
#12793=DIRECTION ( 'NONE',  ( -0.7071067811865389130, -5.024295867788141276E-15, 0.7071067811865561215 ) ) ;
#12797=DIRECTION ( 'NONE',  ( 1.000000000000000000, -0.000000000000000000, 0.000000000000000000 ) ) ;
#12825=CARTESIAN_POINT ( 'NONE',  ( 18.59999999999999076, 76.00000000001170974, -69.52310748452431710 ) ) ;
#12835=ADVANCED_FACE ( 'NONE', ( #135959 ), #175154, .F. ) ;
#12855=CARTESIAN_POINT ( 'NONE',  ( -22.50000000000000000, 76.00000000001203659, -114.6726782920691221 ) ) ;
#12865=ADVANCED_FACE ( 'NONE', ( #199823 ), #113829, .T. ) ;
#12879=ADVANCED_FACE ( 'NONE', ( #139808 ), #195966, .F. ) ;
#12911=ORIENTED_EDGE ( 'NONE', *, *, #148424, .F. ) ;
#12917=CARTESIAN_POINT ( 'NONE',  ( -21.07016717456947319, 69.67905916191169524, -103.0231074845243455 ) ) ;
#12919=CARTESIAN_POINT ( 'NONE',  ( 18.59999999999999432, 77.63717271298224887, -91.44095411905229298 ) ) ;
#12922=FACE_OUTER_BOUND ( 'NONE', #71384, .T. ) ;
#12933=CYLINDRICAL_SURFACE ( 'NONE', #82443, 0.1000000000000028644 ) ;
#12935=ORIENTED_EDGE ( 'NONE', *, *, #108880, .T. ) ;
#13005=FACE_OUTER_BOUND ( 'NONE', #154818, .T. ) ;
#13049=CARTESIAN_POINT ( 'NONE',  ( 21.14999999999999858, 65.28660755661196902, -90.77310748452438816 ) ) ;
#13054=AXIS2_PLACEMENT_3D ( 'NONE', #140867, #101695, #82139 ) ;
#13065=DIRECTION ( 'NONE',  ( 0.000000000000000000, -6.982962677686267499E-15, 1.000000000000000000 ) ) ;
#13075=DIRECTION ( 'NONE',  ( 0.000000000000000000, 0.000000000000000000, 1.000000000000000000 ) ) ;
#13077=DIRECTION ( 'NONE',  ( 0.000000000000000000, 1.000000000000000000, 0.000000000000000000 ) ) ;
#13089=FACE_OUTER_BOUND ( 'NONE', #225380, .T. ) ;
#13128=CARTESIAN_POINT ( 'NONE',  ( -21.14999999999999858, 69.45934304831071415, -103.0231074845243597 ) ) ;
#13150=ORIENTED_EDGE ( 'NONE', *, *, #180459, .T. ) ;
#13166=ADVANCED_FACE ( 'NONE', ( #170994 ), #220008, .T. ) ;
#13194=TOROIDAL_SURFACE ( 'NONE', #196321, 0.2000000000000000111, 0.1000000000000000056 ) ;
#13215=ADVANCED_FACE ( 'NONE', ( #4784 ), #240867, .T. ) ;
#13217=CARTESIAN_POINT ( 'NONE',  ( 21.98333005346336932, 76.00000000001200817, -110.3971828135809830 ) ) ;
#13222=AXIS2_PLACEMENT_3D ( 'NONE', #161628, #241153, #187601 ) ;
#13243=ORIENTED_EDGE ( 'NONE', *, *, #101678, .F. ) ;
#13263=CARTESIAN_POINT ( 'NONE',  ( 20.94999999999999929, 71.00000000001180922, -81.92837350343744163 ) ) ;
#13265=CARTESIAN_POINT ( 'NONE',  ( 21.40925344232283223, 75.90104981139234042, -109.6816263439147576 ) ) ;
#13307=AXIS2_PLACEMENT_3D ( 'NONE', #179032, #219385, #159443 ) ;
#13315=DIRECTION ( 'NONE',  ( -1.000000000000000000, -0.000000000000000000, -0.000000000000000000 ) ) ;
#13335=CARTESIAN_POINT ( 'NONE',  ( -21.52071067811865746, 68.22071067813051570, -90.67310748452436542 ) ) ;
#13353=AXIS2_PLACEMENT_3D ( 'NONE', #66850, #87676, #248049 ) ;
#13367=CIRCLE ( 'NONE', #163211, 0.1000000000000028644 ) ;
#13397=CARTESIAN_POINT ( 'NONE',  ( 21.05000000000000071, 76.10000000001198828, -109.5637644362255543 ) ) ;
#13405=CARTESIAN_POINT ( 'NONE',  ( -20.94999999999999929, 74.25000000001186606, -91.35359592662267403 ) ) ;
#13406=DIRECTION ( 'NONE',  ( 0.000000000000000000, -0.9876197685951265681, -0.1568667991644790149 ) ) ;
#13442=AXIS2_PLACEMENT_3D ( 'NONE', #217066, #38452, #117990 ) ;
#13449=DIRECTION ( 'NONE',  ( 0.000000000000000000, 0.000000000000000000, 1.000000000000000000 ) ) ;
#13452=CARTESIAN_POINT ( 'NONE',  ( -20.07928932188135107, 66.77928932189314537, -81.87310748452438247 ) ) ;
#13508=ADVANCED_FACE ( 'NONE', ( #98426 ), #77599, .F. ) ;
#13516=DIRECTION ( 'NONE',  ( 0.000000000000000000, 0.000000000000000000, -1.000000000000000000 ) ) ;
#13526=VECTOR ( 'NONE', #58486, 999.9999999999998863 ) ;
#13530=EDGE_CURVE ( 'NONE', #161497, #196101, #30825, .T. ) ;
#13535=EDGE_CURVE ( 'NONE', #25250, #160733, #239276, .T. ) ;
#13569=ORIENTED_EDGE ( 'NONE', *, *, #144421, .T. ) ;
#13576=DIRECTION ( 'NONE',  ( 0.000000000000000000, 0.9908441862701605762, 0.1350103645451835310 ) ) ;
#13577=B_SPLINE_CURVE_WITH_KNOTS ( 'NONE', 3,
 ( #72530, #35969, #215849, #37258, #92066, #97158, #176766, #93349, #256207, #77617 ),
 .UNSPECIFIED., .F., .F.,
 ( 4, 2, 2, 2, 4 ),
 ( 0.000000000000000000, 4.221631689687584354E-05, 8.443263379375168709E-05, 0.0001688652675875033742, 0.0003377305351749930332 ),
 .UNSPECIFIED. ) ;
#13581=CARTESIAN_POINT ( 'NONE',  ( 20.87600722750343252, 65.66887361445314752, -63.93298459182691573 ) ) ;
#13584=AXIS2_PLACEMENT_3D ( 'NONE', #46822, #106803, #158182 ) ;
#13586=ORIENTED_EDGE ( 'NONE', *, *, #39696, .F. ) ;
#13587=DIRECTION ( 'NONE',  ( 2.952720810173289112E-16, 1.000000000000000000, -6.088138035986627436E-46 ) ) ;
#13623=ORIENTED_EDGE ( 'NONE', *, *, #56156, .F. ) ;
#13627=DIRECTION ( 'NONE',  ( -1.000000000000000000, 0.000000000000000000, 0.000000000000000000 ) ) ;
#13630=CARTESIAN_POINT ( 'NONE',  ( -23.15000000000000213, 64.35000000001176090, -76.53791325517833855 ) ) ;
#13682=CIRCLE ( 'NONE', #55163, 0.1000000000000028644 ) ;
#13745=ORIENTED_EDGE ( 'NONE', *, *, #179559, .F. ) ;
#13772=CARTESIAN_POINT ( 'NONE',  ( 20.94999999999999574, 77.83534155023627932, -91.46795619196132066 ) ) ;
#13781=ORIENTED_EDGE ( 'NONE', *, *, #218386, .F. ) ;
#13794=AXIS2_PLACEMENT_3D ( 'NONE', #110960, #32752, #49705 ) ;
#13804=ORIENTED_EDGE ( 'NONE', *, *, #247270, .T. ) ;
#13828=CYLINDRICAL_SURFACE ( 'NONE', #18031, 11.74999999999999645 ) ;
#13838=ORIENTED_EDGE ( 'NONE', *, *, #115623, .T. ) ;
#13879=DIRECTION ( 'NONE',  ( 0.000000000000000000, 0.000000000000000000, 1.000000000000000000 ) ) ;
#13896=VECTOR ( 'NONE', #22126, 1000.000000000000000 ) ;
#13914=CARTESIAN_POINT ( 'NONE',  ( 20.94999999999999929, 74.16465844978745281, -91.46795619196133487 ) ) ;
#13923=CYLINDRICAL_SURFACE ( 'NONE', #94986, 0.1000000000000052097 ) ;
#13932=EDGE_CURVE ( 'NONE', #156170, #142842, #75720, .T. ) ;
#13968=VERTEX_POINT ( 'NONE', #106808 ) ;
#13978=ORIENTED_EDGE ( 'NONE', *, *, #65378, .T. ) ;
#13979=DIRECTION ( 'NONE',  ( -1.000000000000000000, 0.000000000000000000, 0.000000000000000000 ) ) ;
#14064=ORIENTED_EDGE ( 'NONE', *, *, #27094, .F. ) ;
#14100=PRODUCT ( 'Injection Molded Chain Links 14', 'Injection Molded Chain Links 14', '', ( #218994 ) ) ;
#14109=FACE_OUTER_BOUND ( 'NONE', #16819, .T. ) ;
#14165=CARTESIAN_POINT ( 'NONE',  ( 21.04999999999953886, 69.55891531154068730, -103.0053880512149789 ) ) ;
#14182=FACE_OUTER_BOUND ( 'NONE', #103693, .T. ) ;
#14183=DIRECTION ( 'NONE',  ( -1.000000000000000000, 0.000000000000000000, -0.000000000000000000 ) ) ;
#14203=DIRECTION ( 'NONE',  ( 1.000000000000000000, 0.000000000000000000, 0.000000000000000000 ) ) ;
#14222=FACE_OUTER_BOUND ( 'NONE', #103721, .T. ) ;
#14237=VERTEX_POINT ( 'NONE', #31181 ) ;
#14246=DIRECTION ( 'NONE',  ( 0.000000000000000000, 6.982962677686266711E-15, -1.000000000000000000 ) ) ;
#14248=ORIENTED_EDGE ( 'NONE', *, *, #172282, .T. ) ;
#14250=ORIENTED_EDGE ( 'NONE', *, *, #51312, .F. ) ;
#14256=VERTEX_POINT ( 'NONE', #137918 ) ;
#14283=CIRCLE ( 'NONE', #193343, 0.1000000000000028644 ) ;
#14285=EDGE_CURVE ( 'NONE', #53093, #60702, #235180, .T. ) ;
#14312=DIRECTION ( 'NONE',  ( 1.000000000000000000, -0.000000000000000000, 0.000000000000000000 ) ) ;
#14317=AXIS2_PLACEMENT_3D ( 'NONE', #214032, #212754, #116230 ) ;
#14335=DIRECTION ( 'NONE',  ( 0.000000000000000000, -7.429790795770647916E-15, 1.000000000000000000 ) ) ;
#14341=VERTEX_POINT ( 'NONE', #158814 ) ;
#14387=AXIS2_PLACEMENT_3D ( 'NONE', #11428, #132652, #250024 ) ;
#14394=DIRECTION ( 'NONE',  ( -1.000000000000000000, 0.000000000000000000, -0.000000000000000000 ) ) ;
#14403=ORIENTED_EDGE ( 'NONE', *, *, #59677, .F. ) ;
#14421=AXIS2_PLACEMENT_3D ( 'NONE', #68066, #126752, #105876 ) ;
#14431=CARTESIAN_POINT ( 'NONE',  ( -21.33487959338958362, 69.27444184810076422, -103.0231074845243597 ) ) ;
#14456=CARTESIAN_POINT ( 'NONE',  ( -21.05000000000000071, 64.35000000001190301, -96.23924182154622997 ) ) ;
#14524=ORIENTED_EDGE ( 'NONE', *, *, #66572, .T. ) ;
#14553=CIRCLE ( 'NONE', #160311, 0.6000000000000033085 ) ;
#14583=CARTESIAN_POINT ( 'NONE',  ( 20.94999999999999574, 87.65000000001192859, -100.1231074845242262 ) ) ;
#14617=EDGE_LOOP ( 'NONE', ( #12692, #159466, #160875, #86077 ) ) ;
#14680=DIRECTION ( 'NONE',  ( 0.000000000000000000, 6.982962677686266711E-15, -1.000000000000000000 ) ) ;
#14702=CARTESIAN_POINT ( 'NONE',  ( 21.07954640115298162, 75.93399229287234675, -109.3523951805481573 ) ) ;
#14721=ORIENTED_EDGE ( 'NONE', *, *, #250746, .T. ) ;
#14743=DIRECTION ( 'NONE',  ( -1.000000000000000000, 0.000000000000000000, -0.000000000000000000 ) ) ;
#14777=ORIENTED_EDGE ( 'NONE', *, *, #43192, .T. ) ;
#14784=CARTESIAN_POINT ( 'NONE',  ( 21.30000000000002558, 76.00000000001195133, -103.0231074845243171 ) ) ;
#14790=CARTESIAN_POINT ( 'NONE',  ( 21.06600267594171783, 67.22483393081196823, -90.81884470214961880 ) ) ;
#14791=ORIENTED_EDGE ( 'NONE', *, *, #114109, .F. ) ;
#14811=CARTESIAN_POINT ( 'NONE',  ( -23.15000000000000213, 87.48912529308779540, -72.62310748452422615 ) ) ;
#14822=AXIS2_PLACEMENT_3D ( 'NONE', #84367, #223914, #13879 ) ;
#14825=ORIENTED_EDGE ( 'NONE', *, *, #231444, .F. ) ;
#14850=EDGE_LOOP ( 'NONE', ( #189057, #86213, #43522, #238866 ) ) ;
#14864=ORIENTED_EDGE ( 'NONE', *, *, #112067, .T. ) ;
#14869=EDGE_CURVE ( 'NONE', #61048, #224619, #212702, .T. ) ;
#14886=DIRECTION ( 'NONE',  ( -1.000000000000000000, 0.000000000000000000, -0.000000000000000000 ) ) ;
#14909=CARTESIAN_POINT ( 'NONE',  ( -18.51024323315077424, 65.68895814178220860, -64.00265578621379348 ) ) ;
#14918=DIRECTION ( 'NONE',  ( 1.000000000000000000, -3.265361837132813093E-16, -2.280189983783949500E-30 ) ) ;
#14922=CARTESIAN_POINT ( 'NONE',  ( -18.59999999999999787, 66.65000000001180069, -81.77310748452437394 ) ) ;
#14926=CARTESIAN_POINT ( 'NONE',  ( 23.24999999999999289, 64.25000000001185185, -90.87310748452438247 ) ) ;
#14933=EDGE_CURVE ( 'NONE', #232638, #155954, #51, .T. ) ;
#14957=CIRCLE ( 'NONE', #119021, 0.1000000000000028644 ) ;
#14965=CARTESIAN_POINT ( 'NONE',  ( -21.05000000000000071, 77.16270174994990327, -94.92310748452430857 ) ) ;
#14984=EDGE_CURVE ( 'NONE', #116632, #69997, #87281, .T. ) ;
#14991=ORIENTED_EDGE ( 'NONE', *, *, #168902, .F. ) ;
#15005=CARTESIAN_POINT ( 'NONE',  ( 22.39999999999999858, 75.90000000001199965, -110.8138870828976934 ) ) ;
#15015=FACE_OUTER_BOUND ( 'NONE', #110839, .T. ) ;
#15043=FACE_OUTER_BOUND ( 'NONE', #176238, .T. ) ;
#15048=ORIENTED_EDGE ( 'NONE', *, *, #178913, .T. ) ;
#15053=CIRCLE ( 'NONE', #115179, 0.09999999999999939493 ) ;
#15072=DIRECTION ( 'NONE',  ( -1.000000000000000000, 2.952720810173289112E-16, 2.061873921506763405E-30 ) ) ;
#15076=CARTESIAN_POINT ( 'NONE',  ( 18.46932045258648714, 85.67068520027744682, -62.84924711152763166 ) ) ;
#15101=EDGE_CURVE ( 'NONE', #159653, #154400, #256506, .T. ) ;
#15104=ORIENTED_EDGE ( 'NONE', *, *, #162087, .T. ) ;
#15132=( BOUNDED_SURFACE ( )  B_SPLINE_SURFACE ( 3, 2, ( 
 ( #182559, #243794, #123859 ),
 ( #104262, #144679, #203393 ),
 ( #183819, #65147, #186405 ),
 ( #208538, #12917, #191553 ) ),
 .UNSPECIFIED., .F., .F., .F. ) 
 B_SPLINE_SURFACE_WITH_KNOTS ( ( 4, 4 ),
 ( 3, 3 ),
 ( 0.04058434257139457990, 0.04256401539001584966 ),
 ( 0.000000000000000000, 1.000000000000000000 ),
 .UNSPECIFIED. ) 
 GEOMETRIC_REPRESENTATION_ITEM ( )  RATIONAL_B_SPLINE_SURFACE ( (
 ( 1.000000000000000000, 0.7103081912008383236, 1.000000000000000000),
 ( 1.000000000000000000, 0.7104998333555154755, 1.000000000000000000),
 ( 1.000000000000000000, 0.7107238315755263214, 1.000000000000000000),
 ( 1.000000000000000000, 0.7110073749539205235, 1.000000000000000000) ) ) 
 REPRESENTATION_ITEM ( '' )  SURFACE ( )  );
#15133=CARTESIAN_POINT ( 'NONE',  ( -22.50000000000000000, 64.35023708198002623, -103.1119174609113145 ) ) ;
#15149=DIRECTION ( 'NONE',  ( -0.000000000000000000, -1.000000000000000000, -6.982962677686266711E-15 ) ) ;
#15205=DIRECTION ( 'NONE',  ( 1.000000000000000000, 0.000000000000000000, 0.000000000000000000 ) ) ;
#15207=ORIENTED_EDGE ( 'NONE', *, *, #96816, .T. ) ;
#15220=ADVANCED_FACE ( 'NONE', ( #233260 ), #114925, .F. ) ;
#15301=ORIENTED_EDGE ( 'NONE', *, *, #59030, .T. ) ;
#15316=DIRECTION ( 'NONE',  ( 1.000000000000000000, -0.000000000000000000, 0.000000000000000000 ) ) ;
#15327=DIRECTION ( 'NONE',  ( 1.000000000000000000, 0.000000000000000000, 0.000000000000000000 ) ) ;
#15331=ORIENTED_EDGE ( 'NONE', *, *, #160148, .F. ) ;
#15373=CARTESIAN_POINT ( 'NONE',  ( 20.94999999999999929, 70.60000000001186038, -90.61784146561124942 ) ) ;
#15395=ADVANCED_FACE ( 'NONE', ( #243487 ), #111445, .T. ) ;
#15411=FACE_OUTER_BOUND ( 'NONE', #18535, .T. ) ;
#15418=AXIS2_PLACEMENT_3D ( 'NONE', #94217, #192069, #55073 ) ;
#15425=CIRCLE ( 'NONE', #161350, 0.1000000000000028644 ) ;
#15430=DIRECTION ( 'NONE',  ( -1.836970198721029934E-16, -1.000000000000000000, -6.982962677686266711E-15 ) ) ;
#15439=CARTESIAN_POINT ( 'NONE',  ( 21.13422380239054732, 69.50667348520630640, -103.0231074845243597 ) ) ;
#15461=ORIENTED_EDGE ( 'NONE', *, *, #228679, .F. ) ;
#15466=DIRECTION ( 'NONE',  ( 0.000000000000000000, -7.147358527629766941E-15, 1.000000000000000000 ) ) ;
#15469=PRODUCT_DEFINITION_FORMATION_WITH_SPECIFIED_SOURCE ( 'ANY', '', #14100, .NOT_KNOWN. ) ;
#15501=CIRCLE ( 'NONE', #65353, 0.09999999999999971412 ) ;
#15505=DIRECTION ( 'NONE',  ( 2.952720810173289112E-16, 1.000000000000000000, -6.088138035986627436E-46 ) ) ;
#15555=DIRECTION ( 'NONE',  ( 0.000000000000000000, 7.116814260417668513E-15, -1.000000000000000000 ) ) ;
#15580=ORIENTED_EDGE ( 'NONE', *, *, #163663, .T. ) ;
#15602=DIRECTION ( 'NONE',  ( 1.000000000000000000, 0.000000000000000000, 0.000000000000000000 ) ) ;
#15605=EDGE_CURVE ( 'NONE', #243331, #92348, #149555, .T. ) ;
#15669=AXIS2_PLACEMENT_3D ( 'NONE', #129632, #30555, #90493 ) ;
#15675=EDGE_CURVE ( 'NONE', #229949, #161543, #6951, .T. ) ;
#15676=AXIS2_PLACEMENT_3D ( 'NONE', #236906, #23028, #42553 ) ;
#15763=DIRECTION ( 'NONE',  ( 0.000000000000000000, 0.000000000000000000, 1.000000000000000000 ) ) ;
#15788=AXIS2_PLACEMENT_3D ( 'NONE', #223456, #46112, #180504 ) ;
#15835=DIRECTION ( 'NONE',  ( 1.000000000000000000, 0.000000000000000000, 0.000000000000000000 ) ) ;
#15841=DIRECTION ( 'NONE',  ( 2.715809747126117987E-16, 1.000000000000000000, 7.604267291953130166E-15 ) ) ;
#15842=CIRCLE ( 'NONE', #86505, 0.1000000000000028644 ) ;
#15857=EDGE_CURVE ( 'NONE', #193457, #29920, #232014, .T. ) ;
#15885=DIRECTION ( 'NONE',  ( 0.000000000000000000, -1.000000000000000000, 0.000000000000000000 ) ) ;
#15892=EDGE_LOOP ( 'NONE', ( #83183, #205712, #155994, #203197 ) ) ;
#15913=CARTESIAN_POINT ( 'NONE',  ( 20.94999999999999929, 76.00000000001195133, -103.0231074845243171 ) ) ;
#15928=DIRECTION ( 'NONE',  ( 1.000000000000000000, 0.000000000000000000, 0.000000000000000000 ) ) ;
#15969=ADVANCED_FACE ( 'NONE', ( #187087 ), #111200, .T. ) ;
#15977=ORIENTED_EDGE ( 'NONE', *, *, #225619, .T. ) ;
#16021=AXIS2_PLACEMENT_3D ( 'NONE', #145026, #27703, #242851 ) ;
#16024=DIRECTION ( 'NONE',  ( 0.000000000000000000, -1.000000000000000000, -6.982962677686265922E-15 ) ) ;
#16037=EDGE_LOOP ( 'NONE', ( #86342, #76349, #203770, #158557 ) ) ;
#16048=ADVANCED_FACE ( 'NONE', ( #56514 ), #33170, .F. ) ;
#16055=DIRECTION ( 'NONE',  ( 1.000000000000000000, 0.000000000000000000, 0.000000000000000000 ) ) ;
#16074=CARTESIAN_POINT ( 'NONE',  ( -18.50000000000000000, 64.25000000001179501, -81.67310748452439384 ) ) ;
#16081=DIRECTION ( 'NONE',  ( 0.000000000000000000, 0.000000000000000000, 1.000000000000000000 ) ) ;
#16116=CARTESIAN_POINT ( 'NONE',  ( 22.49231231312463208, 64.35001509633467265, -103.0841603721257655 ) ) ;
#16127=EDGE_CURVE ( 'NONE', #603, #32631, #144491, .T. ) ;
#16177=VERTEX_POINT ( 'NONE', #143773 ) ;
#16184=ORIENTED_EDGE ( 'NONE', *, *, #220862, .T. ) ;
#16197=DIRECTION ( 'NONE',  ( 0.000000000000000000, -0.9998779222360104635, -0.01562499999996343723 ) ) ;
#16254=TOROIDAL_SURFACE ( 'NONE', #162008, 11.65000000000000036, 0.1000000000000000056 ) ;
#16280=EDGE_CURVE ( 'NONE', #256668, #190582, #10701, .T. ) ;
#16281=AXIS2_PLACEMENT_3D ( 'NONE', #202487, #122958, #98202 ) ;
#16286=CARTESIAN_POINT ( 'NONE',  ( 21.14999999999999858, 76.00000000001195133, -102.9231074845243228 ) ) ;
#16311=DIRECTION ( 'NONE',  ( -0.000000000000000000, -6.982962677686266711E-15, 1.000000000000000000 ) ) ;
#16320=VECTOR ( 'NONE', #253957, 1000.000000000000000 ) ;
#16324=CIRCLE ( 'NONE', #182912, 6.258578643762710669 ) ;
#16345=AXIS2_PLACEMENT_3D ( 'NONE', #170391, #172949, #30856 ) ;
#16350=ORIENTED_EDGE ( 'NONE', *, *, #8978, .F. ) ;
#16379=DIRECTION ( 'NONE',  ( 0.000000000000000000, 6.982962677686266711E-15, -1.000000000000000000 ) ) ;
#16400=EDGE_CURVE ( 'NONE', #56290, #38211, #6840, .T. ) ;
#16404=LINE ( 'NONE', #249860, #50320 ) ;
#16422=DIRECTION ( 'NONE',  ( 0.000000000000000000, 1.000000000000000000, 6.853228547068871147E-15 ) ) ;
#16429=EDGE_CURVE ( 'NONE', #156170, #173939, #232211, .T. ) ;
#16439=VERTEX_POINT ( 'NONE', #160179 ) ;
#16484=DIRECTION ( 'NONE',  ( -1.000000000000000000, 0.000000000000000000, 0.000000000000000000 ) ) ;
#16517=SPHERICAL_SURFACE ( 'NONE', #90130, 0.1000000000000000056 ) ;
#16531=DIRECTION ( 'NONE',  ( 1.000000000000000000, 0.000000000000000000, 0.000000000000000000 ) ) ;
#16536=VERTEX_POINT ( 'NONE', #102711 ) ;
#16537=VERTEX_POINT ( 'NONE', #103994 ) ;
#16538=ORIENTED_EDGE ( 'NONE', *, *, #104654, .T. ) ;
#16550=DIRECTION ( 'NONE',  ( 1.000000000000000000, 0.000000000000000000, 0.000000000000000000 ) ) ;
#16562=DIRECTION ( 'NONE',  ( 0.000000000000000000, 1.000000000000000000, 6.982962677686266711E-15 ) ) ;
#16571=AXIS2_PLACEMENT_3D ( 'NONE', #231489, #32014, #30736 ) ;
#16575=CARTESIAN_POINT ( 'NONE',  ( 20.94999999999999929, 70.60000000001180354, -81.92837350343744163 ) ) ;
#16602=ORIENTED_EDGE ( 'NONE', *, *, #166306, .T. ) ;
#16624=LINE ( 'NONE', #248814, #253801 ) ;
#16659=CARTESIAN_POINT ( 'NONE',  ( -21.14999999999999858, 76.00000000001203659, -114.6726782920691221 ) ) ;
#16664=CIRCLE ( 'NONE', #133178, 0.09999999999999939493 ) ;
#16671=ADVANCED_FACE ( 'NONE', ( #251220 ), #13923, .F. ) ;
#16679=DIRECTION ( 'NONE',  ( -0.000000000000000000, 6.982962677686266711E-15, -1.000000000000000000 ) ) ;
#16692=AXIS2_PLACEMENT_3D ( 'NONE', #48054, #105423, #70222 ) ;
#16700=LINE ( 'NONE', #12855, #76187 ) ;
#16720=CARTESIAN_POINT ( 'NONE',  ( 21.05000000000000071, 69.69548367074791884, -103.0020041764652063 ) ) ;
#16721=VERTEX_POINT ( 'NONE', #231693 ) ;
#16725=LINE ( 'NONE', #50675, #6906 ) ;
#16742=DIRECTION ( 'NONE',  ( -0.7071067811865475727, 0.7071067811865475727, 4.937700262164531476E-15 ) ) ;
#16758=ORIENTED_EDGE ( 'NONE', *, *, #80399, .F. ) ;
#16775=CARTESIAN_POINT ( 'NONE',  ( 22.50497660315936699, 76.07871793023755913, -114.7729029894197339 ) ) ;
#16781=DIRECTION ( 'NONE',  ( 0.000000000000000000, -6.982962677686266711E-15, 1.000000000000000000 ) ) ;
#16783=DIRECTION ( 'NONE',  ( 0.000000000000000000, -0.1350103645451807555, -0.9908441862701610203 ) ) ;
#16785=CARTESIAN_POINT ( 'NONE',  ( 23.15000000000000213, 85.00000000001188027, -93.12913836187181005 ) ) ;
#16787=CARTESIAN_POINT ( 'NONE',  ( -20.64999999999999858, 73.50000000001180922, -82.74772940728642823 ) ) ;
#16819=EDGE_LOOP ( 'NONE', ( #247055, #240239, #145425, #113716 ) ) ;
#16842=ORIENTED_EDGE ( 'NONE', *, *, #198126, .T. ) ;
#16868=ADVANCED_FACE ( 'NONE', ( #21626 ), #125838, .T. ) ;
#16890=CARTESIAN_POINT ( 'NONE',  ( 21.11701782572533048, 65.27839088400440914, -90.77807005501317406 ) ) ;
#16892=CARTESIAN_POINT ( 'NONE',  ( -18.59999999999999787, 85.48068669529064323, -62.58199231576639932 ) ) ;
#16932=AXIS2_PLACEMENT_3D ( 'NONE', #256502, #213584, #75399 ) ;
#16953=B_SPLINE_CURVE_WITH_KNOTS ( 'NONE', 3,
 ( #227050, #246612, #127965, #88805, #247900, #69285 ),
 .UNSPECIFIED., .F., .F.,
 ( 4, 2, 4 ),
 ( 0.000000000000000000, 0.0002113392456165985155, 0.0004226784912331970311 ),
 .UNSPECIFIED. ) ;
#16959=DIRECTION ( 'NONE',  ( 1.000000000000000000, 0.000000000000000000, 0.000000000000000000 ) ) ;
#16963=EDGE_CURVE ( 'NONE', #252190, #157610, #211521, .T. ) ;
#17012=ORIENTED_EDGE ( 'NONE', *, *, #173561, .T. ) ;
#17035=CARTESIAN_POINT ( 'NONE',  ( 23.15000000000000213, 85.50000000001179501, -79.41707660717668205 ) ) ;
#17042=CARTESIAN_POINT ( 'NONE',  ( 18.49999999999999289, 65.50857864377445594, -78.17310748452437963 ) ) ;
#17083=ORIENTED_EDGE ( 'NONE', *, *, #61616, .F. ) ;
#17094=DIRECTION ( 'NONE',  ( 0.000000000000000000, 1.000000000000000000, 0.000000000000000000 ) ) ;
#17122=ORIENTED_EDGE ( 'NONE', *, *, #137893, .T. ) ;
#17131=AXIS2_PLACEMENT_3D ( 'NONE', #61943, #120651, #257503 ) ;
#17151=DIRECTION ( 'NONE',  ( 0.000000000000000000, 6.982962677686266711E-15, -1.000000000000000000 ) ) ;
#17176=ORIENTED_EDGE ( 'NONE', *, *, #242687, .T. ) ;
#17180=ORIENTED_EDGE ( 'NONE', *, *, #102635, .T. ) ;
#17209=DIRECTION ( 'NONE',  ( 0.000000000000000000, 6.982962677686266711E-15, -1.000000000000000000 ) ) ;
#17215=CARTESIAN_POINT ( 'NONE',  ( -23.24999999999999645, 85.60000000001166143, -62.82291809330219223 ) ) ;
#17307=EDGE_LOOP ( 'NONE', ( #109049, #160124, #146554, #241321, #188780, #181521, #137982, #122356, #169313, #97415, #125828, #203504, #148462, #217882, #31061, #129330, #143807, #22161, #55229, #237576, #49712, #143657, #110303, #180685, #227848 ) ) ;
#17308=CARTESIAN_POINT ( 'NONE',  ( -20.94999999999999929, 68.92903212821283887, -65.77654326265606244 ) ) ;
#17324=VERTEX_POINT ( 'NONE', #68172 ) ;
#17353=EDGE_LOOP ( 'NONE', ( #86560, #58983, #96955, #119435 ) ) ;
#17394=ORIENTED_EDGE ( 'NONE', *, *, #28833, .T. ) ;
#17451=DIRECTION ( 'NONE',  ( 0.000000000000000000, 0.000000000000000000, 1.000000000000000000 ) ) ;
#17478=AXIS2_PLACEMENT_3D ( 'NONE', #131396, #212243, #252620 ) ;
#17487=DIRECTION ( 'NONE',  ( -1.000000000000000000, 0.000000000000000000, -0.000000000000000000 ) ) ;
#17496=CARTESIAN_POINT ( 'NONE',  ( 18.49999999999999289, 64.35000000001177511, -78.17310748452437963 ) ) ;
#17499=VERTEX_POINT ( 'NONE', #122732 ) ;
#17548=ADVANCED_FACE ( 'NONE', ( #61452 ), #5292, .T. ) ;
#17611=DIRECTION ( 'NONE',  ( -0.000000000000000000, -6.982962677686266711E-15, 1.000000000000000000 ) ) ;
#17631=ORIENTED_EDGE ( 'NONE', *, *, #136694, .F. ) ;
#17656=DIRECTION ( 'NONE',  ( 1.000000000000000000, 0.000000000000000000, 0.000000000000000000 ) ) ;
#17675=VECTOR ( 'NONE', #253322, 1000.000000000000000 ) ;
#17693=ORIENTED_EDGE ( 'NONE', *, *, #225619, .F. ) ;
#17758=FACE_OUTER_BOUND ( 'NONE', #67536, .T. ) ;
#17825=LINE ( 'NONE', #98616, #52413 ) ;
#17845=CARTESIAN_POINT ( 'NONE',  ( 21.30000000000002558, 76.00000000001197975, -107.0731074845243143 ) ) ;
#17850=FACE_OUTER_BOUND ( 'NONE', #63500, .T. ) ;
#17853=VERTEX_POINT ( 'NONE', #143232 ) ;
#17856=DIRECTION ( 'NONE',  ( 2.840903330521633255E-16, 0.8700118002898357128, -0.4930308989875171188 ) ) ;
#17877=DIRECTION ( 'NONE',  ( 0.000000000000000000, -0.9274965247785504907, -0.3738317757009320674 ) ) ;
#17896=EDGE_CURVE ( 'NONE', #119060, #201799, #139370, .T. ) ;
#17898=CIRCLE ( 'NONE', #76156, 0.1000000000000028644 ) ;
#17911=CARTESIAN_POINT ( 'NONE',  ( -22.39999999999999858, 64.35000000001195986, -103.0231074845244024 ) ) ;
#17916=CYLINDRICAL_SURFACE ( 'NONE', #146382, 2.000000000000001776 ) ;
#17959=ORIENTED_EDGE ( 'NONE', *, *, #59048, .T. ) ;
#17979=CARTESIAN_POINT ( 'NONE',  ( -20.64999999999999858, 71.65000000001180069, -81.77310748452433131 ) ) ;
#17981=ORIENTED_EDGE ( 'NONE', *, *, #14984, .T. ) ;
#18007=AXIS2_PLACEMENT_3D ( 'NONE', #185776, #1986, #201475 ) ;
#18017=EDGE_CURVE ( 'NONE', #202146, #197574, #187531, .T. ) ;
#18031=AXIS2_PLACEMENT_3D ( 'NONE', #236705, #135029, #196302 ) ;
#18073=CARTESIAN_POINT ( 'NONE',  ( -18.50000000000000000, 66.75000000001185185, -90.67310748452436542 ) ) ;
#18082=DIRECTION ( 'NONE',  ( 0.000000000000000000, 0.000000000000000000, 1.000000000000000000 ) ) ;
#18095=ORIENTED_EDGE ( 'NONE', *, *, #77801, .T. ) ;
#18112=CARTESIAN_POINT ( 'NONE',  ( 20.94999999999999574, 74.16465844978745281, -91.46795619196133487 ) ) ;
#18194=DIRECTION ( 'NONE',  ( 0.000000000000000000, 0.000000000000000000, -1.000000000000000000 ) ) ;
#18198=DIRECTION ( 'NONE',  ( -0.000000000000000000, 0.1350103645451945777, -0.9908441862701590219 ) ) ;
#18215=DIRECTION ( 'NONE',  ( 1.000000000000000000, 0.000000000000000000, 0.000000000000000000 ) ) ;
#18236=EDGE_CURVE ( 'NONE', #3343, #170827, #37437, .T. ) ;
#18237=CARTESIAN_POINT ( 'NONE',  ( 20.95512820512820440, 65.37615131629998189, -90.87310748452438247 ) ) ;
#18242=CARTESIAN_POINT ( 'NONE',  ( -18.49999999999997158, 85.32100840337318459, -95.78716923544637041 ) ) ;
#18314=TOROIDAL_SURFACE ( 'NONE', #176551, 4.099999999999999645, 0.1000000000000000056 ) ;
#18327=DIRECTION ( 'NONE',  ( 1.836970198721029934E-16, 1.000000000000000000, 6.982962677686266711E-15 ) ) ;
#18332=AXIS2_PLACEMENT_3D ( 'NONE', #22851, #183194, #123208 ) ;
#18341=CARTESIAN_POINT ( 'NONE',  ( -21.05000000000000071, 74.73821383144687047, -94.93660852097883662 ) ) ;
#18353=ORIENTED_EDGE ( 'NONE', *, *, #142074, .T. ) ;
#18363=AXIS2_PLACEMENT_3D ( 'NONE', #41905, #221767, #171806 ) ;
#18369=ORIENTED_EDGE ( 'NONE', *, *, #84584, .T. ) ;
#18375=AXIS2_PLACEMENT_3D ( 'NONE', #71057, #166322, #29382 ) ;
#18399=CARTESIAN_POINT ( 'NONE',  ( 21.05000000000000071, 64.40000000001175806, -76.45131071479988805 ) ) ;
#18436=VERTEX_POINT ( 'NONE', #89359 ) ;
#18443=CARTESIAN_POINT ( 'NONE',  ( -18.50000000000000711, 85.41920341803854910, -95.77532167409560770 ) ) ;
#18446=ORIENTED_EDGE ( 'NONE', *, *, #211998, .T. ) ;
#18453=FACE_OUTER_BOUND ( 'NONE', #223939, .T. ) ;
#18460=DIRECTION ( 'NONE',  ( 0.000000000000000000, 1.000000000000000000, 0.000000000000000000 ) ) ;
#18466=VERTEX_POINT ( 'NONE', #112799 ) ;
#18503=AXIS2_PLACEMENT_3D ( 'NONE', #130240, #131533, #11609 ) ;
#18512=CARTESIAN_POINT ( 'NONE',  ( 20.94999999999999929, 76.00000000001170974, -69.52310748452431710 ) ) ;
#18525=DIRECTION ( 'NONE',  ( 0.000000000000000000, -1.000000000000000000, -6.982962677686266711E-15 ) ) ;
#18535=EDGE_LOOP ( 'NONE', ( #1421, #12074, #22889, #237767 ) ) ;
#18544=EDGE_LOOP ( 'NONE', ( #229751, #65742, #190842, #17083 ) ) ;
#18551=ORIENTED_EDGE ( 'NONE', *, *, #180633, .T. ) ;
#18562=DIRECTION ( 'NONE',  ( 1.000000000000000000, 0.000000000000000000, 0.000000000000000000 ) ) ;
#18569=CARTESIAN_POINT ( 'NONE',  ( 21.12400247839515899, 65.27851195598147171, -90.77310748452438816 ) ) ;
#18601=CARTESIAN_POINT ( 'NONE',  ( -21.05000000000000071, 61.95000000001191154, -97.50941241376341395 ) ) ;
#18637=ADVANCED_FACE ( 'NONE', ( #116642 ), #196181, .T. ) ;
#18719=DIRECTION ( 'NONE',  ( -1.000000000000000000, -0.000000000000000000, -0.000000000000000000 ) ) ;
#18721=CARTESIAN_POINT ( 'NONE',  ( -21.05000000000000071, 74.75000000001189449, -95.02310748452431710 ) ) ;
#18752=CYLINDRICAL_SURFACE ( 'NONE', #181863, 11.80000000000000426 ) ;
#18771=AXIS2_PLACEMENT_3D ( 'NONE', #127435, #4889, #85697 ) ;
#18786=FACE_OUTER_BOUND ( 'NONE', #179225, .T. ) ;
#18816=ORIENTED_EDGE ( 'NONE', *, *, #87612, .T. ) ;
#18842=DIRECTION ( 'NONE',  ( -1.000000000000000000, 0.000000000000000000, -0.000000000000000000 ) ) ;
#18857=SPHERICAL_SURFACE ( 'NONE', #111804, 0.1000000000000000056 ) ;
#18885=VECTOR ( 'NONE', #116506, 1000.000000000000000 ) ;
#18900=VERTEX_POINT ( 'NONE', #139416 ) ;
#18913=ORIENTED_EDGE ( 'NONE', *, *, #114941, .T. ) ;
#18935=VECTOR ( 'NONE', #98725, 1000.000000000000000 ) ;
#18973=DIRECTION ( 'NONE',  ( 0.000000000000000000, -7.086529944415894657E-15, 1.000000000000000000 ) ) ;
#18991=CARTESIAN_POINT ( 'NONE',  ( -20.64999999999999858, 76.00000000001195133, -103.0231074845243171 ) ) ;
#19014=EDGE_CURVE ( 'NONE', #158859, #124985, #168031, .T. ) ;
#19022=EDGE_CURVE ( 'NONE', #182384, #10704, #224098, .T. ) ;
#19041=CARTESIAN_POINT ( 'NONE',  ( 20.95443524775735256, 67.12144573613906573, -94.48938520892421877 ) ) ;
#19060=CYLINDRICAL_SURFACE ( 'NONE', #111366, 0.1000000000000028644 ) ;
#19068=ORIENTED_EDGE ( 'NONE', *, *, #243088, .T. ) ;
#19069=ORIENTED_EDGE ( 'NONE', *, *, #157422, .F. ) ;
#19079=EDGE_LOOP ( 'NONE', ( #157306, #32382, #196079, #34169 ) ) ;
#19094=ORIENTED_EDGE ( 'NONE', *, *, #126746, .F. ) ;
#19118=ORIENTED_EDGE ( 'NONE', *, *, #176937, .F. ) ;
#19132=DIRECTION ( 'NONE',  ( 0.000000000000000000, -7.056502275159890043E-15, 1.000000000000000000 ) ) ;
#19183=ADVANCED_FACE ( 'NONE', ( #119584 ), #16254, .T. ) ;
#19196=DIRECTION ( 'NONE',  ( -0.000000000000000000, 6.982962677686266711E-15, -1.000000000000000000 ) ) ;
#19217=VECTOR ( 'NONE', #69922, 1000.000000000000114 ) ;
#19224=CARTESIAN_POINT ( 'NONE',  ( 21.05000000000000071, 70.50000000001180922, -81.92837350343744163 ) ) ;
#19231=CARTESIAN_POINT ( 'NONE',  ( -20.94999999999999929, 87.41227409416161720, -100.0231074845242318 ) ) ;
#19262=DIRECTION ( 'NONE',  ( 0.000000000000000000, -7.086529944415894657E-15, 1.000000000000000000 ) ) ;
#19266=DIRECTION ( 'NONE',  ( 0.000000000000000000, -6.982962677686266711E-15, 1.000000000000000000 ) ) ;
#19320=DIRECTION ( 'NONE',  ( 1.000000000000000000, -0.000000000000000000, 0.000000000000000000 ) ) ;
#19352=FACE_OUTER_BOUND ( 'NONE', #118220, .T. ) ;
#19373=ORIENTED_EDGE ( 'NONE', *, *, #152507, .T. ) ;
#19393=CARTESIAN_POINT ( 'NONE',  ( -21.44999999999999929, 68.75000000001185185, -90.67310748452436542 ) ) ;
#19396=ORIENTED_EDGE ( 'NONE', *, *, #223282, .F. ) ;
#19419=DIRECTION ( 'NONE',  ( 0.000000000000000000, -0.01562499999996343723, -0.9998779222360104635 ) ) ;
#19427=EDGE_LOOP ( 'NONE', ( #256072, #100960, #66818, #233692 ) ) ;
#19441=LINE ( 'NONE', #156416, #70676 ) ;
#19444=VECTOR ( 'NONE', #10018, 1000.000000000000000 ) ;
#19447=CARTESIAN_POINT ( 'NONE',  ( -20.64999999999999858, 68.75000000001185185, -90.67310748452436542 ) ) ;
#19474=EDGE_CURVE ( 'NONE', #202146, #107897, #87783, .T. ) ;
#19520=CARTESIAN_POINT ( 'NONE',  ( 18.52351027002948314, 85.64216290470682225, -62.80806053401445865 ) ) ;
#19521=FACE_OUTER_BOUND ( 'NONE', #6472, .T. ) ;
#19527=DIRECTION ( 'NONE',  ( 0.000000000000000000, -0.5000000000000016653, 0.8660254037844377084 ) ) ;
#19529=ADVANCED_FACE ( 'NONE', ( #171557 ), #137659, .T. ) ;
#19535=CARTESIAN_POINT ( 'NONE',  ( -18.51991288638525646, 85.39243678968526297, -95.87984108056610921 ) ) ;
#19541=VERTEX_POINT ( 'NONE', #150683 ) ;
#19546=CARTESIAN_POINT ( 'NONE',  ( -23.15000000000000213, 76.00000000001170974, -69.52310748452431710 ) ) ;
#19550=AXIS2_PLACEMENT_3D ( 'NONE', #50308, #143329, #65081 ) ;
#19593=DIRECTION ( 'NONE',  ( 0.000000000000000000, 0.8660254037844424824, 0.4999999999999934497 ) ) ;
#19605=DIRECTION ( 'NONE',  ( -0.000000000000000000, 6.982962677686266711E-15, -1.000000000000000000 ) ) ;
#19633=CARTESIAN_POINT ( 'NONE',  ( 20.94999999999999574, 67.07338541492480033, -94.55142446530125255 ) ) ;
#19634=ORIENTED_EDGE ( 'NONE', *, *, #154555, .F. ) ;
#19700=DIRECTION ( 'NONE',  ( 2.879366945564059217E-14, 0.9875055080513762684, -0.1575844902526679081 ) ) ;
#19707=FACE_OUTER_BOUND ( 'NONE', #30932, .T. ) ;
#19710=ADVANCED_FACE ( 'NONE', ( #167397 ), #143941, .T. ) ;
#19729=SPHERICAL_SURFACE ( 'NONE', #56424, 0.1000000000000000056 ) ;
#19789=CIRCLE ( 'NONE', #69675, 0.1000000000000028644 ) ;
#19792=ORIENTED_EDGE ( 'NONE', *, *, #35804, .T. ) ;
#19863=CARTESIAN_POINT ( 'NONE',  ( 18.49999999999998934, 69.55000000001187743, -93.00608031408432907 ) ) ;
#19934=TOROIDAL_SURFACE ( 'NONE', #82420, 0.2000000000000000111, 0.1000000000000000056 ) ;
#19977=CARTESIAN_POINT ( 'NONE',  ( -18.31572283045156269, 85.54843783089712872, -62.67248183346567458 ) ) ;
#19978=CARTESIAN_POINT ( 'NONE',  ( 22.00411653962182612, 68.74655713164194992, -103.1221455903250188 ) ) ;
#19998=DIRECTION ( 'NONE',  ( 0.000000000000000000, -1.000000000000000000, -8.717686153663073805E-15 ) ) ;
#20021=CARTESIAN_POINT ( 'NONE',  ( -21.55000000000000426, 68.25000000001179501, -81.77310748452435973 ) ) ;
#20024=CARTESIAN_POINT ( 'NONE',  ( -23.15000000000000213, 84.59626168225477727, -78.97323500167452437 ) ) ;
#20026=VERTEX_POINT ( 'NONE', #255844 ) ;
#20030=VERTEX_POINT ( 'NONE', #99362 ) ;
#20035=CARTESIAN_POINT ( 'NONE',  ( 23.14999999999999858, 76.00000000001170974, -69.52310748452431710 ) ) ;
#20039=CARTESIAN_POINT ( 'NONE',  ( 21.05000000000000071, 87.48912529308779540, -72.62310748452422615 ) ) ;
#20048=VERTEX_POINT ( 'NONE', #201055 ) ;
#20094=LINE ( 'NONE', #244250, #65688 ) ;
#20115=EDGE_LOOP ( 'NONE', ( #170389, #106133, #80148, #8979 ) ) ;
#20129=CIRCLE ( 'NONE', #249267, 11.74999999999999645 ) ;
#20148=ORIENTED_EDGE ( 'NONE', *, *, #151761, .F. ) ;
#20159=DIRECTION ( 'NONE',  ( -1.000000000000000000, 0.000000000000000000, 0.000000000000000000 ) ) ;
#20209=ORIENTED_EDGE ( 'NONE', *, *, #137688, .F. ) ;
#20230=AXIS2_PLACEMENT_3D ( 'NONE', #108640, #13406, #190782 ) ;
#20238=VERTEX_POINT ( 'NONE', #190507 ) ;
#20257=CARTESIAN_POINT ( 'NONE',  ( -23.15000000000000213, 64.35000000001176090, -76.53791325517833855 ) ) ;
#20265=ORIENTED_EDGE ( 'NONE', *, *, #108019, .F. ) ;
#20279=EDGE_LOOP ( 'NONE', ( #139391, #76055, #1369 ) ) ;
#20291=ADVANCED_FACE ( 'NONE', ( #144458 ), #177999, .F. ) ;
#20308=EDGE_CURVE ( 'NONE', #146049, #82068, #182275, .T. ) ;
#20313=EDGE_CURVE ( 'NONE', #164805, #114552, #215574, .T. ) ;
#20315=ORIENTED_EDGE ( 'NONE', *, *, #110811, .T. ) ;
#20318=CARTESIAN_POINT ( 'NONE',  ( 20.94999999999999574, 77.16270174994990327, -94.92310748452430857 ) ) ;
#20322=CARTESIAN_POINT ( 'NONE',  ( -18.59999999999999787, 76.00000000001195133, -103.0231074845243171 ) ) ;
#20323=EDGE_CURVE ( 'NONE', #168899, #4548, #99030, .T. ) ;
#20351=EDGE_CURVE ( 'NONE', #55246, #254433, #190668, .T. ) ;
#20373=DIRECTION ( 'NONE',  ( 0.000000000000000000, -1.000000000000000000, 0.000000000000000000 ) ) ;
#20420=DIRECTION ( 'NONE',  ( -1.000000000000000000, -0.000000000000000000, -0.000000000000000000 ) ) ;
#20448=CARTESIAN_POINT ( 'NONE',  ( 22.47071067811865319, 68.27992525551390202, -103.1221999392269737 ) ) ;
#20455=ORIENTED_EDGE ( 'NONE', *, *, #84131, .F. ) ;
#20462=AXIS2_PLACEMENT_3D ( 'NONE', #131813, #110973, #230945 ) ;
#20472=CARTESIAN_POINT ( 'NONE',  ( -23.15000000000000213, 71.65000000001187175, -90.67310748452433700 ) ) ;
#20476=FACE_OUTER_BOUND ( 'NONE', #184758, .T. ) ;
#20490=DIRECTION ( 'NONE',  ( -0.000000000000000000, -0.1350103645451945777, 0.9908441862701590219 ) ) ;
#20494=CARTESIAN_POINT ( 'NONE',  ( -18.59999999999999787, 76.00000000001170974, -69.52310748452431710 ) ) ;
#20498=CARTESIAN_POINT ( 'NONE',  ( -22.39999999999999858, 76.00000000001199396, -109.2731074845243171 ) ) ;
#20503=VERTEX_POINT ( 'NONE', #174365 ) ;
#20516=DIRECTION ( 'NONE',  ( -1.000000000000000000, 0.000000000000000000, -0.000000000000000000 ) ) ;
#20533=FACE_OUTER_BOUND ( 'NONE', #169753, .T. ) ;
#20551=ORIENTED_EDGE ( 'NONE', *, *, #58726, .F. ) ;
#20592=ORIENTED_EDGE ( 'NONE', *, *, #249436, .T. ) ;
#20600=CARTESIAN_POINT ( 'NONE',  ( -22.39999999999999858, 68.20922040163854660, -103.1231074845243540 ) ) ;
#20647=CYLINDRICAL_SURFACE ( 'NONE', #126766, 12.87499999999999822 ) ;
#20656=DIRECTION ( 'NONE',  ( -1.000000000000000000, 3.265361837132813093E-16, 2.280189983783949500E-30 ) ) ;
#20671=ORIENTED_EDGE ( 'NONE', *, *, #250125, .T. ) ;
#20684=AXIS2_PLACEMENT_3D ( 'NONE', #257062, #176319, #198423 ) ;
#20689=CARTESIAN_POINT ( 'NONE',  ( 18.59999999999999076, 65.50857864377445594, -78.27310748452438816 ) ) ;
#20692=CARTESIAN_POINT ( 'NONE',  ( 21.05000000000000071, 64.25000000001175238, -76.53791325517833855 ) ) ;
#20710=CARTESIAN_POINT ( 'NONE',  ( -23.15000000000000213, 76.00000000001170974, -69.52310748452431710 ) ) ;
#20758=VERTEX_POINT ( 'NONE', #194148 ) ;
#20776=ORIENTED_EDGE ( 'NONE', *, *, #112561, .T. ) ;
#20808=DIRECTION ( 'NONE',  ( 0.000000000000000000, -0.9876197685951263461, 0.1568667991644794590 ) ) ;
#20810=DIRECTION ( 'NONE',  ( -1.000000000000000000, 0.000000000000000000, 0.000000000000000000 ) ) ;
#20829=ORIENTED_EDGE ( 'NONE', *, *, #125804, .T. ) ;
#20838=AXIS2_PLACEMENT_3D ( 'NONE', #247801, #229535, #48314 ) ;
#20848=CARTESIAN_POINT ( 'NONE',  ( 18.59999999999999076, 65.50857864377445594, -78.27310748452438816 ) ) ;
#20861=CARTESIAN_POINT ( 'NONE',  ( -21.05000000000000071, 69.74218538953583391, -103.1208977758331571 ) ) ;
#20873=AXIS2_PLACEMENT_3D ( 'NONE', #108413, #67996, #246623 ) ;
#20882=CIRCLE ( 'NONE', #120833, 0.1000000000000052097 ) ;
#20906=ORIENTED_EDGE ( 'NONE', *, *, #255019, .T. ) ;
#20932=DIRECTION ( 'NONE',  ( -1.000000000000000000, -0.000000000000000000, -0.000000000000000000 ) ) ;
#20966=DIRECTION ( 'NONE',  ( -0.000000000000000000, 1.000000000000000000, 6.982962677686266711E-15 ) ) ;
#20976=AXIS2_PLACEMENT_3D ( 'NONE', #165850, #184103, #82409 ) ;
#20992=EDGE_LOOP ( 'NONE', ( #48696, #111032, #238591, #101560 ) ) ;
#21009=ORIENTED_EDGE ( 'NONE', *, *, #168424, .F. ) ;
#21045=CARTESIAN_POINT ( 'NONE',  ( 21.04999999999999716, 76.03753606329763670, -109.3553797584599749 ) ) ;
#21052=CARTESIAN_POINT ( 'NONE',  ( -21.55000000000000426, 68.25000000001179501, -81.87310748452436826 ) ) ;
#21074=CARTESIAN_POINT ( 'NONE',  ( 20.94999999999999574, 87.48912529308798014, -99.92310748452423752 ) ) ;
#21106=CARTESIAN_POINT ( 'NONE',  ( 22.49066049874202022, 75.94365674847981040, -114.6731197220414202 ) ) ;
#21122=AXIS2_PLACEMENT_3D ( 'NONE', #225903, #190697, #109829 ) ;
#21137=DIRECTION ( 'NONE',  ( 0.000000000000000000, 0.000000000000000000, 1.000000000000000000 ) ) ;
#21138=VECTOR ( 'NONE', #16781, 1000.000000000000000 ) ;
#21139=ORIENTED_EDGE ( 'NONE', *, *, #19014, .F. ) ;
#21162=CARTESIAN_POINT ( 'NONE',  ( 21.05000000000000071, 70.15000000001192859, -92.89061026024637613 ) ) ;
#21170=TOROIDAL_SURFACE ( 'NONE', #41825, 0.2000000000000000111, 0.1000000000000000056 ) ;
#21180=DIRECTION ( 'NONE',  ( -0.000000000000000000, 7.172728831056617961E-15, -1.000000000000000000 ) ) ;
#21201=CARTESIAN_POINT ( 'NONE',  ( -22.59999999999999787, 75.89914163091332000, -114.7726746080137019 ) ) ;
#21206=AXIS2_PLACEMENT_3D ( 'NONE', #68051, #86300, #254054 ) ;
#21227=AXIS2_PLACEMENT_3D ( 'NONE', #41092, #25379, #203985 ) ;
#21246=CIRCLE ( 'NONE', #67004, 0.09999999999999939493 ) ;
#21271=CARTESIAN_POINT ( 'NONE',  ( -18.41809261886927374, 85.68240331476842186, -62.86626393443329874 ) ) ;
#21357=EDGE_CURVE ( 'NONE', #10791, #96147, #209209, .T. ) ;
#21425=CARTESIAN_POINT ( 'NONE',  ( -23.15000000000000213, 85.60000000001178933, -79.41707660717668205 ) ) ;
#21443=FACE_OUTER_BOUND ( 'NONE', #78575, .T. ) ;
#21453=CARTESIAN_POINT ( 'NONE',  ( 21.05000005001280172, 67.12872030824165392, -90.84515989627823274 ) ) ;
#21454=DIRECTION ( 'NONE',  ( 0.000000000000000000, -1.000000000000000000, -6.982962677686265922E-15 ) ) ;
#21468=VERTEX_POINT ( 'NONE', #82514 ) ;
#21472=VERTEX_POINT ( 'NONE', #120430 ) ;
#21474=DIRECTION ( 'NONE',  ( 0.000000000000000000, 1.000000000000000000, 6.853228547068871147E-15 ) ) ;
#21475=ADVANCED_FACE ( 'NONE', ( #156976 ), #11576, .F. ) ;
#21488=EDGE_LOOP ( 'NONE', ( #244772, #88870, #187965, #71 ) ) ;
#21504=DIRECTION ( 'NONE',  ( 1.000000000000000000, 0.000000000000000000, 0.000000000000000000 ) ) ;
#21514=AXIS2_PLACEMENT_3D ( 'NONE', #123433, #142964, #8625 ) ;
#21525=DIRECTION ( 'NONE',  ( 0.000000000000000000, 0.000000000000000000, 1.000000000000000000 ) ) ;
#21540=DIRECTION ( 'NONE',  ( 1.000000000000000000, 0.000000000000000000, 0.000000000000000000 ) ) ;
#21541=CARTESIAN_POINT ( 'NONE',  ( -23.15000000000000213, 85.50000000001188027, -93.12913836187179584 ) ) ;
#21545=CARTESIAN_POINT ( 'NONE',  ( -20.54999999999999716, 74.07476635515199348, -82.25335101765045920 ) ) ;
#21556=DIRECTION ( 'NONE',  ( 0.000000000000000000, 0.8777080977375072424, -0.4791956752371691608 ) ) ;
#21614=VERTEX_POINT ( 'NONE', #126811 ) ;
#21626=FACE_OUTER_BOUND ( 'NONE', #152731, .T. ) ;
#21634=DIRECTION ( 'NONE',  ( 0.000000000000000000, 6.982962677686266711E-15, -1.000000000000000000 ) ) ;
#21647=CIRCLE ( 'NONE', #42475, 0.09999999999999820144 ) ;
#21710=EDGE_LOOP ( 'NONE', ( #209489, #146918, #214353, #205108 ) ) ;
#21736=AXIS2_PLACEMENT_3D ( 'NONE', #86376, #249353, #190678 ) ;
#21752=DIRECTION ( 'NONE',  ( -6.938893903907222856E-15, -1.000000000000000000, -6.982962677686266711E-15 ) ) ;
#21757=CIRCLE ( 'NONE', #200817, 0.1000000000000028644 ) ;
#21773=CARTESIAN_POINT ( 'NONE',  ( -23.15000000000000213, 76.00000000001168132, -65.52310748452430289 ) ) ;
#21779=LINE ( 'NONE', #20498, #169924 ) ;
#21793=DIRECTION ( 'NONE',  ( 0.000000000000000000, 0.000000000000000000, 1.000000000000000000 ) ) ;
#21794=LINE ( 'NONE', #97433, #203741 ) ;
#21825=DIRECTION ( 'NONE',  ( 0.000000000000000000, 0.000000000000000000, -1.000000000000000000 ) ) ;
#21846=ORIENTED_EDGE ( 'NONE', *, *, #115623, .F. ) ;
#21859=DIRECTION ( 'NONE',  ( 1.000000000000000000, 0.000000000000000000, 0.000000000000000000 ) ) ;
#21862=CIRCLE ( 'NONE', #80259, 0.1000000000000028644 ) ;
#21874=EDGE_CURVE ( 'NONE', #88867, #40828, #224628, .T. ) ;
#21907=AXIS2_PLACEMENT_3D ( 'NONE', #247350, #225203, #128707 ) ;
#21934=ORIENTED_EDGE ( 'NONE', *, *, #160921, .F. ) ;
#21957=EDGE_CURVE ( 'NONE', #110239, #16537, #34423, .T. ) ;
#21960=FACE_OUTER_BOUND ( 'NONE', #18544, .T. ) ;
#22042=ORIENTED_EDGE ( 'NONE', *, *, #124653, .F. ) ;
#22058=DIRECTION ( 'NONE',  ( 1.000000000000000000, 0.000000000000000000, 0.000000000000000000 ) ) ;
#22069=DIRECTION ( 'NONE',  ( 0.000000000000000000, 0.9654727137038715545, -0.2605042016806676242 ) ) ;
#22081=DIRECTION ( 'NONE',  ( 1.000000000000000000, 0.000000000000000000, 0.000000000000000000 ) ) ;
#22091=CARTESIAN_POINT ( 'NONE',  ( -18.59999999999999787, 76.00000000001170974, -69.52310748452431710 ) ) ;
#22104=CIRCLE ( 'NONE', #155391, 0.1000000000000028644 ) ;
#22113=EDGE_CURVE ( 'NONE', #178566, #79511, #82441, .T. ) ;
#22119=CARTESIAN_POINT ( 'NONE',  ( -22.40000000000000213, 76.00000000001203659, -114.7735403769829219 ) ) ;
#22125=DIRECTION ( 'NONE',  ( 3.469446951953728416E-14, 0.8660254037844343777, -0.5000000000000074385 ) ) ;
#22126=DIRECTION ( 'NONE',  ( 1.000000000000000000, 0.000000000000000000, 0.000000000000000000 ) ) ;
#22161=ORIENTED_EDGE ( 'NONE', *, *, #6271, .T. ) ;
#22169=CARTESIAN_POINT ( 'NONE',  ( -18.59999999999999787, 70.05000000001193428, -92.71740517948948934 ) ) ;
#22171=ORIENTED_EDGE ( 'NONE', *, *, #78336, .F. ) ;
#22180=CARTESIAN_POINT ( 'NONE',  ( -21.14999999999999858, 87.75000000001193712, -103.0231074845242318 ) ) ;
#22182=ORIENTED_EDGE ( 'NONE', *, *, #54954, .F. ) ;
#22188=EDGE_CURVE ( 'NONE', #236062, #216113, #86901, .T. ) ;
#22209=FACE_OUTER_BOUND ( 'NONE', #242895, .T. ) ;
#22222=DIRECTION ( 'NONE',  ( 0.000000000000000000, -1.000000000000000000, -6.982962677686265922E-15 ) ) ;
#22227=EDGE_CURVE ( 'NONE', #190048, #170518, #49336, .T. ) ;
#22239=CARTESIAN_POINT ( 'NONE',  ( -23.15000000000000213, 80.83132476063475735, -86.05341054232552267 ) ) ;
#22243=CARTESIAN_POINT ( 'NONE',  ( 22.59999954896768770, 76.00882823225448703, -114.7736161585923043 ) ) ;
#22250=EDGE_CURVE ( 'NONE', #189878, #603, #65387, .T. ) ;
#22256=EDGE_LOOP ( 'NONE', ( #46968, #42722, #25951, #93727 ) ) ;
#22287=ADVANCED_FACE ( 'NONE', ( #25006 ), #4126, .T. ) ;
#22293=CARTESIAN_POINT ( 'NONE',  ( -20.64999999999999858, 76.00000000001170974, -69.52310748452431710 ) ) ;
#22313=VERTEX_POINT ( 'NONE', #223165 ) ;
#22332=VERTEX_POINT ( 'NONE', #92644 ) ;
#22357=PRESENTATION_STYLE_ASSIGNMENT (( #61460 ) ) ;
#22367=CARTESIAN_POINT ( 'NONE',  ( -20.94999999999999929, 76.00000000001179501, -81.22310748452430573 ) ) ;
#22371=ORIENTED_EDGE ( 'NONE', *, *, #133395, .F. ) ;
#22404=FACE_OUTER_BOUND ( 'NONE', #196344, .T. ) ;
#22415=EDGE_CURVE ( 'NONE', #86374, #214176, #124357, .T. ) ;
#22420=EDGE_CURVE ( 'NONE', #121706, #118654, #57702, .T. ) ;
#22432=CARTESIAN_POINT ( 'NONE',  ( -21.22070241538126112, 69.53005372714234511, -103.1220265150593889 ) ) ;
#22442=ORIENTED_EDGE ( 'NONE', *, *, #57165, .F. ) ;
#22444=VERTEX_POINT ( 'NONE', #232189 ) ;
#22450=CARTESIAN_POINT ( 'NONE',  ( -18.50000000000000000, 76.00000000001170974, -69.52310748452431710 ) ) ;
#22479=CARTESIAN_POINT ( 'NONE',  ( -21.05000000000000071, 70.10000000001193143, -92.80400771986793984 ) ) ;
#22504=ORIENTED_EDGE ( 'NONE', *, *, #8496, .F. ) ;
#22516=DIRECTION ( 'NONE',  ( 0.000000000000000000, 0.4930308989875575865, 0.8700118002898125091 ) ) ;
#22578=CYLINDRICAL_SURFACE ( 'NONE', #113847, 0.5000000000000004441 ) ;
#22584=PLANE ( 'NONE',  #78652 ) ;
#22588=CIRCLE ( 'NONE', #118447, 0.09999999999999939493 ) ;
#22613=FACE_OUTER_BOUND ( 'NONE', #124923, .T. ) ;
#22618=EDGE_CURVE ( 'NONE', #74828, #46212, #186325, .T. ) ;
#22620=ORIENTED_EDGE ( 'NONE', *, *, #201196, .F. ) ;
#22637=ADVANCED_FACE ( 'NONE', ( #82041 ), #142045, .T. ) ;
#22679=DIRECTION ( 'NONE',  ( -2.940209281316621016E-16, -1.000000000000000000, -7.056502275159890832E-15 ) ) ;
#22707=DIRECTION ( 'NONE',  ( -3.265361837132813093E-16, -1.000000000000000000, -6.982962677686266711E-15 ) ) ;
#22723=ORIENTED_EDGE ( 'NONE', *, *, #52338, .F. ) ;
#22726=CARTESIAN_POINT ( 'NONE',  ( -20.54999999999999716, 74.00000000001186606, -89.79848556176222019 ) ) ;
#22789=DIRECTION ( 'NONE',  ( 0.000000000000000000, 0.000000000000000000, 1.000000000000000000 ) ) ;
#22800=ORIENTED_EDGE ( 'NONE', *, *, #145280, .T. ) ;
#22814=DIRECTION ( 'NONE',  ( 0.000000000000000000, -6.982962677686266711E-15, 1.000000000000000000 ) ) ;
#22851=CARTESIAN_POINT ( 'NONE',  ( -20.00857864376270001, 66.85000000001180354, -81.77310748452437394 ) ) ;
#22861=AXIS2_PLACEMENT_3D ( 'NONE', #110154, #69769, #50171 ) ;
#22871=ORIENTED_EDGE ( 'NONE', *, *, #250390, .F. ) ;
#22889=ORIENTED_EDGE ( 'NONE', *, *, #165970, .F. ) ;
#22895=EDGE_CURVE ( 'NONE', #191564, #98792, #94903, .T. ) ;
#22904=FACE_OUTER_BOUND ( 'NONE', #142100, .T. ) ;
#22915=DIRECTION ( 'NONE',  ( 1.000000000000000000, 0.000000000000000000, 0.000000000000000000 ) ) ;
#22938=CARTESIAN_POINT ( 'NONE',  ( -18.50000000000000000, 76.00000000001170974, -69.52310748452431710 ) ) ;
#22948=CARTESIAN_POINT ( 'NONE',  ( -20.94999999999999929, 87.65000000001192859, -100.0231074845242318 ) ) ;
#22964=ORIENTED_EDGE ( 'NONE', *, *, #4076, .T. ) ;
#22971=CARTESIAN_POINT ( 'NONE',  ( -21.08078803292166725, 75.92081401285429365, -109.3561204489614482 ) ) ;
#22988=LINE ( 'NONE', #241998, #36029 ) ;
#23018=VECTOR ( 'NONE', #22058, 1000.000000000000000 ) ;
#23027=CARTESIAN_POINT ( 'NONE',  ( 21.08376601933332495, 69.65805272873629406, -103.0868834954543587 ) ) ;
#23028=DIRECTION ( 'NONE',  ( -0.000000000000000000, 0.9908441862701591329, 0.1350103645451946055 ) ) ;
#23029=ORIENTED_EDGE ( 'NONE', *, *, #158767, .T. ) ;
#23032=DIRECTION ( 'NONE',  ( 0.000000000000000000, 0.000000000000000000, 1.000000000000000000 ) ) ;
#23092=LINE ( 'NONE', #103861, #139993 ) ;
#23097=CARTESIAN_POINT ( 'NONE',  ( 18.56579813702275317, 65.66974365629644694, -63.93601455626049557 ) ) ;
#23106=CIRCLE ( 'NONE', #147985, 0.1000000000000028644 ) ;
#23133=EDGE_CURVE ( 'NONE', #203922, #2197, #52903, .T. ) ;
#23152=ORIENTED_EDGE ( 'NONE', *, *, #194020, .F. ) ;
#23164=DIRECTION ( 'NONE',  ( 0.000000000000000000, -0.1350103645451974088, 0.9908441862701587999 ) ) ;
#23169=DIRECTION ( 'NONE',  ( 0.7071067811865127117, 0.7071067811865821007, 0.000000000000000000 ) ) ;
#23182=VECTOR ( 'NONE', #113589, 1000.000000000000000 ) ;
#23185=CIRCLE ( 'NONE', #231464, 0.09999999999999520384 ) ;
#23226=EDGE_LOOP ( 'NONE', ( #103309, #245918, #122690, #104024 ) ) ;
#23227=CARTESIAN_POINT ( 'NONE',  ( -20.54999999999999716, 71.75000000001186606, -90.67310748452433700 ) ) ;
#23272=EDGE_CURVE ( 'NONE', #71686, #148851, #55443, .T. ) ;
#23304=VERTEX_POINT ( 'NONE', #234107 ) ;
#23325=ORIENTED_EDGE ( 'NONE', *, *, #253044, .F. ) ;
#23326=VERTEX_POINT ( 'NONE', #77582 ) ;
#23329=DIRECTION ( 'NONE',  ( -3.469446951953515108E-14, -1.000000000000000000, 0.000000000000000000 ) ) ;
#23340=EDGE_LOOP ( 'NONE', ( #60228, #47772, #756, #600 ) ) ;
#23355=CARTESIAN_POINT ( 'NONE',  ( -21.05000000000000071, 64.25000000001176659, -76.53791325517833855 ) ) ;
#23360=DIRECTION ( 'NONE',  ( 1.000000000000000000, 0.000000000000000000, 0.000000000000000000 ) ) ;
#23367=CARTESIAN_POINT ( 'NONE',  ( 20.94999999999999929, 71.00000000001180922, -81.52837350343745015 ) ) ;
#23372=ORIENTED_EDGE ( 'NONE', *, *, #57165, .T. ) ;
#23394=ORIENTED_EDGE ( 'NONE', *, *, #205574, .F. ) ;
#23433=VECTOR ( 'NONE', #251636, 1000.000000000000000 ) ;
#23451=EDGE_CURVE ( 'NONE', #125402, #76326, #121892, .T. ) ;
#23462=DIRECTION ( 'NONE',  ( -0.000000000000000000, 0.1350103645451859180, 0.9908441862701603542 ) ) ;
#23467=CYLINDRICAL_SURFACE ( 'NONE', #224558, 0.1000000000000028644 ) ;
#23470=DIRECTION ( 'NONE',  ( 1.000000000000000000, 0.000000000000000000, 0.000000000000000000 ) ) ;
#23526=EDGE_LOOP ( 'NONE', ( #50340, #42499, #40478 ) ) ;
#23549=EDGE_CURVE ( 'NONE', #155597, #255663, #108340, .T. ) ;
#23559=EDGE_CURVE ( 'NONE', #2690, #127766, #166626, .T. ) ;
#23607=VERTEX_POINT ( 'NONE', #188269 ) ;
#23628=CARTESIAN_POINT ( 'NONE',  ( 21.05000000000000071, 75.90220970870321082, -109.2809220950004345 ) ) ;
#23655=DIRECTION ( 'NONE',  ( 0.000000000000000000, 0.000000000000000000, 1.000000000000000000 ) ) ;
#23687=CARTESIAN_POINT ( 'NONE',  ( 18.49999999999999289, 64.25000000001202238, -114.7731074845243882 ) ) ;
#23698=CARTESIAN_POINT ( 'NONE',  ( -20.64999999999999858, 74.00000000001186606, -89.79848556176222019 ) ) ;
#23726=DIRECTION ( 'NONE',  ( -0.000000000000000000, 0.8700118002898356018, -0.4930308989875170078 ) ) ;
#23758=VERTEX_POINT ( 'NONE', #74727 ) ;
#23781=CARTESIAN_POINT ( 'NONE',  ( -21.05000000000000071, 77.25000000001189449, -95.02310748452430289 ) ) ;
#23789=DIRECTION ( 'NONE',  ( -1.000000000000000000, -0.000000000000000000, -0.000000000000000000 ) ) ;
#23794=DIRECTION ( 'NONE',  ( -0.000000000000000000, -6.982962677686266711E-15, 1.000000000000000000 ) ) ;
#23806=EDGE_CURVE ( 'NONE', #111193, #245252, #154354, .T. ) ;
#23821=FACE_OUTER_BOUND ( 'NONE', #47217, .T. ) ;
#23829=DIRECTION ( 'NONE',  ( 0.000000000000000000, -6.982962677686267499E-15, 1.000000000000000000 ) ) ;
#23839=CIRCLE ( 'NONE', #40604, 0.1000000000000052097 ) ;
#23850=CIRCLE ( 'NONE', #33182, 11.64999999999999325 ) ;
#23871=VECTOR ( 'NONE', #23726, 1000.000000000000114 ) ;
#23876=ORIENTED_EDGE ( 'NONE', *, *, #179472, .T. ) ;
#23918=DIRECTION ( 'NONE',  ( -0.000000000000000000, -1.000000000000000000, -6.982962677686266711E-15 ) ) ;
#23946=DIRECTION ( 'NONE',  ( 0.000000000000000000, -7.272083257015735086E-15, 1.000000000000000000 ) ) ;
#23957=DIRECTION ( 'NONE',  ( 0.000000000000000000, -6.982962677686266711E-15, 1.000000000000000000 ) ) ;
#23980=AXIS2_PLACEMENT_3D ( 'NONE', #220943, #63154, #22789 ) ;
#23983=ORIENTED_EDGE ( 'NONE', *, *, #20313, .T. ) ;
#24046=CIRCLE ( 'NONE', #78174, 11.64999999999999325 ) ;
#24074=DIRECTION ( 'NONE',  ( 0.000000000000000000, 0.000000000000000000, 1.000000000000000000 ) ) ;
#24093=DIRECTION ( 'NONE',  ( 1.000000000000000000, 0.000000000000000000, 0.000000000000000000 ) ) ;
#24108=VERTEX_POINT ( 'NONE', #73213 ) ;
#24130=CARTESIAN_POINT ( 'NONE',  ( 20.95512820512820085, 65.37615131629998189, -90.82294546509999122 ) ) ;
#24153=DIRECTION ( 'NONE',  ( -3.265361837132813093E-16, -1.000000000000000000, 7.445645354460596589E-46 ) ) ;
#24156=VERTEX_POINT ( 'NONE', #30218 ) ;
#24191=ORIENTED_EDGE ( 'NONE', *, *, #28495, .T. ) ;
#24201=DIRECTION ( 'NONE',  ( -2.952720810173289112E-16, -1.000000000000000000, -6.982962677686266711E-15 ) ) ;
#24216=DIRECTION ( 'NONE',  ( 0.000000000000000000, -6.517943393102682774E-15, 1.000000000000000000 ) ) ;
#24219=DIRECTION ( 'NONE',  ( 1.000000000000000000, 0.000000000000000000, 0.000000000000000000 ) ) ;
#24233=( BOUNDED_SURFACE ( )  B_SPLINE_SURFACE ( 3, 2, ( 
 ( #77237, #173840, #156825 ),
 ( #55088, #175121, #135922 ),
 ( #36882, #118962, #236322 ),
 ( #57670, #92956, #137223 ),
 ( #117661, #197192, #18569 ),
 ( #98061, #177671, #172557 ) ),
 .UNSPECIFIED., .F., .F., .F. ) 
 B_SPLINE_SURFACE_WITH_KNOTS ( ( 4, 2, 4 ),
 ( 3, 3 ),
 ( 0.0001342700090130014186, 0.0002909192928057377698, 0.0004475685765984741210 ),
 ( 0.000000000000000000, 1.000000000000000000 ),
 .UNSPECIFIED. ) 
 GEOMETRIC_REPRESENTATION_ITEM ( )  RATIONAL_B_SPLINE_SURFACE ( (
 ( 1.000000000000000000, 0.7250110520819876836, 1.000000000000000000),
 ( 1.000000000000000000, 0.7257599279120965363, 1.000000000000000000),
 ( 1.000000000000000000, 0.7137594617301571409, 1.000000000000000000),
 ( 1.000000000000000000, 0.6959270178792876793, 1.000000000000000000),
 ( 1.000000000000000000, 0.6919879549351505288, 1.000000000000000000),
 ( 1.000000000000000000, 0.7071067811865494601, 1.000000000000000000) ) ) 
 REPRESENTATION_ITEM ( '' )  SURFACE ( )  );
#24270=ORIENTED_EDGE ( 'NONE', *, *, #250133, .T. ) ;
#24277=ORIENTED_EDGE ( 'NONE', *, *, #204205, .F. ) ;
#24282=EDGE_CURVE ( 'NONE', #170827, #189189, #21246, .T. ) ;
#24323=CARTESIAN_POINT ( 'NONE',  ( -20.64999999999999858, 68.85000000001186038, -90.77310748452435973 ) ) ;
#24372=EDGE_CURVE ( 'NONE', #88769, #40263, #355, .T. ) ;
#24377=CARTESIAN_POINT ( 'NONE',  ( 23.14999999999999503, 64.25000000001202238, -114.7731074845243882 ) ) ;
#24394=FACE_OUTER_BOUND ( 'NONE', #174250, .T. ) ;
#24398=DIRECTION ( 'NONE',  ( 0.000000000000000000, 0.000000000000000000, 1.000000000000000000 ) ) ;
#24403=EDGE_CURVE ( 'NONE', #66389, #116798, #133812, .T. ) ;
#24417=ORIENTED_EDGE ( 'NONE', *, *, #82479, .F. ) ;
#24430=DIRECTION ( 'NONE',  ( 0.000000000000000000, 6.982962677686266711E-15, -1.000000000000000000 ) ) ;
#24431=DIRECTION ( 'NONE',  ( -1.000000000000000000, -0.000000000000000000, -0.000000000000000000 ) ) ;
#24434=ORIENTED_EDGE ( 'NONE', *, *, #84952, .F. ) ;
#24447=CARTESIAN_POINT ( 'NONE',  ( 20.94999999999999929, 74.63912941281984104, -94.95010955743335046 ) ) ;
#24465=CARTESIAN_POINT ( 'NONE',  ( -20.00857864376270001, 66.65000000001180069, -81.77310748452437394 ) ) ;
#24518=CARTESIAN_POINT ( 'NONE',  ( 23.14999999999999858, 71.22429906543244726, -91.17433938047835795 ) ) ;
#24533=CYLINDRICAL_SURFACE ( 'NONE', #208668, 0.1000000000000028644 ) ;
#24573=CARTESIAN_POINT ( 'NONE',  ( 22.47071067811865319, 75.90090754530939421, -110.7431822290223522 ) ) ;
#24584=ORIENTED_EDGE ( 'NONE', *, *, #143849, .T. ) ;
#24602=ORIENTED_EDGE ( 'NONE', *, *, #48278, .T. ) ;
#24622=ORIENTED_EDGE ( 'NONE', *, *, #70628, .F. ) ;
#24627=ORIENTED_EDGE ( 'NONE', *, *, #7479, .F. ) ;
#24636=ORIENTED_EDGE ( 'NONE', *, *, #81845, .F. ) ;
#24644=CARTESIAN_POINT ( 'NONE',  ( -23.25000000000000000, 71.85000000001186038, -90.67310748452433700 ) ) ;
#24648=DIRECTION ( 'NONE',  ( 0.000000000000000000, 1.000000000000000000, 6.982962677686266711E-15 ) ) ;
#24668=CIRCLE ( 'NONE', #16281, 4.049999999999998046 ) ;
#24698=DIRECTION ( 'NONE',  ( 0.000000000000000000, -5.956132106358139644E-15, 1.000000000000000000 ) ) ;
#24702=CARTESIAN_POINT ( 'NONE',  ( 20.95325940946048249, 65.47660992931560031, -95.45864535528430395 ) ) ;
#24721=CARTESIAN_POINT ( 'NONE',  ( 20.94999999999999574, 87.48912529308798014, -100.1231074845242262 ) ) ;
#24738=DIRECTION ( 'NONE',  ( -0.000000000000000000, 0.1298341882519735979, 0.9915357197604890427 ) ) ;
#24746=DIRECTION ( 'NONE',  ( 1.000000000000000000, -0.000000000000000000, 0.000000000000000000 ) ) ;
#24748=CARTESIAN_POINT ( 'NONE',  ( -18.59999999999999787, 68.87972903831409610, -65.86354444268503983 ) ) ;
#24768=PLANE ( 'NONE',  #230900 ) ;
#24773=AXIS2_PLACEMENT_3D ( 'NONE', #166134, #66992, #163527 ) ;
#24790=DIRECTION ( 'NONE',  ( 0.000000000000000000, -1.000000000000000000, -6.982962677686265922E-15 ) ) ;
#24803=AXIS2_PLACEMENT_3D ( 'NONE', #27176, #45416, #85787 ) ;
#24816=CARTESIAN_POINT ( 'NONE',  ( 19.99999999738052736, 64.25000000001179501, -78.33593553489176031 ) ) ;
#24817=VECTOR ( 'NONE', #226927, 1000.000000000000000 ) ;
#24852=B_SPLINE_CURVE_WITH_KNOTS ( 'NONE', 3,
 ( #86926, #166522, #50368, #227741, #187356, #8704 ),
 .UNSPECIFIED., .F., .F.,
 ( 4, 2, 4 ),
 ( 0.000000000000000000, 0.0001496588209255877576, 0.0002993176418511755152 ),
 .UNSPECIFIED. ) ;
#24898=CARTESIAN_POINT ( 'NONE',  ( 21.04999999999999716, 76.08561306081597309, -109.4368672183345836 ) ) ;
#24919=LINE ( 'NONE', #186551, #257158 ) ;
#24955=ORIENTED_EDGE ( 'NONE', *, *, #144634, .T. ) ;
#24987=EDGE_LOOP ( 'NONE', ( #244915, #6202, #233455, #229139 ) ) ;
#25006=FACE_OUTER_BOUND ( 'NONE', #50276, .T. ) ;
#25023=ADVANCED_FACE ( 'NONE', ( #172988 ), #77670, .F. ) ;
#25028=AXIS2_PLACEMENT_3D ( 'NONE', #129843, #209390, #230239 ) ;
#25069=CARTESIAN_POINT ( 'NONE',  ( 23.24999999999999645, 76.00000000001195133, -103.0231074845243171 ) ) ;
#25076=CARTESIAN_POINT ( 'NONE',  ( -20.94999999999999929, 87.48912529308798014, -100.1231074845242262 ) ) ;
#25086=ADVANCED_FACE ( 'NONE', ( #141512 ), #72400, .F. ) ;
#25099=ORIENTED_EDGE ( 'NONE', *, *, #36101, .T. ) ;
#25170=ORIENTED_EDGE ( 'NONE', *, *, #254398, .T. ) ;
#25180=CARTESIAN_POINT ( 'NONE',  ( -23.15000000000000213, 71.75000000001186606, -90.77310748452434552 ) ) ;
#25192=FACE_OUTER_BOUND ( 'NONE', #92816, .T. ) ;
#25195=CARTESIAN_POINT ( 'NONE',  ( -23.15000000000000213, 87.41227409416143246, -72.52310748452423184 ) ) ;
#25238=VECTOR ( 'NONE', #56131, 1000.000000000000000 ) ;
#25239=DIRECTION ( 'NONE',  ( -1.000000000000000000, 3.265361837132813093E-16, 2.280189983783949500E-30 ) ) ;
#25247=CARTESIAN_POINT ( 'NONE',  ( 21.05000000000000071, 76.00000000001195133, -103.0231074845243171 ) ) ;
#25250=VERTEX_POINT ( 'NONE', #127091 ) ;
#25275=CARTESIAN_POINT ( 'NONE',  ( 18.59999999999999076, 64.25000000001202238, -114.7731074845243882 ) ) ;
#25304=DIRECTION ( 'NONE',  ( -1.000000000000000000, -0.000000000000000000, -0.000000000000000000 ) ) ;
#25306=FACE_OUTER_BOUND ( 'NONE', #43156, .T. ) ;
#25352=CARTESIAN_POINT ( 'NONE',  ( -21.14999999999999858, 69.74218538953583391, -103.1208977758331571 ) ) ;
#25379=DIRECTION ( 'NONE',  ( 0.000000000000000000, -0.5000000000000016653, 0.8660254037844377084 ) ) ;
#25390=ORIENTED_EDGE ( 'NONE', *, *, #232777, .F. ) ;
#25402=DIRECTION ( 'NONE',  ( -0.000000000000000000, 7.109473446599835262E-15, -1.000000000000000000 ) ) ;
#25415=VERTEX_POINT ( 'NONE', #38854 ) ;
#25416=DIRECTION ( 'NONE',  ( -1.000000000000000000, 3.265361837132813093E-16, 2.280189983783949500E-30 ) ) ;
#25448=ADVANCED_FACE ( 'NONE', ( #49095 ), #223871, .F. ) ;
#25453=ORIENTED_EDGE ( 'NONE', *, *, #6271, .F. ) ;
#25463=CARTESIAN_POINT ( 'NONE',  ( -20.85000000000000142, 64.25000000001176659, -76.30697314750248950 ) ) ;
#25470=CIRCLE ( 'NONE', #146066, 0.1000000000000028644 ) ;
#25476=CARTESIAN_POINT ( 'NONE',  ( -18.59117750673696889, 65.66751761918648356, -63.92826094061123143 ) ) ;
#25490=ORIENTED_EDGE ( 'NONE', *, *, #127172, .T. ) ;
#25520=EDGE_LOOP ( 'NONE', ( #99856, #7419, #122305, #155810, #211536 ) ) ;
#25522=CARTESIAN_POINT ( 'NONE',  ( -21.14250536705909411, 76.00000000001200817, -109.5412796614050563 ) ) ;
#25545=DIRECTION ( 'NONE',  ( 0.000000000000000000, -0.9876197685951263461, 0.1568667991644794590 ) ) ;
#25555=CARTESIAN_POINT ( 'NONE',  ( 23.14999999999999858, 76.00000000001172396, -71.52310748452431710 ) ) ;
#25567=CARTESIAN_POINT ( 'NONE',  ( -18.39999999999999858, 85.51932773110434027, -96.05013110796491560 ) ) ;
#25578=CARTESIAN_POINT ( 'NONE',  ( 21.11101077988997332, 69.57631526528589916, -103.0383927534386714 ) ) ;
#25605=VERTEX_POINT ( 'NONE', #253711 ) ;
#25622=EDGE_CURVE ( 'NONE', #98792, #127648, #251638, .T. ) ;
#25690=DIRECTION ( 'NONE',  ( 1.000000000000000000, 0.000000000000000000, 0.000000000000000000 ) ) ;
#25691=CARTESIAN_POINT ( 'NONE',  ( 20.85000000000000142, 69.06610602788535402, -65.73746165015079157 ) ) ;
#25773=VECTOR ( 'NONE', #82666, 999.9999999999998863 ) ;
#25778=ORIENTED_EDGE ( 'NONE', *, *, #126757, .T. ) ;
#25784=EDGE_LOOP ( 'NONE', ( #81497, #105633, #256559, #198364, #128077, #112117, #54102, #213460, #210791, #146171, #25490 ) ) ;
#25798=CARTESIAN_POINT ( 'NONE',  ( -20.85000000000000142, 64.25000000001175238, -76.30697314750248950 ) ) ;
#25853=CARTESIAN_POINT ( 'NONE',  ( 22.39999999999999503, 76.10000000001203091, -114.6726782920691079 ) ) ;
#25868=ADVANCED_FACE ( 'NONE', ( #73417 ), #254556, .T. ) ;
#25878=CIRCLE ( 'NONE', #17478, 7.800000000000001599 ) ;
#25888=LINE ( 'NONE', #201948, #186681 ) ;
#25917=DIRECTION ( 'NONE',  ( 0.000000000000000000, 0.000000000000000000, 1.000000000000000000 ) ) ;
#25919=VECTOR ( 'NONE', #179276, 1000.000000000000000 ) ;
#25920=ORIENTED_EDGE ( 'NONE', *, *, #50190, .F. ) ;
#25951=ORIENTED_EDGE ( 'NONE', *, *, #176024, .F. ) ;
#25952=VECTOR ( 'NONE', #229413, 1000.000000000000000 ) ;
#25955=DIRECTION ( 'NONE',  ( 0.000000000000000000, 0.000000000000000000, -1.000000000000000000 ) ) ;
#25959=DIRECTION ( 'NONE',  ( 0.000000000000000000, 0.000000000000000000, 1.000000000000000000 ) ) ;
#25962=CARTESIAN_POINT ( 'NONE',  ( -21.09610168723073187, 69.62104428478716045, -103.0566969914158477 ) ) ;
#25966=VECTOR ( 'NONE', #60568, 999.9999999999998863 ) ;
#25979=CARTESIAN_POINT ( 'NONE',  ( -21.05000000000000426, 69.52295361822210396, -102.9231074845243512 ) ) ;
#26006=DIRECTION ( 'NONE',  ( 0.000000000000000000, 6.938893903907030216E-14, -1.000000000000000000 ) ) ;
#26016=ORIENTED_EDGE ( 'NONE', *, *, #142093, .T. ) ;
#26035=ORIENTED_EDGE ( 'NONE', *, *, #43006, .F. ) ;
#26081=PLANE ( 'NONE',  #127060 ) ;
#26091=CARTESIAN_POINT ( 'NONE',  ( 21.05000000000000071, 70.15000000001192859, -92.89061026024637613 ) ) ;
#26133=ORIENTED_EDGE ( 'NONE', *, *, #114491, .T. ) ;
#26154=ORIENTED_EDGE ( 'NONE', *, *, #236306, .F. ) ;
#26157=VECTOR ( 'NONE', #130511, 1000.000000000000000 ) ;
#26262=PLANE ( 'NONE',  #92353 ) ;
#26270=DIRECTION ( 'NONE',  ( 0.7070776581709139474, 0.7071359030027652981, 2.946958787807621248E-14 ) ) ;
#26301=EDGE_LOOP ( 'NONE', ( #144035, #17981, #81912, #245528 ) ) ;
#26303=DIRECTION ( 'NONE',  ( -1.836970198721029934E-16, -1.000000000000000000, -6.982962677686266711E-15 ) ) ;
#26311=CARTESIAN_POINT ( 'NONE',  ( 23.14999999999999503, 69.35000000001186038, -90.87310748452435405 ) ) ;
#26326=EDGE_LOOP ( 'NONE', ( #126224, #101712, #31268, #245920 ) ) ;
#26359=ORIENTED_EDGE ( 'NONE', *, *, #49713, .T. ) ;
#26365=AXIS2_PLACEMENT_3D ( 'NONE', #244199, #107270, #10752 ) ;
#26395=AXIS2_PLACEMENT_3D ( 'NONE', #169945, #49938, #27853 ) ;
#26448=ORIENTED_EDGE ( 'NONE', *, *, #40824, .F. ) ;
#26454=LINE ( 'NONE', #27759, #160714 ) ;
#26466=ORIENTED_EDGE ( 'NONE', *, *, #130824, .F. ) ;
#26493=EDGE_CURVE ( 'NONE', #49226, #129819, #9902, .T. ) ;
#26498=AXIS2_PLACEMENT_3D ( 'NONE', #25853, #127512, #145770 ) ;
#26512=CARTESIAN_POINT ( 'NONE',  ( -18.59999999999999787, 77.83534155023627932, -91.46795619196132066 ) ) ;
#26567=ORIENTED_EDGE ( 'NONE', *, *, #205053, .F. ) ;
#26582=ADVANCED_FACE ( 'NONE', ( #55416 ), #119290, .T. ) ;
#26587=CARTESIAN_POINT ( 'NONE',  ( 18.59999999999999076, 64.35000000001177511, -78.17310748452437963 ) ) ;
#26613=CARTESIAN_POINT ( 'NONE',  ( -23.15000000000000213, 64.35000000001180354, -81.67310748452439384 ) ) ;
#26646=DIRECTION ( 'NONE',  ( 0.000000000000000000, -0.9654727137038715545, -0.2605042016806676242 ) ) ;
#26712=CARTESIAN_POINT ( 'NONE',  ( 18.59999999999999787, 76.00000000001195133, -103.0231074845243171 ) ) ;
#26720=EDGE_LOOP ( 'NONE', ( #204655, #177233, #234310, #92934 ) ) ;
#26723=EDGE_LOOP ( 'NONE', ( #55297, #170434, #134199, #26829 ) ) ;
#26726=SPHERICAL_SURFACE ( 'NONE', #18007, 0.1000000000000000056 ) ;
#26737=AXIS2_PLACEMENT_3D ( 'NONE', #241255, #24790, #104271 ) ;
#26802=AXIS2_PLACEMENT_3D ( 'NONE', #175496, #152084, #16422 ) ;
#26805=EDGE_CURVE ( 'NONE', #59500, #214176, #72565, .T. ) ;
#26817=CARTESIAN_POINT ( 'NONE',  ( -20.54999999999999716, 68.75000000001185185, -90.77310748452435973 ) ) ;
#26829=ORIENTED_EDGE ( 'NONE', *, *, #155562, .F. ) ;
#26841=AXIS2_PLACEMENT_3D ( 'NONE', #248989, #70368, #71636 ) ;
#26845=DIRECTION ( 'NONE',  ( 0.000000000000000000, -0.1568667991644355497, -0.9876197685951332295 ) ) ;
#26878=DIRECTION ( 'NONE',  ( 1.000000000000000000, 0.000000000000000000, 0.000000000000000000 ) ) ;
#26899=CARTESIAN_POINT ( 'NONE',  ( 18.39999999999999858, 85.50000000001166711, -62.92291809330220786 ) ) ;
#26912=DIRECTION ( 'NONE',  ( 1.000000000000000000, 0.000000000000000000, 0.000000000000000000 ) ) ;
#26929=DIRECTION ( 'NONE',  ( 0.000000000000000000, 1.000000000000000000, 6.982962677686266711E-15 ) ) ;
#26944=B_SPLINE_CURVE_WITH_KNOTS ( 'NONE', 3,
 ( #120160, #181402, #24898, #21045, #82239, #161841, #202229, #23628 ),
 .UNSPECIFIED., .F., .F.,
 ( 4, 2, 2, 4 ),
 ( 0.000000000000000000, 0.0001881495939909255417, 0.0002822243909863809941, 0.0003762991879818364466 ),
 .UNSPECIFIED. ) ;
#26960=ADVANCED_FACE ( 'NONE', ( #135957 ), #195965, .F. ) ;
#26977=DIRECTION ( 'NONE',  ( 0.000000000000000000, -0.9654727137038715545, 0.2605042016806676242 ) ) ;
#26981=ORIENTED_EDGE ( 'NONE', *, *, #211806, .F. ) ;
#27015=DIRECTION ( 'NONE',  ( 0.000000000000000000, 0.9915357197604804940, -0.1298341882520397950 ) ) ;
#27026=VECTOR ( 'NONE', #49744, 1000.000000000000000 ) ;
#27027=EDGE_LOOP ( 'NONE', ( #192512, #209647, #254644, #81028 ) ) ;
#27040=DIRECTION ( 'NONE',  ( 5.603264701231745086E-32, 7.172728831056619538E-15, -1.000000000000000000 ) ) ;
#27062=CIRCLE ( 'NONE', #97738, 0.1000000000000055705 ) ;
#27076=DIRECTION ( 'NONE',  ( 1.000000000000000000, 0.000000000000000000, 0.000000000000000000 ) ) ;
#27090=EDGE_CURVE ( 'NONE', #250150, #101654, #64141, .T. ) ;
#27094=EDGE_CURVE ( 'NONE', #116632, #51707, #147567, .T. ) ;
#27142=CARTESIAN_POINT ( 'NONE',  ( 20.94999999999999929, 84.73084112150721126, -93.42503276553991043 ) ) ;
#27143=ORIENTED_EDGE ( 'NONE', *, *, #16127, .T. ) ;
#27161=CARTESIAN_POINT ( 'NONE',  ( 18.49999999999999289, 69.55000000001203375, -114.7731074845243455 ) ) ;
#27174=DIRECTION ( 'NONE',  ( 1.000000000000000000, -0.000000000000000000, 0.000000000000000000 ) ) ;
#27176=CARTESIAN_POINT ( 'NONE',  ( 18.59999999999999076, 64.25000000001188027, -94.92310748452439384 ) ) ;
#27251=CARTESIAN_POINT ( 'NONE',  ( 21.05000000000000071, 76.00000000001170974, -69.52310748452431710 ) ) ;
#27262=AXIS2_PLACEMENT_3D ( 'NONE', #170156, #51409, #192258 ) ;
#27279=EDGE_CURVE ( 'NONE', #157975, #134789, #143643, .T. ) ;
#27292=FACE_OUTER_BOUND ( 'NONE', #104339, .T. ) ;
#27333=EDGE_LOOP ( 'NONE', ( #252121, #1190, #170431, #230798, #99315 ) ) ;
#27336=DIRECTION ( 'NONE',  ( 0.000000000000000000, -6.982962677686266711E-15, 1.000000000000000000 ) ) ;
#27366=ADVANCED_FACE ( 'NONE', ( #169703 ), #93582, .T. ) ;
#27373=CARTESIAN_POINT ( 'NONE',  ( -20.64999999999999858, 74.00000000001180922, -82.74772940728641402 ) ) ;
#27391=ORIENTED_EDGE ( 'NONE', *, *, #141565, .F. ) ;
#27397=ORIENTED_EDGE ( 'NONE', *, *, #153653, .T. ) ;
#27408=AXIS2_PLACEMENT_3D ( 'NONE', #55813, #16742, #23169 ) ;
#27439=AXIS2_PLACEMENT_3D ( 'NONE', #66732, #48433, #246633 ) ;
#27488=EDGE_LOOP ( 'NONE', ( #7079, #70275, #88920, #135124 ) ) ;
#27492=LINE ( 'NONE', #224355, #24817 ) ;
#27500=CIRCLE ( 'NONE', #206514, 0.9750000000000036415 ) ;
#27505=VERTEX_POINT ( 'NONE', #93321 ) ;
#27509=DIRECTION ( 'NONE',  ( -1.000000000000000000, 1.875376730785737719E-16, 1.309568571767809260E-30 ) ) ;
#27513=TOROIDAL_SURFACE ( 'NONE', #168978, 0.2000000000000000111, 0.1000000000000000056 ) ;
#27548=EDGE_CURVE ( 'NONE', #201392, #101974, #226850, .T. ) ;
#27563=DIRECTION ( 'NONE',  ( -0.000000000000000000, 6.982962677686266711E-15, -1.000000000000000000 ) ) ;
#27569=CARTESIAN_POINT ( 'NONE',  ( -20.89878130938411616, 65.67252876774509218, -63.94570419949945261 ) ) ;
#27612=DIRECTION ( 'NONE',  ( 0.000000000000000000, -7.056502275159894776E-15, 1.000000000000000000 ) ) ;
#27647=LINE ( 'NONE', #151424, #97304 ) ;
#27657=EDGE_CURVE ( 'NONE', #22313, #53558, #196275, .T. ) ;
#27682=CARTESIAN_POINT ( 'NONE',  ( -18.59999999999999787, 77.73625713160926409, -91.45445515550680682 ) ) ;
#27688=VERTEX_POINT ( 'NONE', #3195 ) ;
#27703=DIRECTION ( 'NONE',  ( -1.000000000000000000, -0.000000000000000000, -0.000000000000000000 ) ) ;
#27759=CARTESIAN_POINT ( 'NONE',  ( -20.54999999999999716, 68.85000000001183196, -86.27310748452435973 ) ) ;
#27760=PLANE ( 'NONE',  #2376 ) ;
#27769=EDGE_CURVE ( 'NONE', #125280, #53558, #210474, .T. ) ;
#27794=ORIENTED_EDGE ( 'NONE', *, *, #69215, .T. ) ;
#27825=DIRECTION ( 'NONE',  ( 1.000000000000000000, 0.000000000000000000, 0.000000000000000000 ) ) ;
#27837=CARTESIAN_POINT ( 'NONE',  ( 20.44999100639871514, 65.56028929680009298, -95.26403175855385541 ) ) ;
#27853=DIRECTION ( 'NONE',  ( -0.8660254037843878594, 0.000000000000000000, 0.5000000000000880407 ) ) ;
#27858=ORIENTED_EDGE ( 'NONE', *, *, #205053, .T. ) ;
#27910=EDGE_CURVE ( 'NONE', #209120, #255663, #67049, .T. ) ;
#27985=CIRCLE ( 'NONE', #165321, 0.1000000000000028644 ) ;
#27991=CARTESIAN_POINT ( 'NONE',  ( -22.46246831459151494, 75.97808783307259262, -114.6729720457342694 ) ) ;
#27999=DIRECTION ( 'NONE',  ( -1.000000000000000000, 3.265361837132813093E-16, 2.280189983783949500E-30 ) ) ;
#28016=DIRECTION ( 'NONE',  ( 0.000000000000000000, 0.000000000000000000, 1.000000000000000000 ) ) ;
#28042=DIRECTION ( 'NONE',  ( 0.000000000000000000, 0.6728971962616412394, 0.7397360091703134577 ) ) ;
#28049=CIRCLE ( 'NONE', #182147, 4.300000000000025580 ) ;
#28110=AXIS2_PLACEMENT_3D ( 'NONE', #85538, #188528, #110267 ) ;
#28133=VECTOR ( 'NONE', #107915, 1000.000000000000000 ) ;
#28145=EDGE_LOOP ( 'NONE', ( #205571, #191458, #243880, #58234 ) ) ;
#28147=EDGE_LOOP ( 'NONE', ( #77113, #65151, #100248, #129152 ) ) ;
#28164=CARTESIAN_POINT ( 'NONE',  ( 23.14999999999999503, 69.55000000001186322, -90.67310748452435121 ) ) ;
#28169=FACE_OUTER_BOUND ( 'NONE', #26326, .T. ) ;
#28170=DIRECTION ( 'NONE',  ( -3.265361837132813093E-16, -1.000000000000000000, -7.086529944415894657E-15 ) ) ;
#28171=EDGE_CURVE ( 'NONE', #35900, #224021, #148115, .T. ) ;
#28194=DIRECTION ( 'NONE',  ( 0.000000000000000000, 0.000000000000000000, 1.000000000000000000 ) ) ;
#28202=CYLINDRICAL_SURFACE ( 'NONE', #153688, 0.09999999999999939493 ) ;
#28254=CIRCLE ( 'NONE', #15788, 0.1000000000000028644 ) ;
#28262=DIRECTION ( 'NONE',  ( 1.000000000000000000, 0.000000000000000000, 0.000000000000000000 ) ) ;
#28277=AXIS2_PLACEMENT_3D ( 'NONE', #226900, #39634, #225591 ) ;
#28330=ORIENTED_EDGE ( 'NONE', *, *, #201735, .T. ) ;
#28347=DIRECTION ( 'NONE',  ( 1.000000000000000000, 0.000000000000000000, 0.000000000000000000 ) ) ;
#28396=DIRECTION ( 'NONE',  ( -1.000000000000000000, -0.000000000000000000, -0.000000000000000000 ) ) ;
#28404=AXIS2_PLACEMENT_3D ( 'NONE', #217550, #162753, #18082 ) ;
#28409=CARTESIAN_POINT ( 'NONE',  ( -21.05000000000000071, 64.25000000001175238, -76.53791325517833855 ) ) ;
#28450=AXIS2_PLACEMENT_3D ( 'NONE', #97069, #176671, #235332 ) ;
#28459=VERTEX_POINT ( 'NONE', #43024 ) ;
#28467=ORIENTED_EDGE ( 'NONE', *, *, #137886, .F. ) ;
#28493=DIRECTION ( 'NONE',  ( 0.000000000000000000, -6.982962677686266711E-15, 1.000000000000000000 ) ) ;
#28495=EDGE_CURVE ( 'NONE', #6502, #59214, #40173, .T. ) ;
#28501=CARTESIAN_POINT ( 'NONE',  ( 23.15000000000000213, 84.59626168225477727, -78.97323500167453858 ) ) ;
#28537=CARTESIAN_POINT ( 'NONE',  ( 23.15000000000000213, 87.75000000001186606, -90.77310748452423184 ) ) ;
#28551=DIRECTION ( 'NONE',  ( 1.000000000000000000, 0.000000000000000000, 0.000000000000000000 ) ) ;
#28553=CARTESIAN_POINT ( 'NONE',  ( 23.14999999999999858, 76.00000000001170974, -69.52310748452431710 ) ) ;
#28565=VECTOR ( 'NONE', #69248, 1000.000000000000000 ) ;
#28573=CARTESIAN_POINT ( 'NONE',  ( -21.14999999999999858, 69.45934304831071415, -103.0231074845243597 ) ) ;
#28630=ORIENTED_EDGE ( 'NONE', *, *, #176024, .T. ) ;
#28651=EDGE_LOOP ( 'NONE', ( #111008, #246381 ) ) ;
#28660=DIRECTION ( 'NONE',  ( 0.000000000000000000, -6.982962677686266711E-15, 1.000000000000000000 ) ) ;
#28662=VECTOR ( 'NONE', #89989, 1000.000000000000000 ) ;
#28697=CIRCLE ( 'NONE', #49498, 0.1000000000000028644 ) ;
#28714=ORIENTED_EDGE ( 'NONE', *, *, #85096, .F. ) ;
#28723=AXIS2_PLACEMENT_3D ( 'NONE', #157714, #201930, #257994 ) ;
#28762=TOROIDAL_SURFACE ( 'NONE', #70444, 1.900000000000002576, 0.1000000000000000056 ) ;
#28815=DIRECTION ( 'NONE',  ( 0.000000000000000000, 0.000000000000000000, -1.000000000000000000 ) ) ;
#28827=DIRECTION ( 'NONE',  ( 1.000000000000000000, 0.000000000000000000, 0.000000000000000000 ) ) ;
#28833=EDGE_CURVE ( 'NONE', #215370, #127649, #226122, .T. ) ;
#28838=EDGE_LOOP ( 'NONE', ( #30756, #65576, #254759, #190239 ) ) ;
#28840=CIRCLE ( 'NONE', #178663, 7.900000000000003908 ) ;
#28847=CARTESIAN_POINT ( 'NONE',  ( -20.94999999999999929, 77.16270174994990327, -94.92310748452430857 ) ) ;
#28853=EDGE_LOOP ( 'NONE', ( #85268, #107916, #129675, #157360, #229055, #128737, #247357, #41106, #18913, #37693, #82854, #132339, #62139, #128699, #165177, #131992, #13569, #88391 ) ) ;
#28863=CARTESIAN_POINT ( 'NONE',  ( -20.92356734117541706, 65.68026841930881687, -63.97257401318893955 ) ) ;
#28899=CARTESIAN_POINT ( 'NONE',  ( 20.94999999999999574, 74.25000000001186606, -91.35359592662267403 ) ) ;
#28941=DIRECTION ( 'NONE',  ( 0.000000000000000000, 1.000000000000000000, 6.688090509790097607E-15 ) ) ;
#28950=ADVANCED_FACE ( 'NONE', ( #244427 ), #65794, .F. ) ;
#28964=EDGE_CURVE ( 'NONE', #194795, #165593, #98463, .T. ) ;
#28966=CARTESIAN_POINT ( 'NONE',  ( 19.58285714285715073, 65.61500148966047163, -95.39342281713442162 ) ) ;
#29007=ADVANCED_FACE ( 'NONE', ( #107487 ), #111349, .T. ) ;
#29019=EDGE_LOOP ( 'NONE', ( #246473, #107821, #226374, #208374 ) ) ;
#29022=CARTESIAN_POINT ( 'NONE',  ( 20.94999999999999929, 69.45000000001186891, -90.77310748452435973 ) ) ;
#29046=ORIENTED_EDGE ( 'NONE', *, *, #106565, .T. ) ;
#29086=CARTESIAN_POINT ( 'NONE',  ( -20.94999999999999929, 74.63912941281984104, -94.95010955743335046 ) ) ;
#29113=DIRECTION ( 'NONE',  ( 1.000000000000000000, 0.000000000000000000, 0.000000000000000000 ) ) ;
#29125=CIRCLE ( 'NONE', #8417, 0.1000000000000028644 ) ;
#29138=CARTESIAN_POINT ( 'NONE',  ( 20.86036036209901923, 65.37895722344093485, -95.35675906601939289 ) ) ;
#29146=DIRECTION ( 'NONE',  ( 0.000000000000000000, 1.000000000000000000, 6.982962677686266711E-15 ) ) ;
#29194=CARTESIAN_POINT ( 'NONE',  ( 20.94999999999999929, 76.00000000001195133, -103.0231074845243171 ) ) ;
#29208=EDGE_LOOP ( 'NONE', ( #112153, #111300, #139923, #74856 ) ) ;
#29215=ORIENTED_EDGE ( 'NONE', *, *, #101182, .T. ) ;
#29292=FACE_OUTER_BOUND ( 'NONE', #72042, .T. ) ;
#29295=CIRCLE ( 'NONE', #150080, 12.77499999999999503 ) ;
#29347=DIRECTION ( 'NONE',  ( 0.000000000000000000, -7.304098846218139203E-15, 1.000000000000000000 ) ) ;
#29358=CARTESIAN_POINT ( 'NONE',  ( -18.50596464788227635, 65.69367753730635684, -64.01892380663478832 ) ) ;
#29374=AXIS2_PLACEMENT_3D ( 'NONE', #150071, #189182, #229593 ) ;
#29381=DIRECTION ( 'NONE',  ( 0.000000000000000000, -6.853228547068871147E-15, 1.000000000000000000 ) ) ;
#29382=DIRECTION ( 'NONE',  ( 0.000000000000000000, -0.9915357197604892647, 0.1298341882519715440 ) ) ;
#29385=ORIENTED_EDGE ( 'NONE', *, *, #26805, .T. ) ;
#29417=AXIS2_PLACEMENT_3D ( 'NONE', #7371, #222552, #160062 ) ;
#29464=EDGE_LOOP ( 'NONE', ( #210812, #218388, #42491, #59254 ) ) ;
#29466=FACE_OUTER_BOUND ( 'NONE', #68722, .T. ) ;
#29518=FACE_OUTER_BOUND ( 'NONE', #215336, .T. ) ;
#29557=( BOUNDED_SURFACE ( )  B_SPLINE_SURFACE ( 3, 2, ( 
 ( #204422, #44082, #25798 ),
 ( #6221, #4917, #128762 ),
 ( #83167, #225257, #123625 ),
 ( #126167, #8810, #247401 ),
 ( #147013, #162763, #7518 ),
 ( #87029, #207007, #28409 ) ),
 .UNSPECIFIED., .F., .F., .F. ) 
 B_SPLINE_SURFACE_WITH_KNOTS ( ( 4, 2, 4 ),
 ( 3, 3 ),
 ( 1.570796326794897668, 2.356194490192346169, 3.141592653589794448 ),
 ( 0.000000000000000000, 1.000000000000000000 ),
 .UNSPECIFIED. ) 
 GEOMETRIC_REPRESENTATION_ITEM ( )  RATIONAL_B_SPLINE_SURFACE ( (
 ( 1.000000000000000000, 0.7071067811865597852, 1.000000000000000000),
 ( 1.000000000000000000, 0.6611148371778731159, 1.000000000000000000),
 ( 1.000000000000000000, 0.6092287576696180373, 1.000000000000000000),
 ( 1.000000000000000000, 0.5278258667058124409, 1.000000000000000000),
 ( 1.000000000000000000, 0.4993418825333900690, 1.000000000000000000),
 ( 1.000000000000000000, 0.5000000000000154321, 1.000000000000000000) ) ) 
 REPRESENTATION_ITEM ( '' )  SURFACE ( )  );
#29571=DIRECTION ( 'NONE',  ( -0.000000000000000000, 1.000000000000000000, 6.982962677686266711E-15 ) ) ;
#29572=FACE_BOUND ( 'NONE', #236359, .T. ) ;
#29573=CARTESIAN_POINT ( 'NONE',  ( 20.94999999999999574, 87.39257802171759693, -99.94915790469229933 ) ) ;
#29597=CARTESIAN_POINT ( 'NONE',  ( -23.25000000000000000, 76.00000000001195133, -103.0231074845243171 ) ) ;
#29601=DIRECTION ( 'NONE',  ( -0.000000000000000000, 0.1350103645451807555, 0.9908441862701610203 ) ) ;
#29629=( BOUNDED_SURFACE ( )  B_SPLINE_SURFACE ( 3, 2, ( 
 ( #98867, #256635, #71977 ),
 ( #31590, #111092, #58467 ),
 ( #12015, #78046, #158905 ),
 ( #91535, #171117, #250593 ),
 ( #239707, #100156, #240988 ),
 ( #179739, #1057, #63625 ) ),
 .UNSPECIFIED., .F., .F., .F. ) 
 B_SPLINE_SURFACE_WITH_KNOTS ( ( 4, 2, 4 ),
 ( 3, 3 ),
 ( 6.719893378899590472E-05, 0.0002757154632485403294, 0.0004842319927080847406 ),
 ( 0.000000000000000000, 1.000000000000000000 ),
 .UNSPECIFIED. ) 
 GEOMETRIC_REPRESENTATION_ITEM ( )  RATIONAL_B_SPLINE_SURFACE ( (
 ( 1.000000000000000000, 0.7250110520819756932, 1.000000000000000000),
 ( 1.000000000000000000, 0.7277932058368190571, 1.000000000000000000),
 ( 1.000000000000000000, 0.7278452872605407631, 1.000000000000000000),
 ( 1.000000000000000000, 0.7221445671561397273, 1.000000000000000000),
 ( 1.000000000000000000, 0.7163662143770669344, 1.000000000000000000),
 ( 1.000000000000000000, 0.7071067811865475727, 1.000000000000000000) ) ) 
 REPRESENTATION_ITEM ( '' )  SURFACE ( )  );
#29633=AXIS2_PLACEMENT_3D ( 'NONE', #44089, #6228, #124919 ) ;
#29642=EDGE_CURVE ( 'NONE', #99108, #111684, #234983, .T. ) ;
#29648=SPHERICAL_SURFACE ( 'NONE', #200307, 0.1000000000000000056 ) ;
#29703=DIRECTION ( 'NONE',  ( 0.000000000000000000, 0.000000000000000000, -1.000000000000000000 ) ) ;
#29741=CARTESIAN_POINT ( 'NONE',  ( 20.94999999999999929, 76.00000000001173817, -73.52310748452431710 ) ) ;
#29780=EDGE_CURVE ( 'NONE', #112762, #88936, #143196, .T. ) ;
#29786=DIRECTION ( 'NONE',  ( -0.000000000000000000, 1.000000000000000000, 6.982962677686266711E-15 ) ) ;
#29790=CIRCLE ( 'NONE', #246414, 0.5000000000000004441 ) ;
#29826=ORIENTED_EDGE ( 'NONE', *, *, #203270, .F. ) ;
#29855=DIRECTION ( 'NONE',  ( 1.000000000000000000, -3.265361837132813093E-16, -2.280189983783949500E-30 ) ) ;
#29877=CARTESIAN_POINT ( 'NONE',  ( -20.94999999999999929, 74.83729825007388570, -95.12310748452432563 ) ) ;
#29894=DIRECTION ( 'NONE',  ( -1.000000000000000000, 0.000000000000000000, 0.000000000000000000 ) ) ;
#29906=VERTEX_POINT ( 'NONE', #251515 ) ;
#29913=EDGE_LOOP ( 'NONE', ( #202104, #66245, #251538, #171345 ) ) ;
#29920=VERTEX_POINT ( 'NONE', #16787 ) ;
#29946=DIRECTION ( 'NONE',  ( 0.000000000000000000, 0.000000000000000000, -1.000000000000000000 ) ) ;
#29960=AXIS2_PLACEMENT_3D ( 'NONE', #46527, #43978, #27015 ) ;
#29966=CIRCLE ( 'NONE', #59119, 11.80000000000000426 ) ;
#29983=VECTOR ( 'NONE', #161029, 1000.000000000000000 ) ;
#29990=ORIENTED_EDGE ( 'NONE', *, *, #77044, .T. ) ;
#29994=EDGE_LOOP ( 'NONE', ( #163652, #110192, #52928, #249685, #114836, #8278, #32152, #24584, #42163, #170412, #10672, #251547 ) ) ;
#30010=ORIENTED_EDGE ( 'NONE', *, *, #245366, .T. ) ;
#30024=DIRECTION ( 'NONE',  ( 0.000000000000000000, 0.000000000000000000, 1.000000000000000000 ) ) ;
#30033=ORIENTED_EDGE ( 'NONE', *, *, #163048, .T. ) ;
#30066=CARTESIAN_POINT ( 'NONE',  ( -23.15000000000000213, 76.00000000001168132, -65.62310748452431142 ) ) ;
#30112=CIRCLE ( 'NONE', #79925, 0.09999999999999939493 ) ;
#30124=FACE_OUTER_BOUND ( 'NONE', #246390, .T. ) ;
#30126=AXIS2_PLACEMENT_3D ( 'NONE', #200722, #2497, #97731 ) ;
#30151=ORIENTED_EDGE ( 'NONE', *, *, #52883, .F. ) ;
#30192=CARTESIAN_POINT ( 'NONE',  ( 18.52928932188133970, 65.72071067813041623, -78.37310748452439668 ) ) ;
#30218=CARTESIAN_POINT ( 'NONE',  ( 21.05000000000000071, 67.22371710471938400, -90.87310748452436826 ) ) ;
#30243=ORIENTED_EDGE ( 'NONE', *, *, #82959, .F. ) ;
#30252=AXIS2_PLACEMENT_3D ( 'NONE', #90691, #169001, #227634 ) ;
#30267=ADVANCED_FACE ( 'NONE', ( #136360 ), #31000, .T. ) ;
#30371=CARTESIAN_POINT ( 'NONE',  ( 22.39999999999999503, 64.25000000001193712, -102.9231074845243938 ) ) ;
#30387=VERTEX_POINT ( 'NONE', #126785 ) ;
#30389=CARTESIAN_POINT ( 'NONE',  ( 20.54374330479327426, 65.49498968578889446, -95.29742384963557811 ) ) ;
#30410=CARTESIAN_POINT ( 'NONE',  ( 18.49999999999999289, 65.67426406872368716, -78.17310748452437963 ) ) ;
#30435=FACE_OUTER_BOUND ( 'NONE', #73997, .T. ) ;
#30453=FACE_OUTER_BOUND ( 'NONE', #102125, .T. ) ;
#30455=ORIENTED_EDGE ( 'NONE', *, *, #181212, .F. ) ;
#30480=CIRCLE ( 'NONE', #255253, 0.1000000000000028644 ) ;
#30498=ORIENTED_EDGE ( 'NONE', *, *, #175367, .T. ) ;
#30499=CARTESIAN_POINT ( 'NONE',  ( 23.24999999999999289, 69.55000000001179217, -81.87310748452435405 ) ) ;
#30521=CARTESIAN_POINT ( 'NONE',  ( -20.94999999999999929, 70.10000000001177511, -79.74220724918072278 ) ) ;
#30555=DIRECTION ( 'NONE',  ( 1.000000000000000000, 0.000000000000000000, 0.000000000000000000 ) ) ;
#30587=CARTESIAN_POINT ( 'NONE',  ( 20.90851465518106167, 65.67467670974397720, -63.95317318268842399 ) ) ;
#30625=CARTESIAN_POINT ( 'NONE',  ( -18.51697539158857353, 65.68434038414338261, -63.98668807260654745 ) ) ;
#30638=ORIENTED_EDGE ( 'NONE', *, *, #167170, .T. ) ;
#30655=ORIENTED_EDGE ( 'NONE', *, *, #212941, .T. ) ;
#30659=VERTEX_POINT ( 'NONE', #157954 ) ;
#30670=ORIENTED_EDGE ( 'NONE', *, *, #189260, .T. ) ;
#30683=DIRECTION ( 'NONE',  ( -7.304098846217948299E-16, -1.000000000000000000, 0.000000000000000000 ) ) ;
#30711=CARTESIAN_POINT ( 'NONE',  ( -18.59999999999999787, 66.75000000001179501, -81.77310748452437394 ) ) ;
#30731=DIRECTION ( 'NONE',  ( 0.000000000000000000, 6.982962677686266711E-15, -1.000000000000000000 ) ) ;
#30736=DIRECTION ( 'NONE',  ( 0.000000000000000000, 0.000000000000000000, -1.000000000000000000 ) ) ;
#30744=LINE ( 'NONE', #188503, #190893 ) ;
#30756=ORIENTED_EDGE ( 'NONE', *, *, #22420, .T. ) ;
#30767=LINE ( 'NONE', #12482, #184234 ) ;
#30783=LINE ( 'NONE', #17308, #238380 ) ;
#30806=CARTESIAN_POINT ( 'NONE',  ( 18.39999999999999858, 85.68240343348806221, -62.86626410711144786 ) ) ;
#30825=CIRCLE ( 'NONE', #176566, 0.09999999999999520384 ) ;
#30849=CIRCLE ( 'NONE', #160030, 0.1000000000000028644 ) ;
#30853=CARTESIAN_POINT ( 'NONE',  ( 21.05000000000000071, 76.00000000001195133, -103.0231074845243171 ) ) ;
#30856=DIRECTION ( 'NONE',  ( 1.000000000000000000, 0.000000000000000000, 0.000000000000000000 ) ) ;
#30914=DIRECTION ( 'NONE',  ( 0.000000000000000000, 6.982962677686266711E-15, -1.000000000000000000 ) ) ;
#30932=EDGE_LOOP ( 'NONE', ( #258077, #162277, #255382, #144485 ) ) ;
#30945=CIRCLE ( 'NONE', #160112, 0.1000000000000028644 ) ;
#30985=ORIENTED_EDGE ( 'NONE', *, *, #115469, .T. ) ;
#31000=TOROIDAL_SURFACE ( 'NONE', #164258, 11.65000000000000036, 0.1000000000000000056 ) ;
#31061=ORIENTED_EDGE ( 'NONE', *, *, #156338, .T. ) ;
#31062=DIRECTION ( 'NONE',  ( 0.000000000000000000, 1.000000000000000000, 0.000000000000000000 ) ) ;
#31079=DIRECTION ( 'NONE',  ( -1.000000000000000000, -0.000000000000000000, -0.000000000000000000 ) ) ;
#31090=LINE ( 'NONE', #173180, #2315 ) ;
#31103=ORIENTED_EDGE ( 'NONE', *, *, #54517, .T. ) ;
#31181=CARTESIAN_POINT ( 'NONE',  ( -23.15000000000000213, 70.10000000001177511, -79.74220724918072278 ) ) ;
#31185=ORIENTED_EDGE ( 'NONE', *, *, #250928, .F. ) ;
#31229=DIRECTION ( 'NONE',  ( 0.000000000000000000, 1.000000000000000000, 8.717686153663073805E-15 ) ) ;
#31233=CIRCLE ( 'NONE', #176957, 0.1000000000000028644 ) ;
#31250=CARTESIAN_POINT ( 'NONE',  ( 23.14999999999999858, 76.00000000001170974, -69.52310748452431710 ) ) ;
#31262=AXIS2_PLACEMENT_3D ( 'NONE', #74616, #56277, #166326 ) ;
#31263=ORIENTED_EDGE ( 'NONE', *, *, #255330, .F. ) ;
#31268=ORIENTED_EDGE ( 'NONE', *, *, #206744, .F. ) ;
#31283=EDGE_LOOP ( 'NONE', ( #154774, #195519, #115257 ) ) ;
#31327=COLOUR_RGB ( '', 0.66274510, 0.83137255, 0.94901961) ;
#31389=CARTESIAN_POINT ( 'NONE',  ( 20.94999999999999929, 69.15387683765909799, -65.78538121767449809 ) ) ;
#31400=EDGE_LOOP ( 'NONE', ( #48508, #131940, #16758, #112596 ) ) ;
#31442=AXIS2_PLACEMENT_3D ( 'NONE', #65281, #144801, #43162 ) ;
#31444=ORIENTED_EDGE ( 'NONE', *, *, #135373, .F. ) ;
#31455=CARTESIAN_POINT ( 'NONE',  ( -21.05000000000000071, 69.45934304831071415, -102.9231074845243512 ) ) ;
#31462=DIRECTION ( 'NONE',  ( 0.000000000000000000, -0.8660254037844343777, 0.5000000000000074385 ) ) ;
#31472=DIRECTION ( 'NONE',  ( 0.000000000000000000, -6.467318590049456648E-15, 1.000000000000000000 ) ) ;
#31473=DIRECTION ( 'NONE',  ( -1.000000000000000000, 2.952720810173289112E-16, 2.061873921506763405E-30 ) ) ;
#31487=CARTESIAN_POINT ( 'NONE',  ( 18.49999999999999289, 65.79142135624907439, -78.37310748452439668 ) ) ;
#31497=CARTESIAN_POINT ( 'NONE',  ( -18.59999999999999787, 85.50000000001189449, -94.92310748452425173 ) ) ;
#31510=CARTESIAN_POINT ( 'NONE',  ( 20.85000000106584750, 64.25000000001175238, -76.36760282805070688 ) ) ;
#31514=CARTESIAN_POINT ( 'NONE',  ( 22.39999999999999503, 76.00000000001200817, -110.8138870828976934 ) ) ;
#31515=CARTESIAN_POINT ( 'NONE',  ( -20.64999999999999858, 71.65000000001187175, -90.77310748452434552 ) ) ;
#31531=ADVANCED_FACE ( 'NONE', ( #144621 ), #65098, .T. ) ;
#31543=EDGE_CURVE ( 'NONE', #163251, #25250, #176895, .T. ) ;
#31548=DIRECTION ( 'NONE',  ( 1.000000000000000000, -1.836970198721029934E-16, -1.282749433769087582E-30 ) ) ;
#31549=ORIENTED_EDGE ( 'NONE', *, *, #96771, .T. ) ;
#31551=EDGE_LOOP ( 'NONE', ( #171014, #1988, #188610, #169109 ) ) ;
#31568=EDGE_LOOP ( 'NONE', ( #35755, #188677, #31885 ) ) ;
#31590=CARTESIAN_POINT ( 'NONE',  ( 21.05000000000000071, 65.27628318601222190, -95.42870824864037615 ) ) ;
#31606=VERTEX_POINT ( 'NONE', #214873 ) ;
#31640=EDGE_LOOP ( 'NONE', ( #205707, #45684, #85234, #101435, #217644 ) ) ;
#31641=EDGE_CURVE ( 'NONE', #20026, #78455, #181178, .T. ) ;
#31659=ORIENTED_EDGE ( 'NONE', *, *, #256937, .F. ) ;
#31660=AXIS2_PLACEMENT_3D ( 'NONE', #242912, #104655, #142521 ) ;
#31667=DIRECTION ( 'NONE',  ( 0.000000000000000000, 6.853228547068871147E-15, -1.000000000000000000 ) ) ;
#31670=CARTESIAN_POINT ( 'NONE',  ( 18.45036689428371446, 85.49018414334094018, -96.01041165703843205 ) ) ;
#31681=DIRECTION ( 'NONE',  ( 0.000000000000000000, 7.109473446599835262E-15, -1.000000000000000000 ) ) ;
#31684=PLANE ( 'NONE',  #72660 ) ;
#31810=VERTEX_POINT ( 'NONE', #227390 ) ;
#31840=DIRECTION ( 'NONE',  ( 0.7071067811865475727, 0.7071067811865475727, 4.937700262164531476E-15 ) ) ;
#31854=ORIENTED_EDGE ( 'NONE', *, *, #175726, .F. ) ;
#31875=CARTESIAN_POINT ( 'NONE',  ( 20.94788355080264353, 65.69792220476300315, -64.03355541284614105 ) ) ;
#31879=ORIENTED_EDGE ( 'NONE', *, *, #41676, .T. ) ;
#31885=ORIENTED_EDGE ( 'NONE', *, *, #154632, .F. ) ;
#31894=DIRECTION ( 'NONE',  ( 0.000000000000000000, -6.982962677686266711E-15, 1.000000000000000000 ) ) ;
#31911=CARTESIAN_POINT ( 'NONE',  ( -20.64999999999999858, 85.50000000001179501, -79.41707660717668205 ) ) ;
#31940=EDGE_LOOP ( 'NONE', ( #239675, #65514, #249010, #403, #102660 ) ) ;
#31959=DIRECTION ( 'NONE',  ( 0.000000000000000000, 0.9915357197604862671, -0.1298341882519953583 ) ) ;
#31976=AXIS2_PLACEMENT_3D ( 'NONE', #93058, #31840, #68373 ) ;
#32005=ORIENTED_EDGE ( 'NONE', *, *, #202457, .F. ) ;
#32014=DIRECTION ( 'NONE',  ( -1.000000000000000000, 0.000000000000000000, -0.000000000000000000 ) ) ;
#32057=DIRECTION ( 'NONE',  ( 1.000000000000000000, 0.000000000000000000, 0.000000000000000000 ) ) ;
#32082=CARTESIAN_POINT ( 'NONE',  ( 20.95512820512820440, 65.37615131629992504, -81.77310748452438816 ) ) ;
#32101=ORIENTED_EDGE ( 'NONE', *, *, #85862, .F. ) ;
#32120=CARTESIAN_POINT ( 'NONE',  ( -23.25000000000000000, 71.65000000001187175, -90.87310748452432563 ) ) ;
#32152=ORIENTED_EDGE ( 'NONE', *, *, #3321, .F. ) ;
#32166=EDGE_CURVE ( 'NONE', #113736, #253910, #81346, .T. ) ;
#32168=ORIENTED_EDGE ( 'NONE', *, *, #133496, .T. ) ;
#32187=LINE ( 'NONE', #125183, #1719 ) ;
#32263=CARTESIAN_POINT ( 'NONE',  ( 19.92426406871192412, 64.25000000001176659, -78.17310748452437963 ) ) ;
#32269=EDGE_CURVE ( 'NONE', #167954, #22444, #225783, .T. ) ;
#32275=ORIENTED_EDGE ( 'NONE', *, *, #87984, .F. ) ;
#32311=EDGE_LOOP ( 'NONE', ( #121270, #1949, #109539, #179872 ) ) ;
#32329=DIRECTION ( 'NONE',  ( 0.000000000000000000, 0.8660254037844281605, -0.5000000000000185407 ) ) ;
#32350=EDGE_LOOP ( 'NONE', ( #6730, #208573, #83221 ) ) ;
#32380=DIRECTION ( 'NONE',  ( -1.000000000000000000, -0.000000000000000000, 0.000000000000000000 ) ) ;
#32382=ORIENTED_EDGE ( 'NONE', *, *, #89868, .F. ) ;
#32419=CIRCLE ( 'NONE', #207368, 11.90000000000000746 ) ;
#32431=ORIENTED_EDGE ( 'NONE', *, *, #136107, .F. ) ;
#32432=ORIENTED_EDGE ( 'NONE', *, *, #67581, .T. ) ;
#32456=DIRECTION ( 'NONE',  ( 1.000000000000000000, -2.952720810173289112E-16, -2.061873921506763405E-30 ) ) ;
#32463=EDGE_CURVE ( 'NONE', #80661, #214176, #183804, .T. ) ;
#32472=CARTESIAN_POINT ( 'NONE',  ( 23.14999999999999503, 64.35000000001176090, -76.53791325517833855 ) ) ;
#32498=CIRCLE ( 'NONE', #178229, 0.2000000000000057288 ) ;
#32535=CARTESIAN_POINT ( 'NONE',  ( 21.14999999999999503, 64.25000000001195133, -103.0231074845244024 ) ) ;
#32539=FACE_OUTER_BOUND ( 'NONE', #11232, .T. ) ;
#32544=CARTESIAN_POINT ( 'NONE',  ( 21.05000000000000071, 70.15000000001178648, -79.65560470880227228 ) ) ;
#32578=PRODUCT_DEFINITION ( 'UNKNOWN', '', #15469, #94935 ) ;
#32587=SPHERICAL_SURFACE ( 'NONE', #244395, 0.1000000000000000056 ) ;
#32600=DIRECTION ( 'NONE',  ( 0.000000000000000000, 1.000000000000000000, 7.116814260417668513E-15 ) ) ;
#32614=LINE ( 'NONE', #76828, #1038 ) ;
#32628=CARTESIAN_POINT ( 'NONE',  ( -23.25000000000000000, 76.10085836911075319, -114.7726746080137019 ) ) ;
#32631=VERTEX_POINT ( 'NONE', #106818 ) ;
#32639=( BOUNDED_SURFACE ( )  B_SPLINE_SURFACE ( 3, 2, ( 
 ( #190921, #156926, #236428 ),
 ( #210465, #33145, #151791 ),
 ( #112641, #73542, #153091 ),
 ( #117768, #4226, #163329 ),
 ( #103324, #199896, #82462 ),
 ( #197298, #19977, #182898 ),
 ( #139882, #99464, #177771 ),
 ( #61650, #239008, #59044 ),
 ( #240297, #57777, #21271 ),
 ( #100732, #198583, #60355 ) ),
 .UNSPECIFIED., .F., .F., .F. ) 
 B_SPLINE_SURFACE_WITH_KNOTS ( ( 4, 2, 2, 2, 4 ),
 ( 3, 3 ),
 ( 0.0001836757140119223738, 0.0004000170051583624682, 0.0005081876507315825561, 0.0005622729735181925459, 0.0006163582963048025356 ),
 ( 0.000000000000000000, 1.000000000000000000 ),
 .UNSPECIFIED. ) 
 GEOMETRIC_REPRESENTATION_ITEM ( )  RATIONAL_B_SPLINE_SURFACE ( (
 ( 1.000000000000000000, 0.7071067811865475727, 1.000000000000000000),
 ( 1.000000000000000000, 0.6461995200020562713, 1.000000000000000000),
 ( 1.000000000000000000, 0.5776453529561037525, 1.000000000000000000),
 ( 1.000000000000000000, 0.4585233068345877516, 1.000000000000000000),
 ( 1.000000000000000000, 0.4154092989934964342, 1.000000000000000000),
 ( 1.000000000000000000, 0.3550093145838849051, 1.000000000000000000),
 ( 1.000000000000000000, 0.3354498651684990618, 1.000000000000000000),
 ( 1.000000000000000000, 0.3060347992256760019, 1.000000000000000000),
 ( 1.000000000000000000, 0.2963555829626124960, 1.000000000000000000),
 ( 1.000000000000000000, 0.2966190024560606542, 1.000000000000000000) ) ) 
 REPRESENTATION_ITEM ( '' )  SURFACE ( )  );
#32663=CYLINDRICAL_SURFACE ( 'NONE', #74974, 0.1000000000000028644 ) ;
#32688=CARTESIAN_POINT ( 'NONE',  ( -22.50000000000000000, 64.25043287652256652, -103.1239658536230763 ) ) ;
#32719=ORIENTED_EDGE ( 'NONE', *, *, #98257, .F. ) ;
#32730=AXIS2_PLACEMENT_3D ( 'NONE', #115387, #159666, #20159 ) ;
#32752=DIRECTION ( 'NONE',  ( 0.000000000000000000, 1.000000000000000000, 7.272083257015735086E-15 ) ) ;
#32786=DIRECTION ( 'NONE',  ( 0.000000000000000000, 0.000000000000000000, 1.000000000000000000 ) ) ;
#32795=ORIENTED_EDGE ( 'NONE', *, *, #161133, .F. ) ;
#32803=AXIS2_PLACEMENT_3D ( 'NONE', #233472, #73126, #116080 ) ;
#32860=CARTESIAN_POINT ( 'NONE',  ( 21.07928932188134397, 75.90110485435759813, -109.3516241409176217 ) ) ;
#32883=CARTESIAN_POINT ( 'NONE',  ( 20.94999999999999929, 76.00000000001168132, -65.42310748452432279 ) ) ;
#32903=ORIENTED_EDGE ( 'NONE', *, *, #158209, .F. ) ;
#32939=VECTOR ( 'NONE', #99575, 1000.000000000000000 ) ;
#32974=CARTESIAN_POINT ( 'NONE',  ( 22.39999999999999503, 76.10085836911075319, -114.7726746080137019 ) ) ;
#32979=DIRECTION ( 'NONE',  ( 0.000000000000000000, 0.000000000000000000, -1.000000000000000000 ) ) ;
#32980=AXIS2_PLACEMENT_3D ( 'NONE', #179229, #154543, #138749 ) ;
#33006=CARTESIAN_POINT ( 'NONE',  ( 21.14999999999999858, 64.35000000001186038, -90.77310748452438816 ) ) ;
#33012=ORIENTED_EDGE ( 'NONE', *, *, #115588, .F. ) ;
#33024=FACE_OUTER_BOUND ( 'NONE', #183580, .T. ) ;
#33039=AXIS2_PLACEMENT_3D ( 'NONE', #204274, #41390, #240859 ) ;
#33055=DIRECTION ( 'NONE',  ( 0.000000000000000000, 1.000000000000000000, 6.982962677686266711E-15 ) ) ;
#33087=CARTESIAN_POINT ( 'NONE',  ( 21.09706851349342216, 67.22415748653845924, -90.78754126812472691 ) ) ;
#33094=ORIENTED_EDGE ( 'NONE', *, *, #216630, .F. ) ;
#33125=ORIENTED_EDGE ( 'NONE', *, *, #157365, .F. ) ;
#33144=DIRECTION ( 'NONE',  ( 0.000000000000000000, 1.000000000000000000, 7.116814260417668513E-15 ) ) ;
#33145=CARTESIAN_POINT ( 'NONE',  ( -18.48179518609137517, 85.51832530050651826, -62.63340190776217753 ) ) ;
#33170=CYLINDRICAL_SURFACE ( 'NONE', #107097, 0.5000000000000004441 ) ;
#33182=AXIS2_PLACEMENT_3D ( 'NONE', #116928, #196454, #37408 ) ;
#33202=CARTESIAN_POINT ( 'NONE',  ( -23.15000000000000213, 76.00000000001170974, -69.52310748452431710 ) ) ;
#33203=DIRECTION ( 'NONE',  ( 1.000000000000000000, 0.000000000000000000, 0.000000000000000000 ) ) ;
#33212=CARTESIAN_POINT ( 'NONE',  ( -18.50211644919735576, 65.69792220476300315, -64.03355541284614105 ) ) ;
#33213=CIRCLE ( 'NONE', #49912, 0.09999999999999939493 ) ;
#33219=DIRECTION ( 'NONE',  ( -2.915501640297152804E-16, -1.000000000000000000, -6.997203936713167125E-15 ) ) ;
#33240=DIRECTION ( 'NONE',  ( 1.000000000000000000, 0.000000000000000000, 0.000000000000000000 ) ) ;
#33264=CIRCLE ( 'NONE', #120552, 0.09999999999999971412 ) ;
#33265=CARTESIAN_POINT ( 'NONE',  ( -21.07928932188134041, 69.67148334361864670, -103.1220026301787414 ) ) ;
#33285=DIRECTION ( 'NONE',  ( 1.000000000000000000, 0.000000000000000000, 0.000000000000000000 ) ) ;
#33286=DIRECTION ( 'NONE',  ( -0.7071067811865474617, 0.7071067811865474617, 4.937700262164531476E-15 ) ) ;
#33337=LINE ( 'NONE', #175403, #142635 ) ;
#33385=CARTESIAN_POINT ( 'NONE',  ( 18.50000000000000355, 85.42107434499828855, -62.69863542509442311 ) ) ;
#33394=DIRECTION ( 'NONE',  ( -1.000000000000000000, -0.000000000000000000, -0.000000000000000000 ) ) ;
#33399=DIRECTION ( 'NONE',  ( 0.000000000000000000, -1.000000000000000000, -6.982962677686266711E-15 ) ) ;
#33429=DIRECTION ( 'NONE',  ( 0.000000000000000000, 0.000000000000000000, 1.000000000000000000 ) ) ;
#33438=CIRCLE ( 'NONE', #120911, 12.87499999999999822 ) ;
#33470=CIRCLE ( 'NONE', #183272, 0.1999999999999987899 ) ;
#33474=EDGE_LOOP ( 'NONE', ( #102701, #232933, #84603, #6651 ) ) ;
#33488=ADVANCED_FACE ( 'NONE', ( #231320 ), #52646, .T. ) ;
#33500=EDGE_CURVE ( 'NONE', #210647, #220516, #256838, .T. ) ;
#33527=EDGE_CURVE ( 'NONE', #123690, #113902, #27985, .T. ) ;
#33544=DIRECTION ( 'NONE',  ( 1.000000000000000000, 7.304098846218134667E-16, 5.100424963727256530E-30 ) ) ;
#33562=DIRECTION ( 'NONE',  ( 0.000000000000000000, 4.163336342344217877E-13, -1.000000000000000000 ) ) ;
#33608=VECTOR ( 'NONE', #54978, 1000.000000000000000 ) ;
#33631=ORIENTED_EDGE ( 'NONE', *, *, #233406, .F. ) ;
#33646=EDGE_LOOP ( 'NONE', ( #253217, #127986, #222732, #139321 ) ) ;
#33666=CARTESIAN_POINT ( 'NONE',  ( 21.30000000000002558, 76.00000000001192291, -98.97310748452431994 ) ) ;
#33698=AXIS2_PLACEMENT_3D ( 'NONE', #28847, #249145, #193012 ) ;
#33723=DIRECTION ( 'NONE',  ( 0.000000000000000000, -1.000000000000000000, 0.000000000000000000 ) ) ;
#33751=FACE_OUTER_BOUND ( 'NONE', #96376, .T. ) ;
#33782=DIRECTION ( 'NONE',  ( 0.000000000000000000, -0.9908441862701605762, 0.1350103645451835310 ) ) ;
#33809=ORIENTED_EDGE ( 'NONE', *, *, #202714, .F. ) ;
#33841=DIRECTION ( 'NONE',  ( 0.000000000000000000, 1.000000000000000000, 7.272083257015735086E-15 ) ) ;
#33904=CARTESIAN_POINT ( 'NONE',  ( 21.97500000000000497, 66.25000000001186606, -90.77310748452438816 ) ) ;
#33933=AXIS2_PLACEMENT_3D ( 'NONE', #7409, #206908, #128667 ) ;
#33936=CARTESIAN_POINT ( 'NONE',  ( 20.94999999999999929, 85.00000000001179501, -78.91707660717668205 ) ) ;
#33940=CARTESIAN_POINT ( 'NONE',  ( 23.14999999999999858, 78.10000000001171827, -69.52310748452430289 ) ) ;
#33976=DIRECTION ( 'NONE',  ( 1.000000000000000000, 0.000000000000000000, 0.000000000000000000 ) ) ;
#33987=CYLINDRICAL_SURFACE ( 'NONE', #88135, 0.1000000000000026007 ) ;
#33989=CARTESIAN_POINT ( 'NONE',  ( -20.15000000000000568, 66.70857864377455826, -90.67310748452436542 ) ) ;
#34010=CARTESIAN_POINT ( 'NONE',  ( -20.94999999999999929, 77.16412189325286874, -61.80825939895269272 ) ) ;
#34025=CARTESIAN_POINT ( 'NONE',  ( -21.04999999999880345, 69.50298221357996908, -103.0085617939544562 ) ) ;
#34039=DIRECTION ( 'NONE',  ( -1.000000000000000000, 7.304098846218164250E-16, -4.217023435051628197E-16 ) ) ;
#34047=CARTESIAN_POINT ( 'NONE',  ( 19.75857864376268935, 64.35000000001177511, -78.17310748452437963 ) ) ;
#34073=CIRCLE ( 'NONE', #154675, 11.74999999999999645 ) ;
#34086=ADVANCED_FACE ( 'NONE', ( #239662 ), #111344, .F. ) ;
#34091=EDGE_LOOP ( 'NONE', ( #122930, #15331, #204713, #124877 ) ) ;
#34093=CARTESIAN_POINT ( 'NONE',  ( 23.14999999999999858, 70.50000000001180922, -81.92837350343744163 ) ) ;
#34119=CARTESIAN_POINT ( 'NONE',  ( 21.05000000000000071, 67.12872031401624895, -94.46447848938342418 ) ) ;
#34167=VECTOR ( 'NONE', #174507, 1000.000000000000227 ) ;
#34169=ORIENTED_EDGE ( 'NONE', *, *, #106532, .F. ) ;
#34178=ORIENTED_EDGE ( 'NONE', *, *, #170509, .T. ) ;
#34221=DIRECTION ( 'NONE',  ( 1.000000000000000000, 0.000000000000000000, 0.000000000000000000 ) ) ;
#34245=FACE_OUTER_BOUND ( 'NONE', #244607, .T. ) ;
#34268=CARTESIAN_POINT ( 'NONE',  ( 21.09107601085543848, 75.96069283529470795, -109.3869854598841300 ) ) ;
#34305=FACE_OUTER_BOUND ( 'NONE', #136293, .T. ) ;
#34350=ORIENTED_EDGE ( 'NONE', *, *, #243291, .T. ) ;
#34388=DIRECTION ( 'NONE',  ( -4.801466763864314121E-15, 0.2605042016806606298, 0.9654727137038736640 ) ) ;
#34393=CYLINDRICAL_SURFACE ( 'NONE', #208455, 0.5000000000000004441 ) ;
#34397=DIRECTION ( 'NONE',  ( 1.000000000000000000, 0.000000000000000000, 0.000000000000000000 ) ) ;
#34406=AXIS2_PLACEMENT_3D ( 'NONE', #117154, #97546, #78007 ) ;
#34421=AXIS2_PLACEMENT_3D ( 'NONE', #118931, #139738, #38109 ) ;
#34423=LINE ( 'NONE', #134747, #244967 ) ;
#34428=EDGE_CURVE ( 'NONE', #111418, #155591, #222310, .T. ) ;
#34484=CARTESIAN_POINT ( 'NONE',  ( -18.55121869061588669, 65.67252876774509218, -63.94570419949943840 ) ) ;
#34539=SPHERICAL_SURFACE ( 'NONE', #37245, 0.1000000000000000056 ) ;
#34562=AXIS2_PLACEMENT_3D ( 'NONE', #165267, #126124, #205665 ) ;
#34571=EDGE_CURVE ( 'NONE', #72649, #6502, #95139, .T. ) ;
#34627=DIRECTION ( 'NONE',  ( -1.000000000000000000, 2.952720810173289112E-16, 2.061873921506763405E-30 ) ) ;
#34629=VECTOR ( 'NONE', #235834, 1000.000000000000000 ) ;
#34656=CARTESIAN_POINT ( 'NONE',  ( 18.49362639424906263, 85.44260436789974733, -62.75866655101247460 ) ) ;
#34660=CARTESIAN_POINT ( 'NONE',  ( 23.15000000000000213, 88.41227409416141825, -72.52310748452423184 ) ) ;
#34686=ORIENTED_EDGE ( 'NONE', *, *, #173175, .F. ) ;
#34696=DIRECTION ( 'NONE',  ( 0.000000000000000000, -6.982962677686266711E-15, 1.000000000000000000 ) ) ;
#34706=ORIENTED_EDGE ( 'NONE', *, *, #108050, .F. ) ;
#34710=VECTOR ( 'NONE', #36133, 1000.000000000000000 ) ;
#34732=ORIENTED_EDGE ( 'NONE', *, *, #154185, .T. ) ;
#34745=VERTEX_POINT ( 'NONE', #205382 ) ;
#34759=CARTESIAN_POINT ( 'NONE',  ( -22.47071067811865319, 68.27992525551387359, -103.1221999392269737 ) ) ;
#34760=ADVANCED_FACE ( 'NONE', ( #123307 ), #63310, .T. ) ;
#34761=DIRECTION ( 'NONE',  ( 1.000000000000000000, 0.000000000000000000, 0.000000000000000000 ) ) ;
#34782=ADVANCED_FACE ( 'NONE', ( #219822 ), #41226, .T. ) ;
#34793=DIRECTION ( 'NONE',  ( 0.000000000000000000, -0.9908441862701605762, 0.1350103645451835310 ) ) ;
#34801=LINE ( 'NONE', #232991, #234705 ) ;
#34826=DIRECTION ( 'NONE',  ( 0.000000000000000000, 1.000000000000000000, 6.982962677686266711E-15 ) ) ;
#34830=ORIENTED_EDGE ( 'NONE', *, *, #178780, .F. ) ;
#34831=VERTEX_POINT ( 'NONE', #209249 ) ;
#34867=EDGE_CURVE ( 'NONE', #96909, #19541, #207994, .T. ) ;
#34868=CARTESIAN_POINT ( 'NONE',  ( -20.94999999999999929, 76.00000000001170974, -69.52310748452431710 ) ) ;
#34886=DIRECTION ( 'NONE',  ( 1.000000000000000000, 0.000000000000000000, 0.000000000000000000 ) ) ;
#34925=EDGE_CURVE ( 'NONE', #5814, #243331, #36919, .T. ) ;
#34930=EDGE_LOOP ( 'NONE', ( #146529, #212852, #256796, #5516 ) ) ;
#34968=CARTESIAN_POINT ( 'NONE',  ( 21.14999999999999858, 87.75000000001186606, -90.77310748452423184 ) ) ;
#34990=CARTESIAN_POINT ( 'NONE',  ( -21.07928932188134041, 76.00000000001195133, -103.0231074845243171 ) ) ;
#34993=VECTOR ( 'NONE', #159871, 1000.000000000000000 ) ;
#35007=CARTESIAN_POINT ( 'NONE',  ( -20.85000000000000142, 68.87972903831409610, -65.86354444268503983 ) ) ;
#35064=CARTESIAN_POINT ( 'NONE',  ( 21.00000000000000000, 66.25000000001186606, -90.67310748452437963 ) ) ;
#35108=ORIENTED_EDGE ( 'NONE', *, *, #139230, .F. ) ;
#35130=DIRECTION ( 'NONE',  ( 0.000000000000000000, -6.982962677686266711E-15, 1.000000000000000000 ) ) ;
#35132=ORIENTED_EDGE ( 'NONE', *, *, #11079, .T. ) ;
#35146=AXIS2_PLACEMENT_3D ( 'NONE', #39488, #137257, #171610 ) ;
#35154=ORIENTED_EDGE ( 'NONE', *, *, #162087, .F. ) ;
#35191=DIRECTION ( 'NONE',  ( 0.000000000000000000, 0.4999999999999689138, -0.8660254037844565822 ) ) ;
#35195=CARTESIAN_POINT ( 'NONE',  ( 21.06490991615909536, 65.27510865242474836, -90.81939613099125097 ) ) ;
#35244=EDGE_CURVE ( 'NONE', #184113, #112510, #174489, .T. ) ;
#35251=AXIS2_PLACEMENT_3D ( 'NONE', #250550, #15835, #253109 ) ;
#35259=FACE_OUTER_BOUND ( 'NONE', #210571, .T. ) ;
#35300=EDGE_CURVE ( 'NONE', #157067, #221948, #141124, .T. ) ;
#35346=LINE ( 'NONE', #196936, #25238 ) ;
#35351=EDGE_LOOP ( 'NONE', ( #155979, #79098, #84801, #246178 ) ) ;
#35376=EDGE_LOOP ( 'NONE', ( #161953, #36494, #12651, #167338 ) ) ;
#35395=ORIENTED_EDGE ( 'NONE', *, *, #84663, .T. ) ;
#35456=VECTOR ( 'NONE', #176828, 1000.000000000000000 ) ;
#35474=DIRECTION ( 'NONE',  ( 0.000000000000000000, 7.086529944415894657E-15, -1.000000000000000000 ) ) ;
#35477=DIRECTION ( 'NONE',  ( 1.000000000000000000, 0.000000000000000000, 0.000000000000000000 ) ) ;
#35481=CARTESIAN_POINT ( 'NONE',  ( -21.44999999999999929, 68.65000000001180069, -81.77310748452435973 ) ) ;
#35488=EDGE_CURVE ( 'NONE', #47548, #194507, #58838, .T. ) ;
#35489=DIRECTION ( 'NONE',  ( 1.000000000000000000, 0.000000000000000000, 0.000000000000000000 ) ) ;
#35509=AXIS2_PLACEMENT_3D ( 'NONE', #36808, #41611, #81955 ) ;
#35587=CARTESIAN_POINT ( 'NONE',  ( 20.94999999999999929, 87.48912529308779540, -72.62310748452422615 ) ) ;
#35593=EDGE_CURVE ( 'NONE', #193457, #254110, #62192, .T. ) ;
#35634=VECTOR ( 'NONE', #64285, 1000.000000000000000 ) ;
#35640=VERTEX_POINT ( 'NONE', #173101 ) ;
#35726=ORIENTED_EDGE ( 'NONE', *, *, #245544, .F. ) ;
#35755=ORIENTED_EDGE ( 'NONE', *, *, #214977, .F. ) ;
#35784=DIRECTION ( 'NONE',  ( 0.000000000000000000, 6.982962677686266711E-15, -1.000000000000000000 ) ) ;
#35791=EDGE_CURVE ( 'NONE', #116639, #190614, #41546, .T. ) ;
#35794=FACE_OUTER_BOUND ( 'NONE', #62312, .T. ) ;
#35801=CARTESIAN_POINT ( 'NONE',  ( -20.64999999999999858, 74.00000000001186606, -89.79848556176222019 ) ) ;
#35803=EDGE_CURVE ( 'NONE', #123690, #159228, #23850, .T. ) ;
#35804=EDGE_CURVE ( 'NONE', #152778, #151773, #10153, .T. ) ;
#35846=EDGE_CURVE ( 'NONE', #143626, #57915, #39988, .T. ) ;
#35848=CARTESIAN_POINT ( 'NONE',  ( -18.39999999999999858, 85.60000000001167564, -62.92291809330219365 ) ) ;
#35877=DIRECTION ( 'NONE',  ( 0.000000000000000000, 0.000000000000000000, -1.000000000000000000 ) ) ;
#35895=FACE_OUTER_BOUND ( 'NONE', #117160, .T. ) ;
#35900=VERTEX_POINT ( 'NONE', #46355 ) ;
#35907=ADVANCED_FACE ( 'NONE', ( #146727 ), #165035, .F. ) ;
#35913=EDGE_CURVE ( 'NONE', #85340, #3248, #116536, .T. ) ;
#35914=CIRCLE ( 'NONE', #190013, 0.2000000000000057288 ) ;
#35946=DIRECTION ( 'NONE',  ( 1.000000000000000000, -2.952720810173289112E-16, -2.061873921506763405E-30 ) ) ;
#35969=CARTESIAN_POINT ( 'NONE',  ( -18.41418431465368499, 85.50000000001189449, -62.92291809330281893 ) ) ;
#35992=DIRECTION ( 'NONE',  ( 0.000000000000000000, -0.1350103645451945777, 0.9908441862701591329 ) ) ;
#36001=CARTESIAN_POINT ( 'NONE',  ( -23.25000000000000000, 68.97833521811159585, -65.68954208262705663 ) ) ;
#36013=CARTESIAN_POINT ( 'NONE',  ( -20.00857864376270001, 66.85000000001186038, -90.77310748452437394 ) ) ;
#36029=VECTOR ( 'NONE', #63349, 1000.000000000000000 ) ;
#36059=AXIS2_PLACEMENT_3D ( 'NONE', #148061, #33285, #188459 ) ;
#36101=EDGE_CURVE ( 'NONE', #59500, #248733, #245536, .T. ) ;
#36122=ORIENTED_EDGE ( 'NONE', *, *, #48101, .T. ) ;
#36124=CARTESIAN_POINT ( 'NONE',  ( -20.94999999999999929, 64.25000000001190870, -96.00830171387039513 ) ) ;
#36133=DIRECTION ( 'NONE',  ( -1.000000000000000000, -0.000000000000000000, -0.000000000000000000 ) ) ;
#36183=VERTEX_POINT ( 'NONE', #114034 ) ;
#36218=CIRCLE ( 'NONE', #248564, 4.150000000000001243 ) ;
#36226=FACE_OUTER_BOUND ( 'NONE', #79275, .T. ) ;
#36235=EDGE_LOOP ( 'NONE', ( #225423, #245232, #206117 ) ) ;
#36249=CARTESIAN_POINT ( 'NONE',  ( 21.05000000000000071, 74.63912941281984104, -94.95010955743335046 ) ) ;
#36250=CARTESIAN_POINT ( 'NONE',  ( -21.05000000000000071, 77.83534155023627932, -91.36795619196132634 ) ) ;
#36261=AXIS2_PLACEMENT_3D ( 'NONE', #172804, #153232, #228887 ) ;
#36267=DIRECTION ( 'NONE',  ( 0.000000000000000000, -1.000000000000000000, 0.000000000000000000 ) ) ;
#36277=AXIS2_PLACEMENT_3D ( 'NONE', #30853, #66094, #206894 ) ;
#36282=CARTESIAN_POINT ( 'NONE',  ( -18.59999999999999787, 77.14957036958736580, -61.70719500002233815 ) ) ;
#36285=DIRECTION ( 'NONE',  ( 0.000000000000000000, -7.124650136758317602E-15, 1.000000000000000000 ) ) ;
#36302=CARTESIAN_POINT ( 'NONE',  ( 21.05000000000000071, 64.35000000001194564, -103.0231074845244024 ) ) ;
#36324=ORIENTED_EDGE ( 'NONE', *, *, #102635, .F. ) ;
#36340=CARTESIAN_POINT ( 'NONE',  ( 22.60000000000000142, 75.89914163091332000, -114.7726746080137019 ) ) ;
#36350=AXIS2_PLACEMENT_3D ( 'NONE', #157919, #96580, #33144 ) ;
#36362=CIRCLE ( 'NONE', #173764, 0.6000000000000033085 ) ;
#36415=CIRCLE ( 'NONE', #182144, 0.1000000000000028644 ) ;
#36451=CARTESIAN_POINT ( 'NONE',  ( 18.57071067811864040, 65.82071067813045318, -81.67310748452439384 ) ) ;
#36452=EDGE_LOOP ( 'NONE', ( #197808, #95546, #42568, #84021 ) ) ;
#36464=FACE_OUTER_BOUND ( 'NONE', #101030, .T. ) ;
#36466=CARTESIAN_POINT ( 'NONE',  ( 21.05000000000000071, 65.27628289530434813, -90.87310748452438247 ) ) ;
#36494=ORIENTED_EDGE ( 'NONE', *, *, #252667, .T. ) ;
#36498=ADVANCED_FACE ( 'NONE', ( #10800 ), #90314, .T. ) ;
#36500=CARTESIAN_POINT ( 'NONE',  ( 21.05000000000000071, 76.00000000001197975, -107.3231074845243427 ) ) ;
#36508=CIRCLE ( 'NONE', #48929, 0.09999999999999976963 ) ;
#36525=DIRECTION ( 'NONE',  ( -7.304098846217948299E-16, -1.000000000000000000, 0.000000000000000000 ) ) ;
#36526=CARTESIAN_POINT ( 'NONE',  ( 20.94999999999999929, 76.00000000001170974, -69.52310748452431710 ) ) ;
#36538=AXIS2_PLACEMENT_3D ( 'NONE', #11730, #9145, #52097 ) ;
#36540=ORIENTED_EDGE ( 'NONE', *, *, #147888, .T. ) ;
#36545=DIRECTION ( 'NONE',  ( 0.000000000000000000, 0.8660254037844420383, -0.4999999999999943379 ) ) ;
#36567=CARTESIAN_POINT ( 'NONE',  ( -22.50000000000088463, 75.95463834342417897, -114.6736163187350002 ) ) ;
#36576=DIRECTION ( 'NONE',  ( -1.000000000000000000, -0.000000000000000000, -0.000000000000000000 ) ) ;
#36588=DIRECTION ( 'NONE',  ( 0.000000000000000000, 0.000000000000000000, 1.000000000000000000 ) ) ;
#36646=CARTESIAN_POINT ( 'NONE',  ( -21.65000000000000213, 68.29142135624915966, -90.77310748452437394 ) ) ;
#36657=DIRECTION ( 'NONE',  ( -1.000000000000000000, 0.000000000000000000, 0.000000000000000000 ) ) ;
#36661=DIRECTION ( 'NONE',  ( 0.000000000000000000, 0.9999176327611370985, -0.01283462868041286391 ) ) ;
#36732=ORIENTED_EDGE ( 'NONE', *, *, #148365, .T. ) ;
#36745=ADVANCED_FACE ( 'NONE', ( #181447 ), #242676, .T. ) ;
#36760=EDGE_LOOP ( 'NONE', ( #90548, #136489, #125104, #158110 ) ) ;
#36784=CIRCLE ( 'NONE', #207634, 7.900000000000003908 ) ;
#36789=ORIENTED_EDGE ( 'NONE', *, *, #128903, .T. ) ;
#36801=DIRECTION ( 'NONE',  ( -1.000000000000000000, 0.000000000000000000, -0.000000000000000000 ) ) ;
#36803=ORIENTED_EDGE ( 'NONE', *, *, #174791, .T. ) ;
#36808=CARTESIAN_POINT ( 'NONE',  ( -20.85000000000000142, 68.97833521811159585, -65.68954208262705663 ) ) ;
#36810=DIRECTION ( 'NONE',  ( -1.000000000000000000, 0.000000000000000000, 0.000000000000000000 ) ) ;
#36812=ORIENTED_EDGE ( 'NONE', *, *, #56155, .F. ) ;
#36826=CARTESIAN_POINT ( 'NONE',  ( 22.42196299218230493, 75.99755832602473049, -114.6727191871737830 ) ) ;
#36877=DIRECTION ( 'NONE',  ( -0.000000000000000000, -0.6132151058540604716, 0.7899159663865477077 ) ) ;
#36882=CARTESIAN_POINT ( 'NONE',  ( 20.97468175916167255, 65.37473483564083665, -90.76834604911159943 ) ) ;
#36902=ORIENTED_EDGE ( 'NONE', *, *, #145426, .F. ) ;
#36919=CIRCLE ( 'NONE', #203654, 0.1000000000000028644 ) ;
#36925=ORIENTED_EDGE ( 'NONE', *, *, #67027, .T. ) ;
#36932=EDGE_LOOP ( 'NONE', ( #93789, #47347, #107617, #40775 ) ) ;
#36937=DIRECTION ( 'NONE',  ( 0.000000000000000000, 0.000000000000000000, -1.000000000000000000 ) ) ;
#36954=FACE_OUTER_BOUND ( 'NONE', #34930, .T. ) ;
#36992=LINE ( 'NONE', #117779, #18885 ) ;
#37037=EDGE_CURVE ( 'NONE', #167394, #50141, #57299, .T. ) ;
#37044=AXIS2_PLACEMENT_3D ( 'NONE', #49238, #68823, #225286 ) ;
#37053=AXIS2_PLACEMENT_3D ( 'NONE', #212562, #75628, #54746 ) ;
#37067=AXIS2_PLACEMENT_3D ( 'NONE', #166784, #165478, #188882 ) ;
#37085=DIRECTION ( 'NONE',  ( 0.000000000000000000, -6.982962677686266711E-15, 1.000000000000000000 ) ) ;
#37091=TOROIDAL_SURFACE ( 'NONE', #186940, 0.2000000000000000111, 0.1000000000000000056 ) ;
#37094=DIRECTION ( 'NONE',  ( 0.000000000000000000, 0.000000000000000000, 1.000000000000000000 ) ) ;
#37098=CARTESIAN_POINT ( 'NONE',  ( -21.07928932188134041, 75.90110485435759813, -109.3516241409176075 ) ) ;
#37108=CARTESIAN_POINT ( 'NONE',  ( -18.50000000000000000, 64.35000000001190301, -96.00830171387039513 ) ) ;
#37121=PLANE ( 'NONE',  #223386 ) ;
#37180=LINE ( 'NONE', #189822, #57294 ) ;
#37188=AXIS2_PLACEMENT_3D ( 'NONE', #60638, #56770, #140174 ) ;
#37191=LINE ( 'NONE', #116702, #25919 ) ;
#37222=CARTESIAN_POINT ( 'NONE',  ( 23.14999999999999503, 61.90000000001175096, -75.12340509566377023 ) ) ;
#37245=AXIS2_PLACEMENT_3D ( 'NONE', #73670, #192312, #243614 ) ;
#37247=ORIENTED_EDGE ( 'NONE', *, *, #109799, .F. ) ;
#37257=CARTESIAN_POINT ( 'NONE',  ( -21.05000000000000071, 74.16465844978745281, -91.46795619196133487 ) ) ;
#37258=CARTESIAN_POINT ( 'NONE',  ( -18.44448725179913851, 85.49008171549498059, -62.89414719046176572 ) ) ;
#37283=ORIENTED_EDGE ( 'NONE', *, *, #65378, .F. ) ;
#37291=DIRECTION ( 'NONE',  ( 2.952720810173289112E-16, 1.000000000000000000, 6.982962677686266711E-15 ) ) ;
#37300=CARTESIAN_POINT ( 'NONE',  ( 23.14999999999999503, 64.25000000001185185, -90.87310748452438247 ) ) ;
#37325=CARTESIAN_POINT ( 'NONE',  ( -18.50000000000000000, 74.65925378207832352, -113.2959699899454904 ) ) ;
#37345=AXIS2_PLACEMENT_3D ( 'NONE', #111290, #50022, #73475 ) ;
#37377=DIRECTION ( 'NONE',  ( 0.000000000000000000, -6.982962677686266711E-15, 1.000000000000000000 ) ) ;
#37384=ORIENTED_EDGE ( 'NONE', *, *, #103269, .T. ) ;
#37406=ORIENTED_EDGE ( 'NONE', *, *, #119188, .T. ) ;
#37408=DIRECTION ( 'NONE',  ( 0.000000000000000000, -7.147358527629766941E-15, 1.000000000000000000 ) ) ;
#37412=CARTESIAN_POINT ( 'NONE',  ( -18.59999999999999787, 64.25000000001179501, -81.67310748452439384 ) ) ;
#37437=LINE ( 'NONE', #219902, #7481 ) ;
#37453=CYLINDRICAL_SURFACE ( 'NONE', #220927, 0.09999999999999976963 ) ;
#37492=EDGE_CURVE ( 'NONE', #134706, #136972, #185628, .T. ) ;
#37493=VECTOR ( 'NONE', #231132, 1000.000000000000000 ) ;
#37613=ORIENTED_EDGE ( 'NONE', *, *, #246966, .F. ) ;
#37622=AXIS2_PLACEMENT_3D ( 'NONE', #35587, #129525, #189503 ) ;
#37623=AXIS2_PLACEMENT_3D ( 'NONE', #251672, #56009, #95170 ) ;
#37627=VERTEX_POINT ( 'NONE', #48672 ) ;
#37642=VERTEX_POINT ( 'NONE', #133362 ) ;
#37648=ORIENTED_EDGE ( 'NONE', *, *, #61717, .T. ) ;
#37670=ORIENTED_EDGE ( 'NONE', *, *, #70126, .T. ) ;
#37693=ORIENTED_EDGE ( 'NONE', *, *, #160356, .F. ) ;
#37700=CIRCLE ( 'NONE', #54226, 0.09999999999999939493 ) ;
#37712=ORIENTED_EDGE ( 'NONE', *, *, #75035, .T. ) ;
#37726=CIRCLE ( 'NONE', #8483, 0.09999999999999939493 ) ;
#37745=DIRECTION ( 'NONE',  ( -1.000000000000000000, 0.000000000000000000, -0.000000000000000000 ) ) ;
#37750=ORIENTED_EDGE ( 'NONE', *, *, #152780, .T. ) ;
#37751=ORIENTED_EDGE ( 'NONE', *, *, #64005, .T. ) ;
#37771=VERTEX_POINT ( 'NONE', #254550 ) ;
#37781=CARTESIAN_POINT ( 'NONE',  ( 21.13461538461538325, 65.38541703798632909, -90.67310748452437963 ) ) ;
#37783=CARTESIAN_POINT ( 'NONE',  ( 21.05000000000000071, 74.65091558138487926, -95.03660852097883094 ) ) ;
#37786=DIRECTION ( 'NONE',  ( 1.000000000000000000, 0.000000000000000000, 0.000000000000000000 ) ) ;
#37789=VECTOR ( 'NONE', #251101, 1000.000000000000114 ) ;
#37805=DIRECTION ( 'NONE',  ( 0.000000000000000000, 6.982962677686266711E-15, -1.000000000000000000 ) ) ;
#37892=ORIENTED_EDGE ( 'NONE', *, *, #233641, .F. ) ;
#37905=TOROIDAL_SURFACE ( 'NONE', #41993, 11.89999999999999858, 0.1000000000000000056 ) ;
#37957=EDGE_LOOP ( 'NONE', ( #130985, #96310, #152198, #71007 ) ) ;
#38002=DIRECTION ( 'NONE',  ( 0.000000000000000000, 0.4999999999999943379, 0.8660254037844420383 ) ) ;
#38004=( BOUNDED_SURFACE ( )  B_SPLINE_SURFACE ( 3, 2, ( 
 ( #250548, #109747, #229713 ),
 ( #150189, #172357, #95337 ),
 ( #71932, #208863, #151482 ),
 ( #214007, #34119, #154075 ) ),
 .UNSPECIFIED., .F., .F., .F. ) 
 B_SPLINE_SURFACE_WITH_KNOTS ( ( 4, 4 ),
 ( 3, 3 ),
 ( 0.0002700421466196863498, 0.0004789321604330981771 ),
 ( 0.000000000000000000, 1.000000000000000000 ),
 .UNSPECIFIED. ) 
 GEOMETRIC_REPRESENTATION_ITEM ( )  RATIONAL_B_SPLINE_SURFACE ( (
 ( 1.000000000000000000, 0.7071067811865475727, 1.000000000000000000),
 ( 1.000000000000000000, 0.7163411249511595358, 1.000000000000000000),
 ( 1.000000000000000000, 0.7221957104842121611, 1.000000000000000000),
 ( 1.000000000000000000, 0.7250110520819756932, 1.000000000000000000) ) ) 
 REPRESENTATION_ITEM ( '' )  SURFACE ( )  );
#38029=EDGE_CURVE ( 'NONE', #140889, #12289, #88925, .T. ) ;
#38031=ORIENTED_EDGE ( 'NONE', *, *, #204189, .F. ) ;
#38034=CARTESIAN_POINT ( 'NONE',  ( -18.42554971533678199, 85.49715966944965828, -95.98328057097560873 ) ) ;
#38052=VECTOR ( 'NONE', #231486, 1000.000000000000000 ) ;
#38062=CARTESIAN_POINT ( 'NONE',  ( 23.14999999999998437, 76.00000000001195133, -103.0231074845243171 ) ) ;
#38074=ORIENTED_EDGE ( 'NONE', *, *, #177783, .T. ) ;
#38077=DIRECTION ( 'NONE',  ( 0.000000000000000000, -7.056502275159890832E-15, 1.000000000000000000 ) ) ;
#38084=CYLINDRICAL_SURFACE ( 'NONE', #253310, 0.09999999999999939493 ) ;
#38109=DIRECTION ( 'NONE',  ( 0.000000000000000000, 0.000000000000000000, 1.000000000000000000 ) ) ;
#38129=ADVANCED_FACE ( 'NONE', ( #141878 ), #24533, .F. ) ;
#38141=CARTESIAN_POINT ( 'NONE',  ( 21.14999999999999858, 64.35000000001186038, -90.87310748452438247 ) ) ;
#38160=CARTESIAN_POINT ( 'NONE',  ( 21.05000000000000071, 76.00000000001170974, -69.52310748452431710 ) ) ;
#38211=VERTEX_POINT ( 'NONE', #110456 ) ;
#38260=DIRECTION ( 'NONE',  ( 0.000000000000000000, -1.000000000000000000, 0.000000000000000000 ) ) ;
#38274=ORIENTED_EDGE ( 'NONE', *, *, #206141, .T. ) ;
#38285=CARTESIAN_POINT ( 'NONE',  ( -22.59999999999999787, 64.35042919246716053, -103.1231074845243825 ) ) ;
#38298=ORIENTED_EDGE ( 'NONE', *, *, #208401, .T. ) ;
#38304=DIRECTION ( 'NONE',  ( 2.952720810173289112E-16, 1.000000000000000000, 6.467318590049456648E-15 ) ) ;
#38329=CYLINDRICAL_SURFACE ( 'NONE', #142672, 0.5000000000000004441 ) ;
#38387=EDGE_CURVE ( 'NONE', #16536, #125531, #9374, .T. ) ;
#38435=DIRECTION ( 'NONE',  ( -1.000000000000000000, 0.000000000000000000, -0.000000000000000000 ) ) ;
#38440=CARTESIAN_POINT ( 'NONE',  ( -18.59999999999999787, 77.16270174994990327, -94.92310748452430857 ) ) ;
#38442=DIRECTION ( 'NONE',  ( 1.000000000000000000, 0.000000000000000000, 0.000000000000000000 ) ) ;
#38452=DIRECTION ( 'NONE',  ( -0.000000000000000000, 0.4791956752371484551, 0.8777080977375184556 ) ) ;
#38486=CARTESIAN_POINT ( 'NONE',  ( 18.49999999999999289, 69.55000000001179217, -81.87310748452435405 ) ) ;
#38504=CIRCLE ( 'NONE', #9278, 0.1000000000000028644 ) ;
#38527=CARTESIAN_POINT ( 'NONE',  ( -23.25000000000000000, 77.83585931145526615, -58.01866831572577610 ) ) ;
#38566=DIRECTION ( 'NONE',  ( 0.000000000000000000, -1.000000000000000000, 0.000000000000000000 ) ) ;
#38574=ORIENTED_EDGE ( 'NONE', *, *, #96633, .F. ) ;
#38576=EDGE_CURVE ( 'NONE', #123705, #89984, #33337, .T. ) ;
#38579=CARTESIAN_POINT ( 'NONE',  ( -20.00857864376270001, 66.75000000001179501, -81.77310748452437394 ) ) ;
#38598=DIRECTION ( 'NONE',  ( -0.000000000000000000, 1.000000000000000000, 6.982962677686267499E-15 ) ) ;
#38600=AXIS2_PLACEMENT_3D ( 'NONE', #182557, #219079, #136986 ) ;
#38624=CARTESIAN_POINT ( 'NONE',  ( 18.47654891039378455, 85.46527494839416761, -95.89713157932956733 ) ) ;
#38631=CARTESIAN_POINT ( 'NONE',  ( 23.15000000000000213, 87.65000000001172964, -72.62310748452422615 ) ) ;
#38651=FACE_OUTER_BOUND ( 'NONE', #107634, .T. ) ;
#38661=CARTESIAN_POINT ( 'NONE',  ( -21.05000000000000071, 87.65000000001192859, -100.1231074845242262 ) ) ;
#38712=CARTESIAN_POINT ( 'NONE',  ( -23.15000000000000213, 64.35000000001180354, -81.77310748452438816 ) ) ;
#38782=EDGE_LOOP ( 'NONE', ( #7711, #144404, #135113, #138228 ) ) ;
#38783=CIRCLE ( 'NONE', #113610, 0.3999999999999975797 ) ;
#38796=CARTESIAN_POINT ( 'NONE',  ( 18.59999999999996945, 65.66751761918648356, -63.92826094061123143 ) ) ;
#38797=CARTESIAN_POINT ( 'NONE',  ( 18.49999999999999645, 76.00000000001170974, -69.52310748452431710 ) ) ;
#38802=CIRCLE ( 'NONE', #51229, 0.09999999999999976963 ) ;
#38805=ADVANCED_FACE ( 'NONE', ( #25306 ), #201108, .F. ) ;
#38835=ORIENTED_EDGE ( 'NONE', *, *, #22113, .T. ) ;
#38854=CARTESIAN_POINT ( 'NONE',  ( 18.59999999999999076, 68.92903212821283887, -65.77654326265606244 ) ) ;
#38864=AXIS2_PLACEMENT_3D ( 'NONE', #60206, #4090, #139733 ) ;
#38893=ORIENTED_EDGE ( 'NONE', *, *, #46841, .T. ) ;
#38930=CARTESIAN_POINT ( 'NONE',  ( 21.05000000000000071, 71.00000000001180922, -81.42837350343744163 ) ) ;
#38965=CARTESIAN_POINT ( 'NONE',  ( 20.94999999999999929, 71.18691588786226987, -81.46462524104816794 ) ) ;
#38976=CARTESIAN_POINT ( 'NONE',  ( 23.15000000000000213, 87.48912529308779540, -72.62310748452422615 ) ) ;
#38979=ORIENTED_EDGE ( 'NONE', *, *, #193434, .T. ) ;
#38992=ORIENTED_EDGE ( 'NONE', *, *, #201553, .F. ) ;
#39005=EDGE_LOOP ( 'NONE', ( #30638, #185903, #51224, #11639 ) ) ;
#39019=AXIS2_PLACEMENT_3D ( 'NONE', #221276, #243419, #64780 ) ;
#39020=EDGE_CURVE ( 'NONE', #57105, #156346, #247059, .T. ) ;
#39048=AXIS2_PLACEMENT_3D ( 'NONE', #252842, #251562, #233317 ) ;
#39057=ADVANCED_FACE ( 'NONE', ( #178963 ), #42001, .F. ) ;
#39061=DIRECTION ( 'NONE',  ( 0.000000000000000000, -6.938893903907229955E-15, 1.000000000000000000 ) ) ;
#39069=CARTESIAN_POINT ( 'NONE',  ( 21.05000000000000071, 76.00000000001195133, -103.0231074845243171 ) ) ;
#39075=CIRCLE ( 'NONE', #51482, 11.64999999999999325 ) ;
#39108=CARTESIAN_POINT ( 'NONE',  ( -18.59999996769639097, 85.36327376984216642, -95.84161356905833884 ) ) ;
#39117=VERTEX_POINT ( 'NONE', #57671 ) ;
#39151=EDGE_CURVE ( 'NONE', #157067, #147354, #48386, .T. ) ;
#39153=VECTOR ( 'NONE', #180943, 1000.000000000000000 ) ;
#39176=VERTEX_POINT ( 'NONE', #185342 ) ;
#39208=CIRCLE ( 'NONE', #18332, 0.1999999999999987899 ) ;
#39244=CYLINDRICAL_SURFACE ( 'NONE', #201996, 0.09999999999999520384 ) ;
#39247=CARTESIAN_POINT ( 'NONE',  ( 22.50000000000000000, 75.95437663941565631, -114.6736118230756887 ) ) ;
#39268=ORIENTED_EDGE ( 'NONE', *, *, #92631, .T. ) ;
#39349=CARTESIAN_POINT ( 'NONE',  ( -18.59999999999999787, 77.16270174994990327, -94.92310748452430857 ) ) ;
#39350=DIRECTION ( 'NONE',  ( 0.000000000000000000, -6.982962677686266711E-15, 1.000000000000000000 ) ) ;
#39373=FACE_OUTER_BOUND ( 'NONE', #79920, .T. ) ;
#39389=FACE_OUTER_BOUND ( 'NONE', #31400, .T. ) ;
#39391=ORIENTED_EDGE ( 'NONE', *, *, #244189, .F. ) ;
#39392=DIRECTION ( 'NONE',  ( 0.000000000000000000, -6.982962677686266711E-15, 1.000000000000000000 ) ) ;
#39442=DIRECTION ( 'NONE',  ( 1.040834085586049673E-13, 0.7899159663865300551, 0.6132151058540831201 ) ) ;
#39453=AXIS2_PLACEMENT_3D ( 'NONE', #132126, #51265, #186987 ) ;
#39473=CARTESIAN_POINT ( 'NONE',  ( 18.49999999999999289, 68.97833521811159585, -65.68954208262705663 ) ) ;
#39488=CARTESIAN_POINT ( 'NONE',  ( 18.59999999999999432, 70.30054753569044124, -115.5653814410941891 ) ) ;
#39527=B_SPLINE_CURVE_WITH_KNOTS ( 'NONE', 3,
 ( #237891, #198759, #236595, #102198, #200059, #59212, #121816, #123096, #197473, #180498 ),
 .UNSPECIFIED., .F., .F.,
 ( 4, 3, 3, 4 ),
 ( 0.000000000000000000, 0.0002000000000002884074, 0.001000000000045107602, 0.001967863649472132576 ),
 .UNSPECIFIED. ) ;
#39537=DIRECTION ( 'NONE',  ( -1.000000000000000000, 0.000000000000000000, -0.000000000000000000 ) ) ;
#39543=CARTESIAN_POINT ( 'NONE',  ( 21.10257677756355932, 75.97504925044398760, -109.4214892270570658 ) ) ;
#39577=PLANE ( 'NONE',  #73631 ) ;
#39583=CIRCLE ( 'NONE', #72901, 0.1000000000000028783 ) ;
#39634=DIRECTION ( 'NONE',  ( -1.000000000000000000, -0.000000000000000000, -0.000000000000000000 ) ) ;
#39649=CIRCLE ( 'NONE', #231182, 0.1000000000000028644 ) ;
#39666=EDGE_CURVE ( 'NONE', #80661, #2887, #53186, .T. ) ;
#39696=EDGE_CURVE ( 'NONE', #171051, #160189, #232273, .T. ) ;
#39706=CIRCLE ( 'NONE', #185430, 4.299999999999956302 ) ;
#39724=CARTESIAN_POINT ( 'NONE',  ( 21.05000000000000071, 69.65000000001187175, -93.17928539484123007 ) ) ;
#39763=FACE_OUTER_BOUND ( 'NONE', #61953, .T. ) ;
#39768=LINE ( 'NONE', #158433, #25966 ) ;
#39774=AXIS2_PLACEMENT_3D ( 'NONE', #113319, #14246, #252818 ) ;
#39776=VECTOR ( 'NONE', #241111, 1000.000000000000000 ) ;
#39787=DIRECTION ( 'NONE',  ( 0.000000000000000000, 0.000000000000000000, 1.000000000000000000 ) ) ;
#39818=EDGE_CURVE ( 'NONE', #224632, #142820, #136346, .T. ) ;
#39828=CARTESIAN_POINT ( 'NONE',  ( -21.05000000000000071, 74.83729825007388570, -95.02310748452431710 ) ) ;
#39865=FACE_BOUND ( 'NONE', #174938, .T. ) ;
#39920=EDGE_CURVE ( 'NONE', #175899, #243017, #120037, .T. ) ;
#39923=CARTESIAN_POINT ( 'NONE',  ( 20.95083306685154056, 67.08315735812169578, -94.54578263126602167 ) ) ;
#39944=CIRCLE ( 'NONE', #89983, 0.1000000000000028644 ) ;
#39961=ADVANCED_FACE ( 'NONE', ( #224796 ), #111296, .T. ) ;
#39988=LINE ( 'NONE', #257651, #237342 ) ;
#40037=AXIS2_PLACEMENT_3D ( 'NONE', #228507, #231088, #232369 ) ;
#40173=CIRCLE ( 'NONE', #119265, 12.87499999999999822 ) ;
#40185=CYLINDRICAL_SURFACE ( 'NONE', #155059, 0.1000000000000028644 ) ;
#40200=LINE ( 'NONE', #155012, #21138 ) ;
#40263=VERTEX_POINT ( 'NONE', #220666 ) ;
#40265=CARTESIAN_POINT ( 'NONE',  ( 20.93284271247462414, 64.25000000001175238, -76.53791325517833855 ) ) ;
#40290=ORIENTED_EDGE ( 'NONE', *, *, #197169, .F. ) ;
#40338=CARTESIAN_POINT ( 'NONE',  ( 20.94999999999999929, 64.35000000001176090, -76.30697314750248950 ) ) ;
#40411=ADVANCED_FACE ( 'NONE', ( #76982 ), #114830, .F. ) ;
#40424=CARTESIAN_POINT ( 'NONE',  ( 18.52928932188133970, 65.72071067813043044, -78.37310748452438247 ) ) ;
#40430=ORIENTED_EDGE ( 'NONE', *, *, #61673, .T. ) ;
#40444=EDGE_CURVE ( 'NONE', #7823, #221901, #251774, .T. ) ;
#40465=DIRECTION ( 'NONE',  ( -0.000000000000000000, -0.8660254037844420383, 0.4999999999999943379 ) ) ;
#40476=ORIENTED_EDGE ( 'NONE', *, *, #256937, .T. ) ;
#40478=ORIENTED_EDGE ( 'NONE', *, *, #22113, .F. ) ;
#40489=AXIS2_PLACEMENT_3D ( 'NONE', #13630, #172749, #129720 ) ;
#40506=ADVANCED_FACE ( 'NONE', ( #131823 ), #93972, .T. ) ;
#40509=AXIS2_PLACEMENT_3D ( 'NONE', #132679, #34886, #193940 ) ;
#40519=ORIENTED_EDGE ( 'NONE', *, *, #221361, .T. ) ;
#40534=DIRECTION ( 'NONE',  ( -1.000000000000000000, 0.000000000000000000, -0.000000000000000000 ) ) ;
#40561=EDGE_LOOP ( 'NONE', ( #247428, #22871, #188177, #96589 ) ) ;
#40570=AXIS2_PLACEMENT_3D ( 'NONE', #34990, #53228, #131480 ) ;
#40583=ORIENTED_EDGE ( 'NONE', *, *, #4028, .F. ) ;
#40585=ADVANCED_FACE ( 'NONE', ( #157856 ), #142088, .F. ) ;
#40604=AXIS2_PLACEMENT_3D ( 'NONE', #163840, #107705, #248505 ) ;
#40619=CIRCLE ( 'NONE', #169631, 0.1000000000000028644 ) ;
#40644=ORIENTED_EDGE ( 'NONE', *, *, #219814, .T. ) ;
#40660=CARTESIAN_POINT ( 'NONE',  ( 23.24999999999999645, 70.40000000001204228, -114.7731074845243455 ) ) ;
#40670=CARTESIAN_POINT ( 'NONE',  ( -21.05000000000000071, 76.00000000001195133, -103.0231074845243171 ) ) ;
#40684=CARTESIAN_POINT ( 'NONE',  ( 22.40736611211992368, 76.00000000001203659, -114.6726782920691221 ) ) ;
#40696=ADVANCED_FACE ( 'NONE', ( #7734 ), #164244, .F. ) ;
#40702=CARTESIAN_POINT ( 'NONE',  ( -22.39999999999999503, 76.00000000001200817, -110.8138870828977218 ) ) ;
#40710=VECTOR ( 'NONE', #218379, 999.9999999999998863 ) ;
#40760=CARTESIAN_POINT ( 'NONE',  ( 18.59999999999999076, 74.75000000001188027, -95.02310748452431710 ) ) ;
#40763=DIRECTION ( 'NONE',  ( -1.000000000000000000, 0.000000000000000000, 0.000000000000000000 ) ) ;
#40764=DIRECTION ( 'NONE',  ( 0.000000000000000000, -0.8660254037844377084, -0.5000000000000016653 ) ) ;
#40767=CARTESIAN_POINT ( 'NONE',  ( -22.57848426163147693, 76.00426432929513965, -114.7731657914146552 ) ) ;
#40775=ORIENTED_EDGE ( 'NONE', *, *, #19022, .T. ) ;
#40778=ORIENTED_EDGE ( 'NONE', *, *, #84663, .F. ) ;
#40801=CIRCLE ( 'NONE', #140718, 0.09999999999999520384 ) ;
#40812=ORIENTED_EDGE ( 'NONE', *, *, #97194, .F. ) ;
#40824=EDGE_CURVE ( 'NONE', #34745, #216063, #132858, .T. ) ;
#40828=VERTEX_POINT ( 'NONE', #195370 ) ;
#40838=FACE_OUTER_BOUND ( 'NONE', #144431, .T. ) ;
#40854=DIRECTION ( 'NONE',  ( 0.000000000000000000, -7.189901751995755791E-15, 1.000000000000000000 ) ) ;
#40879=ORIENTED_EDGE ( 'NONE', *, *, #104510, .T. ) ;
#40892=EDGE_LOOP ( 'NONE', ( #62664, #146042, #207128, #78973 ) ) ;
#40904=DIRECTION ( 'NONE',  ( 1.000000000000000000, 0.000000000000000000, 0.000000000000000000 ) ) ;
#40944=ORIENTED_EDGE ( 'NONE', *, *, #164843, .T. ) ;
#40970=CARTESIAN_POINT ( 'NONE',  ( -20.64999999999999858, 85.00000000001188027, -93.12913836187181005 ) ) ;
#40972=VERTEX_POINT ( 'NONE', #17979 ) ;
#40975=CARTESIAN_POINT ( 'NONE',  ( 20.74625933824084001, 67.11708647892760382, -94.46793646040403303 ) ) ;
#40985=CIRCLE ( 'NONE', #215901, 0.1000000000000028644 ) ;
#40988=DIRECTION ( 'NONE',  ( 0.000000000000000000, 6.982962677686266711E-15, -1.000000000000000000 ) ) ;
#40994=( BOUNDED_CURVE ( )  B_SPLINE_CURVE ( 3, ( #85380, #3292, #205350, #25463 ),
 .UNSPECIFIED., .F., .F. ) 
 B_SPLINE_CURVE_WITH_KNOTS ( ( 4, 4 ),
 ( 3.141592653589791784, 4.712388980384688786 ),
 .UNSPECIFIED. ) 
 CURVE ( )  GEOMETRIC_REPRESENTATION_ITEM ( )  RATIONAL_B_SPLINE_CURVE ( ( 1.000000000000000000, 0.8047378541243649375, 0.8047378541243649375, 1.000000000000000000 ) ) 
 REPRESENTATION_ITEM ( '' )  );
#40998=VERTEX_POINT ( 'NONE', #137917 ) ;
#41003=ORIENTED_EDGE ( 'NONE', *, *, #126003, .F. ) ;
#41004=CARTESIAN_POINT ( 'NONE',  ( 23.25000000000000000, 85.00000000001188027, -93.12913836187181005 ) ) ;
#41066=CARTESIAN_POINT ( 'NONE',  ( -23.15000000000000213, 64.25000000001203659, -114.7731074845243882 ) ) ;
#41092=CARTESIAN_POINT ( 'NONE',  ( -21.05000000000000071, 61.95000000001191154, -97.50941241376341395 ) ) ;
#41105=AXIS2_PLACEMENT_3D ( 'NONE', #141304, #5612, #124315 ) ;
#41106=ORIENTED_EDGE ( 'NONE', *, *, #45106, .T. ) ;
#41115=LINE ( 'NONE', #217129, #164459 ) ;
#41148=CARTESIAN_POINT ( 'NONE',  ( 21.05000000000000071, 71.18691588786234092, -91.08158972800052311 ) ) ;
#41170=AXIS2_PLACEMENT_3D ( 'NONE', #62707, #87382, #142233 ) ;
#41206=ADVANCED_FACE ( 'NONE', ( #112935 ), #11269, .T. ) ;
#41214=CARTESIAN_POINT ( 'NONE',  ( 20.94999999999999929, 87.48912529308779540, -72.52310748452423184 ) ) ;
#41226=CYLINDRICAL_SURFACE ( 'NONE', #145007, 0.09999999999999939493 ) ;
#41228=CARTESIAN_POINT ( 'NONE',  ( -21.14999999999999858, 76.10000000001203091, -114.6726782920691079 ) ) ;
#41298=FACE_OUTER_BOUND ( 'NONE', #58920, .T. ) ;
#41307=CARTESIAN_POINT ( 'NONE',  ( 21.53551880898957194, 69.21520223859563714, -103.1220772190960275 ) ) ;
#41309=CARTESIAN_POINT ( 'NONE',  ( 21.10320863425824811, 69.59972261355278533, -103.0481297357514876 ) ) ;
#41359=ORIENTED_EDGE ( 'NONE', *, *, #13530, .F. ) ;
#41375=EDGE_CURVE ( 'NONE', #49254, #126928, #158021, .T. ) ;
#41383=CARTESIAN_POINT ( 'NONE',  ( 20.94999999999999574, 69.60000000001187459, -93.09268285446279378 ) ) ;
#41390=DIRECTION ( 'NONE',  ( 1.000000000000000000, 0.000000000000000000, 0.000000000000000000 ) ) ;
#41420=ADVANCED_FACE ( 'NONE', ( #84022 ), #103768, .T. ) ;
#41443=VERTEX_POINT ( 'NONE', #86617 ) ;
#41475=VECTOR ( 'NONE', #64036, 1000.000000000000000 ) ;
#41533=CARTESIAN_POINT ( 'NONE',  ( 18.59999999999999787, 77.83585931145526615, -58.01866831572577610 ) ) ;
#41534=VECTOR ( 'NONE', #158769, 1000.000000000000000 ) ;
#41546=CIRCLE ( 'NONE', #216482, 0.1000000000000028644 ) ;
#41550=ORIENTED_EDGE ( 'NONE', *, *, #230612, .F. ) ;
#41611=DIRECTION ( 'NONE',  ( -1.000000000000000000, 0.000000000000000000, -0.000000000000000000 ) ) ;
#41640=AXIS2_PLACEMENT_3D ( 'NONE', #128469, #222398, #105002 ) ;
#41641=VECTOR ( 'NONE', #55662, 1000.000000000000000 ) ;
#41659=CARTESIAN_POINT ( 'NONE',  ( 21.14999999999999858, 87.65000000001194280, -103.0231074845242318 ) ) ;
#41676=EDGE_CURVE ( 'NONE', #31810, #170631, #99847, .T. ) ;
#41677=VERTEX_POINT ( 'NONE', #241257 ) ;
#41684=DIRECTION ( 'NONE',  ( 0.000000000000000000, -0.4999999999999689138, -0.8660254037844565822 ) ) ;
#41687=CARTESIAN_POINT ( 'NONE',  ( 20.94999999999999574, 65.52661458509899717, -95.44445302027583011 ) ) ;
#41696=VECTOR ( 'NONE', #116124, 1000.000000000000000 ) ;
#41700=AXIS2_PLACEMENT_3D ( 'NONE', #87781, #206469, #126935 ) ;
#41725=EDGE_CURVE ( 'NONE', #190614, #229669, #157902, .T. ) ;
#41728=DIRECTION ( 'NONE',  ( 1.000000000000000000, 0.000000000000000000, 0.000000000000000000 ) ) ;
#41743=CARTESIAN_POINT ( 'NONE',  ( 18.59999999999999787, 87.75000000001176659, -78.17310748452423752 ) ) ;
#41768=EDGE_CURVE ( 'NONE', #215370, #179506, #133214, .T. ) ;
#41813=CARTESIAN_POINT ( 'NONE',  ( 22.40000000000010516, 76.00000000001296030, -114.7735403769832345 ) ) ;
#41825=AXIS2_PLACEMENT_3D ( 'NONE', #137513, #38435, #120566 ) ;
#41834=ORIENTED_EDGE ( 'NONE', *, *, #166418, .F. ) ;
#41855=CARTESIAN_POINT ( 'NONE',  ( 18.58685178364169133, 85.40673308381614959, -95.89868701543650786 ) ) ;
#41858=DIRECTION ( 'NONE',  ( 0.000000000000000000, -6.467318590049456648E-15, 1.000000000000000000 ) ) ;
#41862=ORIENTED_EDGE ( 'NONE', *, *, #39920, .F. ) ;
#41869=VECTOR ( 'NONE', #15327, 1000.000000000000000 ) ;
#41887=CIRCLE ( 'NONE', #50216, 0.1000000000000028644 ) ;
#41895=CARTESIAN_POINT ( 'NONE',  ( -22.50000000000000000, 75.90000000001199965, -110.8138870828977218 ) ) ;
#41898=DIRECTION ( 'NONE',  ( -1.000000000000000000, 2.952720810173289112E-16, 2.061873921506763405E-30 ) ) ;
#41905=CARTESIAN_POINT ( 'NONE',  ( 20.94999999999999929, 76.00000000001170974, -69.52310748452431710 ) ) ;
#41918=CARTESIAN_POINT ( 'NONE',  ( 20.85000000000000142, 87.65000000001170122, -69.52310748452423184 ) ) ;
#41923=TOROIDAL_SURFACE ( 'NONE', #104228, 4.149999999999999467, 0.1000000000000000056 ) ;
#41933=DIRECTION ( 'NONE',  ( 7.304098846218134667E-16, -1.000000000000000000, -6.982962677686267499E-15 ) ) ;
#41948=CIRCLE ( 'NONE', #46190, 12.97499999999999964 ) ;
#41956=EDGE_CURVE ( 'NONE', #119060, #91291, #4201, .T. ) ;
#41993=AXIS2_PLACEMENT_3D ( 'NONE', #241113, #201972, #39061 ) ;
#41998=CARTESIAN_POINT ( 'NONE',  ( -18.59999999999999787, 85.40000000001184333, -95.72584772486095517 ) ) ;
#41999=CYLINDRICAL_SURFACE ( 'NONE', #115037, 0.1000000000000028644 ) ;
#42001=CYLINDRICAL_SURFACE ( 'NONE', #184520, 0.1000000000000028644 ) ;
#42025=CARTESIAN_POINT ( 'NONE',  ( -21.05000000000000071, 87.65000000001172964, -72.42310748452422331 ) ) ;
#42049=EDGE_CURVE ( 'NONE', #91291, #23607, #183275, .T. ) ;
#42050=FACE_OUTER_BOUND ( 'NONE', #27488, .T. ) ;
#42053=AXIS2_PLACEMENT_3D ( 'NONE', #23687, #121502, #125330 ) ;
#42075=DIRECTION ( 'NONE',  ( 1.000000000000000000, -7.304098846218134667E-16, -5.100424963727256530E-30 ) ) ;
#42099=CARTESIAN_POINT ( 'NONE',  ( 21.12230431290520016, 75.99479014832300550, -109.4806741378173456 ) ) ;
#42111=PLANE ( 'NONE',  #184656 ) ;
#42135=EDGE_LOOP ( 'NONE', ( #56063, #62946, #93263, #193294 ) ) ;
#42150=FACE_OUTER_BOUND ( 'NONE', #36932, .T. ) ;
#42163=ORIENTED_EDGE ( 'NONE', *, *, #50153, .T. ) ;
#42184=CARTESIAN_POINT ( 'NONE',  ( -21.05000000000000071, 87.65000000001192859, -100.0231074845242318 ) ) ;
#42188=CARTESIAN_POINT ( 'NONE',  ( 18.49999999999999289, 69.35000000001180354, -81.87310748452435405 ) ) ;
#42204=AXIS2_PLACEMENT_3D ( 'NONE', #83083, #162675, #227767 ) ;
#42221=VECTOR ( 'NONE', #232716, 1000.000000000000000 ) ;
#42266=DIRECTION ( 'NONE',  ( 1.000000000000000000, 0.000000000000000000, 0.000000000000000000 ) ) ;
#42279=EDGE_CURVE ( 'NONE', #89984, #244131, #232801, .T. ) ;
#42303=CARTESIAN_POINT ( 'NONE',  ( -23.15000000000000213, 76.00000000001170974, -69.52310748452431710 ) ) ;
#42335=CARTESIAN_POINT ( 'NONE',  ( -20.54999999999999716, 74.05981308412395947, -82.35222669557765585 ) ) ;
#42358=DIRECTION ( 'NONE',  ( 1.000000000000000000, -0.000000000000000000, 0.000000000000000000 ) ) ;
#42363=ORIENTED_EDGE ( 'NONE', *, *, #147036, .F. ) ;
#42386=CARTESIAN_POINT ( 'NONE',  ( 18.59999999999999076, 65.79142135624910281, -81.67310748452439384 ) ) ;
#42437=CARTESIAN_POINT ( 'NONE',  ( -21.05000000000000071, 76.00000000001200817, -109.5637644362255401 ) ) ;
#42441=DIRECTION ( 'NONE',  ( 0.000000000000000000, 0.000000000000000000, 1.000000000000000000 ) ) ;
#42447=ORIENTED_EDGE ( 'NONE', *, *, #77039, .T. ) ;
#42456=ORIENTED_EDGE ( 'NONE', *, *, #14285, .T. ) ;
#42475=AXIS2_PLACEMENT_3D ( 'NONE', #249536, #74779, #209106 ) ;
#42491=ORIENTED_EDGE ( 'NONE', *, *, #163048, .F. ) ;
#42498=CARTESIAN_POINT ( 'NONE',  ( -20.64999999999999858, 68.85000000001180354, -81.87310748452436826 ) ) ;
#42499=ORIENTED_EDGE ( 'NONE', *, *, #169552, .F. ) ;
#42553=DIRECTION ( 'NONE',  ( 0.000000000000000000, -0.1350103645451945777, 0.9908441862701590219 ) ) ;
#42568=ORIENTED_EDGE ( 'NONE', *, *, #3930, .T. ) ;
#42586=AXIS2_PLACEMENT_3D ( 'NONE', #73024, #53419, #195526 ) ;
#42622=CARTESIAN_POINT ( 'NONE',  ( -18.59999999999999787, 66.65000000001187175, -90.87310748452436826 ) ) ;
#42722=ORIENTED_EDGE ( 'NONE', *, *, #170509, .F. ) ;
#42789=VECTOR ( 'NONE', #47736, 1000.000000000000000 ) ;
#42796=DIRECTION ( 'NONE',  ( 0.000000000000000000, 0.000000000000000000, 1.000000000000000000 ) ) ;
#42828=CARTESIAN_POINT ( 'NONE',  ( -18.59999999999999787, 77.83585931145526615, -58.01866831572577610 ) ) ;
#42896=CARTESIAN_POINT ( 'NONE',  ( 20.02499999999999858, 66.25000000001179501, -81.87310748452438247 ) ) ;
#42921=CIRCLE ( 'NONE', #167838, 0.6000000000000033085 ) ;
#42984=VERTEX_POINT ( 'NONE', #149699 ) ;
#42995=EDGE_LOOP ( 'NONE', ( #139803, #57980, #158477, #71939 ) ) ;
#43004=DIRECTION ( 'NONE',  ( 1.000000000000000000, 0.000000000000000000, 0.000000000000000000 ) ) ;
#43006=EDGE_CURVE ( 'NONE', #55514, #199047, #139052, .T. ) ;
#43011=DIRECTION ( 'NONE',  ( 0.000000000000000000, -6.467318590049456648E-15, 1.000000000000000000 ) ) ;
#43016=DIRECTION ( 'NONE',  ( -0.000000000000000000, 6.982962677686266711E-15, -1.000000000000000000 ) ) ;
#43024=CARTESIAN_POINT ( 'NONE',  ( -20.64999999999999858, 76.00000000001179501, -82.39810748452430289 ) ) ;
#43026=EDGE_CURVE ( 'NONE', #167682, #40972, #173139, .T. ) ;
#43052=CARTESIAN_POINT ( 'NONE',  ( 23.24999999999999645, 71.00000000001186606, -90.61784146561124942 ) ) ;
#43069=CARTESIAN_POINT ( 'NONE',  ( 21.13461538461538325, 67.11458296203740304, -90.67310748452436542 ) ) ;
#43089=VERTEX_POINT ( 'NONE', #193946 ) ;
#43091=ORIENTED_EDGE ( 'NONE', *, *, #87118, .T. ) ;
#43101=VECTOR ( 'NONE', #72055, 1000.000000000000000 ) ;
#43104=AXIS2_PLACEMENT_3D ( 'NONE', #167135, #228365, #249212 ) ;
#43146=ORIENTED_EDGE ( 'NONE', *, *, #170055, .F. ) ;
#43156=EDGE_LOOP ( 'NONE', ( #23325, #257247, #161749, #225030 ) ) ;
#43162=DIRECTION ( 'NONE',  ( 0.000000000000000000, 0.000000000000000000, 1.000000000000000000 ) ) ;
#43189=EDGE_CURVE ( 'NONE', #215026, #34831, #77518, .T. ) ;
#43192=EDGE_CURVE ( 'NONE', #51707, #233834, #65976, .T. ) ;
#43200=DIRECTION ( 'NONE',  ( 0.000000000000000000, -1.000000000000000000, 2.771150684185008344E-14 ) ) ;
#43262=DIRECTION ( 'NONE',  ( 1.000000000000000000, 0.000000000000000000, 0.000000000000000000 ) ) ;
#43276=CARTESIAN_POINT ( 'NONE',  ( 21.00023020733502577, 76.00000000001200817, -109.4139767297926653 ) ) ;
#43285=DIRECTION ( 'NONE',  ( 1.000000000000000000, -0.000000000000000000, -0.000000000000000000 ) ) ;
#43299=VECTOR ( 'NONE', #34039, 1000.000000000000000 ) ;
#43332=EDGE_CURVE ( 'NONE', #120417, #56583, #229058, .T. ) ;
#43335=CARTESIAN_POINT ( 'NONE',  ( 21.05000000000000071, 76.00000000001170974, -69.52310748452431710 ) ) ;
#43390=FACE_OUTER_BOUND ( 'NONE', #156948, .T. ) ;
#43410=VERTEX_POINT ( 'NONE', #234026 ) ;
#43416=DIRECTION ( 'NONE',  ( 0.000000000000000000, -0.9999631594459053030, -0.008583690987162452199 ) ) ;
#43489=EDGE_CURVE ( 'NONE', #209005, #112762, #129286, .T. ) ;
#43505=CARTESIAN_POINT ( 'NONE',  ( -23.25000000000000000, 71.85000000001178933, -81.77310748452433131 ) ) ;
#43522=ORIENTED_EDGE ( 'NONE', *, *, #44656, .F. ) ;
#43535=TOROIDAL_SURFACE ( 'NONE', #151719, 11.65000000000000036, 0.1000000000000000056 ) ;
#43565=EDGE_CURVE ( 'NONE', #4874, #221355, #37726, .T. ) ;
#43569=DIRECTION ( 'NONE',  ( 7.304098846218134667E-16, 1.000000000000000000, 6.982962677686267499E-15 ) ) ;
#43582=DIRECTION ( 'NONE',  ( 0.000000000000000000, 0.8660254037844378194, 0.5000000000000016653 ) ) ;
#43593=EDGE_CURVE ( 'NONE', #189189, #209120, #4396, .T. ) ;
#43622=DIRECTION ( 'NONE',  ( 0.000000000000000000, 0.000000000000000000, 1.000000000000000000 ) ) ;
#43670=DIRECTION ( 'NONE',  ( -2.578261006436899437E-14, -0.1350103645451973811, 0.9908441862701586889 ) ) ;
#43676=CARTESIAN_POINT ( 'NONE',  ( 21.13461538461538325, 65.38541703798632909, -90.67310748452437963 ) ) ;
#43690=ADVANCED_FACE ( 'NONE', ( #89069 ), #69539, .T. ) ;
#43711=EDGE_LOOP ( 'NONE', ( #194823, #36812, #179584, #125060 ) ) ;
#43726=CARTESIAN_POINT ( 'NONE',  ( -21.05000000000000071, 75.90220970870321082, -109.2809220950004203 ) ) ;
#43745=FACE_OUTER_BOUND ( 'NONE', #232720, .T. ) ;
#43747=CARTESIAN_POINT ( 'NONE',  ( -23.15000000000000213, 76.00000000001169553, -67.42310748452430857 ) ) ;
#43750=ORIENTED_EDGE ( 'NONE', *, *, #108712, .F. ) ;
#43753=DIRECTION ( 'NONE',  ( 0.000000000000000000, -6.982962677686267499E-15, 1.000000000000000000 ) ) ;
#43757=CARTESIAN_POINT ( 'NONE',  ( -23.25000000000000000, 77.73670573947921980, -58.00568489690056850 ) ) ;
#43768=ORIENTED_EDGE ( 'NONE', *, *, #41676, .F. ) ;
#43792=CARTESIAN_POINT ( 'NONE',  ( -21.09813707148783379, 75.96864850048257267, -109.4081695902609965 ) ) ;
#43804=DIRECTION ( 'NONE',  ( 0.000000000000000000, 1.000000000000000000, 6.982962677686267499E-15 ) ) ;
#43805=EDGE_LOOP ( 'NONE', ( #6550, #250061, #131199 ) ) ;
#43830=AXIS2_PLACEMENT_3D ( 'NONE', #188656, #72585, #232948 ) ;
#43857=CARTESIAN_POINT ( 'NONE',  ( 22.49999999999999645, 64.25043287652256652, -103.1239658536230763 ) ) ;
#43895=AXIS2_PLACEMENT_3D ( 'NONE', #124624, #85451, #166347 ) ;
#43904=CARTESIAN_POINT ( 'NONE',  ( -23.15000000000000213, 76.00000000001173817, -73.42310748452430857 ) ) ;
#43916=CARTESIAN_POINT ( 'NONE',  ( -20.54999999999999716, 68.85000000001186038, -90.67310748452435121 ) ) ;
#43931=AXIS2_PLACEMENT_3D ( 'NONE', #68244, #104761, #107355 ) ;
#43941=DIRECTION ( 'NONE',  ( 0.000000000000000000, 7.056502275159890043E-15, -1.000000000000000000 ) ) ;
#43978=DIRECTION ( 'NONE',  ( 0.000000000000000000, -0.1298341882519953583, -0.9915357197604861561 ) ) ;
#44030=EDGE_CURVE ( 'NONE', #20048, #123690, #11503, .T. ) ;
#44032=AXIS2_PLACEMENT_3D ( 'NONE', #154877, #234371, #118296 ) ;
#44037=ORIENTED_EDGE ( 'NONE', *, *, #179746, .T. ) ;
#44043=PLANE ( 'NONE',  #239194 ) ;
#44082=CARTESIAN_POINT ( 'NONE',  ( -20.94999999999999929, 64.25000000001175238, -76.30697314750247529 ) ) ;
#44089=CARTESIAN_POINT ( 'NONE',  ( -23.15000000000000213, 85.00000000001188027, -93.12913836187181005 ) ) ;
#44130=ORIENTED_EDGE ( 'NONE', *, *, #21874, .T. ) ;
#44131=VERTEX_POINT ( 'NONE', #54455 ) ;
#44181=EDGE_LOOP ( 'NONE', ( #89470, #38835, #83219, #121920 ) ) ;
#44225=CARTESIAN_POINT ( 'NONE',  ( -23.25000000000000000, 77.14957036958736580, -61.70719500002233815 ) ) ;
#44229=CARTESIAN_POINT ( 'NONE',  ( -18.59999999999999787, 64.35000000001180354, -81.67310748452439384 ) ) ;
#44242=DIRECTION ( 'NONE',  ( 0.000000000000000000, -7.086529944415894657E-15, 1.000000000000000000 ) ) ;
#44247=CARTESIAN_POINT ( 'NONE',  ( 20.95265033839679347, 65.48774916754473452, -95.45734372849443616 ) ) ;
#44265=ADVANCED_FACE ( 'NONE', ( #99971 ), #118294, .T. ) ;
#44274=CIRCLE ( 'NONE', #206573, 0.09999999999999939493 ) ;
#44283=ADVANCED_FACE ( 'NONE', ( #103831 ), #85536, .F. ) ;
#44299=ORIENTED_EDGE ( 'NONE', *, *, #44691, .F. ) ;
#44301=ORIENTED_EDGE ( 'NONE', *, *, #58735, .F. ) ;
#44313=AXIS2_PLACEMENT_3D ( 'NONE', #118665, #36576, #216446 ) ;
#44317=CIRCLE ( 'NONE', #190052, 4.049999999999998046 ) ;
#44323=EDGE_CURVE ( 'NONE', #216625, #50141, #620, .T. ) ;
#44356=ORIENTED_EDGE ( 'NONE', *, *, #157656, .T. ) ;
#44360=FACE_OUTER_BOUND ( 'NONE', #224035, .T. ) ;
#44370=DIRECTION ( 'NONE',  ( 0.000000000000000000, -6.467318590049456648E-15, 1.000000000000000000 ) ) ;
#44372=CARTESIAN_POINT ( 'NONE',  ( -21.05000000000000071, 76.10000000001203091, -114.6726782920691079 ) ) ;
#44378=EDGE_LOOP ( 'NONE', ( #87354, #194189, #61152, #146985 ) ) ;
#44414=DIRECTION ( 'NONE',  ( -1.000000000000000000, -0.000000000000000000, -0.000000000000000000 ) ) ;
#44415=DIRECTION ( 'NONE',  ( 0.000000000000000000, -6.982962677686266711E-15, 1.000000000000000000 ) ) ;
#44468=ORIENTED_EDGE ( 'NONE', *, *, #250746, .F. ) ;
#44481=ADVANCED_FACE ( 'NONE', ( #208114 ), #88096, .T. ) ;
#44482=DIRECTION ( 'NONE',  ( 1.000000000000000000, 0.000000000000000000, 0.000000000000000000 ) ) ;
#44500=CARTESIAN_POINT ( 'NONE',  ( 20.85000000000000142, 76.32388570108204817, -69.56551789521031992 ) ) ;
#44590=DIRECTION ( 'NONE',  ( 0.000000000000000000, 1.000000000000000000, 6.982962677686266711E-15 ) ) ;
#44605=CYLINDRICAL_SURFACE ( 'NONE', #115694, 0.09999999999999976963 ) ;
#44609=DIRECTION ( 'NONE',  ( 0.000000000000000000, -7.086529944415894657E-15, 1.000000000000000000 ) ) ;
#44610=ORIENTED_EDGE ( 'NONE', *, *, #11079, .F. ) ;
#44625=EDGE_LOOP ( 'NONE', ( #203191, #58081, #207072, #28467 ) ) ;
#44649=EDGE_CURVE ( 'NONE', #195497, #142060, #121655, .T. ) ;
#44656=EDGE_CURVE ( 'NONE', #242308, #12289, #140088, .T. ) ;
#44667=CARTESIAN_POINT ( 'NONE',  ( 20.94999999999999929, 68.87972903831409610, -65.86354444268503983 ) ) ;
#44691=EDGE_CURVE ( 'NONE', #97749, #204570, #183103, .T. ) ;
#44732=ORIENTED_EDGE ( 'NONE', *, *, #57919, .T. ) ;
#44762=ORIENTED_EDGE ( 'NONE', *, *, #220416, .T. ) ;
#44780=EDGE_LOOP ( 'NONE', ( #30655, #195036, #124952, #115502 ) ) ;
#44791=SURFACE_STYLE_FILL_AREA ( #242978 ) ;
#44846=DIRECTION ( 'NONE',  ( 0.000000000000000000, -7.034366652768082711E-15, 1.000000000000000000 ) ) ;
#44895=AXIS2_PLACEMENT_3D ( 'NONE', #212522, #172135, #35191 ) ;
#44897=AXIS2_PLACEMENT_3D ( 'NONE', #243582, #208330, #29703 ) ;
#44904=VERTEX_POINT ( 'NONE', #13452 ) ;
#44991=CARTESIAN_POINT ( 'NONE',  ( -20.64999999999999858, 73.60000000001180354, -82.74772940728642823 ) ) ;
#44998=FACE_OUTER_BOUND ( 'NONE', #107788, .T. ) ;
#45004=CARTESIAN_POINT ( 'NONE',  ( -23.15000000000000213, 84.59626168225486254, -93.57297996737396772 ) ) ;
#45009=ORIENTED_EDGE ( 'NONE', *, *, #50197, .T. ) ;
#45010=CARTESIAN_POINT ( 'NONE',  ( -21.09096482362058467, 75.96055172123791976, -109.3866518499287963 ) ) ;
#45039=ORIENTED_EDGE ( 'NONE', *, *, #112042, .F. ) ;
#45040=LINE ( 'NONE', #43757, #232994 ) ;
#45062=ORIENTED_EDGE ( 'NONE', *, *, #159810, .T. ) ;
#45064=CARTESIAN_POINT ( 'NONE',  ( -18.39999999999999858, 85.50000000001168132, -62.92291809330220786 ) ) ;
#45070=CARTESIAN_POINT ( 'NONE',  ( -21.07933241753356413, 75.90662040959273327, -109.3517534329040615 ) ) ;
#45077=EDGE_LOOP ( 'NONE', ( #29046, #13745, #188858, #79352 ) ) ;
#45106=EDGE_CURVE ( 'NONE', #153107, #44131, #171734, .T. ) ;
#45130=ORIENTED_EDGE ( 'NONE', *, *, #121237, .F. ) ;
#45133=CARTESIAN_POINT ( 'NONE',  ( 22.59999999999999432, 64.25043287652255231, -103.1239658536231047 ) ) ;
#45155=EDGE_CURVE ( 'NONE', #171051, #212250, #46785, .T. ) ;
#45214=DIRECTION ( 'NONE',  ( -1.000000000000000000, 2.952720810173289112E-16, 2.061873921506763405E-30 ) ) ;
#45241=DIRECTION ( 'NONE',  ( 1.000000000000000000, 0.000000000000000000, 0.000000000000000000 ) ) ;
#45362=CARTESIAN_POINT ( 'NONE',  ( -20.94999999999999929, 76.00000000001169553, -65.42310748452432279 ) ) ;
#45365=ORIENTED_EDGE ( 'NONE', *, *, #35300, .F. ) ;
#45416=DIRECTION ( 'NONE',  ( -3.265361837132813093E-16, -1.000000000000000000, -6.982962677686266711E-15 ) ) ;
#45423=ORIENTED_EDGE ( 'NONE', *, *, #204635, .T. ) ;
#45501=ORIENTED_EDGE ( 'NONE', *, *, #85096, .T. ) ;
#45504=CIRCLE ( 'NONE', #70664, 11.79999999999999716 ) ;
#45522=AXIS2_PLACEMENT_3D ( 'NONE', #254175, #75585, #115982 ) ;
#45537=DIRECTION ( 'NONE',  ( 0.000000000000000000, 0.000000000000000000, 1.000000000000000000 ) ) ;
#45541=ORIENTED_EDGE ( 'NONE', *, *, #28833, .F. ) ;
#45563=DIRECTION ( 'NONE',  ( 0.000000000000000000, 0.000000000000000000, 1.000000000000000000 ) ) ;
#45585=DIRECTION ( 'NONE',  ( 7.304098846218134667E-16, 1.000000000000000000, 6.982962677686266711E-15 ) ) ;
#45637=VECTOR ( 'NONE', #80978, 1000.000000000000000 ) ;
#45676=VERTEX_POINT ( 'NONE', #131111 ) ;
#45684=ORIENTED_EDGE ( 'NONE', *, *, #156338, .F. ) ;
#45698=EDGE_CURVE ( 'NONE', #191619, #231923, #213767, .T. ) ;
#45760=EDGE_LOOP ( 'NONE', ( #19396, #83261, #60030, #179653 ) ) ;
#45806=EDGE_CURVE ( 'NONE', #27688, #14341, #176191, .T. ) ;
#45807=DIRECTION ( 'NONE',  ( 0.000000000000000000, 0.8660254037844420383, -0.4999999999999943379 ) ) ;
#45835=CARTESIAN_POINT ( 'NONE',  ( 21.07016717457010913, 76.00000000001200817, -109.3440483226251985 ) ) ;
#45853=CIRCLE ( 'NONE', #145792, 0.5000000000000004441 ) ;
#45894=ORIENTED_EDGE ( 'NONE', *, *, #251995, .F. ) ;
#45921=DIRECTION ( 'NONE',  ( 0.000000000000000000, -1.000000000000000000, -6.982962677686265922E-15 ) ) ;
#45930=VECTOR ( 'NONE', #72226, 1000.000000000000000 ) ;
#45932=CARTESIAN_POINT ( 'NONE',  ( 22.59999999999999432, 75.90000000001202807, -114.6726782920691221 ) ) ;
#45951=CIRCLE ( 'NONE', #229319, 0.09999999999999976963 ) ;
#45969=AXIS2_PLACEMENT_3D ( 'NONE', #67901, #127886, #69214 ) ;
#46020=CARTESIAN_POINT ( 'NONE',  ( -20.54999999999999716, 87.75000000001183764, -86.27310748452423184 ) ) ;
#46038=EDGE_CURVE ( 'NONE', #13968, #51672, #255591, .T. ) ;
#46047=CARTESIAN_POINT ( 'NONE',  ( -23.15000000000000213, 76.00000000001195133, -103.0231074845243171 ) ) ;
#46079=ORIENTED_EDGE ( 'NONE', *, *, #123838, .T. ) ;
#46112=DIRECTION ( 'NONE',  ( 1.000000000000000000, 0.000000000000000000, -0.000000000000000000 ) ) ;
#46115=ORIENTED_EDGE ( 'NONE', *, *, #219682, .F. ) ;
#46122=AXIS2_PLACEMENT_3D ( 'NONE', #124494, #204012, #11941 ) ;
#46157=CIRCLE ( 'NONE', #204364, 0.1000000000000028644 ) ;
#46159=DIRECTION ( 'NONE',  ( 0.000000000000000000, 6.938893903907222067E-15, -1.000000000000000000 ) ) ;
#46179=DIRECTION ( 'NONE',  ( 0.000000000000000000, -6.982962677686266711E-15, 1.000000000000000000 ) ) ;
#46184=ADVANCED_FACE ( 'NONE', ( #157805 ), #108856, .T. ) ;
#46190=AXIS2_PLACEMENT_3D ( 'NONE', #209207, #93112, #129676 ) ;
#46194=AXIS2_PLACEMENT_3D ( 'NONE', #119538, #179515, #80359 ) ;
#46208=ORIENTED_EDGE ( 'NONE', *, *, #69448, .F. ) ;
#46212=VERTEX_POINT ( 'NONE', #225410 ) ;
#46215=CARTESIAN_POINT ( 'NONE',  ( 19.97071067811864609, 64.27928932189314537, -81.67310748452439384 ) ) ;
#46217=DIRECTION ( 'NONE',  ( 1.000000000000000000, 0.000000000000000000, 0.000000000000000000 ) ) ;
#46221=EDGE_CURVE ( 'NONE', #94746, #7823, #55689, .T. ) ;
#46225=AXIS2_PLACEMENT_3D ( 'NONE', #108169, #53321, #187717 ) ;
#46226=VERTEX_POINT ( 'NONE', #144591 ) ;
#46231=DIRECTION ( 'NONE',  ( 0.000000000000000000, 0.000000000000000000, 1.000000000000000000 ) ) ;
#46238=CIRCLE ( 'NONE', #54442, 0.1000000000000028644 ) ;
#46287=CARTESIAN_POINT ( 'NONE',  ( -23.25000000000000000, 64.25000000001186606, -90.87310748452438247 ) ) ;
#46301=CARTESIAN_POINT ( 'NONE',  ( -21.05000000000000071, 87.65000000001172964, -72.52310748452423184 ) ) ;
#46306=CARTESIAN_POINT ( 'NONE',  ( 18.42555734704284731, 85.49715836194860685, -95.98327698678932052 ) ) ;
#46319=LINE ( 'NONE', #127156, #242583 ) ;
#46335=ORIENTED_EDGE ( 'NONE', *, *, #220862, .F. ) ;
#46353=ADVANCED_FACE ( 'NONE', ( #149773 ), #122373, .F. ) ;
#46355=CARTESIAN_POINT ( 'NONE',  ( -23.15000000000000213, 87.75000000001193712, -103.0231074845242318 ) ) ;
#46378=CIRCLE ( 'NONE', #192169, 0.2000000000000057288 ) ;
#46399=CARTESIAN_POINT ( 'NONE',  ( 22.59066674512252249, 64.25000000001193712, -103.0536116081550375 ) ) ;
#46402=EDGE_CURVE ( 'NONE', #197574, #18900, #188875, .T. ) ;
#46423=DIRECTION ( 'NONE',  ( 0.000000000000000000, 6.938893903907270030E-14, -1.000000000000000000 ) ) ;
#46432=DIRECTION ( 'NONE',  ( 0.000000000000000000, 6.982962677686266711E-15, -1.000000000000000000 ) ) ;
#46440=DIRECTION ( 'NONE',  ( 0.000000000000000000, -1.000000000000000000, -6.982962677686266711E-15 ) ) ;
#46441=CIRCLE ( 'NONE', #79746, 0.09999999999999939493 ) ;
#46500=CIRCLE ( 'NONE', #196356, 6.258578643762696458 ) ;
#46527=CARTESIAN_POINT ( 'NONE',  ( -20.85000000000000142, 76.32388570108204817, -69.56551789521031992 ) ) ;
#46530=DIRECTION ( 'NONE',  ( -0.000000000000000000, 0.4791956752371485107, 0.8777080977375185666 ) ) ;
#46544=DIRECTION ( 'NONE',  ( 0.000000000000000000, -6.982962677686266711E-15, 1.000000000000000000 ) ) ;
#46555=CARTESIAN_POINT ( 'NONE',  ( -22.50000000000000000, 64.35042919246716053, -103.1231074845243825 ) ) ;
#46564=DIRECTION ( 'NONE',  ( 3.469446951953514477E-14, 0.9999176327611370985, 0.01283462868040226822 ) ) ;
#46565=EDGE_LOOP ( 'NONE', ( #208967, #15301, #205136, #130803, #232105, #136505, #195426, #164392, #25170, #214993, #48649, #106031 ) ) ;
#46566=AXIS2_PLACEMENT_3D ( 'NONE', #61898, #108727, #43622 ) ;
#46615=CARTESIAN_POINT ( 'NONE',  ( 21.05000000000000071, 71.00000000001180922, -81.92837350343744163 ) ) ;
#46664=ORIENTED_EDGE ( 'NONE', *, *, #192188, .F. ) ;
#46712=DIRECTION ( 'NONE',  ( 1.000000000000000000, 0.000000000000000000, 0.000000000000000000 ) ) ;
#46718=ADVANCED_FACE ( 'NONE', ( #112879 ), #209403, .F. ) ;
#46720=ORIENTED_EDGE ( 'NONE', *, *, #142074, .F. ) ;
#46746=EDGE_CURVE ( 'NONE', #237421, #194022, #111597, .T. ) ;
#46765=EDGE_CURVE ( 'NONE', #239334, #256668, #80426, .T. ) ;
#46785=CIRCLE ( 'NONE', #80075, 0.1000000000000009492 ) ;
#46791=EDGE_LOOP ( 'NONE', ( #223335, #249026, #176910, #200235 ) ) ;
#46806=DIRECTION ( 'NONE',  ( 0.000000000000000000, -7.172728831056617961E-15, 1.000000000000000000 ) ) ;
#46822=CARTESIAN_POINT ( 'NONE',  ( -22.39999999999999858, 75.90000000001199965, -110.8138870828977218 ) ) ;
#46841=EDGE_CURVE ( 'NONE', #3248, #157975, #198831, .T. ) ;
#46855=TOROIDAL_SURFACE ( 'NONE', #163404, 0.2000000000000000111, 0.1000000000000000056 ) ;
#46860=CARTESIAN_POINT ( 'NONE',  ( -23.25000000000000000, 76.00000000001170974, -69.52310748452431710 ) ) ;
#46882=CARTESIAN_POINT ( 'NONE',  ( -23.15000000000000213, 76.00000000001170974, -69.52310748452431710 ) ) ;
#46893=CIRCLE ( 'NONE', #67760, 0.09999999999999938105 ) ;
#46894=FACE_OUTER_BOUND ( 'NONE', #12073, .T. ) ;
#46941=ADVANCED_FACE ( 'NONE', ( #143985 ), #7050, .F. ) ;
#46968=ORIENTED_EDGE ( 'NONE', *, *, #236087, .F. ) ;
#46979=CARTESIAN_POINT ( 'NONE',  ( -18.50000000000000000, 85.40000000001191438, -95.72584772486095517 ) ) ;
#46980=ORIENTED_EDGE ( 'NONE', *, *, #184480, .F. ) ;
#46989=CARTESIAN_POINT ( 'NONE',  ( 23.14999999999999503, 64.35000000001178933, -81.67310748452439384 ) ) ;
#47016=EDGE_CURVE ( 'NONE', #249207, #102678, #213739, .T. ) ;
#47026=ORIENTED_EDGE ( 'NONE', *, *, #123725, .T. ) ;
#47065=DIRECTION ( 'NONE',  ( 0.000000000000000000, 0.8700118002898393765, -0.4930308989875104575 ) ) ;
#47119=LINE ( 'NONE', #244053, #196650 ) ;
#47146=CIRCLE ( 'NONE', #192926, 0.1000000000000017680 ) ;
#47162=EDGE_CURVE ( 'NONE', #99108, #86349, #97166, .T. ) ;
#47188=EDGE_LOOP ( 'NONE', ( #135178, #84263, #135071, #97048 ) ) ;
#47190=CIRCLE ( 'NONE', #51275, 11.90000000000000746 ) ;
#47208=AXIS2_PLACEMENT_3D ( 'NONE', #180050, #19700, #99195 ) ;
#47217=EDGE_LOOP ( 'NONE', ( #170117, #173078, #148880, #26466 ) ) ;
#47226=VERTEX_POINT ( 'NONE', #56442 ) ;
#47264=EDGE_CURVE ( 'NONE', #246499, #51208, #101444, .T. ) ;
#47274=ORIENTED_EDGE ( 'NONE', *, *, #80399, .T. ) ;
#47335=FACE_OUTER_BOUND ( 'NONE', #8812, .T. ) ;
#47345=CARTESIAN_POINT ( 'NONE',  ( 20.30531438145591139, 65.90309893892053594, -95.22708967725128559 ) ) ;
#47347=ORIENTED_EDGE ( 'NONE', *, *, #110653, .T. ) ;
#47351=VECTOR ( 'NONE', #10302, 1000.000000000000000 ) ;
#47391=CARTESIAN_POINT ( 'NONE',  ( 21.13461538461538680, 67.11458296203740304, -90.67310748452436542 ) ) ;
#47405=VECTOR ( 'NONE', #172884, 1000.000000000000000 ) ;
#47427=TOROIDAL_SURFACE ( 'NONE', #59888, 4.099999999999999645, 0.1000000000000000056 ) ;
#47480=ADVANCED_FACE ( 'NONE', ( #109690 ), #240605, .T. ) ;
#47497=CARTESIAN_POINT ( 'NONE',  ( -22.50000000000000000, 75.90736249940255220, -114.6728046915650765 ) ) ;
#47510=AXIS2_PLACEMENT_3D ( 'NONE', #25076, #184109, #162014 ) ;
#47534=ORIENTED_EDGE ( 'NONE', *, *, #210127, .F. ) ;
#47540=ADVANCED_FACE ( 'NONE', ( #58692 ), #195690, .T. ) ;
#47548=VERTEX_POINT ( 'NONE', #216503 ) ;
#47559=EDGE_CURVE ( 'NONE', #171995, #6826, #201639, .T. ) ;
#47623=EDGE_LOOP ( 'NONE', ( #161218, #137374, #203458, #31185, #67730 ) ) ;
#47624=DIRECTION ( 'NONE',  ( 0.000000000000000000, 6.982962677686266711E-15, -1.000000000000000000 ) ) ;
#47638=AXIS2_PLACEMENT_3D ( 'NONE', #140688, #46712, #64999 ) ;
#47644=EDGE_CURVE ( 'NONE', #173596, #183385, #220373, .T. ) ;
#47648=ORIENTED_EDGE ( 'NONE', *, *, #46746, .T. ) ;
#47660=LINE ( 'NONE', #209313, #87870 ) ;
#47693=DIRECTION ( 'NONE',  ( 0.000000000000000000, 0.000000000000000000, -1.000000000000000000 ) ) ;
#47708=ORIENTED_EDGE ( 'NONE', *, *, #248501, .F. ) ;
#47736=DIRECTION ( 'NONE',  ( -0.000000000000000000, -6.982962677686266711E-15, 1.000000000000000000 ) ) ;
#47743=ORIENTED_EDGE ( 'NONE', *, *, #126746, .T. ) ;
#47745=ORIENTED_EDGE ( 'NONE', *, *, #174886, .F. ) ;
#47757=EDGE_CURVE ( 'NONE', #83423, #168199, #101658, .T. ) ;
#47772=ORIENTED_EDGE ( 'NONE', *, *, #114256, .F. ) ;
#47774=DIRECTION ( 'NONE',  ( 0.000000000000000000, -6.982962677686266711E-15, 1.000000000000000000 ) ) ;
#47793=CARTESIAN_POINT ( 'NONE',  ( -23.25000000000000000, 76.00000000001195133, -103.0231074845243171 ) ) ;
#47803=DIRECTION ( 'NONE',  ( -1.000000000000000000, 0.000000000000000000, 0.000000000000000000 ) ) ;
#47814=EDGE_LOOP ( 'NONE', ( #4668, #36540, #189453, #243950, #119582, #4876, #1693, #14777, #81039, #64571, #227862, #38893, #2093, #148009, #19068, #212946 ) ) ;
#47822=TOROIDAL_SURFACE ( 'NONE', #226911, 0.2000000000000000111, 0.1000000000000000056 ) ;
#47839=CARTESIAN_POINT ( 'NONE',  ( -23.15000000000000213, 87.65000000001172964, -72.52310748452423184 ) ) ;
#47842=VECTOR ( 'NONE', #185819, 1000.000000000000000 ) ;
#47843=EDGE_CURVE ( 'NONE', #246499, #147363, #243147, .T. ) ;
#47873=FACE_OUTER_BOUND ( 'NONE', #143229, .T. ) ;
#47891=( BOUNDED_SURFACE ( )  B_SPLINE_SURFACE ( 3, 2, ( 
 ( #222969, #146004, #203427 ),
 ( #185141, #224255, #205988 ),
 ( #165594, #225518, #3937 ),
 ( #182591, #243822, #6490 ),
 ( #106872, #24816, #247682 ),
 ( #86003, #84713, #88585 ) ),
 .UNSPECIFIED., .F., .F., .F. ) 
 B_SPLINE_SURFACE_WITH_KNOTS ( ( 4, 2, 4 ),
 ( 3, 3 ),
 ( 4.712388980384689674, 5.497787143782137953, 6.283185307179586232 ),
 ( 0.000000000000000000, 1.000000000000000000 ),
 .UNSPECIFIED. ) 
 GEOMETRIC_REPRESENTATION_ITEM ( )  RATIONAL_B_SPLINE_SURFACE ( (
 ( 1.000000000000000000, 0.7071067811865475727, 1.000000000000000000),
 ( 1.000000000000000000, 0.7727932973487947610, 1.000000000000000000),
 ( 1.000000000000000000, 0.8282379607654274389, 1.000000000000000000),
 ( 1.000000000000000000, 0.9038128468035014906, 1.000000000000000000),
 ( 1.000000000000000000, 0.9240297172246950685, 1.000000000000000000),
 ( 1.000000000000000000, 0.9238795325112961754, 1.000000000000000000) ) ) 
 REPRESENTATION_ITEM ( '' )  SURFACE ( )  );
#47921=ORIENTED_EDGE ( 'NONE', *, *, #227679, .F. ) ;
#47940=CIRCLE ( 'NONE', #172902, 0.1000000000000026007 ) ;
#48029=VECTOR ( 'NONE', #191546, 1000.000000000000000 ) ;
#48054=CARTESIAN_POINT ( 'NONE',  ( -22.39999999999999858, 76.10000000001203091, -114.6726782920691079 ) ) ;
#48055=CARTESIAN_POINT ( 'NONE',  ( -18.59999999999999787, 68.92903212821283887, -65.77654326265606244 ) ) ;
#48064=CIRCLE ( 'NONE', #27262, 0.3999999999999975797 ) ;
#48077=CARTESIAN_POINT ( 'NONE',  ( -21.13614978966382196, 69.50089529817815048, -103.0231074845243739 ) ) ;
#48081=CARTESIAN_POINT ( 'NONE',  ( 20.95556889135987788, 65.37805641227680553, -95.38071326266687322 ) ) ;
#48101=EDGE_CURVE ( 'NONE', #88561, #200905, #146576, .T. ) ;
#48105=LINE ( 'NONE', #226739, #243108 ) ;
#48168=CARTESIAN_POINT ( 'NONE',  ( 22.16821283564876666, 68.44102665923118423, -103.0231074845243739 ) ) ;
#48189=DIRECTION ( 'NONE',  ( -1.000000000000000000, 0.000000000000000000, 0.000000000000000000 ) ) ;
#48227=DIRECTION ( 'NONE',  ( -1.000000000000000000, 0.000000000000000000, -0.000000000000000000 ) ) ;
#48271=CARTESIAN_POINT ( 'NONE',  ( -23.15000000000000213, 85.00000000001188027, -93.12913836187181005 ) ) ;
#48278=EDGE_CURVE ( 'NONE', #64660, #158833, #181181, .T. ) ;
#48279=LINE ( 'NONE', #69154, #209171 ) ;
#48289=CARTESIAN_POINT ( 'NONE',  ( -20.94999999999999929, 87.75000000001192291, -99.92310748452422331 ) ) ;
#48295=DIRECTION ( 'NONE',  ( -1.836970198721029934E-16, -1.000000000000000000, -6.982962677686266711E-15 ) ) ;
#48314=DIRECTION ( 'NONE',  ( 0.000000000000000000, 0.000000000000000000, 1.000000000000000000 ) ) ;
#48370=CARTESIAN_POINT ( 'NONE',  ( 21.05000000000000071, 67.12338541492479749, -94.63802700567968884 ) ) ;
#48382=VECTOR ( 'NONE', #143635, 1000.000000000000000 ) ;
#48384=LINE ( 'NONE', #83629, #48382 ) ;
#48386=LINE ( 'NONE', #6698, #193112 ) ;
#48387=TOROIDAL_SURFACE ( 'NONE', #110938, 2.100000000000002309, 0.1000000000000000056 ) ;
#48389=CIRCLE ( 'NONE', #223173, 0.1000000000000028644 ) ;
#48418=ADVANCED_FACE ( 'NONE', ( #23821 ), #120358, .F. ) ;
#48433=DIRECTION ( 'NONE',  ( -1.000000000000000000, -0.000000000000000000, 0.000000000000000000 ) ) ;
#48508=ORIENTED_EDGE ( 'NONE', *, *, #221981, .F. ) ;
#48531=ORIENTED_EDGE ( 'NONE', *, *, #104701, .T. ) ;
#48548=FACE_OUTER_BOUND ( 'NONE', #17353, .T. ) ;
#48574=B_SPLINE_CURVE_WITH_KNOTS ( 'NONE', 3,
 ( #115011, #194581, #112461, #255765 ),
 .UNSPECIFIED., .F., .F.,
 ( 4, 4 ),
 ( 0.000000000000000000, 0.0001048066582182452479 ),
 .UNSPECIFIED. ) ;
#48584=CARTESIAN_POINT ( 'NONE',  ( 20.94999999999999574, 65.52661458509899717, -95.44445302027583011 ) ) ;
#48587=CARTESIAN_POINT ( 'NONE',  ( 18.59999999999999076, 69.01799029515522932, -65.82695536626806643 ) ) ;
#48620=DIRECTION ( 'NONE',  ( 0.000000000000000000, 0.9915357197604892647, -0.1298341882519715440 ) ) ;
#48635=EDGE_LOOP ( 'NONE', ( #89607, #123788, #226804, #102956 ) ) ;
#48638=CARTESIAN_POINT ( 'NONE',  ( 20.21567752745066215, 65.80188589877991490, -95.14048713687273562 ) ) ;
#48642=AXIS2_PLACEMENT_3D ( 'NONE', #44991, #204051, #104914 ) ;
#48649=ORIENTED_EDGE ( 'NONE', *, *, #59596, .T. ) ;
#48672=CARTESIAN_POINT ( 'NONE',  ( -20.54999999999999716, 68.85000000001180354, -81.87310748452436826 ) ) ;
#48696=ORIENTED_EDGE ( 'NONE', *, *, #108463, .T. ) ;
#48799=AXIS2_PLACEMENT_3D ( 'NONE', #155441, #233663, #117552 ) ;
#48806=CYLINDRICAL_SURFACE ( 'NONE', #51534, 11.74999999999999645 ) ;
#48825=AXIS2_PLACEMENT_3D ( 'NONE', #78035, #177180, #195452 ) ;
#48831=VERTEX_POINT ( 'NONE', #159175 ) ;
#48857=ORIENTED_EDGE ( 'NONE', *, *, #231385, .F. ) ;
#48923=ORIENTED_EDGE ( 'NONE', *, *, #231910, .T. ) ;
#48929=AXIS2_PLACEMENT_3D ( 'NONE', #24748, #147225, #125117 ) ;
#48934=AXIS2_PLACEMENT_3D ( 'NONE', #140184, #123215, #202747 ) ;
#48969=CARTESIAN_POINT ( 'NONE',  ( -18.59999999999999787, 68.97833521811159585, -65.68954208262705663 ) ) ;
#48988=EDGE_LOOP ( 'NONE', ( #180839, #58779, #30498, #195843, #63127, #177502, #147951 ) ) ;
#49004=AXIS2_PLACEMENT_3D ( 'NONE', #50168, #52739, #110152 ) ;
#49025=CARTESIAN_POINT ( 'NONE',  ( -20.54999999999999716, 87.75000000001186606, -90.67310748452422331 ) ) ;
#49035=CARTESIAN_POINT ( 'NONE',  ( 21.05000000000000071, 85.00000000001188027, -93.12913836187181005 ) ) ;
#49047=FACE_OUTER_BOUND ( 'NONE', #57468, .T. ) ;
#49095=FACE_OUTER_BOUND ( 'NONE', #26720, .T. ) ;
#49098=CIRCLE ( 'NONE', #115747, 0.1000000000000028644 ) ;
#49108=CARTESIAN_POINT ( 'NONE',  ( 20.85000000000000142, 69.15387683765909799, -65.78538121767449809 ) ) ;
#49117=FACE_OUTER_BOUND ( 'NONE', #95515, .T. ) ;
#49127=DIRECTION ( 'NONE',  ( 0.000000000000000000, -6.853228547068871147E-15, 1.000000000000000000 ) ) ;
#49136=AXIS2_PLACEMENT_3D ( 'NONE', #193408, #73473, #151726 ) ;
#49173=ADVANCED_FACE ( 'NONE', ( #30435 ), #226014, .T. ) ;
#49219=CARTESIAN_POINT ( 'NONE',  ( -23.25000000000000000, 76.00000000001170974, -69.52310748452431710 ) ) ;
#49220=AXIS2_PLACEMENT_3D ( 'NONE', #118711, #225468, #27336 ) ;
#49226=VERTEX_POINT ( 'NONE', #49976 ) ;
#49234=CARTESIAN_POINT ( 'NONE',  ( 21.05000000000000071, 76.00000000001186606, -90.14810748452431710 ) ) ;
#49238=CARTESIAN_POINT ( 'NONE',  ( -1.820710678118658388, 85.92928932189310842, -78.37310748452424036 ) ) ;
#49254=VERTEX_POINT ( 'NONE', #129523 ) ;
#49270=EDGE_LOOP ( 'NONE', ( #89828, #134132, #173243, #223578 ) ) ;
#49271=EDGE_LOOP ( 'NONE', ( #182364, #133661, #72347, #203382 ) ) ;
#49276=ADVANCED_FACE ( 'NONE', ( #167390, #190812, #128243 ), #12166, .F. ) ;
#49295=DIRECTION ( 'NONE',  ( 0.000000000000000000, -0.4930308989875575865, -0.8700118002898125091 ) ) ;
#49300=ORIENTED_EDGE ( 'NONE', *, *, #104701, .F. ) ;
#49301=DIRECTION ( 'NONE',  ( 1.000000000000000000, 0.000000000000000000, 0.000000000000000000 ) ) ;
#49336=CIRCLE ( 'NONE', #195107, 0.1000000000000033223 ) ;
#49345=( BOUNDED_SURFACE ( )  B_SPLINE_SURFACE ( 3, 2, ( 
 ( #148752, #32688, #110893 ),
 ( #129183, #229569, #150041 ),
 ( #210006, #53490, #251685 ),
 ( #93890, #172206, #133038 ) ),
 .UNSPECIFIED., .F., .F., .F. ) 
 B_SPLINE_SURFACE_WITH_KNOTS ( ( 4, 4 ),
 ( 3, 3 ),
 ( 0.0006461284895274040097, 0.0007503702773986319378 ),
 ( 0.000000000000000000, 1.000000000000000000 ),
 .UNSPECIFIED. ) 
 GEOMETRIC_REPRESENTATION_ITEM ( )  RATIONAL_B_SPLINE_SURFACE ( (
 ( 1.000000000000000000, 0.7071067811865471286, 1.000000000000000000),
 ( 1.000000000000000000, 0.7076476444648849284, 1.000000000000000000),
 ( 1.000000000000000000, 0.7075727925191714895, 1.000000000000000000),
 ( 1.000000000000000000, 0.7071067811865475727, 1.000000000000000000) ) ) 
 REPRESENTATION_ITEM ( '' )  SURFACE ( )  );
#49429=DIRECTION ( 'NONE',  ( 1.000000000000000000, 0.000000000000000000, 0.000000000000000000 ) ) ;
#49433=CARTESIAN_POINT ( 'NONE',  ( 20.04142135623730070, 64.25000000001202238, -114.7731074845243882 ) ) ;
#49476=DIRECTION ( 'NONE',  ( 1.000000000000000000, 0.000000000000000000, 0.000000000000000000 ) ) ;
#49485=AXIS2_PLACEMENT_3D ( 'NONE', #103865, #200428, #83006 ) ;
#49498=AXIS2_PLACEMENT_3D ( 'NONE', #83447, #87314, #246409 ) ;
#49502=AXIS2_PLACEMENT_3D ( 'NONE', #4721, #125963, #28194 ) ;
#49519=ORIENTED_EDGE ( 'NONE', *, *, #135607, .T. ) ;
#49523=VECTOR ( 'NONE', #204583, 1000.000000000000000 ) ;
#49544=ORIENTED_EDGE ( 'NONE', *, *, #257622, .F. ) ;
#49546=ORIENTED_EDGE ( 'NONE', *, *, #156998, .F. ) ;
#49549=CARTESIAN_POINT ( 'NONE',  ( 23.14999999999999858, 72.10000000001170406, -69.52310748452433131 ) ) ;
#49560=FACE_OUTER_BOUND ( 'NONE', #179884, .T. ) ;
#49611=CYLINDRICAL_SURFACE ( 'NONE', #123867, 0.1000000000000028644 ) ;
#49636=FACE_OUTER_BOUND ( 'NONE', #62383, .T. ) ;
#49649=DIRECTION ( 'NONE',  ( 0.000000000000000000, 0.000000000000000000, -1.000000000000000000 ) ) ;
#49676=DIRECTION ( 'NONE',  ( -0.000000000000000000, 1.000000000000000000, 6.982962677686266711E-15 ) ) ;
#49690=EDGE_CURVE ( 'NONE', #47548, #186482, #7644, .T. ) ;
#49701=ORIENTED_EDGE ( 'NONE', *, *, #15857, .T. ) ;
#49703=DIRECTION ( 'NONE',  ( 0.000000000000000000, 0.000000000000000000, -1.000000000000000000 ) ) ;
#49705=DIRECTION ( 'NONE',  ( 0.000000000000000000, 0.000000000000000000, 1.000000000000000000 ) ) ;
#49712=ORIENTED_EDGE ( 'NONE', *, *, #125508, .T. ) ;
#49713=EDGE_CURVE ( 'NONE', #45676, #229726, #162452, .T. ) ;
#49741=CYLINDRICAL_SURFACE ( 'NONE', #214133, 0.1000000000000028644 ) ;
#49744=DIRECTION ( 'NONE',  ( 1.000000000000000000, -1.836970198721029934E-16, -1.282749433769087582E-30 ) ) ;
#49755=EDGE_CURVE ( 'NONE', #187906, #71369, #174271, .T. ) ;
#49786=ORIENTED_EDGE ( 'NONE', *, *, #163022, .T. ) ;
#49802=VERTEX_POINT ( 'NONE', #99043 ) ;
#49805=FACE_OUTER_BOUND ( 'NONE', #42995, .T. ) ;
#49806=ORIENTED_EDGE ( 'NONE', *, *, #108880, .F. ) ;
#49865=DIRECTION ( 'NONE',  ( -1.000000000000000000, 2.952720810173289112E-16, 2.061873921506763405E-30 ) ) ;
#49906=FACE_OUTER_BOUND ( 'NONE', #36452, .T. ) ;
#49909=CARTESIAN_POINT ( 'NONE',  ( 18.58703555225010007, 85.40633674080056892, -95.89816284327731921 ) ) ;
#49912=AXIS2_PLACEMENT_3D ( 'NONE', #88229, #173951, #167830 ) ;
#49928=CARTESIAN_POINT ( 'NONE',  ( 20.59588692710267921, 65.63127657884309940, -95.38402639001375860 ) ) ;
#49938=DIRECTION ( 'NONE',  ( 0.5000000000001141309, -6.047423072554455661E-15, 0.8660254037843729824 ) ) ;
#49944=CARTESIAN_POINT ( 'NONE',  ( 21.05000000000000071, 76.10000000001203091, -114.6726782920691079 ) ) ;
#49949=ORIENTED_EDGE ( 'NONE', *, *, #235914, .F. ) ;
#49968=EDGE_CURVE ( 'NONE', #167954, #23326, #7827, .T. ) ;
#49975=CONICAL_SURFACE ( 'NONE', #95746, 7.750000000000020428, 0.7853981633974531640 ) ;
#49976=CARTESIAN_POINT ( 'NONE',  ( -18.50000000000000000, 66.65000000001187175, -90.87310748452436826 ) ) ;
#49981=DIRECTION ( 'NONE',  ( 0.000000000000000000, -6.938893903907270030E-14, 1.000000000000000000 ) ) ;
#50022=DIRECTION ( 'NONE',  ( -0.000000000000000000, 6.982962677686266711E-15, -1.000000000000000000 ) ) ;
#50023=DIRECTION ( 'NONE',  ( 0.000000000000000000, 6.853228547068871147E-15, -1.000000000000000000 ) ) ;
#50026=DIRECTION ( 'NONE',  ( 0.000000000000000000, 6.982962677686266711E-15, -1.000000000000000000 ) ) ;
#50031=CARTESIAN_POINT ( 'NONE',  ( 21.05000000000000071, 76.00000000001195133, -103.0231074845243171 ) ) ;
#50081=CARTESIAN_POINT ( 'NONE',  ( -22.45372860728439690, 75.98507938046353161, -114.6729046192281913 ) ) ;
#50092=EDGE_CURVE ( 'NONE', #205047, #57915, #95302, .T. ) ;
#50141=VERTEX_POINT ( 'NONE', #36249 ) ;
#50153=EDGE_CURVE ( 'NONE', #116247, #213696, #115760, .T. ) ;
#50162=CIRCLE ( 'NONE', #191869, 0.09999999999999971412 ) ;
#50168=CARTESIAN_POINT ( 'NONE',  ( 21.05000000000000071, 87.75000000001172396, -72.42310748452422331 ) ) ;
#50171=DIRECTION ( 'NONE',  ( 0.000000000000000000, -0.9908441862701605762, -0.1350103645451835310 ) ) ;
#50189=VERTEX_POINT ( 'NONE', #158766 ) ;
#50190=EDGE_CURVE ( 'NONE', #251279, #77493, #87273, .T. ) ;
#50197=EDGE_CURVE ( 'NONE', #209005, #98180, #53961, .T. ) ;
#50213=ORIENTED_EDGE ( 'NONE', *, *, #134950, .F. ) ;
#50216=AXIS2_PLACEMENT_3D ( 'NONE', #229584, #186613, #49649 ) ;
#50262=CARTESIAN_POINT ( 'NONE',  ( 21.05000000000000071, 76.00000000001170974, -69.52310748452431710 ) ) ;
#50276=EDGE_LOOP ( 'NONE', ( #204316, #221502, #76163, #50213, #158239 ) ) ;
#50285=CIRCLE ( 'NONE', #220980, 0.09999999999999939493 ) ;
#50305=DIRECTION ( 'NONE',  ( 0.000000000000000000, 6.938893903907222067E-15, -1.000000000000000000 ) ) ;
#50308=CARTESIAN_POINT ( 'NONE',  ( -23.15000000000000213, 64.35000000001203091, -114.7731074845243882 ) ) ;
#50320=VECTOR ( 'NONE', #170374, 1000.000000000000000 ) ;
#50321=CARTESIAN_POINT ( 'NONE',  ( -21.05000000000000071, 87.48912529308798014, -99.92310748452423752 ) ) ;
#50331=ADVANCED_FACE ( 'NONE', ( #146849 ), #70579, .F. ) ;
#50340=ORIENTED_EDGE ( 'NONE', *, *, #153064, .T. ) ;
#50342=VERTEX_POINT ( 'NONE', #128600 ) ;
#50368=CARTESIAN_POINT ( 'NONE',  ( 20.97239005616515684, 67.12515615866173846, -90.77295468237119280 ) ) ;
#50372=DIRECTION ( 'NONE',  ( 1.000000000000000000, 7.304098846218133681E-16, 5.311601492717083645E-30 ) ) ;
#50402=CARTESIAN_POINT ( 'NONE',  ( 20.85000000000000142, 76.00000000001170974, -69.52310748452431710 ) ) ;
#50411=DIRECTION ( 'NONE',  ( -1.000000000000000000, 2.952720810173289112E-16, 2.061873921506763405E-30 ) ) ;
#50420=ADVANCED_FACE ( 'NONE', ( #9929 ), #2223, .T. ) ;
#50425=DIRECTION ( 'NONE',  ( 0.000000000000000000, 0.000000000000000000, 1.000000000000000000 ) ) ;
#50466=ORIENTED_EDGE ( 'NONE', *, *, #144014, .F. ) ;
#50474=DIRECTION ( 'NONE',  ( 0.000000000000000000, -0.1575844902526579161, -0.9875055080513779338 ) ) ;
#50478=AXIS2_PLACEMENT_3D ( 'NONE', #224584, #223293, #186767 ) ;
#50510=DIRECTION ( 'NONE',  ( 0.000000000000000000, -1.000000000000000000, 0.000000000000000000 ) ) ;
#50530=ORIENTED_EDGE ( 'NONE', *, *, #254957, .F. ) ;
#50544=DIRECTION ( 'NONE',  ( 0.000000000000000000, -0.1350103645451945777, 0.9908441862701590219 ) ) ;
#50579=CARTESIAN_POINT ( 'NONE',  ( 21.05000000000000071, 76.00000000001195133, -103.0231074845243171 ) ) ;
#50601=EDGE_CURVE ( 'NONE', #8175, #246385, #146237, .T. ) ;
#50623=EDGE_CURVE ( 'NONE', #204844, #224804, #224835, .T. ) ;
#50665=CARTESIAN_POINT ( 'NONE',  ( 23.14999999999998437, 76.00000000001195133, -103.0231074845243171 ) ) ;
#50671=VERTEX_POINT ( 'NONE', #127979 ) ;
#50675=CARTESIAN_POINT ( 'NONE',  ( 18.49999999999998934, 69.45000000001188312, -93.00608031408432907 ) ) ;
#50677=ORIENTED_EDGE ( 'NONE', *, *, #11175, .F. ) ;
#50702=ADVANCED_FACE ( 'NONE', ( #50970 ), #130530, .T. ) ;
#50769=CARTESIAN_POINT ( 'NONE',  ( 20.94999999999999574, 67.07338541492480033, -94.55142446530125255 ) ) ;
#50781=CARTESIAN_POINT ( 'NONE',  ( -20.07928932188135107, 66.77928932189321642, -90.67310748452436542 ) ) ;
#50785=ORIENTED_EDGE ( 'NONE', *, *, #16400, .T. ) ;
#50800=ORIENTED_EDGE ( 'NONE', *, *, #126082, .T. ) ;
#50803=DIRECTION ( 'NONE',  ( 3.616040088954490704E-32, 7.105427357601001859E-15, -1.000000000000000000 ) ) ;
#50805=CARTESIAN_POINT ( 'NONE',  ( -23.15000000000000213, 71.75000000001186606, -90.67310748452433700 ) ) ;
#50833=DIRECTION ( 'NONE',  ( 0.000000000000000000, 0.000000000000000000, -1.000000000000000000 ) ) ;
#50834=DIRECTION ( 'NONE',  ( 0.000000000000000000, 1.000000000000000000, 7.272083257015735086E-15 ) ) ;
#50842=ORIENTED_EDGE ( 'NONE', *, *, #18017, .T. ) ;
#50853=EDGE_CURVE ( 'NONE', #102162, #51895, #84637, .T. ) ;
#50872=DIRECTION ( 'NONE',  ( 0.000000000000000000, 0.000000000000000000, 1.000000000000000000 ) ) ;
#50886=EDGE_CURVE ( 'NONE', #125402, #249684, #179267, .T. ) ;
#50896=EDGE_CURVE ( 'NONE', #16721, #202516, #241208, .T. ) ;
#50957=B_SPLINE_CURVE_WITH_KNOTS ( 'NONE', 3,
 ( #74607, #154147, #38034, #181395, #199675, #83516, #78404, #2715, #18443, #142237 ),
 .UNSPECIFIED., .F., .F.,
 ( 4, 2, 2, 2, 4 ),
 ( 0.000000000000000000, 3.990160268013534029E-05, 7.980320536027068058E-05, 0.0001596064107205331212, 0.0003192128214410723140 ),
 .UNSPECIFIED. ) ;
#50970=FACE_OUTER_BOUND ( 'NONE', #223894, .T. ) ;
#51002=CARTESIAN_POINT ( 'NONE',  ( 20.94999999999999929, 64.25000000001175238, -76.30697314750247529 ) ) ;
#51028=ORIENTED_EDGE ( 'NONE', *, *, #143010, .F. ) ;
#51033=ORIENTED_EDGE ( 'NONE', *, *, #104010, .T. ) ;
#51037=CIRCLE ( 'NONE', #38600, 0.5000000000000004441 ) ;
#51050=ORIENTED_EDGE ( 'NONE', *, *, #83079, .F. ) ;
#51053=DIRECTION ( 'NONE',  ( 0.000000000000000000, 6.982962677686266711E-15, -1.000000000000000000 ) ) ;
#51066=AXIS2_PLACEMENT_3D ( 'NONE', #100212, #58528, #179796 ) ;
#51082=EDGE_LOOP ( 'NONE', ( #23983, #177765, #246948 ) ) ;
#51085=AXIS2_PLACEMENT_3D ( 'NONE', #96278, #135410, #76723 ) ;
#51089=ORIENTED_EDGE ( 'NONE', *, *, #11670, .F. ) ;
#51095=EDGE_CURVE ( 'NONE', #7674, #17853, #54315, .T. ) ;
#51108=FACE_OUTER_BOUND ( 'NONE', #220192, .T. ) ;
#51163=FACE_OUTER_BOUND ( 'NONE', #98575, .T. ) ;
#51164=DIRECTION ( 'NONE',  ( 0.000000000000000000, -0.008583690987135041833, 0.9999631594459055250 ) ) ;
#51166=CARTESIAN_POINT ( 'NONE',  ( 18.49713797159848383, 85.44648232759099926, -95.95164936291408253 ) ) ;
#51174=CARTESIAN_POINT ( 'NONE',  ( 21.05000000000000071, 77.16270174994990327, -95.12310748452431142 ) ) ;
#51175=CARTESIAN_POINT ( 'NONE',  ( 20.94999999999999929, 77.34915357198771346, -61.73561014893441978 ) ) ;
#51177=DIRECTION ( 'NONE',  ( 1.000000000000000000, -1.836970198721029934E-16, -1.282749433769087582E-30 ) ) ;
#51179=FACE_OUTER_BOUND ( 'NONE', #64857, .T. ) ;
#51185=CARTESIAN_POINT ( 'NONE',  ( 20.52683494730046476, 67.01946918171053369, -94.51785476198718072 ) ) ;
#51208=VERTEX_POINT ( 'NONE', #162637 ) ;
#51224=ORIENTED_EDGE ( 'NONE', *, *, #212538, .F. ) ;
#51229=AXIS2_PLACEMENT_3D ( 'NONE', #35007, #234432, #74124 ) ;
#51265=DIRECTION ( 'NONE',  ( -0.000000000000000000, -6.982962677686266711E-15, 1.000000000000000000 ) ) ;
#51275=AXIS2_PLACEMENT_3D ( 'NONE', #156999, #14918, #33219 ) ;
#51312=EDGE_CURVE ( 'NONE', #75286, #111418, #71108, .T. ) ;
#51341=DIRECTION ( 'NONE',  ( -1.000000000000000000, -0.000000000000000000, -0.000000000000000000 ) ) ;
#51346=ADVANCED_FACE ( 'NONE', ( #100052 ), #2247, .T. ) ;
#51365=ORIENTED_EDGE ( 'NONE', *, *, #229567, .F. ) ;
#51369=CARTESIAN_POINT ( 'NONE',  ( 20.89192007715127986, 65.67101464000481315, -63.94043916224794089 ) ) ;
#51387=AXIS2_PLACEMENT_3D ( 'NONE', #103373, #180375, #4281 ) ;
#51393=EDGE_LOOP ( 'NONE', ( #147326, #169971, #177538, #147509 ) ) ;
#51409=DIRECTION ( 'NONE',  ( -1.000000000000000000, -0.000000000000000000, -0.000000000000000000 ) ) ;
#51452=CIRCLE ( 'NONE', #39048, 0.1000000000000028644 ) ;
#51457=ORIENTED_EDGE ( 'NONE', *, *, #213636, .T. ) ;
#51465=DIRECTION ( 'NONE',  ( 0.000000000000000000, 0.000000000000000000, 1.000000000000000000 ) ) ;
#51467=CYLINDRICAL_SURFACE ( 'NONE', #98024, 0.1000000000000028644 ) ;
#51469=DIRECTION ( 'NONE',  ( 0.000000000000000000, 7.086529944415894657E-15, -1.000000000000000000 ) ) ;
#51482=AXIS2_PLACEMENT_3D ( 'NONE', #12301, #69702, #128378 ) ;
#51491=DIRECTION ( 'NONE',  ( 0.000000000000000000, 6.982962677686266711E-15, -1.000000000000000000 ) ) ;
#51499=EDGE_LOOP ( 'NONE', ( #174658, #12258, #159551, #91355 ) ) ;
#51501=DIRECTION ( 'NONE',  ( 0.000000000000000000, 0.000000000000000000, -1.000000000000000000 ) ) ;
#51534=AXIS2_PLACEMENT_3D ( 'NONE', #69681, #189620, #249594 ) ;
#51602=EDGE_CURVE ( 'NONE', #3343, #209120, #154686, .T. ) ;
#51609=ADVANCED_FACE ( 'NONE', ( #58058 ), #256206, .F. ) ;
#51672=VERTEX_POINT ( 'NONE', #3224 ) ;
#51706=CYLINDRICAL_SURFACE ( 'NONE', #181533, 0.09999999999999939493 ) ;
#51707=VERTEX_POINT ( 'NONE', #63199 ) ;
#51740=CARTESIAN_POINT ( 'NONE',  ( 20.12500000000000355, 66.74195072709457577, -94.65976864738193797 ) ) ;
#51752=CIRCLE ( 'NONE', #234955, 0.1000000000000028644 ) ;
#51753=CARTESIAN_POINT ( 'NONE',  ( -21.14999999999999858, 69.45934304831071415, -102.9231074845243512 ) ) ;
#51765=ORIENTED_EDGE ( 'NONE', *, *, #109033, .T. ) ;
#51786=ORIENTED_EDGE ( 'NONE', *, *, #11175, .T. ) ;
#51789=CIRCLE ( 'NONE', #18503, 0.1000000000000028644 ) ;
#51809=SPHERICAL_SURFACE ( 'NONE', #128316, 0.1000000000000000056 ) ;
#51834=ORIENTED_EDGE ( 'NONE', *, *, #186549, .F. ) ;
#51859=CARTESIAN_POINT ( 'NONE',  ( 22.39999999999999503, 64.35000000001194564, -103.0231074845244024 ) ) ;
#51868=VERTEX_POINT ( 'NONE', #110049 ) ;
#51895=VERTEX_POINT ( 'NONE', #112629 ) ;
#51977=DIRECTION ( 'NONE',  ( 0.000000000000000000, -7.487053152578127080E-15, 1.000000000000000000 ) ) ;
#51991=EDGE_CURVE ( 'NONE', #252315, #243292, #125452, .T. ) ;
#52002=FACE_OUTER_BOUND ( 'NONE', #109331, .T. ) ;
#52025=EDGE_CURVE ( 'NONE', #111063, #192857, #167973, .T. ) ;
#52049=ORIENTED_EDGE ( 'NONE', *, *, #250360, .T. ) ;
#52070=CARTESIAN_POINT ( 'NONE',  ( -22.39999999999999858, 64.35000000001195986, -103.1231074845243825 ) ) ;
#52078=ADVANCED_FACE ( 'NONE', ( #103312 ), #86305, .T. ) ;
#52097=DIRECTION ( 'NONE',  ( 0.000000000000000000, 0.000000000000000000, 1.000000000000000000 ) ) ;
#52131=FACE_OUTER_BOUND ( 'NONE', #195793, .T. ) ;
#52158=AXIS2_PLACEMENT_3D ( 'NONE', #112686, #187104, #68422 ) ;
#52161=EDGE_LOOP ( 'NONE', ( #154093, #86383, #251853, #221151 ) ) ;
#52242=CARTESIAN_POINT ( 'NONE',  ( -21.04999999999999716, 69.55922910635004541, -103.0055102975163521 ) ) ;
#52249=AXIS2_PLACEMENT_3D ( 'NONE', #187181, #43804, #184584 ) ;
#52270=ORIENTED_EDGE ( 'NONE', *, *, #106532, .T. ) ;
#52278=CARTESIAN_POINT ( 'NONE',  ( 18.58143601961842961, 65.56427058491711080, -78.27310748452438816 ) ) ;
#52281=ORIENTED_EDGE ( 'NONE', *, *, #184061, .T. ) ;
#52290=CIRCLE ( 'NONE', #189683, 0.09999999999999939493 ) ;
#52338=EDGE_CURVE ( 'NONE', #214176, #74197, #233945, .T. ) ;
#52354=ORIENTED_EDGE ( 'NONE', *, *, #239136, .T. ) ;
#52372=ADVANCED_FACE ( 'NONE', ( #62283 ), #179679, .T. ) ;
#52392=ADVANCED_FACE ( 'NONE', ( #239645 ), #40185, .T. ) ;
#52413=VECTOR ( 'NONE', #114375, 1000.000000000000000 ) ;
#52453=AXIS2_PLACEMENT_3D ( 'NONE', #218198, #237789, #17451 ) ;
#52457=FACE_OUTER_BOUND ( 'NONE', #241279, .T. ) ;
#52484=CARTESIAN_POINT ( 'NONE',  ( 20.41140022480505323, 65.58956915761027062, -95.40810618088978856 ) ) ;
#52513=CARTESIAN_POINT ( 'NONE',  ( -22.50000000000000000, 64.25000000001195133, -103.0231074845244024 ) ) ;
#52519=DIRECTION ( 'NONE',  ( -1.000000000000000000, 0.000000000000000000, 0.000000000000000000 ) ) ;
#52534=DIRECTION ( 'NONE',  ( 1.000000000000000000, -3.265361837132813093E-16, -2.280189983783949500E-30 ) ) ;
#52583=DIRECTION ( 'NONE',  ( -1.000000000000000000, 0.000000000000000000, -0.000000000000000000 ) ) ;
#52589=ORIENTED_EDGE ( 'NONE', *, *, #120913, .T. ) ;
#52606=LINE ( 'NONE', #193429, #77741 ) ;
#52630=ORIENTED_EDGE ( 'NONE', *, *, #104510, .F. ) ;
#52646=CYLINDRICAL_SURFACE ( 'NONE', #140364, 0.1000000000000028644 ) ;
#52651=ADVANCED_FACE ( 'NONE', ( #124396 ), #119261, .F. ) ;
#52678=CARTESIAN_POINT ( 'NONE',  ( 20.94999999999999929, 65.70729864260985664, -64.06574559737245522 ) ) ;
#52734=CIRCLE ( 'NONE', #181929, 11.90000000000000746 ) ;
#52739=DIRECTION ( 'NONE',  ( 1.836970198721029934E-16, 1.000000000000000000, 6.982962677686266711E-15 ) ) ;
#52740=AXIS2_PLACEMENT_3D ( 'NONE', #190741, #211563, #29113 ) ;
#52753=CARTESIAN_POINT ( 'NONE',  ( 20.94999999999999929, 85.00000000001179501, -79.01707660717669057 ) ) ;
#52835=EDGE_LOOP ( 'NONE', ( #138447, #255144, #177648, #205050 ) ) ;
#52866=CYLINDRICAL_SURFACE ( 'NONE', #155119, 0.5000000000000004441 ) ;
#52883=EDGE_CURVE ( 'NONE', #171051, #156829, #173502, .T. ) ;
#52887=TOROIDAL_SURFACE ( 'NONE', #48799, 11.90000000000000213, 0.1000000000000000056 ) ;
#52900=CARTESIAN_POINT ( 'NONE',  ( 18.44206774312970154, 85.49102735755175786, -62.89687997982598944 ) ) ;
#52903=LINE ( 'NONE', #191163, #8205 ) ;
#52928=ORIENTED_EDGE ( 'NONE', *, *, #163355, .T. ) ;
#52931=CARTESIAN_POINT ( 'NONE',  ( 21.05000000000000071, 76.00000000001170974, -69.52310748452431710 ) ) ;
#52954=CYLINDRICAL_SURFACE ( 'NONE', #213262, 0.09999999999999939493 ) ;
#52971=DIRECTION ( 'NONE',  ( 0.000000000000000000, 0.000000000000000000, -1.000000000000000000 ) ) ;
#52983=AXIS2_PLACEMENT_3D ( 'NONE', #106071, #207801, #233768 ) ;
#52993=CIRCLE ( 'NONE', #198742, 0.09999999999999939493 ) ;
#53047=EDGE_CURVE ( 'NONE', #246470, #120433, #210570, .T. ) ;
#53093=VERTEX_POINT ( 'NONE', #54053 ) ;
#53101=AXIS2_PLACEMENT_3D ( 'NONE', #42188, #218216, #95715 ) ;
#53102=LINE ( 'NONE', #174393, #88643 ) ;
#53132=CARTESIAN_POINT ( 'NONE',  ( -18.59999999999999787, 77.13501884592184865, -61.80613060109197932 ) ) ;
#53136=EDGE_CURVE ( 'NONE', #49802, #72649, #29790, .T. ) ;
#53143=CARTESIAN_POINT ( 'NONE',  ( 20.94999999999999574, 87.48912529308798014, -100.0231074845242318 ) ) ;
#53149=EDGE_CURVE ( 'NONE', #56583, #41677, #55303, .T. ) ;
#53186=CIRCLE ( 'NONE', #61374, 0.8750000000000007772 ) ;
#53220=DIRECTION ( 'NONE',  ( -0.000000000000000000, -0.8660254037844468122, -0.4999999999999860112 ) ) ;
#53223=VECTOR ( 'NONE', #253048, 1000.000000000000000 ) ;
#53228=DIRECTION ( 'NONE',  ( -1.000000000000000000, 0.000000000000000000, 0.000000000000000000 ) ) ;
#53235=CARTESIAN_POINT ( 'NONE',  ( -23.15000000000000213, 85.50000000001188027, -93.12913836187179584 ) ) ;
#53238=DIRECTION ( 'NONE',  ( -1.000000000000000000, 0.000000000000000000, -0.000000000000000000 ) ) ;
#53253=AXIS2_PLACEMENT_3D ( 'NONE', #59091, #198639, #201208 ) ;
#53272=CARTESIAN_POINT ( 'NONE',  ( 23.24999999999999645, 76.00000000001170974, -69.52310748452431710 ) ) ;
#53278=EDGE_LOOP ( 'NONE', ( #204668, #214963, #252794, #15461 ) ) ;
#53306=TOROIDAL_SURFACE ( 'NONE', #232395, 0.2000000000000000111, 0.1000000000000000056 ) ;
#53309=AXIS2_PLACEMENT_3D ( 'NONE', #252123, #153078, #93052 ) ;
#53314=DIRECTION ( 'NONE',  ( 0.000000000000000000, -7.429790795770644761E-15, 1.000000000000000000 ) ) ;
#53321=DIRECTION ( 'NONE',  ( 1.000000000000000000, -3.265361837132813093E-16, -2.280189983783949500E-30 ) ) ;
#53382=EDGE_LOOP ( 'NONE', ( #121803, #46980, #228766, #211546 ) ) ;
#53400=B_SPLINE_CURVE_WITH_KNOTS ( 'NONE', 3,
 ( #108804, #9705, #113944, #13581, #129662, #51369, #173981, #30587, #110093, #228777, #132234, #252163, #210493, #31875, #130949, #172695, #89241, #73574, #52678 ),
 .UNSPECIFIED., .F., .F.,
 ( 4, 3, 3, 3, 3, 3, 4 ),
 ( 1.387778780781445676E-17, 2.646747978909012316E-05, 5.271166642128706850E-05, 9.008788829884963154E-05, 0.0001426648776560992193, 0.0001897378458659761016, 0.0001917382627806360094 ),
 .UNSPECIFIED. ) ;
#53418=ORIENTED_EDGE ( 'NONE', *, *, #192188, .T. ) ;
#53419=DIRECTION ( 'NONE',  ( 1.000000000000000000, -1.836970198721029934E-16, -1.282749433769087582E-30 ) ) ;
#53426=ADVANCED_FACE ( 'NONE', ( #80006 ), #13194, .F. ) ;
#53490=CARTESIAN_POINT ( 'NONE',  ( -22.49544290803753199, 64.25012976215464278, -103.0884194437819730 ) ) ;
#53513=CARTESIAN_POINT ( 'NONE',  ( -18.42609945526404402, 85.49999971050237946, -96.02374499427590138 ) ) ;
#53518=EDGE_CURVE ( 'NONE', #142842, #152113, #125771, .T. ) ;
#53543=DIRECTION ( 'NONE',  ( 1.000000000000000000, -0.000000000000000000, 0.000000000000000000 ) ) ;
#53558=VERTEX_POINT ( 'NONE', #40338 ) ;
#53569=EDGE_CURVE ( 'NONE', #208155, #18900, #167503, .T. ) ;
#53612=DIRECTION ( 'NONE',  ( -3.265361837132813093E-16, -1.000000000000000000, 7.445645354460596589E-46 ) ) ;
#53615=CARTESIAN_POINT ( 'NONE',  ( 21.56666275994539461, 76.00000000001200817, -109.9804758914176404 ) ) ;
#53675=ORIENTED_EDGE ( 'NONE', *, *, #16429, .F. ) ;
#53676=EDGE_CURVE ( 'NONE', #135352, #199332, #13367, .T. ) ;
#53719=ORIENTED_EDGE ( 'NONE', *, *, #220058, .T. ) ;
#53765=DIRECTION ( 'NONE',  ( 1.836970198721029934E-16, 1.000000000000000000, 6.982962677686266711E-15 ) ) ;
#53794=CARTESIAN_POINT ( 'NONE',  ( 21.04999999999907700, 75.94851711812999895, -109.3232873024352045 ) ) ;
#53829=VECTOR ( 'NONE', #226666, 1000.000000000000000 ) ;
#53889=CARTESIAN_POINT ( 'NONE',  ( 21.10710606213542206, 67.22310597611866001, -90.78211095812494591 ) ) ;
#53918=CIRCLE ( 'NONE', #149227, 11.64999999999999325 ) ;
#53923=CARTESIAN_POINT ( 'NONE',  ( 23.14999999999999858, 71.22429906543236200, -81.37187558857031888 ) ) ;
#53932=FACE_OUTER_BOUND ( 'NONE', #227693, .T. ) ;
#53934=DIRECTION ( 'NONE',  ( -1.000000000000000000, -0.000000000000000000, -0.000000000000000000 ) ) ;
#53961=CIRCLE ( 'NONE', #141270, 7.720710678118663850 ) ;
#53965=CARTESIAN_POINT ( 'NONE',  ( -21.14999999999999858, 64.35000000001195986, -102.9231074845243938 ) ) ;
#53997=VERTEX_POINT ( 'NONE', #99925 ) ;
#54027=DIRECTION ( 'NONE',  ( 1.000000000000000000, -1.875376730785737719E-16, -1.309568571767809260E-30 ) ) ;
#54042=CARTESIAN_POINT ( 'NONE',  ( 20.94999999999999929, 69.35000000001180354, -81.77310748452435973 ) ) ;
#54049=CARTESIAN_POINT ( 'NONE',  ( 21.00000000000000000, 66.25000000001179501, -81.87310748452438247 ) ) ;
#54053=CARTESIAN_POINT ( 'NONE',  ( -21.44999999999999929, 68.85000000001180354, -81.77310748452435973 ) ) ;
#54069=DIRECTION ( 'NONE',  ( 1.000000000000000000, 0.000000000000000000, 0.000000000000000000 ) ) ;
#54085=ORIENTED_EDGE ( 'NONE', *, *, #140784, .T. ) ;
#54092=ORIENTED_EDGE ( 'NONE', *, *, #223839, .T. ) ;
#54102=ORIENTED_EDGE ( 'NONE', *, *, #169593, .T. ) ;
#54121=ORIENTED_EDGE ( 'NONE', *, *, #3930, .F. ) ;
#54127=AXIS2_PLACEMENT_3D ( 'NONE', #68973, #188901, #229321 ) ;
#54174=CARTESIAN_POINT ( 'NONE',  ( 23.25000000000000000, 87.65000000001172964, -72.62310748452422615 ) ) ;
#54178=EDGE_LOOP ( 'NONE', ( #181119, #241060, #136086, #96596 ) ) ;
#54182=CARTESIAN_POINT ( 'NONE',  ( 18.40916198585730257, 85.50000000001166711, -62.92291785270108306 ) ) ;
#54226=AXIS2_PLACEMENT_3D ( 'NONE', #195193, #92201, #176909 ) ;
#54252=AXIS2_PLACEMENT_3D ( 'NONE', #10881, #250759, #207819 ) ;
#54267=DIRECTION ( 'NONE',  ( 0.000000000000000000, -1.000000000000000000, -6.982962677686265922E-15 ) ) ;
#54269=FACE_OUTER_BOUND ( 'NONE', #96438, .T. ) ;
#54305=CARTESIAN_POINT ( 'NONE',  ( 20.95289811251229750, 67.10683199555329281, -94.52129799060584503 ) ) ;
#54310=ORIENTED_EDGE ( 'NONE', *, *, #229229, .T. ) ;
#54315=CIRCLE ( 'NONE', #245880, 7.800000000000001599 ) ;
#54342=ORIENTED_EDGE ( 'NONE', *, *, #65620, .T. ) ;
#54350=ADVANCED_FACE ( 'NONE', ( #237875 ), #130235, .F. ) ;
#54384=AXIS2_PLACEMENT_3D ( 'NONE', #45004, #125814, #28042 ) ;
#54407=VECTOR ( 'NONE', #69455, 1000.000000000000000 ) ;
#54424=CARTESIAN_POINT ( 'NONE',  ( 21.07928932188134397, 75.90110485435759813, -109.3516241409176217 ) ) ;
#54442=AXIS2_PLACEMENT_3D ( 'NONE', #42896, #78148, #18194 ) ;
#54449=ADVANCED_FACE ( 'NONE', ( #180477 ), #123075, .F. ) ;
#54455=CARTESIAN_POINT ( 'NONE',  ( -21.05000000000000071, 77.83534155023627932, -91.46795619196130644 ) ) ;
#54475=VERTEX_POINT ( 'NONE', #183053 ) ;
#54480=DIRECTION ( 'NONE',  ( 0.000000000000000000, -0.9908441862701605762, -0.1350103645451835310 ) ) ;
#54489=DIRECTION ( 'NONE',  ( 1.000000000000000000, 0.000000000000000000, 0.000000000000000000 ) ) ;
#54492=ADVANCED_FACE ( 'NONE', ( #124356 ), #238576, .T. ) ;
#54517=EDGE_CURVE ( 'NONE', #103813, #71577, #122056, .T. ) ;
#54546=CARTESIAN_POINT ( 'NONE',  ( -21.44999999999999929, 68.85000000001180354, -81.87310748452436826 ) ) ;
#54550=ORIENTED_EDGE ( 'NONE', *, *, #50896, .F. ) ;
#54570=LINE ( 'NONE', #175829, #9686 ) ;
#54616=VECTOR ( 'NONE', #159753, 1000.000000000000000 ) ;
#54620=EDGE_CURVE ( 'NONE', #175899, #92498, #201344, .T. ) ;
#54626=DIRECTION ( 'NONE',  ( -1.000000000000000000, 0.000000000000000000, -0.000000000000000000 ) ) ;
#54639=FACE_OUTER_BOUND ( 'NONE', #91628, .T. ) ;
#54705=FACE_OUTER_BOUND ( 'NONE', #190061, .T. ) ;
#54746=DIRECTION ( 'NONE',  ( 0.000000000000000000, 0.000000000000000000, 1.000000000000000000 ) ) ;
#54768=CARTESIAN_POINT ( 'NONE',  ( 18.58719872626880587, 85.56664439761028973, -62.70062928812723868 ) ) ;
#54782=CARTESIAN_POINT ( 'NONE',  ( -18.49346865148321584, 85.44307379853681539, -95.83791122920942485 ) ) ;
#54797=ADVANCED_FACE ( 'NONE', ( #202300 ), #79751, .F. ) ;
#54800=DIRECTION ( 'NONE',  ( 0.000000000000000000, 0.000000000000000000, 1.000000000000000000 ) ) ;
#54847=CARTESIAN_POINT ( 'NONE',  ( 18.59999999999999432, 65.50857864377445594, -78.27310748452438816 ) ) ;
#54859=ORIENTED_EDGE ( 'NONE', *, *, #86724, .F. ) ;
#54873=EDGE_CURVE ( 'NONE', #222093, #24156, #61510, .T. ) ;
#54929=ORIENTED_EDGE ( 'NONE', *, *, #218440, .T. ) ;
#54949=ADVANCED_FACE ( 'NONE', ( #229575 ), #204845, .F. ) ;
#54954=EDGE_CURVE ( 'NONE', #164178, #65545, #122243, .T. ) ;
#54956=ORIENTED_EDGE ( 'NONE', *, *, #251155, .T. ) ;
#54962=EDGE_LOOP ( 'NONE', ( #144449, #221618, #168730, #153549 ) ) ;
#54965=ORIENTED_EDGE ( 'NONE', *, *, #82467, .T. ) ;
#54969=VECTOR ( 'NONE', #1857, 1000.000000000000000 ) ;
#54978=DIRECTION ( 'NONE',  ( -0.000000000000000000, -1.000000000000000000, -7.272083257015735086E-15 ) ) ;
#55046=AXIS2_PLACEMENT_3D ( 'NONE', #85216, #203914, #104781 ) ;
#55053=ORIENTED_EDGE ( 'NONE', *, *, #35593, .F. ) ;
#55073=DIRECTION ( 'NONE',  ( 0.000000000000000000, 0.000000000000000000, 1.000000000000000000 ) ) ;
#55088=CARTESIAN_POINT ( 'NONE',  ( 20.95512840106821528, 65.37615130623854043, -90.82062826372546738 ) ) ;
#55091=CIRCLE ( 'NONE', #121782, 2.100000000000004530 ) ;
#55103=DIRECTION ( 'NONE',  ( -1.000000000000000000, -0.000000000000000000, -0.000000000000000000 ) ) ;
#55138=AXIS2_PLACEMENT_3D ( 'NONE', #233541, #230982, #134398 ) ;
#55163=AXIS2_PLACEMENT_3D ( 'NONE', #94313, #212987, #13516 ) ;
#55189=DIRECTION ( 'NONE',  ( 1.000000000000000000, 0.000000000000000000, 0.000000000000000000 ) ) ;
#55197=CARTESIAN_POINT ( 'NONE',  ( -21.05000000000000071, 74.83729825007388570, -94.92310748452432279 ) ) ;
#55203=CARTESIAN_POINT ( 'NONE',  ( -20.94999999999999929, 77.16270174994990327, -95.12310748452431142 ) ) ;
#55229=ORIENTED_EDGE ( 'NONE', *, *, #129604, .T. ) ;
#55246=VERTEX_POINT ( 'NONE', #104158 ) ;
#55253=AXIS2_PLACEMENT_3D ( 'NONE', #232200, #53543, #148801 ) ;
#55261=EDGE_CURVE ( 'NONE', #221652, #41677, #176434, .T. ) ;
#55297=ORIENTED_EDGE ( 'NONE', *, *, #216567, .T. ) ;
#55299=CIRCLE ( 'NONE', #121976, 0.1000000000000028644 ) ;
#55303=LINE ( 'NONE', #158332, #42221 ) ;
#55313=LINE ( 'NONE', #134858, #212588 ) ;
#55324=DIRECTION ( 'NONE',  ( -0.000000000000000000, 6.982962677686266711E-15, -1.000000000000000000 ) ) ;
#55333=CARTESIAN_POINT ( 'NONE',  ( 23.25000000000000000, 87.75000000001202238, -114.7731074845242318 ) ) ;
#55386=VECTOR ( 'NONE', #127086, 1000.000000000000114 ) ;
#55387=CARTESIAN_POINT ( 'NONE',  ( 23.14999999999999858, 71.00000000001186606, -90.61784146561124942 ) ) ;
#55391=DIRECTION ( 'NONE',  ( 1.000000000000000000, 0.000000000000000000, 0.000000000000000000 ) ) ;
#55403=CARTESIAN_POINT ( 'NONE',  ( 20.85000000000000142, 64.25000000001170974, -69.52310748452438816 ) ) ;
#55416=FACE_OUTER_BOUND ( 'NONE', #152086, .T. ) ;
#55425=ADVANCED_FACE ( 'NONE', ( #204553 ), #93370, .T. ) ;
#55431=AXIS2_PLACEMENT_3D ( 'NONE', #224812, #61903, #46179 ) ;
#55443=LINE ( 'NONE', #217096, #133102 ) ;
#55470=CARTESIAN_POINT ( 'NONE',  ( 21.05000000000000071, 76.00000000001186606, -90.87310748452429721 ) ) ;
#55474=AXIS2_PLACEMENT_3D ( 'NONE', #244880, #144478, #50510 ) ;
#55503=ORIENTED_EDGE ( 'NONE', *, *, #218976, .F. ) ;
#55514=VERTEX_POINT ( 'NONE', #256125 ) ;
#55516=DIRECTION ( 'NONE',  ( 1.000000000000000000, 0.000000000000000000, 0.000000000000000000 ) ) ;
#55557=VECTOR ( 'NONE', #64065, 1000.000000000000000 ) ;
#55574=EDGE_CURVE ( 'NONE', #237061, #88867, #235042, .T. ) ;
#55577=CARTESIAN_POINT ( 'NONE',  ( -20.64999999999999858, 84.73084112150721126, -93.42503276553991043 ) ) ;
#55590=AXIS2_PLACEMENT_3D ( 'NONE', #200266, #85407, #103696 ) ;
#55628=CARTESIAN_POINT ( 'NONE',  ( -21.14999999999999858, 64.25000000001190870, -96.23924182154622997 ) ) ;
#55629=AXIS2_PLACEMENT_3D ( 'NONE', #160785, #179066, #79893 ) ;
#55637=CARTESIAN_POINT ( 'NONE',  ( 23.14999999999999858, 76.00000000001173817, -73.52310748452431710 ) ) ;
#55638=DIRECTION ( 'NONE',  ( 0.000000000000000000, 0.9908441862701605762, -0.1350103645451835310 ) ) ;
#55662=DIRECTION ( 'NONE',  ( 0.000000000000000000, 6.982962677686266711E-15, -1.000000000000000000 ) ) ;
#55689=CIRCLE ( 'NONE', #180629, 0.1000000000000028644 ) ;
#55747=DIRECTION ( 'NONE',  ( 0.000000000000000000, -6.982962677686266711E-15, 1.000000000000000000 ) ) ;
#55749=DIRECTION ( 'NONE',  ( -1.000000000000000000, 0.000000000000000000, 0.000000000000000000 ) ) ;
#55763=DIRECTION ( 'NONE',  ( -0.000000000000000000, -6.982962677686266711E-15, 1.000000000000000000 ) ) ;
#55780=ADVANCED_FACE ( 'NONE', ( #112547 ), #210363, .T. ) ;
#55786=CARTESIAN_POINT ( 'NONE',  ( -21.14999999999999858, 76.00000000001199396, -109.2816861282870065 ) ) ;
#55813=CARTESIAN_POINT ( 'NONE',  ( -20.15000000000000568, 66.70857864377450142, -81.87310748452438247 ) ) ;
#55911=CARTESIAN_POINT ( 'NONE',  ( 21.00000000000000000, 66.25000000001186606, -90.67310748452437963 ) ) ;
#55926=DIRECTION ( 'NONE',  ( 1.000000000000000000, 0.000000000000000000, 0.000000000000000000 ) ) ;
#55930=ORIENTED_EDGE ( 'NONE', *, *, #50601, .T. ) ;
#55932=FACE_OUTER_BOUND ( 'NONE', #91239, .T. ) ;
#55937=EDGE_LOOP ( 'NONE', ( #134462, #183548, #48923, #168804 ) ) ;
#55958=VECTOR ( 'NONE', #181536, 1000.000000000000000 ) ;
#55963=ORIENTED_EDGE ( 'NONE', *, *, #27548, .F. ) ;
#55988=DIRECTION ( 'NONE',  ( 0.000000000000000000, -1.000000000000000000, 0.000000000000000000 ) ) ;
#56009=DIRECTION ( 'NONE',  ( -1.000000000000000000, 0.000000000000000000, -0.000000000000000000 ) ) ;
#56033=CARTESIAN_POINT ( 'NONE',  ( 18.60000000000000497, 85.52394631232935751, -62.64107948918602631 ) ) ;
#56041=CARTESIAN_POINT ( 'NONE',  ( -20.12071067811865888, 66.67928932189320790, -90.67310748452437963 ) ) ;
#56057=CIRCLE ( 'NONE', #164246, 12.87499999999999822 ) ;
#56063=ORIENTED_EDGE ( 'NONE', *, *, #174825, .T. ) ;
#56089=AXIS2_PLACEMENT_3D ( 'NONE', #54546, #254021, #257828 ) ;
#56102=EDGE_LOOP ( 'NONE', ( #102742, #22442, #178948, #33012 ) ) ;
#56130=DIRECTION ( 'NONE',  ( -0.000000000000000000, 1.000000000000000000, 6.982962677686267499E-15 ) ) ;
#56131=DIRECTION ( 'NONE',  ( -1.000000000000000000, 0.000000000000000000, 0.000000000000000000 ) ) ;
#56145=CIRCLE ( 'NONE', #230977, 0.1000000000000052097 ) ;
#56155=EDGE_CURVE ( 'NONE', #20030, #158859, #139530, .T. ) ;
#56156=EDGE_CURVE ( 'NONE', #161481, #121706, #47940, .T. ) ;
#56179=EDGE_CURVE ( 'NONE', #67031, #199047, #197794, .T. ) ;
#56209=DIRECTION ( 'NONE',  ( -1.000000000000000000, -0.000000000000000000, -0.000000000000000000 ) ) ;
#56229=PLANE ( 'NONE',  #117570 ) ;
#56237=CARTESIAN_POINT ( 'NONE',  ( 18.60000000000001563, 85.36423601037868991, -95.84285308379965329 ) ) ;
#56271=ORIENTED_EDGE ( 'NONE', *, *, #96790, .T. ) ;
#56275=ORIENTED_EDGE ( 'NONE', *, *, #89119, .F. ) ;
#56277=DIRECTION ( 'NONE',  ( 0.000000000000000000, 6.982962677686266711E-15, -1.000000000000000000 ) ) ;
#56279=CARTESIAN_POINT ( 'NONE',  ( 20.94999999999999929, 76.00000000001170974, -69.52310748452431710 ) ) ;
#56288=DIRECTION ( 'NONE',  ( 0.000000000000000000, -7.086529944415894657E-15, 1.000000000000000000 ) ) ;
#56290=VERTEX_POINT ( 'NONE', #251270 ) ;
#56298=DIRECTION ( 'NONE',  ( 0.000000000000000000, 0.000000000000000000, 1.000000000000000000 ) ) ;
#56299=CARTESIAN_POINT ( 'NONE',  ( -20.54999999999999716, 84.73084112150711178, -79.12118220350858167 ) ) ;
#56309=ORIENTED_EDGE ( 'NONE', *, *, #149713, .T. ) ;
#56310=DIRECTION ( 'NONE',  ( 1.000000000000000000, -0.000000000000000000, 0.000000000000000000 ) ) ;
#56328=DIRECTION ( 'NONE',  ( 1.000000000000000000, 0.000000000000000000, 0.000000000000000000 ) ) ;
#56335=ORIENTED_EDGE ( 'NONE', *, *, #229567, .T. ) ;
#56342=DIRECTION ( 'NONE',  ( 1.000000000000000000, 0.000000000000000000, 0.000000000000000000 ) ) ;
#56364=DIRECTION ( 'NONE',  ( 0.000000000000000000, -6.982962677686266711E-15, 1.000000000000000000 ) ) ;
#56380=PLANE ( 'NONE',  #186711 ) ;
#56385=CARTESIAN_POINT ( 'NONE',  ( -23.15000000000000213, 87.48912529308779540, -72.62310748452422615 ) ) ;
#56401=CARTESIAN_POINT ( 'NONE',  ( -21.05000000000000071, 77.36087058720393372, -94.95010955743333625 ) ) ;
#56424=AXIS2_PLACEMENT_3D ( 'NONE', #237484, #58810, #96646 ) ;
#56442=CARTESIAN_POINT ( 'NONE',  ( -23.15000000000000213, 64.25000000001195133, -103.0231074845244024 ) ) ;
#56479=CARTESIAN_POINT ( 'NONE',  ( 21.07946286933444568, 75.92331615675561807, -109.3521448035320560 ) ) ;
#56493=DIRECTION ( 'NONE',  ( 0.000000000000000000, 0.000000000000000000, 1.000000000000000000 ) ) ;
#56496=ORIENTED_EDGE ( 'NONE', *, *, #211998, .F. ) ;
#56500=AXIS2_PLACEMENT_3D ( 'NONE', #204517, #49301, #168011 ) ;
#56502=VERTEX_POINT ( 'NONE', #218174 ) ;
#56514=FACE_OUTER_BOUND ( 'NONE', #106979, .T. ) ;
#56515=ORIENTED_EDGE ( 'NONE', *, *, #190425, .T. ) ;
#56526=CARTESIAN_POINT ( 'NONE',  ( -18.59999999999999787, 76.00000000001170974, -69.52310748452431710 ) ) ;
#56531=DIRECTION ( 'NONE',  ( -1.000000000000000000, 0.000000000000000000, -0.000000000000000000 ) ) ;
#56537=AXIS2_PLACEMENT_3D ( 'NONE', #78691, #194837, #16197 ) ;
#56542=DIRECTION ( 'NONE',  ( 0.000000000000000000, -6.982962677686266711E-15, 1.000000000000000000 ) ) ;
#56577=CIRCLE ( 'NONE', #181539, 0.1000000000000011990 ) ;
#56583=VERTEX_POINT ( 'NONE', #59086 ) ;
#56584=LINE ( 'NONE', #136125, #216351 ) ;
#56616=EDGE_CURVE ( 'NONE', #130365, #209310, #181437, .T. ) ;
#56637=CYLINDRICAL_SURFACE ( 'NONE', #250677, 0.1000000000000028644 ) ;
#56641=CARTESIAN_POINT ( 'NONE',  ( 23.14999999999999858, 70.05000000001177796, -79.82880978955917328 ) ) ;
#56726=EDGE_LOOP ( 'NONE', ( #156111, #22171, #6513, #90564, #164317 ) ) ;
#56770=DIRECTION ( 'NONE',  ( -0.7070776581709311559, 4.937903618720164857E-15, -0.7071359030027479786 ) ) ;
#56809=ORIENTED_EDGE ( 'NONE', *, *, #152054, .F. ) ;
#56819=EDGE_LOOP ( 'NONE', ( #193390, #253903, #172400, #184265 ) ) ;
#56827=AXIS2_PLACEMENT_3D ( 'NONE', #105767, #185335, #124091 ) ;
#56833=DIRECTION ( 'NONE',  ( 1.000000000000000000, 0.000000000000000000, 0.000000000000000000 ) ) ;
#56888=ADVANCED_FACE ( 'NONE', ( #238417 ), #169158, .T. ) ;
#56889=VECTOR ( 'NONE', #157683, 1000.000000000000000 ) ;
#56958=AXIS2_PLACEMENT_3D ( 'NONE', #39349, #159287, #176288 ) ;
#56987=ORIENTED_EDGE ( 'NONE', *, *, #50623, .F. ) ;
#57020=AXIS2_PLACEMENT_3D ( 'NONE', #236006, #195631, #256800 ) ;
#57021=ORIENTED_EDGE ( 'NONE', *, *, #205198, .T. ) ;
#57029=CARTESIAN_POINT ( 'NONE',  ( 19.97071067811864609, 64.27928932189311695, -78.27310748452438816 ) ) ;
#57084=CARTESIAN_POINT ( 'NONE',  ( 21.05000000000001492, 69.45934304831069994, -103.0231074845243597 ) ) ;
#57105=VERTEX_POINT ( 'NONE', #187445 ) ;
#57111=CARTESIAN_POINT ( 'NONE',  ( -22.50000000000000000, 76.00000000001195133, -103.0231074845243171 ) ) ;
#57113=CIRCLE ( 'NONE', #20684, 0.09999999999999739653 ) ;
#57127=DIRECTION ( 'NONE',  ( 1.000000000000000000, 0.000000000000000000, 0.000000000000000000 ) ) ;
#57145=UNCERTAINTY_MEASURE_WITH_UNIT (LENGTH_MEASURE( 1.000000000000000082E-05 ), #185580, 'distance_accuracy_value', 'NONE');
#57165=EDGE_CURVE ( 'NONE', #130365, #171995, #189974, .T. ) ;
#57217=EDGE_CURVE ( 'NONE', #101654, #1640, #247454, .T. ) ;
#57273=ORIENTED_EDGE ( 'NONE', *, *, #6371, .F. ) ;
#57294=VECTOR ( 'NONE', #115405, 1000.000000000000000 ) ;
#57299=LINE ( 'NONE', #37783, #187266 ) ;
#57301=VECTOR ( 'NONE', #88821, 1000.000000000000000 ) ;
#57319=DIRECTION ( 'NONE',  ( 0.000000000000000000, 0.1350103645451974088, -0.9908441862701587999 ) ) ;
#57322=CIRCLE ( 'NONE', #11573, 2.000000000000001776 ) ;
#57340=CARTESIAN_POINT ( 'NONE',  ( -18.58693740092120805, 85.40643215026499036, -95.89829102802303851 ) ) ;
#57383=CARTESIAN_POINT ( 'NONE',  ( -21.05000000000000071, 64.37928932189323916, -96.15469083218333424 ) ) ;
#57468=EDGE_LOOP ( 'NONE', ( #190805, #42456, #161203, #105145 ) ) ;
#57472=ORIENTED_EDGE ( 'NONE', *, *, #200961, .T. ) ;
#57497=CYLINDRICAL_SURFACE ( 'NONE', #14317, 12.87499999999999822 ) ;
#57540=CARTESIAN_POINT ( 'NONE',  ( 23.15000000000000213, 87.65000000001172964, -72.62310748452422615 ) ) ;
#57555=DIRECTION ( 'NONE',  ( 0.000000000000000000, -1.000000000000000000, -7.272083257015735086E-15 ) ) ;
#57563=EDGE_CURVE ( 'NONE', #209310, #82517, #152599, .T. ) ;
#57573=EDGE_CURVE ( 'NONE', #97655, #10791, #145416, .T. ) ;
#57574=VERTEX_POINT ( 'NONE', #14922 ) ;
#57586=AXIS2_PLACEMENT_3D ( 'NONE', #68329, #155271, #76973 ) ;
#57617=CARTESIAN_POINT ( 'NONE',  ( -23.15000000000000213, 71.65000000001180069, -81.87310748452433984 ) ) ;
#57656=CARTESIAN_POINT ( 'NONE',  ( -18.50000000000000000, 77.68707439010360360, -115.8376804510659497 ) ) ;
#57665=DIRECTION ( 'NONE',  ( -1.000000000000000000, 3.265361837132813093E-16, 2.280189983783949500E-30 ) ) ;
#57670=CARTESIAN_POINT ( 'NONE',  ( 21.04116576186320486, 65.37533692126049800, -90.69452571589661716 ) ) ;
#57671=CARTESIAN_POINT ( 'NONE',  ( -21.05000000000000071, 74.63912941281984104, -94.95010955743335046 ) ) ;
#57696=ORIENTED_EDGE ( 'NONE', *, *, #69932, .F. ) ;
#57702=CIRCLE ( 'NONE', #203467, 0.09999999999999939493 ) ;
#57733=AXIS2_PLACEMENT_3D ( 'NONE', #125629, #22707, #223431 ) ;
#57755=EDGE_CURVE ( 'NONE', #200940, #182384, #136101, .T. ) ;
#57777=CARTESIAN_POINT ( 'NONE',  ( -18.36527282682033402, 85.50000060001060831, -62.60095852002528716 ) ) ;
#57805=ORIENTED_EDGE ( 'NONE', *, *, #175363, .T. ) ;
#57820=DIRECTION ( 'NONE',  ( -6.938893903907222067E-15, -1.000000000000000000, -6.982962677686266711E-15 ) ) ;
#57824=DIRECTION ( 'NONE',  ( 0.000000000000000000, 1.069579021796875354E-15, 1.000000000000000000 ) ) ;
#57825=DIRECTION ( 'NONE',  ( -0.000000000000000000, -6.982962677686266711E-15, 1.000000000000000000 ) ) ;
#57840=AXIS2_PLACEMENT_3D ( 'NONE', #70121, #113071, #252562 ) ;
#57849=AXIS2_PLACEMENT_3D ( 'NONE', #87274, #166869, #169440 ) ;
#57855=DIRECTION ( 'NONE',  ( 1.000000000000000000, -0.000000000000000000, 0.000000000000000000 ) ) ;
#57915=VERTEX_POINT ( 'NONE', #48584 ) ;
#57919=EDGE_CURVE ( 'NONE', #199102, #82775, #152204, .T. ) ;
#57921=CARTESIAN_POINT ( 'NONE',  ( 23.14999999999999503, 64.35000000001176090, -76.53791325517833855 ) ) ;
#57925=EDGE_CURVE ( 'NONE', #56502, #187906, #4311, .T. ) ;
#57927=TOROIDAL_SURFACE ( 'NONE', #170247, 0.6000000000000006439, 0.1000000000000000056 ) ;
#57948=ORIENTED_EDGE ( 'NONE', *, *, #72787, .T. ) ;
#57952=DIRECTION ( 'NONE',  ( 0.000000000000000000, 0.000000000000000000, -1.000000000000000000 ) ) ;
#57980=ORIENTED_EDGE ( 'NONE', *, *, #44030, .F. ) ;
#58058=FACE_OUTER_BOUND ( 'NONE', #127759, .T. ) ;
#58079=FACE_OUTER_BOUND ( 'NONE', #84319, .T. ) ;
#58081=ORIENTED_EDGE ( 'NONE', *, *, #114941, .F. ) ;
#58101=EDGE_CURVE ( 'NONE', #211497, #30659, #227369, .T. ) ;
#58104=ORIENTED_EDGE ( 'NONE', *, *, #53136, .F. ) ;
#58124=ORIENTED_EDGE ( 'NONE', *, *, #70060, .F. ) ;
#58125=CARTESIAN_POINT ( 'NONE',  ( -18.59999999999999787, 64.35000000001190301, -96.00830171387039513 ) ) ;
#58143=DIRECTION ( 'NONE',  ( 0.000000000000000000, -1.000000000000000000, -6.982962677686265922E-15 ) ) ;
#58152=DIRECTION ( 'NONE',  ( 0.000000000000000000, -0.9908441862701610203, 0.1350103645451807555 ) ) ;
#58186=ORIENTED_EDGE ( 'NONE', *, *, #121612, .F. ) ;
#58211=CARTESIAN_POINT ( 'NONE',  ( 20.94999999999999574, 87.65000000001191438, -99.92310748452422331 ) ) ;
#58234=ORIENTED_EDGE ( 'NONE', *, *, #254583, .F. ) ;
#58281=CARTESIAN_POINT ( 'NONE',  ( -20.64999999999999858, 76.00000000001169553, -67.52310748452430289 ) ) ;
#58299=CIRCLE ( 'NONE', #191632, 0.09999999999999971412 ) ;
#58303=CARTESIAN_POINT ( 'NONE',  ( 23.14999999999999858, 76.00000000001170974, -69.52310748452431710 ) ) ;
#58312=DIRECTION ( 'NONE',  ( 0.000000000000000000, 6.982962677686266711E-15, -1.000000000000000000 ) ) ;
#58316=EDGE_LOOP ( 'NONE', ( #12149, #110208, #116999, #148118 ) ) ;
#58375=DIRECTION ( 'NONE',  ( 0.000000000000000000, 0.000000000000000000, 1.000000000000000000 ) ) ;
#58379=LINE ( 'NONE', #36302, #127062 ) ;
#58391=CARTESIAN_POINT ( 'NONE',  ( 18.59999999999999787, 74.14897176987101091, -91.36919421510182815 ) ) ;
#58393=AXIS2_PLACEMENT_3D ( 'NONE', #65665, #121809, #42266 ) ;
#58395=DIRECTION ( 'NONE',  ( 0.000000000000000000, 0.000000000000000000, -1.000000000000000000 ) ) ;
#58411=B_SPLINE_CURVE_WITH_KNOTS ( 'NONE', 3,
 ( #198425, #40684, #254520, #36826, #155490, #98012, #61491, #156763, #117608, #60190, #120216, #21106, #255789, #217, #176321, #197131 ),
 .UNSPECIFIED., .F., .F.,
 ( 4, 3, 3, 3, 3, 4 ),
 ( 0.000000000000000000, 2.209833635978094077E-05, 5.595056164119021838E-05, 8.979992002654949078E-05, 0.0001236482757198866932, 0.0001574984039362965229 ),
 .UNSPECIFIED. ) ;
#58431=EDGE_CURVE ( 'NONE', #87934, #121241, #177344, .T. ) ;
#58467=CARTESIAN_POINT ( 'NONE',  ( 20.95595624212461416, 65.37610879691773391, -95.39347457039747269 ) ) ;
#58486=DIRECTION ( 'NONE',  ( -0.000000000000000000, -0.1350103645451807555, -0.9908441862701610203 ) ) ;
#58497=CARTESIAN_POINT ( 'NONE',  ( 18.49999999999999289, 65.50857864377445594, -78.17310748452437963 ) ) ;
#58502=DIRECTION ( 'NONE',  ( -0.000000000000000000, 7.272083257015735086E-15, -1.000000000000000000 ) ) ;
#58528=DIRECTION ( 'NONE',  ( -0.000000000000000000, 6.982962677686266711E-15, -1.000000000000000000 ) ) ;
#58546=EDGE_CURVE ( 'NONE', #35900, #96396, #22988, .T. ) ;
#58548=ORIENTED_EDGE ( 'NONE', *, *, #230450, .T. ) ;
#58602=LINE ( 'NONE', #152941, #254068 ) ;
#58603=FACE_OUTER_BOUND ( 'NONE', #102769, .T. ) ;
#58639=EDGE_CURVE ( 'NONE', #236062, #147420, #252475, .T. ) ;
#58654=EDGE_CURVE ( 'NONE', #210647, #86355, #248395, .T. ) ;
#58690=FACE_OUTER_BOUND ( 'NONE', #11568, .T. ) ;
#58692=FACE_OUTER_BOUND ( 'NONE', #83802, .T. ) ;
#58699=ORIENTED_EDGE ( 'NONE', *, *, #97333, .F. ) ;
#58715=AXIS2_PLACEMENT_3D ( 'NONE', #255511, #117344, #196864 ) ;
#58726=EDGE_CURVE ( 'NONE', #146605, #107898, #169339, .T. ) ;
#58734=DIRECTION ( 'NONE',  ( 0.000000000000000000, 1.000000000000000000, 6.982962677686266711E-15 ) ) ;
#58735=EDGE_CURVE ( 'NONE', #1640, #237421, #130927, .T. ) ;
#58745=EDGE_CURVE ( 'NONE', #2197, #16537, #156675, .T. ) ;
#58765=EDGE_LOOP ( 'NONE', ( #73256, #214693, #52589, #99949 ) ) ;
#58773=EDGE_CURVE ( 'NONE', #218485, #124985, #185849, .T. ) ;
#58779=ORIENTED_EDGE ( 'NONE', *, *, #97333, .T. ) ;
#58793=DIRECTION ( 'NONE',  ( 0.000000000000000000, -0.8660254037844420383, 0.4999999999999943379 ) ) ;
#58810=DIRECTION ( 'NONE',  ( 0.000000000000000000, -1.000000000000000000, -6.982962677686265922E-15 ) ) ;
#58817=ORIENTED_EDGE ( 'NONE', *, *, #243117, .F. ) ;
#58825=ADVANCED_FACE ( 'NONE', ( #18786 ), #194451, .T. ) ;
#58833=DIRECTION ( 'NONE',  ( 0.000000000000000000, 0.5000000000000209832, -0.8660254037844264952 ) ) ;
#58838=LINE ( 'NONE', #1450, #253694 ) ;
#58844=B_SPLINE_CURVE_WITH_KNOTS ( 'NONE', 3,
 ( #204084, #25476, #104956, #85393, #73610, #71033, #34484, #230085, #93133, #130984, #30625, #14909, #29358, #33212, #110131, #151860, #94415, #150555, #168871 ),
 .UNSPECIFIED., .F., .F.,
 ( 4, 3, 3, 3, 3, 3, 4 ),
 ( 0.000000000000000000, 2.646747978908424136E-05, 5.271166642127926225E-05, 9.008788829883960267E-05, 0.0001426648776560873473, 0.0001897378458659781616, 0.0001917382627806208306 ),
 .UNSPECIFIED. ) ;
#58860=( LENGTH_UNIT ( ) NAMED_UNIT ( * ) SI_UNIT ( .MILLI., .METRE. ) );
#58862=DIRECTION ( 'NONE',  ( -1.000000000000000000, -0.000000000000000000, -0.000000000000000000 ) ) ;
#58877=EDGE_LOOP ( 'NONE', ( #221359, #16842, #63293 ) ) ;
#58880=DIRECTION ( 'NONE',  ( 0.000000000000000000, 0.000000000000000000, -1.000000000000000000 ) ) ;
#58887=DIRECTION ( 'NONE',  ( 0.000000000000000000, -7.116814260417668513E-15, 1.000000000000000000 ) ) ;
#58893=ORIENTED_EDGE ( 'NONE', *, *, #201559, .F. ) ;
#58920=EDGE_LOOP ( 'NONE', ( #32432, #71990, #159264, #170936 ) ) ;
#58951=CARTESIAN_POINT ( 'NONE',  ( -21.05000000000000071, 76.00000000001173817, -73.52310748452431710 ) ) ;
#58983=ORIENTED_EDGE ( 'NONE', *, *, #113980, .F. ) ;
#58987=DIRECTION ( 'NONE',  ( 0.000000000000000000, -0.9908441862701610203, 0.1350103645451807555 ) ) ;
#59030=EDGE_CURVE ( 'NONE', #66328, #43089, #188152, .T. ) ;
#59044=CARTESIAN_POINT ( 'NONE',  ( -18.43634282235120736, 85.67978719993963921, -62.86245559907034419 ) ) ;
#59048=EDGE_CURVE ( 'NONE', #127649, #82517, #2865, .T. ) ;
#59066=FACE_OUTER_BOUND ( 'NONE', #21488, .T. ) ;
#59072=CARTESIAN_POINT ( 'NONE',  ( -20.94999999999999929, 74.16465844978745281, -91.46795619196133487 ) ) ;
#59086=CARTESIAN_POINT ( 'NONE',  ( 23.14999999999999503, 69.45000000001186891, -90.67310748452435121 ) ) ;
#59091=CARTESIAN_POINT ( 'NONE',  ( -21.05000000000000071, 76.00000000001170974, -69.52310748452431710 ) ) ;
#59109=AXIS2_PLACEMENT_3D ( 'NONE', #224675, #125583, #206411 ) ;
#59112=VERTEX_POINT ( 'NONE', #32974 ) ;
#59119=AXIS2_PLACEMENT_3D ( 'NONE', #74600, #12797, #149741 ) ;
#59121=CYLINDRICAL_SURFACE ( 'NONE', #93000, 0.1000000000000028644 ) ;
#59170=CARTESIAN_POINT ( 'NONE',  ( 18.59999999999999076, 65.79142135624907439, -78.37310748452438247 ) ) ;
#59171=EDGE_CURVE ( 'NONE', #146439, #61685, #125103, .T. ) ;
#59180=FACE_BOUND ( 'NONE', #95813, .T. ) ;
#59202=DIRECTION ( 'NONE',  ( -0.000000000000000000, 6.982962677686266711E-15, -1.000000000000000000 ) ) ;
#59205=DIRECTION ( 'NONE',  ( 0.000000000000000000, 1.000000000000000000, 0.000000000000000000 ) ) ;
#59212=CARTESIAN_POINT ( 'NONE',  ( -21.95218792049438861, 75.90097156021208491, -110.2246150457710030 ) ) ;
#59214=VERTEX_POINT ( 'NONE', #216696 ) ;
#59231=FACE_OUTER_BOUND ( 'NONE', #182988, .T. ) ;
#59238=DIRECTION ( 'NONE',  ( 0.000000000000000000, 1.000000000000000000, 6.982962677686266711E-15 ) ) ;
#59254=ORIENTED_EDGE ( 'NONE', *, *, #140940, .F. ) ;
#59277=DIRECTION ( 'NONE',  ( 1.000000000000000000, -0.000000000000000000, 0.000000000000000000 ) ) ;
#59288=DIRECTION ( 'NONE',  ( 0.000000000000000000, -0.8700118002898356018, 0.4930308989875170078 ) ) ;
#59324=LINE ( 'NONE', #138860, #244650 ) ;
#59328=CARTESIAN_POINT ( 'NONE',  ( 18.59999999999999432, 77.16270174994990327, -95.02310748452430289 ) ) ;
#59350=ORIENTED_EDGE ( 'NONE', *, *, #134950, .T. ) ;
#59366=ADVANCED_FACE ( 'NONE', ( #170907 ), #195848, .T. ) ;
#59381=ORIENTED_EDGE ( 'NONE', *, *, #207472, .F. ) ;
#59391=CARTESIAN_POINT ( 'NONE',  ( -18.59999999999999787, 85.40000000001167280, -62.64106563635157698 ) ) ;
#59406=CARTESIAN_POINT ( 'NONE',  ( -23.25000000000000000, 87.65000000001192859, -99.92310748452422331 ) ) ;
#59476=ORIENTED_EDGE ( 'NONE', *, *, #28171, .T. ) ;
#59500=VERTEX_POINT ( 'NONE', #37781 ) ;
#59504=CIRCLE ( 'NONE', #205269, 0.1000000000000052097 ) ;
#59519=ORIENTED_EDGE ( 'NONE', *, *, #32166, .F. ) ;
#59520=CARTESIAN_POINT ( 'NONE',  ( 21.14999999999999858, 64.25000000001202238, -114.7731074845243882 ) ) ;
#59564=DIRECTION ( 'NONE',  ( 1.000000000000000000, 0.000000000000000000, 0.000000000000000000 ) ) ;
#59596=EDGE_CURVE ( 'NONE', #225545, #20026, #98979, .T. ) ;
#59607=AXIS2_PLACEMENT_3D ( 'NONE', #252333, #77533, #133683 ) ;
#59636=DIRECTION ( 'NONE',  ( 1.000000000000000000, 0.000000000000000000, 0.000000000000000000 ) ) ;
#59640=CARTESIAN_POINT ( 'NONE',  ( 22.50000000000000000, 76.00000000001195133, -103.0231074845243171 ) ) ;
#59649=EDGE_LOOP ( 'NONE', ( #89685, #42363, #155791, #5141, #119840 ) ) ;
#59666=DIRECTION ( 'NONE',  ( 0.000000000000000000, 0.000000000000000000, 1.000000000000000000 ) ) ;
#59677=EDGE_CURVE ( 'NONE', #156346, #204844, #46157, .T. ) ;
#59683=DIRECTION ( 'NONE',  ( -1.000000000000000000, 0.000000000000000000, 0.000000000000000000 ) ) ;
#59708=VERTEX_POINT ( 'NONE', #166727 ) ;
#59728=CARTESIAN_POINT ( 'NONE',  ( -21.44999999999999929, 68.65000000001180069, -81.87310748452436826 ) ) ;
#59782=CIRCLE ( 'NONE', #126452, 0.5000000000000004441 ) ;
#59829=DIRECTION ( 'NONE',  ( 1.000000000000000000, -3.469446951953718318E-14, 2.003086131649645455E-14 ) ) ;
#59849=CARTESIAN_POINT ( 'NONE',  ( 20.94999999999999574, 74.83729825007388570, -94.92310748452432279 ) ) ;
#59857=FACE_OUTER_BOUND ( 'NONE', #47623, .T. ) ;
#59888=AXIS2_PLACEMENT_3D ( 'NONE', #93142, #172740, #210538 ) ;
#59906=ORIENTED_EDGE ( 'NONE', *, *, #118891, .T. ) ;
#59953=ORIENTED_EDGE ( 'NONE', *, *, #189260, .F. ) ;
#59956=DIRECTION ( 'NONE',  ( 0.000000000000000000, 0.000000000000000000, 1.000000000000000000 ) ) ;
#60030=ORIENTED_EDGE ( 'NONE', *, *, #80591, .F. ) ;
#60050=ORIENTED_EDGE ( 'NONE', *, *, #193888, .F. ) ;
#60060=CIRCLE ( 'NONE', #18375, 0.1000000000000055705 ) ;
#60066=AXIS2_PLACEMENT_3D ( 'NONE', #99388, #215505, #16055 ) ;
#60094=ORIENTED_EDGE ( 'NONE', *, *, #243010, .T. ) ;
#60098=ORIENTED_EDGE ( 'NONE', *, *, #230450, .F. ) ;
#60130=CARTESIAN_POINT ( 'NONE',  ( -21.59142135623730852, 68.15000000001187175, -90.77310748452437394 ) ) ;
#60142=ORIENTED_EDGE ( 'NONE', *, *, #199663, .T. ) ;
#60157=LINE ( 'NONE', #220540, #79836 ) ;
#60165=CARTESIAN_POINT ( 'NONE',  ( -20.54999999999999716, 74.00000000001186606, -90.29848556176222019 ) ) ;
#60175=DIRECTION ( 'NONE',  ( 1.000000000000000000, 0.000000000000000000, 0.000000000000000000 ) ) ;
#60190=CARTESIAN_POINT ( 'NONE',  ( 22.47809213839789066, 75.96246293238351655, -114.6730808193121192 ) ) ;
#60202=AXIS2_PLACEMENT_3D ( 'NONE', #65789, #145314, #46217 ) ;
#60206=CARTESIAN_POINT ( 'NONE',  ( -21.05000000000000071, 74.16465844978745281, -91.46795619196133487 ) ) ;
#60209=DIRECTION ( 'NONE',  ( 1.000000000000000000, 0.000000000000000000, 0.000000000000000000 ) ) ;
#60216=CARTESIAN_POINT ( 'NONE',  ( 18.59999999999999432, 74.83729825007388570, -94.92310748452432279 ) ) ;
#60223=DIRECTION ( 'NONE',  ( -0.000000000000000000, 1.000000000000000000, 6.982962677686266711E-15 ) ) ;
#60225=ORIENTED_EDGE ( 'NONE', *, *, #20323, .F. ) ;
#60228=ORIENTED_EDGE ( 'NONE', *, *, #193434, .F. ) ;
#60237=CYLINDRICAL_SURFACE ( 'NONE', #102621, 0.1000000000000028644 ) ;
#60259=DIRECTION ( 'NONE',  ( 1.000000000000000000, -0.000000000000000000, 0.000000000000000000 ) ) ;
#60282=CARTESIAN_POINT ( 'NONE',  ( -20.94999999999999929, 76.00000000001170974, -69.52310748452431710 ) ) ;
#60320=CARTESIAN_POINT ( 'NONE',  ( -21.05000000000000071, 64.35000000001195986, -102.9231074845243938 ) ) ;
#60333=EDGE_CURVE ( 'NONE', #155916, #212250, #46500, .T. ) ;
#60339=CARTESIAN_POINT ( 'NONE',  ( 21.05000000000000071, 71.14953271029217774, -81.55737489352601699 ) ) ;
#60355=CARTESIAN_POINT ( 'NONE',  ( -18.40000000000000213, 85.68240343348806221, -62.86626410711146207 ) ) ;
#60357=CARTESIAN_POINT ( 'NONE',  ( 21.07094088545303734, 69.67983277809545939, -103.1220011870765774 ) ) ;
#60387=DIRECTION ( 'NONE',  ( 0.000000000000000000, -0.8660254037844445918, -0.4999999999999897304 ) ) ;
#60405=B_SPLINE_CURVE_WITH_KNOTS ( 'NONE', 3,
 ( #194709, #172601, #76015, #117706, #192134, #252079, #14790, #236371, #212961, #176424, #33087, #53889, #115146, #91728, #153028, #255882 ),
 .UNSPECIFIED., .F., .F.,
 ( 4, 3, 3, 3, 3, 4 ),
 ( 0.000000000000000000, 2.372700795693547977E-05, 5.739057815866958510E-05, 9.073899019179559378E-05, 0.0001243544287365697066, 0.0001585386695601189160 ),
 .UNSPECIFIED. ) ;
#60421=FACE_OUTER_BOUND ( 'NONE', #203744, .T. ) ;
#60430=DIRECTION ( 'NONE',  ( 0.000000000000000000, 0.000000000000000000, -1.000000000000000000 ) ) ;
#60531=DIRECTION ( 'NONE',  ( 0.000000000000000000, -0.1568667991644355497, 0.9876197685951332295 ) ) ;
#60540=EDGE_CURVE ( 'NONE', #153107, #85086, #71498, .T. ) ;
#60558=CARTESIAN_POINT ( 'NONE',  ( -23.25000000000000000, 65.66751761918648356, -63.92826094061123143 ) ) ;
#60568=DIRECTION ( 'NONE',  ( -0.000000000000000000, -0.8660254037844420383, 0.4999999999999943379 ) ) ;
#60571=EDGE_LOOP ( 'NONE', ( #211809, #104784, #210136, #85687 ) ) ;
#60580=CARTESIAN_POINT ( 'NONE',  ( -21.56666275994539816, 76.00000000001200817, -109.9804758914176404 ) ) ;
#60585=DIRECTION ( 'NONE',  ( 0.000000000000000000, 0.000000000000000000, -1.000000000000000000 ) ) ;
#60590=DIRECTION ( 'NONE',  ( 1.713247197920696616E-14, -0.9876197685951263461, 0.1568667991644794590 ) ) ;
#60603=ORIENTED_EDGE ( 'NONE', *, *, #23272, .F. ) ;
#60604=CARTESIAN_POINT ( 'NONE',  ( 20.94999999999999929, 76.00000000001165290, -61.72310748452430573 ) ) ;
#60638=CARTESIAN_POINT ( 'NONE',  ( -22.39999999999999858, 75.90000000001199965, -110.8138870828977218 ) ) ;
#60685=VECTOR ( 'NONE', #156869, 1000.000000000000000 ) ;
#60699=CARTESIAN_POINT ( 'NONE',  ( -21.05000000000000071, 75.96824164695651405, -109.2819546076052859 ) ) ;
#60702=VERTEX_POINT ( 'NONE', #63172 ) ;
#60704=AXIS2_PLACEMENT_3D ( 'NONE', #12825, #126652, #223172 ) ;
#60716=ORIENTED_EDGE ( 'NONE', *, *, #60783, .F. ) ;
#60733=DIRECTION ( 'NONE',  ( 0.000000000000000000, -6.982962677686266711E-15, 1.000000000000000000 ) ) ;
#60755=CIRCLE ( 'NONE', #189780, 0.1000000000000028644 ) ;
#60783=EDGE_CURVE ( 'NONE', #75696, #208239, #80139, .T. ) ;
#60784=ORIENTED_EDGE ( 'NONE', *, *, #255155, .F. ) ;
#60785=DIRECTION ( 'NONE',  ( 0.000000000000000000, -7.429790795770644761E-15, 1.000000000000000000 ) ) ;
#60804=AXIS2_PLACEMENT_3D ( 'NONE', #195882, #116340, #177615 ) ;
#60867=DIRECTION ( 'NONE',  ( -1.000000000000000000, -0.000000000000000000, -0.000000000000000000 ) ) ;
#60869=CARTESIAN_POINT ( 'NONE',  ( -22.50000000000000000, 75.90000000001202807, -114.6726782920691221 ) ) ;
#60893=CARTESIAN_POINT ( 'NONE',  ( -20.54999999999999716, 76.00000000001170974, -69.52310748452431710 ) ) ;
#60911=CARTESIAN_POINT ( 'NONE',  ( -21.05000000000000071, 76.00000000001195133, -103.0231074845243171 ) ) ;
#60943=FACE_OUTER_BOUND ( 'NONE', #175256, .T. ) ;
#60989=DIRECTION ( 'NONE',  ( 0.000000000000000000, -6.982962677686266711E-15, 1.000000000000000000 ) ) ;
#61040=ORIENTED_EDGE ( 'NONE', *, *, #88298, .T. ) ;
#61048=VERTEX_POINT ( 'NONE', #155608 ) ;
#61053=DIRECTION ( 'NONE',  ( -2.827886303505248766E-16, -0.8660254037844377084, -0.5000000000000015543 ) ) ;
#61063=ORIENTED_EDGE ( 'NONE', *, *, #50092, .F. ) ;
#61084=ORIENTED_EDGE ( 'NONE', *, *, #49690, .T. ) ;
#61112=VERTEX_POINT ( 'NONE', #185069 ) ;
#61139=DIRECTION ( 'NONE',  ( 0.000000000000000000, 1.000000000000000000, 6.982962677686266711E-15 ) ) ;
#61152=ORIENTED_EDGE ( 'NONE', *, *, #216778, .F. ) ;
#61155=CIRCLE ( 'NONE', #206891, 0.1000000000000028644 ) ;
#61156=LINE ( 'NONE', #179838, #251680 ) ;
#61162=ORIENTED_EDGE ( 'NONE', *, *, #156567, .T. ) ;
#61174=ADVANCED_FACE ( 'NONE', ( #65117 ), #66411, .F. ) ;
#61176=CIRCLE ( 'NONE', #127824, 0.1000000000000028644 ) ;
#61177=CARTESIAN_POINT ( 'NONE',  ( 20.94999999999999574, 76.00000000001195133, -103.0231074845243171 ) ) ;
#61193=AXIS2_PLACEMENT_3D ( 'NONE', #3114, #98337, #82635 ) ;
#61221=VERTEX_POINT ( 'NONE', #69000 ) ;
#61222=ORIENTED_EDGE ( 'NONE', *, *, #23559, .T. ) ;
#61258=CARTESIAN_POINT ( 'NONE',  ( -20.64999999999999858, 68.75000000001179501, -81.77310748452435973 ) ) ;
#61276=DIRECTION ( 'NONE',  ( 0.7071067811865487940, -4.937700262164522799E-15, 0.7071067811865463515 ) ) ;
#61286=DIRECTION ( 'NONE',  ( 0.000000000000000000, 0.000000000000000000, 1.000000000000000000 ) ) ;
#61309=CARTESIAN_POINT ( 'NONE',  ( 18.49999999999999645, 74.13328508995456900, -91.27043223824230722 ) ) ;
#61315=VECTOR ( 'NONE', #129158, 1000.000000000000000 ) ;
#61346=DIRECTION ( 'NONE',  ( 0.000000000000000000, -0.8660254037844420383, 0.4999999999999942824 ) ) ;
#61374=AXIS2_PLACEMENT_3D ( 'NONE', #212323, #109329, #89772 ) ;
#61392=CARTESIAN_POINT ( 'NONE',  ( 18.39999999999999858, 85.51932773110434027, -96.05013110796491560 ) ) ;
#61399=ORIENTED_EDGE ( 'NONE', *, *, #67681, .T. ) ;
#61426=ORIENTED_EDGE ( 'NONE', *, *, #236624, .F. ) ;
#61434=DIRECTION ( 'NONE',  ( -2.827886303505249259E-16, -0.8660254037844378194, -0.5000000000000016653 ) ) ;
#61452=FACE_OUTER_BOUND ( 'NONE', #74348, .T. ) ;
#61460=SURFACE_STYLE_USAGE ( .BOTH. , #117578 ) ;
#61485=DIRECTION ( 'NONE',  ( 0.000000000000000000, -0.9915357197604804940, 0.1298341882520397950 ) ) ;
#61491=CARTESIAN_POINT ( 'NONE',  ( 22.45301702632625762, 75.98478912030185484, -114.6728997087847119 ) ) ;
#61510=LINE ( 'NONE', #159341, #55557 ) ;
#61555=CARTESIAN_POINT ( 'NONE',  ( 22.59080734064467677, 64.25000000001195133, -103.0538571926214644 ) ) ;
#61560=CARTESIAN_POINT ( 'NONE',  ( -21.05000000000000071, 76.00000000001195133, -103.0231074845243171 ) ) ;
#61595=( BOUNDED_SURFACE ( )  B_SPLINE_SURFACE ( 3, 2, ( 
 ( #198585, #379, #255946 ),
 ( #19978, #116497, #99465 ),
 ( #96883, #176483, #77346 ),
 ( #60357, #120380, #199897 ) ),
 .UNSPECIFIED., .F., .F., .F. ) 
 B_SPLINE_SURFACE_WITH_KNOTS ( ( 4, 4 ),
 ( 3, 3 ),
 ( 0.04058434257139476031, 0.04256401539001599538 ),
 ( 0.000000000000000000, 1.000000000000000000 ),
 .UNSPECIFIED. ) 
 GEOMETRIC_REPRESENTATION_ITEM ( )  RATIONAL_B_SPLINE_SURFACE ( (
 ( 1.000000000000000000, 0.7103081912008298859, 1.000000000000000000),
 ( 1.000000000000000000, 0.7104998333555329060, 1.000000000000000000),
 ( 1.000000000000000000, 0.7107238315755145530, 1.000000000000000000),
 ( 1.000000000000000000, 0.7110073749539290722, 1.000000000000000000) ) ) 
 REPRESENTATION_ITEM ( '' )  SURFACE ( )  );
#61599=VECTOR ( 'NONE', #248209, 1000.000000000000000 ) ;
#61616=EDGE_CURVE ( 'NONE', #3181, #87379, #113711, .T. ) ;
#61622=ADVANCED_FACE ( 'NONE', ( #163918 ), #123506, .T. ) ;
#61633=CARTESIAN_POINT ( 'NONE',  ( 23.15000000000000213, 85.00000000001188027, -93.12913836187181005 ) ) ;
#61640=DIRECTION ( 'NONE',  ( 0.000000000000000000, 1.000000000000000000, 0.000000000000000000 ) ) ;
#61650=CARTESIAN_POINT ( 'NONE',  ( -18.41817142474039670, 85.49870306661377128, -62.91914199688723386 ) ) ;
#61673=EDGE_CURVE ( 'NONE', #39176, #110160, #59504, .T. ) ;
#61685=VERTEX_POINT ( 'NONE', #111639 ) ;
#61717=EDGE_CURVE ( 'NONE', #19541, #39176, #234508, .T. ) ;
#61781=SURFACE_SIDE_STYLE ('',( #44791 ) ) ;
#61782=DIRECTION ( 'NONE',  ( -1.000000000000000000, -0.000000000000000000, -0.000000000000000000 ) ) ;
#61790=DIRECTION ( 'NONE',  ( 0.000000000000000000, 0.000000000000000000, 1.000000000000000000 ) ) ;
#61803=ADVANCED_FACE ( 'NONE', ( #256210 ), #13828, .T. ) ;
#61846=CARTESIAN_POINT ( 'NONE',  ( 20.95512828230159030, 67.12384868768657498, -90.82067721902097901 ) ) ;
#61863=EDGE_LOOP ( 'NONE', ( #199403, #227172, #203157, #90559 ) ) ;
#61871=AXIS2_PLACEMENT_3D ( 'NONE', #205488, #86815, #47693 ) ;
#61898=CARTESIAN_POINT ( 'NONE',  ( -23.24999999999999645, 85.60000000001166143, -62.92291809330219365 ) ) ;
#61903=DIRECTION ( 'NONE',  ( 1.000000000000000000, 0.000000000000000000, 0.000000000000000000 ) ) ;
#61909=CYLINDRICAL_SURFACE ( 'NONE', #235795, 0.09999999999999867328 ) ;
#61943=CARTESIAN_POINT ( 'NONE',  ( 18.59999999999999076, 64.35000000001177511, -78.17310748452437963 ) ) ;
#61953=EDGE_LOOP ( 'NONE', ( #204421, #92150, #151564 ) ) ;
#61986=CARTESIAN_POINT ( 'NONE',  ( 18.59999999999999076, 74.16465844978745281, -91.46795619196133487 ) ) ;
#62003=AXIS2_PLACEMENT_3D ( 'NONE', #137127, #172439, #35489 ) ;
#62041=ORIENTED_EDGE ( 'NONE', *, *, #146236, .F. ) ;
#62049=DIRECTION ( 'NONE',  ( 0.000000000000000000, 1.072103779144465041E-14, -1.000000000000000000 ) ) ;
#62052=CIRCLE ( 'NONE', #11998, 0.09999999999999939493 ) ;
#62095=VECTOR ( 'NONE', #194024, 1000.000000000000000 ) ;
#62096=AXIS2_PLACEMENT_3D ( 'NONE', #208023, #9799, #51465 ) ;
#62098=DIRECTION ( 'NONE',  ( 1.000000000000000000, 0.000000000000000000, 0.000000000000000000 ) ) ;
#62109=CARTESIAN_POINT ( 'NONE',  ( 20.04142135623730070, 64.35000000001180354, -81.67310748452439384 ) ) ;
#62125=DIRECTION ( 'NONE',  ( 0.000000000000000000, 0.000000000000000000, 1.000000000000000000 ) ) ;
#62139=ORIENTED_EDGE ( 'NONE', *, *, #177151, .T. ) ;
#62146=DIRECTION ( 'NONE',  ( -1.000000000000000000, -0.000000000000000000, -0.000000000000000000 ) ) ;
#62170=DIRECTION ( 'NONE',  ( 0.000000000000000000, 0.000000000000000000, 1.000000000000000000 ) ) ;
#62173=CARTESIAN_POINT ( 'NONE',  ( -20.64999999999999858, 71.75000000001186606, -90.67310748452433700 ) ) ;
#62191=DIRECTION ( 'NONE',  ( 0.000000000000000000, 0.000000000000000000, -1.000000000000000000 ) ) ;
#62192=CIRCLE ( 'NONE', #132932, 0.3999999999999975797 ) ;
#62227=CIRCLE ( 'NONE', #116412, 0.1000000000000028644 ) ;
#62239=ORIENTED_EDGE ( 'NONE', *, *, #195812, .T. ) ;
#62248=DIRECTION ( 'NONE',  ( 0.000000000000000000, -6.517943393102682774E-15, 1.000000000000000000 ) ) ;
#62283=FACE_OUTER_BOUND ( 'NONE', #250825, .T. ) ;
#62303=( BOUNDED_SURFACE ( )  B_SPLINE_SURFACE ( 3, 2, ( 
 ( #62643, #198287, #78 ),
 ( #39247, #200861, #22243 ),
 ( #239998, #181318, #221683 ),
 ( #180029, #41813, #2646 ) ),
 .UNSPECIFIED., .F., .F., .F. ) 
 B_SPLINE_SURFACE_WITH_KNOTS ( ( 4, 4 ),
 ( 3, 3 ),
 ( 3.550762114890027021E-18, 0.0003124336600439677055 ),
 ( 0.000000000000000000, 1.000000000000000000 ),
 .UNSPECIFIED. ) 
 GEOMETRIC_REPRESENTATION_ITEM ( )  RATIONAL_B_SPLINE_SURFACE ( (
 ( 1.000000000000000000, 0.7071067811865475727, 1.000000000000000000),
 ( 1.000000000000000000, 0.7089187706049929760, 1.000000000000000000),
 ( 1.000000000000000000, 0.7039288185051876257, 1.000000000000000000),
 ( 1.000000000000000000, 0.7040654476015342222, 1.000000000000000000) ) ) 
 REPRESENTATION_ITEM ( '' )  SURFACE ( )  );
#62312=EDGE_LOOP ( 'NONE', ( #71898, #188173, #96314, #46335 ) ) ;
#62336=EDGE_CURVE ( 'NONE', #231733, #173596, #138976, .T. ) ;
#62358=CARTESIAN_POINT ( 'NONE',  ( 23.25000000000000000, 87.75000000001186606, -90.87310748452424036 ) ) ;
#62360=CIRCLE ( 'NONE', #174839, 4.300000000000025580 ) ;
#62383=EDGE_LOOP ( 'NONE', ( #54085, #95269, #174163, #218546 ) ) ;
#62396=PLANE ( 'NONE',  #12373 ) ;
#62398=FACE_OUTER_BOUND ( 'NONE', #29464, .T. ) ;
#62407=ORIENTED_EDGE ( 'NONE', *, *, #112003, .F. ) ;
#62445=ORIENTED_EDGE ( 'NONE', *, *, #165970, .T. ) ;
#62455=DIRECTION ( 'NONE',  ( 1.000000000000000000, 0.000000000000000000, 0.000000000000000000 ) ) ;
#62474=TOROIDAL_SURFACE ( 'NONE', #41640, 0.4000000000000009104, 0.1000000000000000056 ) ;
#62479=TOROIDAL_SURFACE ( 'NONE', #108262, 4.099999999999999645, 0.1000000000000000056 ) ;
#62494=CARTESIAN_POINT ( 'NONE',  ( -18.39999999999999858, 85.40000000001204228, -114.7731074845242460 ) ) ;
#62635=CARTESIAN_POINT ( 'NONE',  ( -2.995603634470891112E-16, 87.75000000001186606, -90.77310748452423184 ) ) ;
#62643=CARTESIAN_POINT ( 'NONE',  ( 22.49999999999999645, 75.90000000001202807, -114.6726782920691221 ) ) ;
#62664=ORIENTED_EDGE ( 'NONE', *, *, #206301, .T. ) ;
#62706=CARTESIAN_POINT ( 'NONE',  ( 20.85000000000000142, 77.83585931145526615, -58.01866831572577610 ) ) ;
#62707=CARTESIAN_POINT ( 'NONE',  ( 21.14999999999999503, 76.00000000001195133, -103.0231074845243171 ) ) ;
#62729=CARTESIAN_POINT ( 'NONE',  ( -2.995603634470891112E-16, 69.35000000001180354, -81.77310748452435973 ) ) ;
#62740=EDGE_LOOP ( 'NONE', ( #96365, #61399 ) ) ;
#62760=B_SPLINE_CURVE_WITH_KNOTS ( 'NONE', 3,
 ( #236719, #159778, #239310, #213309, #193763, #15133, #174243 ),
 .UNSPECIFIED., .F., .F.,
 ( 4, 3, 4 ),
 ( 0.000000000000000000, 1.860045280644891661E-05, 5.251155757304066840E-05 ),
 .UNSPECIFIED. ) ;
#62781=DIRECTION ( 'NONE',  ( 0.000000000000000000, 7.026728003956683390E-15, -1.000000000000000000 ) ) ;
#62791=CARTESIAN_POINT ( 'NONE',  ( -21.46681500597874148, 76.00000000001200817, -109.8806186439521611 ) ) ;
#62849=LINE ( 'NONE', #40760, #221873 ) ;
#62920=FACE_OUTER_BOUND ( 'NONE', #249907, .T. ) ;
#62946=ORIENTED_EDGE ( 'NONE', *, *, #41725, .F. ) ;
#62949=ORIENTED_EDGE ( 'NONE', *, *, #20351, .T. ) ;
#62951=LINE ( 'NONE', #202468, #179535 ) ;
#62975=ORIENTED_EDGE ( 'NONE', *, *, #225571, .T. ) ;
#62983=ORIENTED_EDGE ( 'NONE', *, *, #507, .T. ) ;
#62994=CARTESIAN_POINT ( 'NONE',  ( 20.94999999999999929, 85.50000000001179501, -79.41707660717668205 ) ) ;
#63004=CARTESIAN_POINT ( 'NONE',  ( 18.49999999999999289, 65.75000000001179501, -81.67310748452439384 ) ) ;
#63033=CARTESIAN_POINT ( 'NONE',  ( -21.45000000000000284, 68.29142135624915966, -90.67310748452436542 ) ) ;
#63091=( BOUNDED_CURVE ( )  B_SPLINE_CURVE ( 3, ( #40424, #119957, #255524, #20848 ),
 .UNSPECIFIED., .F., .T. ) 
 B_SPLINE_CURVE_WITH_KNOTS ( ( 4, 4 ),
 ( 3.141592653589917017, 4.712388980384686121 ),
 .UNSPECIFIED. ) 
 CURVE ( )  GEOMETRIC_REPRESENTATION_ITEM ( )  RATIONAL_B_SPLINE_CURVE ( ( 1.000000000000000000, 0.8047378541243951355, 0.8047378541243951355, 1.000000000000000000 ) ) 
 REPRESENTATION_ITEM ( '' )  );
#63107=FACE_OUTER_BOUND ( 'NONE', #197094, .T. ) ;
#63112=ADVANCED_FACE ( 'NONE', ( #91166 ), #151156, .F. ) ;
#63114=DIRECTION ( 'NONE',  ( 0.000000000000000000, 6.982962677686266711E-15, -1.000000000000000000 ) ) ;
#63127=ORIENTED_EDGE ( 'NONE', *, *, #120685, .T. ) ;
#63154=DIRECTION ( 'NONE',  ( 0.000000000000000000, 1.000000000000000000, 6.982962677686266711E-15 ) ) ;
#63172=CARTESIAN_POINT ( 'NONE',  ( -21.44999999999999929, 68.75000000001179501, -81.87310748452436826 ) ) ;
#63176=DIRECTION ( 'NONE',  ( 0.000000000000000000, 0.000000000000000000, 1.000000000000000000 ) ) ;
#63186=ADVANCED_FACE ( 'NONE', ( #243172 ), #26726, .T. ) ;
#63199=CARTESIAN_POINT ( 'NONE',  ( -20.94999999999999929, 87.65000000001172964, -72.42310748452422331 ) ) ;
#63213=CARTESIAN_POINT ( 'NONE',  ( -21.05000000000000071, 74.14897176987101091, -91.36919421510182815 ) ) ;
#63254=EDGE_CURVE ( 'NONE', #224632, #155597, #151812, .T. ) ;
#63265=CARTESIAN_POINT ( 'NONE',  ( 22.39999999999999503, 75.90000000001199965, -110.8138870828976934 ) ) ;
#63288=EDGE_CURVE ( 'NONE', #101606, #256898, #39075, .T. ) ;
#63293=ORIENTED_EDGE ( 'NONE', *, *, #134350, .T. ) ;
#63302=CARTESIAN_POINT ( 'NONE',  ( 23.14999999999999147, 80.15000000001194280, -103.0231074845242887 ) ) ;
#63310=CYLINDRICAL_SURFACE ( 'NONE', #165898, 11.74999999999999645 ) ;
#63349=DIRECTION ( 'NONE',  ( 0.000000000000000000, -6.982962677686266711E-15, 1.000000000000000000 ) ) ;
#63375=ORIENTED_EDGE ( 'NONE', *, *, #208230, .F. ) ;
#63424=AXIS2_PLACEMENT_3D ( 'NONE', #196809, #255461, #76865 ) ;
#63446=ADVANCED_FACE ( 'NONE', ( #95654 ), #98190, .F. ) ;
#63479=DIRECTION ( 'NONE',  ( 0.000000000000000000, 0.000000000000000000, 1.000000000000000000 ) ) ;
#63482=ORIENTED_EDGE ( 'NONE', *, *, #46765, .F. ) ;
#63486=EDGE_CURVE ( 'NONE', #136972, #14256, #255481, .T. ) ;
#63500=EDGE_LOOP ( 'NONE', ( #137331, #61162, #36732, #192034 ) ) ;
#63509=CARTESIAN_POINT ( 'NONE',  ( -23.25000000000000000, 76.00000000001170974, -69.52310748452431710 ) ) ;
#63538=DIRECTION ( 'NONE',  ( 0.7071359030027593029, 0.7070776581709197206, 0.000000000000000000 ) ) ;
#63560=VECTOR ( 'NONE', #37377, 1000.000000000000000 ) ;
#63594=CARTESIAN_POINT ( 'NONE',  ( 20.95512820512820440, 65.37615131630001031, -95.35819391543677170 ) ) ;
#63625=CARTESIAN_POINT ( 'NONE',  ( 20.94999999999999929, 65.52661458509899717, -95.44445302027584432 ) ) ;
#63630=FACE_OUTER_BOUND ( 'NONE', #56102, .T. ) ;
#63655=DIRECTION ( 'NONE',  ( 0.000000000000000000, 0.8068669527896844551, 0.5907332058517525963 ) ) ;
#63656=CIRCLE ( 'NONE', #55253, 11.74999999999999645 ) ;
#63668=DIRECTION ( 'NONE',  ( -1.000000000000000000, 0.000000000000000000, 0.000000000000000000 ) ) ;
#63673=CARTESIAN_POINT ( 'NONE',  ( -20.94999999999999929, 76.00000000001195133, -103.0231074845243171 ) ) ;
#63706=DIRECTION ( 'NONE',  ( 0.000000000000000000, 0.000000000000000000, 1.000000000000000000 ) ) ;
#63718=VECTOR ( 'NONE', #179403, 1000.000000000000114 ) ;
#63784=AXIS2_PLACEMENT_3D ( 'NONE', #80634, #203167, #239742 ) ;
#63788=CARTESIAN_POINT ( 'NONE',  ( 20.94999999999999574, 77.73625713160926409, -91.45445515550680682 ) ) ;
#63799=CARTESIAN_POINT ( 'NONE',  ( -23.15000000000000213, 64.35000000001176090, -76.53791325517833855 ) ) ;
#63802=DIRECTION ( 'NONE',  ( 1.000000000000000000, 0.000000000000000000, 0.000000000000000000 ) ) ;
#63819=ADVANCED_FACE ( 'NONE', ( #173676 ), #57497, .T. ) ;
#63825=ADVANCED_FACE ( 'NONE', ( #191928 ), #253140, .F. ) ;
#63840=CARTESIAN_POINT ( 'NONE',  ( -23.15000000000000213, 64.25000000001176659, -76.53791325517833855 ) ) ;
#63908=ADVANCED_FACE ( 'NONE', ( #135467 ), #138030, .F. ) ;
#63957=ORIENTED_EDGE ( 'NONE', *, *, #194020, .T. ) ;
#64005=EDGE_CURVE ( 'NONE', #49226, #91113, #201533, .T. ) ;
#64021=CARTESIAN_POINT ( 'NONE',  ( 18.50000000000000000, 85.50000000001166711, -62.92291809330219365 ) ) ;
#64036=DIRECTION ( 'NONE',  ( 0.000000000000000000, -1.000000000000000000, -6.352154140967427193E-15 ) ) ;
#64065=DIRECTION ( 'NONE',  ( -0.000000000000000000, -6.982962677686266711E-15, 1.000000000000000000 ) ) ;
#64079=EDGE_CURVE ( 'NONE', #195497, #143163, #56145, .T. ) ;
#64080=EDGE_LOOP ( 'NONE', ( #99267, #63957 ) ) ;
#64083=VECTOR ( 'NONE', #123619, 1000.000000000000000 ) ;
#64101=CARTESIAN_POINT ( 'NONE',  ( 20.04142135623730070, 64.35000000001180354, -81.77310748452438816 ) ) ;
#64120=CARTESIAN_POINT ( 'NONE',  ( 22.57320508075687115, 64.25000000001195133, -103.0231074845244024 ) ) ;
#64127=CARTESIAN_POINT ( 'NONE',  ( 21.05000000000000071, 85.50000000001179501, -79.41707660717668205 ) ) ;
#64135=AXIS2_PLACEMENT_3D ( 'NONE', #42386, #106190, #185752 ) ;
#64141=LINE ( 'NONE', #1580, #55958 ) ;
#64155=CARTESIAN_POINT ( 'NONE',  ( 23.15000000000000213, 85.00000000001179501, -78.91707660717668205 ) ) ;
#64160=ORIENTED_EDGE ( 'NONE', *, *, #188927, .F. ) ;
#64177=DIRECTION ( 'NONE',  ( 0.000000000000000000, -6.608470384673558123E-15, 1.000000000000000000 ) ) ;
#64216=AXIS2_PLACEMENT_3D ( 'NONE', #87248, #230643, #148536 ) ;
#64263=ORIENTED_EDGE ( 'NONE', *, *, #112633, .T. ) ;
#64285=DIRECTION ( 'NONE',  ( -0.000000000000000000, 6.982962677686266711E-15, -1.000000000000000000 ) ) ;
#64296=CARTESIAN_POINT ( 'NONE',  ( -18.59999999999999787, 66.65000000001180069, -81.87310748452438247 ) ) ;
#64308=LINE ( 'NONE', #48587, #103335 ) ;
#64310=AXIS2_PLACEMENT_3D ( 'NONE', #215266, #36661, #195730 ) ;
#64319=VERTEX_POINT ( 'NONE', #176892 ) ;
#64340=CYLINDRICAL_SURFACE ( 'NONE', #41105, 0.1000000000000064587 ) ;
#64367=ORIENTED_EDGE ( 'NONE', *, *, #77044, .F. ) ;
#64448=AXIS2_PLACEMENT_3D ( 'NONE', #22293, #44414, #41858 ) ;
#64457=TOROIDAL_SURFACE ( 'NONE', #10300, 0.2000000000000000111, 0.1000000000000000056 ) ;
#64468=ORIENTED_EDGE ( 'NONE', *, *, #200097, .T. ) ;
#64469=DIRECTION ( 'NONE',  ( 0.000000000000000000, 0.9915357197604892647, -0.1298341882519715440 ) ) ;
#64514=EDGE_LOOP ( 'NONE', ( #251873, #18551, #78434, #187711, #62949 ) ) ;
#64527=ORIENTED_EDGE ( 'NONE', *, *, #812, .T. ) ;
#64555=DIRECTION ( 'NONE',  ( 0.000000000000000000, 7.056502275159890832E-15, -1.000000000000000000 ) ) ;
#64558=PLANE ( 'NONE',  #183394 ) ;
#64571=ORIENTED_EDGE ( 'NONE', *, *, #88772, .T. ) ;
#64585=CIRCLE ( 'NONE', #210358, 0.1000000000000028644 ) ;
#64599=ADVANCED_FACE ( 'NONE', ( #127165 ), #91571, .T. ) ;
#64620=ORIENTED_EDGE ( 'NONE', *, *, #117147, .F. ) ;
#64641=VERTEX_POINT ( 'NONE', #60130 ) ;
#64642=FACE_OUTER_BOUND ( 'NONE', #186737, .T. ) ;
#64660=VERTEX_POINT ( 'NONE', #41895 ) ;
#64682=DIRECTION ( 'NONE',  ( 0.000000000000000000, 1.000000000000000000, 6.982962677686266711E-15 ) ) ;
#64717=EDGE_LOOP ( 'NONE', ( #31854, #183373, #44037, #230576 ) ) ;
#64719=ADVANCED_FACE ( 'NONE', ( #18453 ), #256013, .T. ) ;
#64724=ADVANCED_FACE ( 'NONE', ( #82241 ), #158010, .T. ) ;
#64739=CARTESIAN_POINT ( 'NONE',  ( 18.59999999999999076, 69.35000000001180354, -81.67310748452436542 ) ) ;
#64769=CIRCLE ( 'NONE', #181324, 0.09999999999999939493 ) ;
#64771=DIRECTION ( 'NONE',  ( 0.000000000000000000, 0.000000000000000000, -1.000000000000000000 ) ) ;
#64774=AXIS2_PLACEMENT_3D ( 'NONE', #207325, #169508, #112071 ) ;
#64780=DIRECTION ( 'NONE',  ( 1.000000000000000000, 0.000000000000000000, 0.000000000000000000 ) ) ;
#64838=ADVANCED_FACE ( 'NONE', ( #221758 ), #187822, .T. ) ;
#64857=EDGE_LOOP ( 'NONE', ( #68025, #235432, #247002, #82719, #8559, #7552, #144755, #15048, #245534, #222717, #202398 ) ) ;
#64862=AXIS2_PLACEMENT_3D ( 'NONE', #230805, #229509, #50833 ) ;
#64903=DIRECTION ( 'NONE',  ( 0.000000000000000000, 0.000000000000000000, 1.000000000000000000 ) ) ;
#64904=CARTESIAN_POINT ( 'NONE',  ( -20.54999999999999716, 71.65000000001187175, -90.67310748452433700 ) ) ;
#64932=LINE ( 'NONE', #67504, #28133 ) ;
#64937=CARTESIAN_POINT ( 'NONE',  ( 18.59999999999999787, 85.40000000001165859, -62.64106563635156277 ) ) ;
#64984=CARTESIAN_POINT ( 'NONE',  ( 19.99999999999998934, 64.25000000001179501, -81.67310748452439384 ) ) ;
#64999=DIRECTION ( 'NONE',  ( 0.000000000000000000, 0.000000000000000000, 1.000000000000000000 ) ) ;
#65022=DIRECTION ( 'NONE',  ( -1.000000000000000000, 0.000000000000000000, 0.000000000000000000 ) ) ;
#65046=DIRECTION ( 'NONE',  ( -1.000000000000000000, 1.836970198721029934E-16, 1.282749433769087757E-30 ) ) ;
#65081=DIRECTION ( 'NONE',  ( -1.000000000000000000, 0.000000000000000000, 0.000000000000000000 ) ) ;
#65085=VECTOR ( 'NONE', #237877, 1000.000000000000000 ) ;
#65098=CYLINDRICAL_SURFACE ( 'NONE', #193463, 0.1000000000000028644 ) ;
#65107=AXIS2_PLACEMENT_3D ( 'NONE', #191166, #152040, #112894 ) ;
#65117=FACE_OUTER_BOUND ( 'NONE', #156663, .T. ) ;
#65125=AXIS2_PLACEMENT_3D ( 'NONE', #75841, #219188, #197053 ) ;
#65136=CARTESIAN_POINT ( 'NONE',  ( 23.24999999999999289, 64.25000000001202238, -114.7731074845243882 ) ) ;
#65142=EDGE_LOOP ( 'NONE', ( #68054, #108101, #21846, #238429 ) ) ;
#65147=CARTESIAN_POINT ( 'NONE',  ( -21.53699400379683127, 69.21228820681116645, -103.0231074845243455 ) ) ;
#65151=ORIENTED_EDGE ( 'NONE', *, *, #97641, .F. ) ;
#65163=DIRECTION ( 'NONE',  ( -1.000000000000000000, 2.952720810173289112E-16, 2.061873921506763405E-30 ) ) ;
#65186=DIRECTION ( 'NONE',  ( 1.000000000000000000, 0.000000000000000000, 0.000000000000000000 ) ) ;
#65238=EDGE_CURVE ( 'NONE', #215983, #142842, #143214, .T. ) ;
#65248=ORIENTED_EDGE ( 'NONE', *, *, #89683, .T. ) ;
#65281=CARTESIAN_POINT ( 'NONE',  ( -18.59999999999999787, 68.75000000001179501, -81.67310748452436542 ) ) ;
#65353=AXIS2_PLACEMENT_3D ( 'NONE', #237701, #34388, #76047 ) ;
#65370=DIRECTION ( 'NONE',  ( -0.000000000000000000, -6.982962677686266711E-15, 1.000000000000000000 ) ) ;
#65378=EDGE_CURVE ( 'NONE', #23758, #192851, #17825, .T. ) ;
#65387=LINE ( 'NONE', #2828, #253513 ) ;
#65453=ORIENTED_EDGE ( 'NONE', *, *, #59030, .F. ) ;
#65514=ORIENTED_EDGE ( 'NONE', *, *, #246424, .T. ) ;
#65537=EDGE_CURVE ( 'NONE', #7336, #3248, #11107, .T. ) ;
#65545=VERTEX_POINT ( 'NONE', #25555 ) ;
#65550=AXIS2_PLACEMENT_3D ( 'NONE', #164057, #148335, #227871 ) ;
#65562=FACE_OUTER_BOUND ( 'NONE', #150190, .T. ) ;
#65576=ORIENTED_EDGE ( 'NONE', *, *, #158900, .F. ) ;
#65614=DIRECTION ( 'NONE',  ( 0.000000000000000000, 0.000000000000000000, -1.000000000000000000 ) ) ;
#65620=EDGE_CURVE ( 'NONE', #164805, #197574, #223285, .T. ) ;
#65638=ADVANCED_FACE ( 'NONE', ( #187204 ), #6820, .T. ) ;
#65650=AXIS2_PLACEMENT_3D ( 'NONE', #4521, #163618, #243143 ) ;
#65651=DIRECTION ( 'NONE',  ( 1.000000000000000000, 0.000000000000000000, 0.000000000000000000 ) ) ;
#65660=CARTESIAN_POINT ( 'NONE',  ( -20.94999999999999929, 88.41227409416143246, -72.52310748452423184 ) ) ;
#65665=CARTESIAN_POINT ( 'NONE',  ( 20.94999999999999929, 88.41227409416143246, -72.52310748452423184 ) ) ;
#65683=AXIS2_PLACEMENT_3D ( 'NONE', #22169, #19593, #121291 ) ;
#65684=CARTESIAN_POINT ( 'NONE',  ( 21.12400222705965547, 67.22148809293476290, -90.77310748452437394 ) ) ;
#65688=VECTOR ( 'NONE', #181730, 1000.000000000000000 ) ;
#65723=CIRCLE ( 'NONE', #240683, 0.1999999999999987899 ) ;
#65735=DIRECTION ( 'NONE',  ( 0.000000000000000000, -0.01562499999999307672, 0.9998779222360100194 ) ) ;
#65742=ORIENTED_EDGE ( 'NONE', *, *, #39666, .F. ) ;
#65757=ORIENTED_EDGE ( 'NONE', *, *, #47016, .F. ) ;
#65772=VERTEX_POINT ( 'NONE', #211898 ) ;
#65789=CARTESIAN_POINT ( 'NONE',  ( -18.59999999999999787, 64.35000000001180354, -81.67310748452439384 ) ) ;
#65794=PLANE ( 'NONE',  #31976 ) ;
#65884=CARTESIAN_POINT ( 'NONE',  ( 18.44364597020196328, 85.49048731717419969, -95.96512959484043392 ) ) ;
#65901=CIRCLE ( 'NONE', #107586, 0.09999999999999939493 ) ;
#65923=AXIS2_PLACEMENT_3D ( 'NONE', #162981, #143393, #80834 ) ;
#65945=DIRECTION ( 'NONE',  ( 0.000000000000000000, -0.9999631594459057471, 0.008583690987121077309 ) ) ;
#65976=LINE ( 'NONE', #119549, #170850 ) ;
#66012=ADVANCED_FACE ( 'NONE', ( #224703 ), #112654, .T. ) ;
#66032=LINE ( 'NONE', #225085, #125738 ) ;
#66090=LINE ( 'NONE', #187341, #72516 ) ;
#66093=CARTESIAN_POINT ( 'NONE',  ( -18.50000000000000000, 68.87972903831409610, -65.86354444268502561 ) ) ;
#66094=DIRECTION ( 'NONE',  ( -1.000000000000000000, -0.000000000000000000, -0.000000000000000000 ) ) ;
#66147=ORIENTED_EDGE ( 'NONE', *, *, #202714, .T. ) ;
#66235=CARTESIAN_POINT ( 'NONE',  ( 22.47071067811865319, 68.27992525551390202, -103.1221999392269737 ) ) ;
#66239=AXIS2_PLACEMENT_3D ( 'NONE', #54049, #128459, #170205 ) ;
#66245=ORIENTED_EDGE ( 'NONE', *, *, #159794, .T. ) ;
#66254=VECTOR ( 'NONE', #106092, 1000.000000000000000 ) ;
#66312=CARTESIAN_POINT ( 'NONE',  ( -21.55000000000000426, 68.29142135624915966, -90.67310748452436542 ) ) ;
#66313=ORIENTED_EDGE ( 'NONE', *, *, #257376, .T. ) ;
#66328=VERTEX_POINT ( 'NONE', #24644 ) ;
#66362=B_SPLINE_CURVE_WITH_KNOTS ( 'NONE', 3,
 ( #36340, #130272, #115861, #16775, #70349, #217500 ),
 .UNSPECIFIED., .F., .F.,
 ( 4, 2, 4 ),
 ( 0.000000000000000000, 0.0001569047307838632198, 0.0003138094615677264397 ),
 .UNSPECIFIED. ) ;
#66365=CARTESIAN_POINT ( 'NONE',  ( -21.08479644141223019, 69.65496134228006042, -103.0816619270884473 ) ) ;
#66389=VERTEX_POINT ( 'NONE', #85830 ) ;
#66406=ADVANCED_FACE ( 'NONE', ( #207109 ), #8901, .T. ) ;
#66411=SPHERICAL_SURFACE ( 'NONE', #13584, 0.1000000000000000056 ) ;
#66418=DIRECTION ( 'NONE',  ( 0.000000000000000000, -1.000000000000000000, -6.982962677686266711E-15 ) ) ;
#66435=ORIENTED_EDGE ( 'NONE', *, *, #39818, .T. ) ;
#66463=AXIS2_PLACEMENT_3D ( 'NONE', #59170, #55324, #138709 ) ;
#66557=EDGE_LOOP ( 'NONE', ( #193240, #150625, #132469, #128527 ) ) ;
#66559=EDGE_CURVE ( 'NONE', #205047, #123180, #80385, .T. ) ;
#66572=EDGE_CURVE ( 'NONE', #170827, #103624, #182168, .T. ) ;
#66588=CARTESIAN_POINT ( 'NONE',  ( -21.05000000000000071, 76.00000000001170974, -69.52310748452431710 ) ) ;
#66596=FACE_OUTER_BOUND ( 'NONE', #203725, .T. ) ;
#66613=CIRCLE ( 'NONE', #20838, 0.1000000000000028644 ) ;
#66640=VECTOR ( 'NONE', #138135, 1000.000000000000000 ) ;
#66709=EDGE_CURVE ( 'NONE', #216113, #216303, #115704, .T. ) ;
#66732=CARTESIAN_POINT ( 'NONE',  ( 21.05000000000000071, 64.35000000001176090, -76.53791325517833855 ) ) ;
#66739=CARTESIAN_POINT ( 'NONE',  ( -23.25000000000000000, 76.00000000001170974, -69.52310748452431710 ) ) ;
#66742=DIRECTION ( 'NONE',  ( 1.000000000000000000, 0.000000000000000000, 0.000000000000000000 ) ) ;
#66759=CARTESIAN_POINT ( 'NONE',  ( 20.94560253601876809, 64.25000000001175238, -76.51302397200892358 ) ) ;
#66812=AXIS2_PLACEMENT_3D ( 'NONE', #239921, #23462, #119994 ) ;
#66818=ORIENTED_EDGE ( 'NONE', *, *, #154673, .T. ) ;
#66840=AXIS2_PLACEMENT_3D ( 'NONE', #176546, #78686, #138645 ) ;
#66850=CARTESIAN_POINT ( 'NONE',  ( 21.00000000000000000, 66.25000000001186606, -90.77310748452438816 ) ) ;
#66860=VERTEX_POINT ( 'NONE', #94524 ) ;
#66942=DIRECTION ( 'NONE',  ( -0.000000000000000000, 0.1350103645451945777, -0.9908441862701590219 ) ) ;
#66977=VECTOR ( 'NONE', #25402, 1000.000000000000000 ) ;
#66984=DIRECTION ( 'NONE',  ( 1.040834085586049673E-13, 0.7899159663865300551, 0.6132151058540831201 ) ) ;
#66992=DIRECTION ( 'NONE',  ( -0.000000000000000000, 7.272083257015735086E-15, -1.000000000000000000 ) ) ;
#66995=LINE ( 'NONE', #226034, #61599 ) ;
#67004=AXIS2_PLACEMENT_3D ( 'NONE', #157906, #156612, #36657 ) ;
#67027=EDGE_CURVE ( 'NONE', #16177, #51868, #28254, .T. ) ;
#67031=VERTEX_POINT ( 'NONE', #125652 ) ;
#67037=CARTESIAN_POINT ( 'NONE',  ( -20.94999999999999929, 87.48912529308798014, -100.0231074845242318 ) ) ;
#67049=LINE ( 'NONE', #206556, #189629 ) ;
#67054=DIRECTION ( 'NONE',  ( 1.000000000000000000, 0.000000000000000000, 0.000000000000000000 ) ) ;
#67064=ORIENTED_EDGE ( 'NONE', *, *, #241972, .F. ) ;
#67088=FACE_OUTER_BOUND ( 'NONE', #208585, .T. ) ;
#67137=DIRECTION ( 'NONE',  ( 0.000000000000000000, 0.1350103645451974088, -0.9908441862701587999 ) ) ;
#67157=VECTOR ( 'NONE', #69791, 1000.000000000000000 ) ;
#67163=CIRCLE ( 'NONE', #146433, 0.1000000000000028644 ) ;
#67187=AXIS2_PLACEMENT_3D ( 'NONE', #200379, #21752, #204215 ) ;
#67255=CARTESIAN_POINT ( 'NONE',  ( -20.64999999999999858, 71.65000000001180069, -81.87310748452433984 ) ) ;
#67275=CARTESIAN_POINT ( 'NONE',  ( 18.42636655943171320, 85.49694431578232923, -62.91402691336873687 ) ) ;
#67364=FACE_OUTER_BOUND ( 'NONE', #61863, .T. ) ;
#67382=CARTESIAN_POINT ( 'NONE',  ( -21.55000000000000071, 68.65000000001180069, -81.87310748452436826 ) ) ;
#67389=ORIENTED_EDGE ( 'NONE', *, *, #153643, .T. ) ;
#67395=CARTESIAN_POINT ( 'NONE',  ( -18.50000000000000000, 64.35000000001187459, -90.87310748452438247 ) ) ;
#67414=EDGE_LOOP ( 'NONE', ( #54956, #14991, #2841, #106305 ) ) ;
#67417=CARTESIAN_POINT ( 'NONE',  ( -20.85000000000000142, 77.16412189325286874, -61.80825939895269272 ) ) ;
#67459=DIRECTION ( 'NONE',  ( 0.000000000000000000, 0.000000000000000000, -1.000000000000000000 ) ) ;
#67485=CARTESIAN_POINT ( 'NONE',  ( 21.05000000000000071, 76.00000000001195133, -103.0231074845243171 ) ) ;
#67504=CARTESIAN_POINT ( 'NONE',  ( -23.25000000000000000, 70.05000000001176375, -79.82880978955917328 ) ) ;
#67528=EDGE_CURVE ( 'NONE', #160733, #29906, #177875, .T. ) ;
#67535=CARTESIAN_POINT ( 'NONE',  ( -18.50000000000000000, 66.85000000001203091, -114.7731074845243739 ) ) ;
#67536=EDGE_LOOP ( 'NONE', ( #44610, #74553, #192252 ) ) ;
#67544=LINE ( 'NONE', #29741, #140770 ) ;
#67581=EDGE_CURVE ( 'NONE', #39176, #200766, #107127, .T. ) ;
#67637=CIRCLE ( 'NONE', #55138, 0.1000000000000028644 ) ;
#67643=CIRCLE ( 'NONE', #142636, 0.1000000000000028644 ) ;
#67661=CYLINDRICAL_SURFACE ( 'NONE', #206098, 0.09999999999999939493 ) ;
#67681=EDGE_CURVE ( 'NONE', #9869, #171947, #28049, .T. ) ;
#67717=CARTESIAN_POINT ( 'NONE',  ( -21.05000000000000071, 77.85102823015273543, -91.36919421510179973 ) ) ;
#67730=ORIENTED_EDGE ( 'NONE', *, *, #82554, .F. ) ;
#67737=ORIENTED_EDGE ( 'NONE', *, *, #84312, .F. ) ;
#67740=VECTOR ( 'NONE', #103855, 1000.000000000000000 ) ;
#67760=AXIS2_PLACEMENT_3D ( 'NONE', #2098, #25545, #26845 ) ;
#67845=ORIENTED_EDGE ( 'NONE', *, *, #123725, .F. ) ;
#67901=CARTESIAN_POINT ( 'NONE',  ( 18.39999999999999858, 85.60000000001166143, -62.92291809330219365 ) ) ;
#67922=CARTESIAN_POINT ( 'NONE',  ( 23.15000000000000213, 84.59626168225486254, -93.57297996737396772 ) ) ;
#67934=CARTESIAN_POINT ( 'NONE',  ( -20.85000000000000142, 65.66751761918648356, -63.92826094061123143 ) ) ;
#67996=DIRECTION ( 'NONE',  ( 1.000000000000000000, -0.000000000000000000, 0.000000000000000000 ) ) ;
#68025=ORIENTED_EDGE ( 'NONE', *, *, #35593, .T. ) ;
#68051=CARTESIAN_POINT ( 'NONE',  ( 20.94999999999999929, 74.16465844978745281, -91.46795619196133487 ) ) ;
#68054=ORIENTED_EDGE ( 'NONE', *, *, #13530, .T. ) ;
#68066=CARTESIAN_POINT ( 'NONE',  ( 18.59999999999999076, 69.55000000001187743, -93.00608031408432907 ) ) ;
#68110=ADVANCED_FACE ( 'NONE', ( #147549 ), #44605, .T. ) ;
#68111=ORIENTED_EDGE ( 'NONE', *, *, #112067, .F. ) ;
#68125=ORIENTED_EDGE ( 'NONE', *, *, #69466, .F. ) ;
#68131=VECTOR ( 'NONE', #240252, 1000.000000000000000 ) ;
#68137=DIRECTION ( 'NONE',  ( -0.000000000000000000, -6.982962677686266711E-15, 1.000000000000000000 ) ) ;
#68140=ORIENTED_EDGE ( 'NONE', *, *, #4037, .T. ) ;
#68155=DIRECTION ( 'NONE',  ( -1.000000000000000000, 0.000000000000000000, -0.000000000000000000 ) ) ;
#68172=CARTESIAN_POINT ( 'NONE',  ( -21.14999999999999858, 64.25000000001195133, -102.9231074845243938 ) ) ;
#68244=CARTESIAN_POINT ( 'NONE',  ( -20.54999999999999716, 76.00000000001170974, -69.52310748452431710 ) ) ;
#68277=DIRECTION ( 'NONE',  ( 1.000000000000000000, 0.000000000000000000, 0.000000000000000000 ) ) ;
#68281=ADVANCED_FACE ( 'NONE', ( #97809 ), #2578, .T. ) ;
#68282=ADVANCED_FACE ( 'NONE', ( #160415 ), #139524, .T. ) ;
#68316=DIRECTION ( 'NONE',  ( 1.000000000000000000, 0.000000000000000000, 0.000000000000000000 ) ) ;
#68329=CARTESIAN_POINT ( 'NONE',  ( 20.94999999999999929, 76.00000000001170974, -69.52310748452431710 ) ) ;
#68339=EDGE_CURVE ( 'NONE', #113549, #223315, #157425, .T. ) ;
#68348=VERTEX_POINT ( 'NONE', #221614 ) ;
#68373=DIRECTION ( 'NONE',  ( 0.7071067811865474617, -0.7071067811865474617, -4.937700262164531476E-15 ) ) ;
#68379=CYLINDRICAL_SURFACE ( 'NONE', #80819, 7.900000000000003908 ) ;
#68413=ADVANCED_FACE ( 'NONE', ( #58690 ), #138229, .T. ) ;
#68422=DIRECTION ( 'NONE',  ( 0.000000000000000000, 0.000000000000000000, 1.000000000000000000 ) ) ;
#68424=CIRCLE ( 'NONE', #76791, 0.1000000000000028644 ) ;
#68459=B_SPLINE_CURVE_WITH_KNOTS ( 'NONE', 3,
 ( #10252, #246290, #66365, #25962, #87185, #229298, #48077, #28573 ),
 .UNSPECIFIED., .F., .F.,
 ( 4, 2, 2, 4 ),
 ( 0.000000000000000000, 6.534141206310559820E-05, 0.0001306828241262111964, 0.0002613656482524725371 ),
 .UNSPECIFIED. ) ;
#68476=ORIENTED_EDGE ( 'NONE', *, *, #166418, .T. ) ;
#68503=ORIENTED_EDGE ( 'NONE', *, *, #238983, .T. ) ;
#68511=CARTESIAN_POINT ( 'NONE',  ( -20.85000000000000142, 87.65000000001172964, -72.42310748452422331 ) ) ;
#68536=ORIENTED_EDGE ( 'NONE', *, *, #123236, .F. ) ;
#68537=AXIS2_PLACEMENT_3D ( 'NONE', #236734, #78928, #176797 ) ;
#68555=CARTESIAN_POINT ( 'NONE',  ( 22.48660254037843131, 64.25000000001193712, -103.0731074845243853 ) ) ;
#68556=AXIS2_PLACEMENT_3D ( 'NONE', #57617, #56328, #180166 ) ;
#68565=ORIENTED_EDGE ( 'NONE', *, *, #113471, .T. ) ;
#68589=DIRECTION ( 'NONE',  ( 0.000000000000000000, 0.000000000000000000, -1.000000000000000000 ) ) ;
#68612=AXIS2_PLACEMENT_3D ( 'NONE', #90304, #169909, #249407 ) ;
#68613=DIRECTION ( 'NONE',  ( 0.000000000000000000, 0.000000000000000000, 1.000000000000000000 ) ) ;
#68714=ORIENTED_EDGE ( 'NONE', *, *, #106530, .T. ) ;
#68722=EDGE_LOOP ( 'NONE', ( #133920, #255515, #99528, #26154, #221656 ) ) ;
#68734=DIRECTION ( 'NONE',  ( 0.000000000000000000, 0.000000000000000000, -1.000000000000000000 ) ) ;
#68770=AXIS2_PLACEMENT_3D ( 'NONE', #101368, #19320, #201797 ) ;
#68823=DIRECTION ( 'NONE',  ( 0.7071067811865475727, -0.7071067811865475727, -4.937700262164531476E-15 ) ) ;
#68862=CIRCLE ( 'NONE', #168840, 0.1000000000000028644 ) ;
#68873=CARTESIAN_POINT ( 'NONE',  ( -21.05000000000000071, 75.74389420791972327, -103.0580039261966050 ) ) ;
#68948=ORIENTED_EDGE ( 'NONE', *, *, #63288, .F. ) ;
#68959=CARTESIAN_POINT ( 'NONE',  ( 20.95566103547454517, 65.38175234906483979, -95.39126729154378381 ) ) ;
#68973=CARTESIAN_POINT ( 'NONE',  ( -20.54999999999999716, 68.85000000001186038, -90.67310748452435121 ) ) ;
#69000=CARTESIAN_POINT ( 'NONE',  ( -20.94999999999999929, 69.15387683765909799, -65.78538121767449809 ) ) ;
#69022=AXIS2_PLACEMENT_3D ( 'NONE', #74711, #56364, #52519 ) ;
#69035=CARTESIAN_POINT ( 'NONE',  ( -20.54999999999999716, 76.00000000001170974, -69.52310748452431710 ) ) ;
#69049=B_SPLINE_CURVE_WITH_KNOTS ( 'NONE', 3,
 ( #41687, #161643, #1235, #182482, #203316, #222863, #44247, #24702, #104189, #111933, #8961, #208469, #188884, #152355, #250143, #151049, #148478, #186323, #68959, #48081, #106762, #168081 ),
 .UNSPECIFIED., .F., .F.,
 ( 4, 3, 3, 3, 3, 3, 3, 4 ),
 ( 0.000000000000000000, 7.307836821080529321E-06, 4.161455748548037811E-05, 7.576591810648371868E-05, 0.0001098090429817550825, 0.0001438003617351050036, 0.0001777914035423659516, 0.0002117966137403016797 ),
 .UNSPECIFIED. ) ;
#69062=ORIENTED_EDGE ( 'NONE', *, *, #50886, .T. ) ;
#69080=AXIS2_PLACEMENT_3D ( 'NONE', #124510, #129638, #89219 ) ;
#69099=DIRECTION ( 'NONE',  ( -1.000000000000000000, -0.000000000000000000, -0.000000000000000000 ) ) ;
#69106=ORIENTED_EDGE ( 'NONE', *, *, #212081, .T. ) ;
#69107=CIRCLE ( 'NONE', #27439, 0.1000000000000028644 ) ;
#69154=CARTESIAN_POINT ( 'NONE',  ( -22.50000000000000000, 64.35000000001195986, -103.0231074845244024 ) ) ;
#69155=DIRECTION ( 'NONE',  ( -1.000000000000000000, 0.000000000000000000, -0.000000000000000000 ) ) ;
#69214=DIRECTION ( 'NONE',  ( 0.000000000000000000, 0.000000000000000000, 1.000000000000000000 ) ) ;
#69215=EDGE_CURVE ( 'NONE', #236062, #30387, #130578, .T. ) ;
#69222=EDGE_CURVE ( 'NONE', #116663, #202146, #105793, .T. ) ;
#69228=EDGE_CURVE ( 'NONE', #75286, #222763, #39208, .T. ) ;
#69241=CARTESIAN_POINT ( 'NONE',  ( -20.91682497891422798, 65.67736539654923433, -63.96251168765719797 ) ) ;
#69243=CARTESIAN_POINT ( 'NONE',  ( -18.39999999999999858, 85.50000000001189449, -95.99103808782457747 ) ) ;
#69248=DIRECTION ( 'NONE',  ( -2.952720810173289112E-16, -1.000000000000000000, -6.982962677686266711E-15 ) ) ;
#69254=FACE_OUTER_BOUND ( 'NONE', #44625, .T. ) ;
#69272=EDGE_CURVE ( 'NONE', #59500, #194022, #128724, .T. ) ;
#69282=CARTESIAN_POINT ( 'NONE',  ( 20.95512820512820440, 67.12384868372375024, -90.87310748452436826 ) ) ;
#69285=CARTESIAN_POINT ( 'NONE',  ( 21.05000000000000071, 65.27628289530437655, -95.35819391543677170 ) ) ;
#69342=CARTESIAN_POINT ( 'NONE',  ( 20.94999999999999574, 65.52661458509899717, -95.44445302027583011 ) ) ;
#69348=VECTOR ( 'NONE', #232980, 1000.000000000000000 ) ;
#69355=ORIENTED_EDGE ( 'NONE', *, *, #154632, .T. ) ;
#69365=CIRCLE ( 'NONE', #56827, 0.1000000000000028644 ) ;
#69403=CARTESIAN_POINT ( 'NONE',  ( 20.94999999999999929, 71.00000000001180922, -81.42837350343744163 ) ) ;
#69439=CIRCLE ( 'NONE', #148538, 0.09999999999999939493 ) ;
#69448=EDGE_CURVE ( 'NONE', #64660, #49254, #85115, .T. ) ;
#69455=DIRECTION ( 'NONE',  ( 3.265361837132813093E-16, 1.000000000000000000, 6.982962677686266711E-15 ) ) ;
#69461=CARTESIAN_POINT ( 'NONE',  ( -23.15000000000000213, 76.00000000001170974, -69.52310748452431710 ) ) ;
#69466=EDGE_CURVE ( 'NONE', #108089, #156778, #210072, .T. ) ;
#69469=AXIS2_PLACEMENT_3D ( 'NONE', #163345, #180337, #38260 ) ;
#69474=EDGE_LOOP ( 'NONE', ( #189758, #240484, #201227, #132672 ) ) ;
#69516=EDGE_LOOP ( 'NONE', ( #114174, #65453, #218884, #103061 ) ) ;
#69520=CARTESIAN_POINT ( 'NONE',  ( 20.19326291201646129, 65.84393901210796685, -95.26124567692161804 ) ) ;
#69528=CARTESIAN_POINT ( 'NONE',  ( 21.05000000000000071, 75.90220970870277029, -109.2809220950058346 ) ) ;
#69539=PLANE ( 'NONE',  #237615 ) ;
#69559=DIRECTION ( 'NONE',  ( 0.000000000000000000, 0.000000000000000000, 1.000000000000000000 ) ) ;
#69569=DIRECTION ( 'NONE',  ( 0.000000000000000000, -6.454785026890510900E-15, 1.000000000000000000 ) ) ;
#69612=ORIENTED_EDGE ( 'NONE', *, *, #170920, .T. ) ;
#69671=CARTESIAN_POINT ( 'NONE',  ( -22.50000000000000000, 75.90000000001202807, -114.6726782920691221 ) ) ;
#69675=AXIS2_PLACEMENT_3D ( 'NONE', #20472, #176992, #221200 ) ;
#69679=DIRECTION ( 'NONE',  ( 0.000000000000000000, 0.000000000000000000, 1.000000000000000000 ) ) ;
#69681=CARTESIAN_POINT ( 'NONE',  ( -23.25000000000000000, 76.00000000001170974, -69.52310748452431710 ) ) ;
#69698=VERTEX_POINT ( 'NONE', #129012 ) ;
#69702=DIRECTION ( 'NONE',  ( -1.000000000000000000, 0.000000000000000000, -0.000000000000000000 ) ) ;
#69729=ORIENTED_EDGE ( 'NONE', *, *, #35803, .F. ) ;
#69749=AXIS2_PLACEMENT_3D ( 'NONE', #199089, #76566, #257716 ) ;
#69769=DIRECTION ( 'NONE',  ( -2.342056488767301376E-15, 0.1350103645451974088, -0.9908441862701587999 ) ) ;
#69779=DIRECTION ( 'NONE',  ( 0.000000000000000000, -0.4999999999999689138, 0.8660254037844565822 ) ) ;
#69791=DIRECTION ( 'NONE',  ( -0.000000000000000000, 0.8660254037844377084, 0.5000000000000016653 ) ) ;
#69830=EDGE_CURVE ( 'NONE', #208704, #59112, #66362, .T. ) ;
#69833=AXIS2_PLACEMENT_3D ( 'NONE', #128412, #207968, #89269 ) ;
#69848=CARTESIAN_POINT ( 'NONE',  ( -20.94999999999999929, 76.00000000001173817, -73.52310748452431710 ) ) ;
#69861=AXIS2_PLACEMENT_3D ( 'NONE', #186186, #128782, #242289 ) ;
#69888=DIRECTION ( 'NONE',  ( 2.952720810173289112E-16, 1.000000000000000000, 6.938893903907222067E-15 ) ) ;
#69897=CIRCLE ( 'NONE', #215600, 0.5000000000000004441 ) ;
#69903=VECTOR ( 'NONE', #34826, 1000.000000000000000 ) ;
#69914=DIRECTION ( 'NONE',  ( 0.000000000000000000, 0.000000000000000000, 1.000000000000000000 ) ) ;
#69922=DIRECTION ( 'NONE',  ( -4.408576920032447355E-17, -0.1350103645451945777, 0.9908441862701589109 ) ) ;
#69929=CARTESIAN_POINT ( 'NONE',  ( 18.54271179734060127, 85.62408429011053101, -62.78214263182413646 ) ) ;
#69932=EDGE_CURVE ( 'NONE', #97655, #99793, #197758, .T. ) ;
#69955=CIRCLE ( 'NONE', #207328, 3.900000000000000799 ) ;
#69963=EDGE_CURVE ( 'NONE', #201799, #69997, #160384, .T. ) ;
#69997=VERTEX_POINT ( 'NONE', #47839 ) ;
#69998=DIRECTION ( 'NONE',  ( 1.000000000000000000, 0.000000000000000000, 0.000000000000000000 ) ) ;
#70000=TOROIDAL_SURFACE ( 'NONE', #86510, 0.6000000000000009770, 0.1000000000000000056 ) ;
#70008=ORIENTED_EDGE ( 'NONE', *, *, #16127, .F. ) ;
#70019=DIRECTION ( 'NONE',  ( -1.000000000000000000, -0.000000000000000000, -0.000000000000000000 ) ) ;
#70036=FACE_OUTER_BOUND ( 'NONE', #156452, .T. ) ;
#70040=DIRECTION ( 'NONE',  ( 1.000000000000000000, 0.000000000000000000, 0.000000000000000000 ) ) ;
#70060=EDGE_CURVE ( 'NONE', #213743, #158833, #39583, .T. ) ;
#70082=DIRECTION ( 'NONE',  ( -0.7071067811865474617, 0.7071067811865474617, 4.937700262164531476E-15 ) ) ;
#70104=ORIENTED_EDGE ( 'NONE', *, *, #129670, .F. ) ;
#70121=CARTESIAN_POINT ( 'NONE',  ( -23.15000000000000213, 76.00000000001172396, -71.62310748452431142 ) ) ;
#70126=EDGE_CURVE ( 'NONE', #145746, #278, #127215, .T. ) ;
#70179=DIRECTION ( 'NONE',  ( 1.000000000000000000, -2.952720810173289112E-16, -2.061873921506763405E-30 ) ) ;
#70182=DIRECTION ( 'NONE',  ( 0.000000000000000000, -6.938893903907222067E-15, 1.000000000000000000 ) ) ;
#70194=ADVANCED_FACE ( 'NONE', ( #54269 ), #239647, .F. ) ;
#70210=ORIENTED_EDGE ( 'NONE', *, *, #227679, .T. ) ;
#70219=AXIS2_PLACEMENT_3D ( 'NONE', #125273, #48295, #185241 ) ;
#70222=DIRECTION ( 'NONE',  ( 0.000000000000000000, 0.000000000000000000, -1.000000000000000000 ) ) ;
#70224=DIRECTION ( 'NONE',  ( 0.000000000000000000, 6.938893903907229955E-15, -1.000000000000000000 ) ) ;
#70226=EDGE_CURVE ( 'NONE', #174804, #56502, #92121, .T. ) ;
#70244=CARTESIAN_POINT ( 'NONE',  ( 18.50000000000000000, 86.35479209693714608, -75.76656650145046967 ) ) ;
#70275=ORIENTED_EDGE ( 'NONE', *, *, #250133, .F. ) ;
#70284=LINE ( 'NONE', #230622, #99695 ) ;
#70313=DIRECTION ( 'NONE',  ( 0.000000000000000000, 6.982962677686266711E-15, -1.000000000000000000 ) ) ;
#70343=DIRECTION ( 'NONE',  ( 1.000000000000000000, 0.000000000000000000, 0.000000000000000000 ) ) ;
#70349=CARTESIAN_POINT ( 'NONE',  ( 22.45305468355011058, 76.10085836911173374, -114.7726746080140288 ) ) ;
#70352=EDGE_LOOP ( 'NONE', ( #23029, #165674, #149243, #143538 ) ) ;
#70368=DIRECTION ( 'NONE',  ( 0.000000000000000000, -6.982962677686266711E-15, 1.000000000000000000 ) ) ;
#70373=VERTEX_POINT ( 'NONE', #118108 ) ;
#70378=EDGE_CURVE ( 'NONE', #101254, #44131, #122946, .T. ) ;
#70409=AXIS2_PLACEMENT_3D ( 'NONE', #48271, #192931, #30024 ) ;
#70423=CARTESIAN_POINT ( 'NONE',  ( 18.59999999999999432, 77.16270174994990327, -94.92310748452430857 ) ) ;
#70431=ORIENTED_EDGE ( 'NONE', *, *, #194607, .F. ) ;
#70444=AXIS2_PLACEMENT_3D ( 'NONE', #244094, #9338, #4199 ) ;
#70493=CARTESIAN_POINT ( 'NONE',  ( 18.59999999999998366, 76.00000000001170974, -69.52310748452431710 ) ) ;
#70509=AXIS2_PLACEMENT_3D ( 'NONE', #84280, #45214, #163874 ) ;
#70523=AXIS2_PLACEMENT_3D ( 'NONE', #163622, #4525, #162350 ) ;
#70532=EDGE_LOOP ( 'NONE', ( #1906, #75531, #68111, #208930 ) ) ;
#70541=CARTESIAN_POINT ( 'NONE',  ( -18.40000000000000568, 85.50000000001192291, -96.02374538734412113 ) ) ;
#70547=EDGE_CURVE ( 'NONE', #40998, #208239, #53400, .T. ) ;
#70551=AXIS2_PLACEMENT_3D ( 'NONE', #171473, #209270, #136126 ) ;
#70579=TOROIDAL_SURFACE ( 'NONE', #224648, 0.2000000000000000111, 0.1000000000000000056 ) ;
#70582=LINE ( 'NONE', #11886, #26157 ) ;
#70597=CARTESIAN_POINT ( 'NONE',  ( -23.15000000000000213, 76.00000000001172396, -71.52310748452431710 ) ) ;
#70618=CARTESIAN_POINT ( 'NONE',  ( -23.25000000000000000, 76.00000000001197975, -107.0731074845243143 ) ) ;
#70628=EDGE_CURVE ( 'NONE', #120433, #129506, #23185, .T. ) ;
#70649=CARTESIAN_POINT ( 'NONE',  ( 20.94999999999999929, 71.14953271029224879, -90.98884007552265984 ) ) ;
#70664=AXIS2_PLACEMENT_3D ( 'NONE', #242158, #24431, #162641 ) ;
#70676=VECTOR ( 'NONE', #237206, 1000.000000000000000 ) ;
#70689=DIRECTION ( 'NONE',  ( -0.7071067811865474617, 0.7071067811865474617, 5.142139384388980375E-15 ) ) ;
#70710=ORIENTED_EDGE ( 'NONE', *, *, #125621, .T. ) ;
#70727=ORIENTED_EDGE ( 'NONE', *, *, #171023, .F. ) ;
#70731=ORIENTED_EDGE ( 'NONE', *, *, #217665, .T. ) ;
#70823=CARTESIAN_POINT ( 'NONE',  ( -21.65000000000000213, 68.29142135624915966, -90.67310748452436542 ) ) ;
#70825=EDGE_LOOP ( 'NONE', ( #55930, #100609, #110248, #56515 ) ) ;
#70859=DIRECTION ( 'NONE',  ( 0.000000000000000000, -1.000000000000000000, 0.000000000000000000 ) ) ;
#70872=VERTEX_POINT ( 'NONE', #12005 ) ;
#70873=AXIS2_PLACEMENT_3D ( 'NONE', #27251, #247546, #188851 ) ;
#70909=DIRECTION ( 'NONE',  ( -7.304098846218134667E-16, 1.000000000000000000, 6.982962677686267499E-15 ) ) ;
#70912=ORIENTED_EDGE ( 'NONE', *, *, #194834, .T. ) ;
#70970=CIRCLE ( 'NONE', #66840, 2.100000000000004530 ) ;
#70984=DIRECTION ( 'NONE',  ( 0.000000000000000000, 0.000000000000000000, -1.000000000000000000 ) ) ;
#71007=ORIENTED_EDGE ( 'NONE', *, *, #54517, .F. ) ;
#71020=ORIENTED_EDGE ( 'NONE', *, *, #141925, .T. ) ;
#71033=CARTESIAN_POINT ( 'NONE',  ( -18.55807992284872299, 65.67101464000481315, -63.94043916224792667 ) ) ;
#71048=DIRECTION ( 'NONE',  ( 0.000000000000000000, -1.000000000000000000, -7.272083257015735086E-15 ) ) ;
#71057=CARTESIAN_POINT ( 'NONE',  ( 20.85000000000000142, 77.83585931145526615, -58.01866831572577610 ) ) ;
#71063=AXIS2_PLACEMENT_3D ( 'NONE', #114123, #211969, #152009 ) ;
#71108=CIRCLE ( 'NONE', #237692, 0.1000000000000028644 ) ;
#71164=FACE_OUTER_BOUND ( 'NONE', #168299, .T. ) ;
#71171=CARTESIAN_POINT ( 'NONE',  ( -21.14999999999999858, 76.10000000001203091, -114.6726782920691079 ) ) ;
#71179=ADVANCED_FACE ( 'NONE', ( #225208 ), #166574, .T. ) ;
#71183=DIRECTION ( 'NONE',  ( -0.000000000000000000, 0.9887567792719327286, 0.1495327102803745423 ) ) ;
#71236=ADVANCED_FACE ( 'NONE', ( #70036 ), #181749, .T. ) ;
#71239=EDGE_LOOP ( 'NONE', ( #106216, #134075 ) ) ;
#71244=ORIENTED_EDGE ( 'NONE', *, *, #202457, .T. ) ;
#71281=CARTESIAN_POINT ( 'NONE',  ( 21.14999999999999858, 64.35000000001195986, -102.9231074845243938 ) ) ;
#71304=AXIS2_PLACEMENT_3D ( 'NONE', #211958, #230219, #68589 ) ;
#71318=ORIENTED_EDGE ( 'NONE', *, *, #178063, .T. ) ;
#71328=DIRECTION ( 'NONE',  ( 0.000000000000000000, 0.000000000000000000, 1.000000000000000000 ) ) ;
#71365=EDGE_LOOP ( 'NONE', ( #90038, #143693, #241980 ) ) ;
#71366=EDGE_CURVE ( 'NONE', #114547, #50189, #52734, .T. ) ;
#71369=VERTEX_POINT ( 'NONE', #80238 ) ;
#71380=ORIENTED_EDGE ( 'NONE', *, *, #45155, .F. ) ;
#71384=EDGE_LOOP ( 'NONE', ( #20776, #240758, #1365 ) ) ;
#71412=EDGE_CURVE ( 'NONE', #111684, #20030, #231837, .T. ) ;
#71420=CIRCLE ( 'NONE', #167287, 0.1000000000000052097 ) ;
#71479=VERTEX_POINT ( 'NONE', #202791 ) ;
#71498=CIRCLE ( 'NONE', #213111, 0.2000000000000057288 ) ;
#71499=AXIS2_PLACEMENT_3D ( 'NONE', #228257, #246515, #130421 ) ;
#71544=CYLINDRICAL_SURFACE ( 'NONE', #54127, 0.1000000000000028644 ) ;
#71565=DIRECTION ( 'NONE',  ( 2.952720810173289605E-16, 1.000000000000000000, 7.086529944415894657E-15 ) ) ;
#71577=VERTEX_POINT ( 'NONE', #111405 ) ;
#71589=LINE ( 'NONE', #49433, #226777 ) ;
#71619=CARTESIAN_POINT ( 'NONE',  ( -21.05000000000000071, 76.25610579210417939, -103.0580039261966050 ) ) ;
#71633=CARTESIAN_POINT ( 'NONE',  ( 18.59999999999999076, 74.16465844978745281, -91.46795619196133487 ) ) ;
#71636=DIRECTION ( 'NONE',  ( -1.000000000000000000, 0.000000000000000000, 0.000000000000000000 ) ) ;
#71653=LINE ( 'NONE', #136727, #92828 ) ;
#71686=VERTEX_POINT ( 'NONE', #188368 ) ;
#71689=DIRECTION ( 'NONE',  ( 1.000000000000000000, -0.000000000000000000, 0.000000000000000000 ) ) ;
#71697=ORIENTED_EDGE ( 'NONE', *, *, #128426, .F. ) ;
#71706=VERTEX_POINT ( 'NONE', #227481 ) ;
#71741=ADVANCED_FACE ( 'NONE', ( #150536 ), #95678, .F. ) ;
#71761=ORIENTED_EDGE ( 'NONE', *, *, #160406, .F. ) ;
#71774=FACE_OUTER_BOUND ( 'NONE', #120124, .T. ) ;
#71780=DIRECTION ( 'NONE',  ( -2.252264143451594314E-15, 0.1298341882520054891, 0.9915357197604850459 ) ) ;
#71795=CARTESIAN_POINT ( 'NONE',  ( 23.14999999999999858, 76.00000000001170974, -69.52310748452431710 ) ) ;
#71849=CARTESIAN_POINT ( 'NONE',  ( -21.05000000000000071, 87.48912529308798014, -100.0231074845242318 ) ) ;
#71856=CARTESIAN_POINT ( 'NONE',  ( 21.05000000000000071, 76.00000000001170974, -69.52310748452431710 ) ) ;
#71866=CARTESIAN_POINT ( 'NONE',  ( -23.25000000000000000, 73.40000000001185754, -89.79848556176223440 ) ) ;
#71880=CARTESIAN_POINT ( 'NONE',  ( 18.56308993302888055, 65.61930884468753788, -78.28388484558554694 ) ) ;
#71898=ORIENTED_EDGE ( 'NONE', *, *, #93179, .T. ) ;
#71913=CARTESIAN_POINT ( 'NONE',  ( 22.39999999999999858, 68.20922040163857503, -103.1231074845243540 ) ) ;
#71932=CARTESIAN_POINT ( 'NONE',  ( 21.05000000000000071, 67.22371735104076151, -94.53551510600442498 ) ) ;
#71939=ORIENTED_EDGE ( 'NONE', *, *, #152785, .F. ) ;
#71977=CARTESIAN_POINT ( 'NONE',  ( 20.95512820512820085, 65.37615131630002452, -95.35819391543677170 ) ) ;
#71989=AXIS2_PLACEMENT_3D ( 'NONE', #204339, #15149, #94667 ) ;
#71990=ORIENTED_EDGE ( 'NONE', *, *, #110712, .F. ) ;
#72016=CARTESIAN_POINT ( 'NONE',  ( 18.59999999999999076, 69.45000000001181206, -81.77310748452434552 ) ) ;
#72024=DIRECTION ( 'NONE',  ( 0.000000000000000000, 0.000000000000000000, 1.000000000000000000 ) ) ;
#72042=EDGE_LOOP ( 'NONE', ( #65757, #93715, #176719, #189250 ) ) ;
#72055=DIRECTION ( 'NONE',  ( 1.000000000000000000, -7.304098846218134667E-16, -4.639676173203993355E-30 ) ) ;
#72101=VERTEX_POINT ( 'NONE', #251879 ) ;
#72115=CARTESIAN_POINT ( 'NONE',  ( -20.94999999999999929, 87.39257802171759693, -99.94915790469229933 ) ) ;
#72197=ORIENTED_EDGE ( 'NONE', *, *, #143324, .T. ) ;
#72226=DIRECTION ( 'NONE',  ( 1.000000000000000000, -0.000000000000000000, 0.000000000000000000 ) ) ;
#72246=AXIS2_PLACEMENT_3D ( 'NONE', #7104, #218765, #5810 ) ;
#72260=ORIENTED_EDGE ( 'NONE', *, *, #162043, .F. ) ;
#72274=AXIS2_PLACEMENT_3D ( 'NONE', #199276, #158885, #161446 ) ;
#72276=EDGE_CURVE ( 'NONE', #256668, #252315, #98297, .T. ) ;
#72299=FACE_OUTER_BOUND ( 'NONE', #35376, .T. ) ;
#72304=LINE ( 'NONE', #46287, #136413 ) ;
#72332=DIRECTION ( 'NONE',  ( 1.000000000000000000, 0.000000000000000000, 0.000000000000000000 ) ) ;
#72342=AXIS2_PLACEMENT_3D ( 'NONE', #78410, #200938, #57555 ) ;
#72347=ORIENTED_EDGE ( 'NONE', *, *, #239019, .T. ) ;
#72377=CARTESIAN_POINT ( 'NONE',  ( -20.64999999999999858, 76.00000000001170974, -69.52310748452431710 ) ) ;
#72382=CIRCLE ( 'NONE', #184780, 0.1000000000000028644 ) ;
#72389=EDGE_LOOP ( 'NONE', ( #96729, #135267, #135666, #90869 ) ) ;
#72400=TOROIDAL_SURFACE ( 'NONE', #197279, 12.97499999999999609, 0.1000000000000000056 ) ;
#72423=B_SPLINE_CURVE_WITH_KNOTS ( 'NONE', 3,
 ( #145983, #187709, #144693, #165573, #245094, #48168, #169452 ),
 .UNSPECIFIED., .F., .F.,
 ( 4, 3, 4 ),
 ( 0.000000000000000000, 0.0007844235214594318627, 0.001767853679404347454 ),
 .UNSPECIFIED. ) ;
#72428=ORIENTED_EDGE ( 'NONE', *, *, #253693, .F. ) ;
#72490=CARTESIAN_POINT ( 'NONE',  ( 18.40000000000000213, 85.50000000001166711, -62.60095763519380796 ) ) ;
#72498=ADVANCED_FACE ( 'NONE', ( #159882 ), #16517, .T. ) ;
#72515=ADVANCED_FACE ( 'NONE', ( #17758 ), #76459, .T. ) ;
#72516=VECTOR ( 'NONE', #11261, 1000.000000000000000 ) ;
#72530=CARTESIAN_POINT ( 'NONE',  ( -18.39999999999999858, 85.50000000001168132, -62.92291809330220786 ) ) ;
#72563=AXIS2_PLACEMENT_3D ( 'NONE', #133208, #154101, #75802 ) ;
#72565=CIRCLE ( 'NONE', #39453, 0.8750000000000007772 ) ;
#72577=ORIENTED_EDGE ( 'NONE', *, *, #253733, .T. ) ;
#72585=DIRECTION ( 'NONE',  ( 0.000000000000000000, 1.000000000000000000, 6.982962677686266711E-15 ) ) ;
#72599=ORIENTED_EDGE ( 'NONE', *, *, #72787, .F. ) ;
#72622=CARTESIAN_POINT ( 'NONE',  ( -23.15000000000000213, 64.35000000001180354, -81.67310748452439384 ) ) ;
#72624=CIRCLE ( 'NONE', #135121, 0.5000000000000004441 ) ;
#72649=VERTEX_POINT ( 'NONE', #224949 ) ;
#72660=AXIS2_PLACEMENT_3D ( 'NONE', #132032, #92894, #134577 ) ;
#72771=AXIS2_PLACEMENT_3D ( 'NONE', #237159, #79340, #158924 ) ;
#72787=EDGE_CURVE ( 'NONE', #191564, #16721, #248545, .T. ) ;
#72880=DIRECTION ( 'NONE',  ( 0.000000000000000000, 0.000000000000000000, 1.000000000000000000 ) ) ;
#72883=EDGE_CURVE ( 'NONE', #221901, #187906, #165351, .T. ) ;
#72901=AXIS2_PLACEMENT_3D ( 'NONE', #208243, #105221, #46564 ) ;
#72977=DIRECTION ( 'NONE',  ( -1.000000000000000000, -0.000000000000000000, -0.000000000000000000 ) ) ;
#72979=VERTEX_POINT ( 'NONE', #141276 ) ;
#73012=EDGE_LOOP ( 'NONE', ( #13586, #78234, #7350, #20148 ) ) ;
#73018=CYLINDRICAL_SURFACE ( 'NONE', #255039, 0.1000000000000026007 ) ;
#73024=CARTESIAN_POINT ( 'NONE',  ( -23.25000000000000000, 87.65000000001172964, -72.62310748452422615 ) ) ;
#73035=CARTESIAN_POINT ( 'NONE',  ( 21.09696443733127325, 65.27599011609339641, -90.78832995747616508 ) ) ;
#73058=ORIENTED_EDGE ( 'NONE', *, *, #202811, .F. ) ;
#73121=AXIS2_PLACEMENT_3D ( 'NONE', #20024, #237766, #196078 ) ;
#73126=DIRECTION ( 'NONE',  ( 1.000000000000000000, -0.000000000000000000, 0.000000000000000000 ) ) ;
#73166=CARTESIAN_POINT ( 'NONE',  ( 23.14999999999999147, 76.00000000001195133, -103.0231074845243171 ) ) ;
#73168=DIRECTION ( 'NONE',  ( 0.000000000000000000, 0.000000000000000000, 1.000000000000000000 ) ) ;
#73169=EDGE_CURVE ( 'NONE', #41677, #169820, #215237, .T. ) ;
#73172=DIRECTION ( 'NONE',  ( -1.000000000000000000, -7.304098846218164250E-16, 4.217023435051628197E-16 ) ) ;
#73177=CIRCLE ( 'NONE', #239550, 0.09999999999999939493 ) ;
#73202=DIRECTION ( 'NONE',  ( 0.000000000000000000, 0.000000000000000000, 1.000000000000000000 ) ) ;
#73213=CARTESIAN_POINT ( 'NONE',  ( -18.50000000000000000, 74.36282728704149747, -91.44095411905230719 ) ) ;
#73256=ORIENTED_EDGE ( 'NONE', *, *, #98166, .T. ) ;
#73279=ORIENTED_EDGE ( 'NONE', *, *, #88844, .T. ) ;
#73286=AXIS2_PLACEMENT_3D ( 'NONE', #180796, #64682, #222446 ) ;
#73320=EDGE_LOOP ( 'NONE', ( #73717, #100503, #45365, #97436 ) ) ;
#73344=DIRECTION ( 'NONE',  ( -0.000000000000000000, 1.000000000000000000, 6.982962677686267499E-15 ) ) ;
#73399=LINE ( 'NONE', #159034, #66640 ) ;
#73417=FACE_OUTER_BOUND ( 'NONE', #28145, .T. ) ;
#73473=DIRECTION ( 'NONE',  ( 0.000000000000000000, 6.982962677686267499E-15, -1.000000000000000000 ) ) ;
#73475=DIRECTION ( 'NONE',  ( -1.000000000000000000, 0.000000000000000000, 0.000000000000000000 ) ) ;
#73501=EDGE_LOOP ( 'NONE', ( #111642, #79221, #52281, #257730 ) ) ;
#73535=ORIENTED_EDGE ( 'NONE', *, *, #32166, .T. ) ;
#73542=CARTESIAN_POINT ( 'NONE',  ( -18.44232395689959247, 85.55228255706151685, -62.68085549971750936 ) ) ;
#73574=CARTESIAN_POINT ( 'NONE',  ( 20.94999999999999929, 65.70711192142346135, -64.06510546851221477 ) ) ;
#73580=CARTESIAN_POINT ( 'NONE',  ( -18.50000000000000000, 77.63717271298224887, -91.44095411905229298 ) ) ;
#73600=AXIS2_PLACEMENT_3D ( 'NONE', #57921, #137462, #136157 ) ;
#73610=CARTESIAN_POINT ( 'NONE',  ( -18.56579813702276027, 65.66974365629646115, -63.93601455626048136 ) ) ;
#73631=AXIS2_PLACEMENT_3D ( 'NONE', #198607, #1684, #19998 ) ;
#73657=ORIENTED_EDGE ( 'NONE', *, *, #184695, .F. ) ;
#73667=DIRECTION ( 'NONE',  ( 1.000000000000000000, 0.000000000000000000, 0.000000000000000000 ) ) ;
#73670=CARTESIAN_POINT ( 'NONE',  ( 18.59999999999999076, 65.79142135624910281, -81.67310748452439384 ) ) ;
#73717=ORIENTED_EDGE ( 'NONE', *, *, #215843, .T. ) ;
#73721=DIRECTION ( 'NONE',  ( -0.000000000000000000, -6.982962677686266711E-15, 1.000000000000000000 ) ) ;
#73729=AXIS2_PLACEMENT_3D ( 'NONE', #118399, #14183, #96242 ) ;
#73737=CARTESIAN_POINT ( 'NONE',  ( -20.64999999999999858, 84.73084112150711178, -79.12118220350858167 ) ) ;
#73744=DIRECTION ( 'NONE',  ( 0.000000000000000000, 0.000000000000000000, -1.000000000000000000 ) ) ;
#73747=CARTESIAN_POINT ( 'NONE',  ( -23.15000000000000213, 71.85000000001203091, -114.7731074845243313 ) ) ;
#73763=EDGE_CURVE ( 'NONE', #246499, #226147, #67544, .T. ) ;
#73770=CARTESIAN_POINT ( 'NONE',  ( -20.94999999999999929, 76.00000000001170974, -69.52310748452431710 ) ) ;
#73780=B_SPLINE_CURVE_WITH_KNOTS ( 'NONE', 3,
 ( #116429, #78563, #158157, #40767, #120313, #21201 ),
 .UNSPECIFIED., .F., .F.,
 ( 4, 2, 4 ),
 ( 0.000000000000000000, 0.0001568709654583424031, 0.0003137419309166848062 ),
 .UNSPECIFIED. ) ;
#73785=DIRECTION ( 'NONE',  ( 1.000000000000000000, 0.000000000000000000, 0.000000000000000000 ) ) ;
#73787=CARTESIAN_POINT ( 'NONE',  ( 18.39999999999999858, 85.50000000001166711, -62.92291809330219365 ) ) ;
#73875=ADVANCED_FACE ( 'NONE', ( #12738 ), #51809, .T. ) ;
#73893=DIRECTION ( 'NONE',  ( 0.000000000000000000, -7.086529944415894657E-15, 1.000000000000000000 ) ) ;
#73904=ORIENTED_EDGE ( 'NONE', *, *, #168008, .T. ) ;
#73933=DIRECTION ( 'NONE',  ( -0.000000000000000000, -6.982962677686266711E-15, 1.000000000000000000 ) ) ;
#73953=CARTESIAN_POINT ( 'NONE',  ( -18.59999999999999787, 77.83585931145526615, -58.01866831572577610 ) ) ;
#73956=CYLINDRICAL_SURFACE ( 'NONE', #98876, 11.74999999999999645 ) ;
#73997=EDGE_LOOP ( 'NONE', ( #143488, #18095, #191936 ) ) ;
#74032=CYLINDRICAL_SURFACE ( 'NONE', #204363, 0.09999999999999939493 ) ;
#74085=DIRECTION ( 'NONE',  ( -1.000000000000000000, -0.000000000000000000, -0.000000000000000000 ) ) ;
#74106=CIRCLE ( 'NONE', #219799, 0.3999999999999975797 ) ;
#74124=DIRECTION ( 'NONE',  ( 0.000000000000000000, 0.4930308989875575865, 0.8700118002898125091 ) ) ;
#74147=VERTEX_POINT ( 'NONE', #51174 ) ;
#74197=VERTEX_POINT ( 'NONE', #43069 ) ;
#74212=ADVANCED_FACE ( 'NONE', ( #44360 ), #47891, .T. ) ;
#74222=VERTEX_POINT ( 'NONE', #246402 ) ;
#74233=TOROIDAL_SURFACE ( 'NONE', #219943, 0.4000000000000005773, 0.1000000000000000056 ) ;
#74234=LINE ( 'NONE', #153786, #185488 ) ;
#74239=ADVANCED_FACE ( 'NONE', ( #207291 ), #78396, .T. ) ;
#74242=EDGE_LOOP ( 'NONE', ( #40290, #90827, #1043, #147618 ) ) ;
#74243=LINE ( 'NONE', #172061, #76284 ) ;
#74256=CARTESIAN_POINT ( 'NONE',  ( -18.59999999999999787, 72.08710075277841156, -91.54128451151336776 ) ) ;
#74260=DIRECTION ( 'NONE',  ( 1.000000000000000000, 7.304098846218135653E-16, 5.100424963727256530E-30 ) ) ;
#74277=ORIENTED_EDGE ( 'NONE', *, *, #11566, .T. ) ;
#74348=EDGE_LOOP ( 'NONE', ( #28630, #196534, #22042, #179868 ) ) ;
#74363=CYLINDRICAL_SURFACE ( 'NONE', #75049, 0.1000000000000028644 ) ;
#74374=DIRECTION ( 'NONE',  ( -1.000000000000000000, -0.000000000000000000, -0.000000000000000000 ) ) ;
#74387=DIRECTION ( 'NONE',  ( 0.000000000000000000, 6.982962677686266711E-15, -1.000000000000000000 ) ) ;
#74401=CARTESIAN_POINT ( 'NONE',  ( -18.50000000000000000, 66.85000000001180354, -81.87310748452438247 ) ) ;
#74429=DIRECTION ( 'NONE',  ( -1.000000000000000000, 0.000000000000000000, -0.000000000000000000 ) ) ;
#74446=CARTESIAN_POINT ( 'NONE',  ( -20.85000000000000142, 68.97833521811159585, -65.68954208262705663 ) ) ;
#74486=CARTESIAN_POINT ( 'NONE',  ( -20.54999999999999716, 76.00000000001172396, -71.42310748452430857 ) ) ;
#74529=ADVANCED_FACE ( 'NONE', ( #107154 ), #28762, .F. ) ;
#74553=ORIENTED_EDGE ( 'NONE', *, *, #33527, .T. ) ;
#74564=ORIENTED_EDGE ( 'NONE', *, *, #64079, .T. ) ;
#74590=ORIENTED_EDGE ( 'NONE', *, *, #69272, .T. ) ;
#74600=CARTESIAN_POINT ( 'NONE',  ( -18.59999999999999787, 76.00000000001195133, -103.0231074845243171 ) ) ;
#74607=CARTESIAN_POINT ( 'NONE',  ( -18.39999999999999858, 85.50000000001189449, -95.99103808782457747 ) ) ;
#74614=DIRECTION ( 'NONE',  ( 0.000000000000000000, 6.982962677686267499E-15, -1.000000000000000000 ) ) ;
#74616=CARTESIAN_POINT ( 'NONE',  ( -18.59999999999999787, 66.85000000001203091, -114.7731074845243739 ) ) ;
#74618=PLANE ( 'NONE',  #190489 ) ;
#74625=DIRECTION ( 'NONE',  ( 1.000000000000000000, -2.952720810173289112E-16, -2.061873921506763405E-30 ) ) ;
#74645=DIRECTION ( 'NONE',  ( 0.000000000000000000, -0.9654727137038715545, -0.2605042016806676242 ) ) ;
#74666=ADVANCED_FACE ( 'NONE', ( #113580 ), #116215, .T. ) ;
#74701=DIRECTION ( 'NONE',  ( -1.000000000000000000, 0.000000000000000000, 0.000000000000000000 ) ) ;
#74711=CARTESIAN_POINT ( 'NONE',  ( 18.59999999999999076, 64.35000000001201670, -114.7731074845243882 ) ) ;
#74727=CARTESIAN_POINT ( 'NONE',  ( 21.05000000000000071, 76.00000000001169553, -67.52310748452430289 ) ) ;
#74739=CARTESIAN_POINT ( 'NONE',  ( 21.87500000000000355, 66.25000000001179501, -81.87310748452438247 ) ) ;
#74748=DIRECTION ( 'NONE',  ( -1.000000000000000000, -0.000000000000000000, -0.000000000000000000 ) ) ;
#74779=DIRECTION ( 'NONE',  ( -0.4999999999999799050, -6.047423072554995242E-15, 0.8660254037844502539 ) ) ;
#74828=VERTEX_POINT ( 'NONE', #36646 ) ;
#74852=AXIS2_PLACEMENT_3D ( 'NONE', #125415, #210092, #31472 ) ;
#74856=ORIENTED_EDGE ( 'NONE', *, *, #150368, .F. ) ;
#74859=DIRECTION ( 'NONE',  ( 0.000000000000000000, 0.000000000000000000, 1.000000000000000000 ) ) ;
#74861=ORIENTED_EDGE ( 'NONE', *, *, #189455, .T. ) ;
#74871=AXIS2_PLACEMENT_3D ( 'NONE', #81607, #7228, #226263 ) ;
#74917=CARTESIAN_POINT ( 'NONE',  ( -20.94999999999999929, 87.65000000001172964, -72.52310748452423184 ) ) ;
#74953=DIRECTION ( 'NONE',  ( 0.1538461538461484146, -0.9880948137434723000, 0.000000000000000000 ) ) ;
#74963=TOROIDAL_SURFACE ( 'NONE', #70873, 1.900000000000002576, 0.1000000000000000056 ) ;
#74967=DIRECTION ( 'NONE',  ( 2.952720810173289112E-16, 1.000000000000000000, 6.982962677686266711E-15 ) ) ;
#74974=AXIS2_PLACEMENT_3D ( 'NONE', #112175, #191722, #13075 ) ;
#75035=EDGE_CURVE ( 'NONE', #76326, #25605, #224521, .T. ) ;
#75049=AXIS2_PLACEMENT_3D ( 'NONE', #195575, #37786, #215115 ) ;
#75050=ORIENTED_EDGE ( 'NONE', *, *, #176301, .T. ) ;
#75073=CARTESIAN_POINT ( 'NONE',  ( 18.47135592147649774, 85.47108861327741636, -62.83951254468078673 ) ) ;
#75142=FACE_OUTER_BOUND ( 'NONE', #252628, .T. ) ;
#75219=AXIS2_PLACEMENT_3D ( 'NONE', #127573, #252633, #136529 ) ;
#75232=AXIS2_PLACEMENT_3D ( 'NONE', #20039, #96947, #177836 ) ;
#75250=CARTESIAN_POINT ( 'NONE',  ( -23.15000000000000213, 87.48912529308779540, -72.62310748452422615 ) ) ;
#75262=DIRECTION ( 'NONE',  ( 0.000000000000000000, -0.8660254037844377084, -0.5000000000000016653 ) ) ;
#75269=DIRECTION ( 'NONE',  ( -0.000000000000000000, -6.982962677686266711E-15, 1.000000000000000000 ) ) ;
#75277=DIRECTION ( 'NONE',  ( 0.000000000000000000, 0.000000000000000000, -1.000000000000000000 ) ) ;
#75286=VERTEX_POINT ( 'NONE', #24465 ) ;
#75309=AXIS2_PLACEMENT_3D ( 'NONE', #76716, #220094, #163979 ) ;
#75323=CARTESIAN_POINT ( 'NONE',  ( -20.54999999999999716, 71.65000000001180069, -81.87310748452433984 ) ) ;
#75332=EDGE_CURVE ( 'NONE', #129819, #16537, #33213, .T. ) ;
#75374=CYLINDRICAL_SURFACE ( 'NONE', #121468, 0.1000000000000028644 ) ;
#75388=AXIS2_PLACEMENT_3D ( 'NONE', #95886, #218394, #254912 ) ;
#75391=CIRCLE ( 'NONE', #171272, 0.5000000000000004441 ) ;
#75396=AXIS2_PLACEMENT_3D ( 'NONE', #121223, #142023, #239857 ) ;
#75398=CARTESIAN_POINT ( 'NONE',  ( -21.05000000000000071, 76.00000000001170974, -69.52310748452431710 ) ) ;
#75399=DIRECTION ( 'NONE',  ( 0.000000000000000000, 0.000000000000000000, 1.000000000000000000 ) ) ;
#75400=ADVANCED_FACE ( 'NONE', ( #155656 ), #215579, .F. ) ;
#75425=CARTESIAN_POINT ( 'NONE',  ( 21.05000000000041993, 69.65564095796835886, -103.0379631194186345 ) ) ;
#75453=ADVANCED_FACE ( 'NONE', ( #154377 ), #233871, .T. ) ;
#75454=AXIS2_PLACEMENT_3D ( 'NONE', #238166, #218596, #159954 ) ;
#75458=ORIENTED_EDGE ( 'NONE', *, *, #108463, .F. ) ;
#75494=DIRECTION ( 'NONE',  ( 0.000000000000000000, -0.9915357197604892647, 0.1298341882519715440 ) ) ;
#75523=CARTESIAN_POINT ( 'NONE',  ( -20.94999999999999929, 76.00000000001170974, -69.52310748452431710 ) ) ;
#75531=ORIENTED_EDGE ( 'NONE', *, *, #224822, .F. ) ;
#75585=DIRECTION ( 'NONE',  ( 0.000000000000000000, -1.000000000000000000, -7.109473446599835262E-15 ) ) ;
#75588=CARTESIAN_POINT ( 'NONE',  ( 23.14999999999999858, 78.00000000001170974, -69.52310748452430289 ) ) ;
#75591=CARTESIAN_POINT ( 'NONE',  ( 18.49999999999998934, 69.35000000001186038, -90.67310748452435121 ) ) ;
#75628=DIRECTION ( 'NONE',  ( -1.000000000000000000, -0.000000000000000000, -0.000000000000000000 ) ) ;
#75654=ORIENTED_EDGE ( 'NONE', *, *, #71412, .T. ) ;
#75656=CARTESIAN_POINT ( 'NONE',  ( 21.05000000000000071, 70.15000000001178648, -79.65560470880227228 ) ) ;
#75658=DIRECTION ( 'NONE',  ( 0.7071067811865475727, -0.7071067811865475727, -5.142139384388981164E-15 ) ) ;
#75661=DIRECTION ( 'NONE',  ( 0.7071067811865127117, 0.7071067811865821007, 0.000000000000000000 ) ) ;
#75662=ORIENTED_EDGE ( 'NONE', *, *, #212952, .T. ) ;
#75667=CARTESIAN_POINT ( 'NONE',  ( -18.49719636458544869, 85.44636535923997656, -95.95149361464065407 ) ) ;
#75692=LINE ( 'NONE', #213898, #228512 ) ;
#75696=VERTEX_POINT ( 'NONE', #44667 ) ;
#75720=LINE ( 'NONE', #17035, #193314 ) ;
#75728=DIRECTION ( 'NONE',  ( -1.000000000000000000, 0.000000000000000000, 0.000000000000000000 ) ) ;
#75751=EDGE_CURVE ( 'NONE', #160204, #88769, #29295, .T. ) ;
#75765=ORIENTED_EDGE ( 'NONE', *, *, #192449, .F. ) ;
#75802=DIRECTION ( 'NONE',  ( 0.000000000000000000, 6.938893903907222067E-15, -1.000000000000000000 ) ) ;
#75841=CARTESIAN_POINT ( 'NONE',  ( -20.94999999999999929, 76.00000000001170974, -69.52310748452431710 ) ) ;
#75901=CARTESIAN_POINT ( 'NONE',  ( -20.94999999999999929, 87.75000000001192291, -100.1231074845242262 ) ) ;
#75917=DIRECTION ( 'NONE',  ( 0.000000000000000000, -6.982962677686266711E-15, 1.000000000000000000 ) ) ;
#76015=CARTESIAN_POINT ( 'NONE',  ( 21.05095171578076574, 67.22382012124081996, -90.85723420788649207 ) ) ;
#76028=AXIS2_PLACEMENT_3D ( 'NONE', #83074, #204333, #239635 ) ;
#76037=ORIENTED_EDGE ( 'NONE', *, *, #23272, .T. ) ;
#76043=AXIS2_PLACEMENT_3D ( 'NONE', #130876, #135996, #229985 ) ;
#76047=DIRECTION ( 'NONE',  ( 0.000000000000000000, -0.9654727137038715545, 0.2605042016806676242 ) ) ;
#76055=ORIENTED_EDGE ( 'NONE', *, *, #5726, .T. ) ;
#76062=CIRCLE ( 'NONE', #163549, 4.000000000000003553 ) ;
#76065=ORIENTED_EDGE ( 'NONE', *, *, #168274, .F. ) ;
#76070=CARTESIAN_POINT ( 'NONE',  ( 20.94999999999999574, 62.00000000001190870, -97.59601495414186445 ) ) ;
#76071=CARTESIAN_POINT ( 'NONE',  ( 21.05000000000000071, 67.12338541492479749, -94.63802700567968884 ) ) ;
#76099=DIRECTION ( 'NONE',  ( 1.000000000000000000, 0.000000000000000000, 0.000000000000000000 ) ) ;
#76156=AXIS2_PLACEMENT_3D ( 'NONE', #257430, #217058, #201368 ) ;
#76163=ORIENTED_EDGE ( 'NONE', *, *, #120580, .F. ) ;
#76187=VECTOR ( 'NONE', #171948, 1000.000000000000000 ) ;
#76195=DIRECTION ( 'NONE',  ( 0.000000000000000000, 7.086529944415894657E-15, -1.000000000000000000 ) ) ;
#76215=DIRECTION ( 'NONE',  ( 0.000000000000000000, -1.000000000000000000, -6.352154140967427193E-15 ) ) ;
#76239=CIRCLE ( 'NONE', #63784, 7.900000000000003908 ) ;
#76284=VECTOR ( 'NONE', #134168, 999.9999999999998863 ) ;
#76319=EDGE_CURVE ( 'NONE', #200940, #60702, #212796, .T. ) ;
#76326=VERTEX_POINT ( 'NONE', #143122 ) ;
#76349=ORIENTED_EDGE ( 'NONE', *, *, #63486, .T. ) ;
#76367=EDGE_CURVE ( 'NONE', #254207, #178561, #225219, .T. ) ;
#76401=LINE ( 'NONE', #153442, #201645 ) ;
#76444=AXIS2_PLACEMENT_3D ( 'NONE', #176503, #153116, #253441 ) ;
#76456=CARTESIAN_POINT ( 'NONE',  ( -21.55000000000000426, 68.29142135624910281, -81.77310748452435973 ) ) ;
#76459=SPHERICAL_SURFACE ( 'NONE', #77648, 0.1000000000000000056 ) ;
#76472=ORIENTED_EDGE ( 'NONE', *, *, #216710, .T. ) ;
#76476=CARTESIAN_POINT ( 'NONE',  ( 23.14999999999999147, 76.00000000001195133, -103.0231074845243171 ) ) ;
#76480=VERTEX_POINT ( 'NONE', #131278 ) ;
#76486=ORIENTED_EDGE ( 'NONE', *, *, #210708, .F. ) ;
#76502=DIRECTION ( 'NONE',  ( 0.000000000000000000, 0.000000000000000000, 1.000000000000000000 ) ) ;
#76515=ADVANCED_FACE ( 'NONE', ( #210820 ), #29648, .T. ) ;
#76528=ORIENTED_EDGE ( 'NONE', *, *, #112042, .T. ) ;
#76551=AXIS2_PLACEMENT_3D ( 'NONE', #221402, #162759, #42796 ) ;
#76566=DIRECTION ( 'NONE',  ( -1.000000000000000000, 3.265361837132813093E-16, 2.280189983783949500E-30 ) ) ;
#76583=CARTESIAN_POINT ( 'NONE',  ( 18.39999999999999858, 85.68240343348806221, -62.86626410711144786 ) ) ;
#76606=ORIENTED_EDGE ( 'NONE', *, *, #198986, .T. ) ;
#76650=CARTESIAN_POINT ( 'NONE',  ( 21.05000000000000071, 87.29603075034721371, -99.97520832486037534 ) ) ;
#76666=DIRECTION ( 'NONE',  ( -1.000000000000000000, 1.836970198721029934E-16, 1.282749433769087582E-30 ) ) ;
#76680=DIRECTION ( 'NONE',  ( 0.000000000000000000, -6.308085367188367561E-15, 1.000000000000000000 ) ) ;
#76688=ORIENTED_EDGE ( 'NONE', *, *, #175363, .F. ) ;
#76716=CARTESIAN_POINT ( 'NONE',  ( 23.14999999999999858, 71.00000000001180922, -81.92837350343744163 ) ) ;
#76723=DIRECTION ( 'NONE',  ( 0.000000000000000000, 0.000000000000000000, 1.000000000000000000 ) ) ;
#76750=ADVANCED_FACE ( 'NONE', ( #7161 ), #83915, .F. ) ;
#76755=EDGE_CURVE ( 'NONE', #143163, #225625, #201518, .T. ) ;
#76775=DIRECTION ( 'NONE',  ( -1.000000000000000000, 0.000000000000000000, -0.000000000000000000 ) ) ;
#76791=AXIS2_PLACEMENT_3D ( 'NONE', #42498, #182025, #202856 ) ;
#76826=ORIENTED_EDGE ( 'NONE', *, *, #101820, .F. ) ;
#76828=CARTESIAN_POINT ( 'NONE',  ( -21.05000000000000426, 64.40000000001188596, -96.09490425424884563 ) ) ;
#76832=ORIENTED_EDGE ( 'NONE', *, *, #100825, .T. ) ;
#76865=DIRECTION ( 'NONE',  ( 1.000000000000000000, 0.000000000000000000, 0.000000000000000000 ) ) ;
#76880=CARTESIAN_POINT ( 'NONE',  ( -18.50000000000000000, 74.83729825007388570, -94.92310748452432279 ) ) ;
#76892=DIRECTION ( 'NONE',  ( -1.000000000000000000, 7.304098846218134667E-16, 5.100424963727256530E-30 ) ) ;
#76896=CARTESIAN_POINT ( 'NONE',  ( -20.85000000000000142, 77.16412189325286874, -61.60825939895269698 ) ) ;
#76912=ORIENTED_EDGE ( 'NONE', *, *, #123892, .F. ) ;
#76914=AXIS2_PLACEMENT_3D ( 'NONE', #191497, #233189, #33723 ) ;
#76928=DIRECTION ( 'NONE',  ( 0.000000000000000000, -6.688090509790097607E-15, 1.000000000000000000 ) ) ;
#76945=CARTESIAN_POINT ( 'NONE',  ( 21.14999999999999503, 64.35000000001194564, -102.9231074845243938 ) ) ;
#76957=ADVANCED_FACE ( 'NONE', ( #107552 ), #41923, .T. ) ;
#76960=VERTEX_POINT ( 'NONE', #128414 ) ;
#76973=DIRECTION ( 'NONE',  ( 0.000000000000000000, -6.982962677686266711E-15, 1.000000000000000000 ) ) ;
#76977=LINE ( 'NONE', #118699, #41696 ) ;
#76982=FACE_OUTER_BOUND ( 'NONE', #27027, .T. ) ;
#76996=CARTESIAN_POINT ( 'NONE',  ( -20.64999999999999858, 85.00000000001179501, -79.41707660717668205 ) ) ;
#77007=ORIENTED_EDGE ( 'NONE', *, *, #59677, .T. ) ;
#77039=EDGE_CURVE ( 'NONE', #88959, #4968, #166828, .T. ) ;
#77044=EDGE_CURVE ( 'NONE', #242842, #157610, #70970, .T. ) ;
#77064=CIRCLE ( 'NONE', #139585, 0.6000000000000033085 ) ;
#77073=VERTEX_POINT ( 'NONE', #194832 ) ;
#77074=ADVANCED_FACE ( 'NONE', ( #133545 ), #193534, .F. ) ;
#77078=ORIENTED_EDGE ( 'NONE', *, *, #154185, .F. ) ;
#77084=CARTESIAN_POINT ( 'NONE',  ( 20.99142135623731065, 64.40000000001175806, -76.45131071479988805 ) ) ;
#77113=ORIENTED_EDGE ( 'NONE', *, *, #87984, .T. ) ;
#77183=CARTESIAN_POINT ( 'NONE',  ( 21.05000000000000071, 84.66355140188093742, -79.04720860259155302 ) ) ;
#77198=CYLINDRICAL_SURFACE ( 'NONE', #204514, 0.1000000000000028644 ) ;
#77227=EDGE_LOOP ( 'NONE', ( #232355, #176915, #152889, #120099 ) ) ;
#77237=CARTESIAN_POINT ( 'NONE',  ( 20.95512820512820440, 65.37615131629999610, -90.87310748452438247 ) ) ;
#77242=CIRCLE ( 'NONE', #64774, 0.1000000000000028644 ) ;
#77285=ORIENTED_EDGE ( 'NONE', *, *, #250390, .T. ) ;
#77302=VECTOR ( 'NONE', #45807, 999.9999999999998863 ) ;
#77316=VECTOR ( 'NONE', #1324, 1000.000000000000000 ) ;
#77330=CARTESIAN_POINT ( 'NONE',  ( 22.49436431346199683, 64.35004905235850003, -103.0900110142466417 ) ) ;
#77346=CARTESIAN_POINT ( 'NONE',  ( 21.46681500593529535, 69.14248884062985212, -103.0231074845243597 ) ) ;
#77406=CARTESIAN_POINT ( 'NONE',  ( -21.05000000000000071, 76.00000000001195133, -103.0231074845243171 ) ) ;
#77450=AXIS2_PLACEMENT_3D ( 'NONE', #59406, #239375, #179415 ) ;
#77461=DIRECTION ( 'NONE',  ( 0.000000000000000000, -1.000000000000000000, -6.982962677686265922E-15 ) ) ;
#77486=DIRECTION ( 'NONE',  ( 0.000000000000000000, 0.000000000000000000, 1.000000000000000000 ) ) ;
#77493=VERTEX_POINT ( 'NONE', #220165 ) ;
#77518=B_SPLINE_CURVE_WITH_KNOTS ( 'NONE', 3,
 ( #221182, #244602, #159965, #140363, #123388, #25578, #41309, #120849, #103789, #183367, #201629, #23027, #84190, #182080, #223747, #165075, #5982, #101202, #161236 ),
 .UNSPECIFIED., .F., .F.,
 ( 4, 3, 3, 3, 3, 3, 4 ),
 ( 0.000000000000000000, 7.110282409890569127E-05, 0.0001508797727291477891, 0.0002027344179858564716, 0.0002343294522349123317, 0.0002454816334821249683, 0.0002619873080085630829 ),
 .UNSPECIFIED. ) ;
#77533=DIRECTION ( 'NONE',  ( -1.000000000000000000, -0.000000000000000000, -0.000000000000000000 ) ) ;
#77556=EDGE_CURVE ( 'NONE', #81484, #69698, #142027, .T. ) ;
#77582=CARTESIAN_POINT ( 'NONE',  ( -23.15000000000000213, 76.00000000001192291, -98.97310748452431994 ) ) ;
#77599=CYLINDRICAL_SURFACE ( 'NONE', #255605, 0.1000000000000028644 ) ;
#77606=VERTEX_POINT ( 'NONE', #234261 ) ;
#77617=CARTESIAN_POINT ( 'NONE',  ( -18.50000000000000000, 85.40000000001167280, -62.64106563635157698 ) ) ;
#77628=ORIENTED_EDGE ( 'NONE', *, *, #189300, .F. ) ;
#77629=EDGE_CURVE ( 'NONE', #99108, #158859, #183547, .T. ) ;
#77644=EDGE_LOOP ( 'NONE', ( #114086, #51050, #244969, #129450 ) ) ;
#77648=AXIS2_PLACEMENT_3D ( 'NONE', #41228, #256320, #198982 ) ;
#77670=SPHERICAL_SURFACE ( 'NONE', #142902, 0.1000000000000000056 ) ;
#77677=EDGE_CURVE ( 'NONE', #132438, #88936, #215975, .T. ) ;
#77702=DIRECTION ( 'NONE',  ( 0.000000000000000000, 0.000000000000000000, -1.000000000000000000 ) ) ;
#77723=CARTESIAN_POINT ( 'NONE',  ( 18.49505832270841310, 85.43802806279482809, -95.82463430963039741 ) ) ;
#77733=AXIS2_PLACEMENT_3D ( 'NONE', #100268, #84530, #164132 ) ;
#77741=VECTOR ( 'NONE', #173898, 1000.000000000000000 ) ;
#77751=CIRCLE ( 'NONE', #169412, 0.09999999999999939493 ) ;
#77801=EDGE_CURVE ( 'NONE', #42984, #209120, #13682, .T. ) ;
#77821=EDGE_CURVE ( 'NONE', #147420, #142551, #151071, .T. ) ;
#77858=FACE_OUTER_BOUND ( 'NONE', #185712, .T. ) ;
#77890=DIRECTION ( 'NONE',  ( 1.000000000000000000, 0.000000000000000000, 0.000000000000000000 ) ) ;
#77892=AXIS2_PLACEMENT_3D ( 'NONE', #158453, #1894, #64469 ) ;
#77903=DIRECTION ( 'NONE',  ( 1.000000000000000000, 0.000000000000000000, 0.000000000000000000 ) ) ;
#77904=CARTESIAN_POINT ( 'NONE',  ( 23.15000000000000213, 85.60000000001177511, -79.41707660717668205 ) ) ;
#77930=CIRCLE ( 'NONE', #56500, 0.3999999999999975797 ) ;
#77932=ORIENTED_EDGE ( 'NONE', *, *, #237723, .F. ) ;
#77945=CARTESIAN_POINT ( 'NONE',  ( 20.94999999999999574, 77.85102823015273543, -91.36919421510179973 ) ) ;
#78007=DIRECTION ( 'NONE',  ( 0.000000000000000000, -1.756682000989170847E-15, 1.000000000000000000 ) ) ;
#78035=CARTESIAN_POINT ( 'NONE',  ( 23.15000000000000213, 85.60000000001188880, -93.12913836187179584 ) ) ;
#78046=CARTESIAN_POINT ( 'NONE',  ( 21.05000000000036309, 65.39167043205783614, -95.43142247122897004 ) ) ;
#78116=CARTESIAN_POINT ( 'NONE',  ( -18.54270223418607699, 85.62410550289459366, -62.78217243411680926 ) ) ;
#78148=DIRECTION ( 'NONE',  ( 1.224646799147353207E-16, -1.000000000000000000, -6.982962677686266711E-15 ) ) ;
#78162=AXIS2_PLACEMENT_3D ( 'NONE', #4655, #221143, #60785 ) ;
#78174=AXIS2_PLACEMENT_3D ( 'NONE', #243716, #5068, #24698 ) ;
#78176=CIRCLE ( 'NONE', #223915, 0.1000000000000055705 ) ;
#78190=FACE_OUTER_BOUND ( 'NONE', #170500, .T. ) ;
#78234=ORIENTED_EDGE ( 'NONE', *, *, #45155, .T. ) ;
#78240=TOROIDAL_SURFACE ( 'NONE', #53309, 0.4000000000000003553, 0.1000000000000000056 ) ;
#78244=DIRECTION ( 'NONE',  ( -1.000000000000000000, 0.000000000000000000, -0.000000000000000000 ) ) ;
#78246=CARTESIAN_POINT ( 'NONE',  ( 23.14999999999999858, 70.40000000001180069, -81.92837350343744163 ) ) ;
#78336=EDGE_CURVE ( 'NONE', #216063, #71479, #42921, .T. ) ;
#78346=ORIENTED_EDGE ( 'NONE', *, *, #204267, .F. ) ;
#78369=ORIENTED_EDGE ( 'NONE', *, *, #242563, .T. ) ;
#78384=ORIENTED_EDGE ( 'NONE', *, *, #245366, .F. ) ;
#78396=TOROIDAL_SURFACE ( 'NONE', #211713, 0.2000000000000000111, 0.1000000000000000056 ) ;
#78404=CARTESIAN_POINT ( 'NONE',  ( -18.47653818581420992, 85.46528038777485392, -95.89714666838439427 ) ) ;
#78407=CARTESIAN_POINT ( 'NONE',  ( 18.59999999999998366, 76.00000000001170974, -69.52310748452431710 ) ) ;
#78410=CARTESIAN_POINT ( 'NONE',  ( -21.44999999999999929, 68.65000000001187175, -90.67310748452436542 ) ) ;
#78434=ORIENTED_EDGE ( 'NONE', *, *, #112404, .T. ) ;
#78437=DIRECTION ( 'NONE',  ( 1.000000000000000000, 0.000000000000000000, 0.000000000000000000 ) ) ;
#78455=VERTEX_POINT ( 'NONE', #92873 ) ;
#78493=EDGE_CURVE ( 'NONE', #199047, #131339, #111171, .T. ) ;
#78509=AXIS2_PLACEMENT_3D ( 'NONE', #84931, #43285, #182812 ) ;
#78539=CARTESIAN_POINT ( 'NONE',  ( -18.50000000000000000, 77.13501884592184865, -61.80613060109197932 ) ) ;
#78546=ORIENTED_EDGE ( 'NONE', *, *, #204635, .F. ) ;
#78550=CIRCLE ( 'NONE', #95126, 0.1000000000000028644 ) ;
#78563=CARTESIAN_POINT ( 'NONE',  ( -22.45305610364635385, 76.10085836911078161, -114.7726746080137019 ) ) ;
#78575=EDGE_LOOP ( 'NONE', ( #211923, #1935, #104532, #102647 ) ) ;
#78652=AXIS2_PLACEMENT_3D ( 'NONE', #20021, #99506, #57820 ) ;
#78678=ORIENTED_EDGE ( 'NONE', *, *, #14285, .F. ) ;
#78686=DIRECTION ( 'NONE',  ( 1.000000000000000000, 0.000000000000000000, 0.000000000000000000 ) ) ;
#78691=CARTESIAN_POINT ( 'NONE',  ( 21.14999999999999858, 69.74218538953583391, -103.1208977758331571 ) ) ;
#78710=DIRECTION ( 'NONE',  ( 0.000000000000000000, 0.000000000000000000, -1.000000000000000000 ) ) ;
#78720=AXIS2_PLACEMENT_3D ( 'NONE', #66588, #109537, #146105 ) ;
#78742=CARTESIAN_POINT ( 'NONE',  ( 23.24999999999999289, 69.35000000001186038, -90.67310748452435121 ) ) ;
#78748=DIRECTION ( 'NONE',  ( -0.000000000000000000, 1.000000000000000000, 6.352154140967427193E-15 ) ) ;
#78758=DIRECTION ( 'NONE',  ( -1.000000000000000000, 0.000000000000000000, -0.000000000000000000 ) ) ;
#78802=DIRECTION ( 'NONE',  ( 1.000000000000000000, 0.000000000000000000, 0.000000000000000000 ) ) ;
#78804=EDGE_LOOP ( 'NONE', ( #190422, #222376, #149565, #198231 ) ) ;
#78818=CIRCLE ( 'NONE', #87004, 0.5000000000000004441 ) ;
#78852=CARTESIAN_POINT ( 'NONE',  ( -21.14999999999999858, 76.00000000001200817, -109.5637644362255543 ) ) ;
#78863=DIRECTION ( 'NONE',  ( 0.000000000000000000, -2.775557561562888827E-14, 1.000000000000000000 ) ) ;
#78922=ORIENTED_EDGE ( 'NONE', *, *, #133471, .F. ) ;
#78928=DIRECTION ( 'NONE',  ( -1.000000000000000000, 2.952720810173289112E-16, 2.061873921506763405E-30 ) ) ;
#78931=DIRECTION ( 'NONE',  ( -4.239556034732056743E-17, -0.1298341882519953583, -0.9915357197604862671 ) ) ;
#78973=ORIENTED_EDGE ( 'NONE', *, *, #151761, .T. ) ;
#78975=EDGE_LOOP ( 'NONE', ( #174356, #117507, #20455, #174374, #92229 ) ) ;
#79045=ORIENTED_EDGE ( 'NONE', *, *, #48278, .F. ) ;
#79077=ORIENTED_EDGE ( 'NONE', *, *, #254583, .T. ) ;
#79079=AXIS2_PLACEMENT_3D ( 'NONE', #34047, #205247, #73168 ) ;
#79084=PLANE ( 'NONE',  #75454 ) ;
#79098=ORIENTED_EDGE ( 'NONE', *, *, #6908, .F. ) ;
#79176=CARTESIAN_POINT ( 'NONE',  ( 18.58222699835054570, 65.66799936921511005, -63.92993998886009877 ) ) ;
#79201=DIRECTION ( 'NONE',  ( -1.000000000000000000, 0.000000000000000000, -0.000000000000000000 ) ) ;
#79215=CARTESIAN_POINT ( 'NONE',  ( -20.00857864376270001, 66.65000000001180069, -81.87310748452438247 ) ) ;
#79221=ORIENTED_EDGE ( 'NONE', *, *, #72276, .T. ) ;
#79227=CIRCLE ( 'NONE', #91723, 11.74999999999999645 ) ;
#79260=CARTESIAN_POINT ( 'NONE',  ( 20.94999999999999929, 76.00000000001170974, -69.52310748452431710 ) ) ;
#79269=CARTESIAN_POINT ( 'NONE',  ( -23.15000000000000213, 87.65000000001172964, -72.62310748452422615 ) ) ;
#79275=EDGE_LOOP ( 'NONE', ( #225271, #254945, #62983, #103045 ) ) ;
#79321=CARTESIAN_POINT ( 'NONE',  ( -21.14999999999999858, 76.00000000001195133, -103.0231074845243171 ) ) ;
#79336=DIRECTION ( 'NONE',  ( 0.000000000000000000, 6.982962677686266711E-15, -1.000000000000000000 ) ) ;
#79340=DIRECTION ( 'NONE',  ( 1.000000000000000000, -0.000000000000000000, 0.000000000000000000 ) ) ;
#79352=ORIENTED_EDGE ( 'NONE', *, *, #48101, .F. ) ;
#79361=LINE ( 'NONE', #178511, #56889 ) ;
#79386=EDGE_CURVE ( 'NONE', #20026, #83116, #179216, .T. ) ;
#79397=ORIENTED_EDGE ( 'NONE', *, *, #112760, .T. ) ;
#79464=VECTOR ( 'NONE', #122423, 1000.000000000000000 ) ;
#79511=VERTEX_POINT ( 'NONE', #33006 ) ;
#79514=DIRECTION ( 'NONE',  ( 0.000000000000000000, -1.000000000000000000, -6.982962677686266711E-15 ) ) ;
#79548=ORIENTED_EDGE ( 'NONE', *, *, #6908, .T. ) ;
#79557=ORIENTED_EDGE ( 'NONE', *, *, #241972, .T. ) ;
#79559=ORIENTED_EDGE ( 'NONE', *, *, #168274, .T. ) ;
#79647=EDGE_CURVE ( 'NONE', #102088, #171936, #61176, .T. ) ;
#79685=ADVANCED_FACE ( 'NONE', ( #199757 ), #1432, .F. ) ;
#79729=CARTESIAN_POINT ( 'NONE',  ( -20.94999999999999929, 68.97833521811159585, -65.68954208262705663 ) ) ;
#79739=CARTESIAN_POINT ( 'NONE',  ( -22.39999999999999858, 75.90000000001194280, -103.0231074845243171 ) ) ;
#79746=AXIS2_PLACEMENT_3D ( 'NONE', #238250, #58312, #162590 ) ;
#79751=CYLINDRICAL_SURFACE ( 'NONE', #38864, 0.1000000000000028644 ) ;
#79826=DIRECTION ( 'NONE',  ( 0.000000000000000000, -0.5000000000000016653, 0.8660254037844377084 ) ) ;
#79836=VECTOR ( 'NONE', #104407, 1000.000000000000000 ) ;
#79869=AXIS2_PLACEMENT_3D ( 'NONE', #252961, #57319, #232143 ) ;
#79880=CARTESIAN_POINT ( 'NONE',  ( 18.49999999999999289, 69.55000000001187743, -93.00608031408432907 ) ) ;
#79893=DIRECTION ( 'NONE',  ( 0.000000000000000000, 0.000000000000000000, 1.000000000000000000 ) ) ;
#79911=CARTESIAN_POINT ( 'NONE',  ( 20.94999999999999929, 87.39257802171739797, -72.59705706435616435 ) ) ;
#79920=EDGE_LOOP ( 'NONE', ( #91556, #130695, #16538, #70210 ) ) ;
#79925=AXIS2_PLACEMENT_3D ( 'NONE', #106919, #142204, #3976 ) ;
#79938=CARTESIAN_POINT ( 'NONE',  ( 20.94999999999999929, 76.00000000001195133, -103.0231074845243171 ) ) ;
#79952=DIRECTION ( 'NONE',  ( -1.000000000000000000, 2.952720810173289112E-16, 2.061873921506763405E-30 ) ) ;
#79988=DIRECTION ( 'NONE',  ( 1.000000000000000000, 0.000000000000000000, 0.000000000000000000 ) ) ;
#80006=FACE_OUTER_BOUND ( 'NONE', #188117, .T. ) ;
#80031=CARTESIAN_POINT ( 'NONE',  ( 20.97217846901851956, 67.12455827530222052, -94.52187980058714345 ) ) ;
#80033=FACE_BOUND ( 'NONE', #82835, .T. ) ;
#80052=DIRECTION ( 'NONE',  ( -0.000000000000000000, 6.982962677686266711E-15, -1.000000000000000000 ) ) ;
#80053=DIRECTION ( 'NONE',  ( 0.000000000000000000, 0.4999999999999689138, 0.8660254037844565822 ) ) ;
#80059=CARTESIAN_POINT ( 'NONE',  ( -21.59142135623730852, 68.15000000001180069, -81.77310748452435973 ) ) ;
#80064=VERTEX_POINT ( 'NONE', #200716 ) ;
#80075=AXIS2_PLACEMENT_3D ( 'NONE', #213759, #234603, #19419 ) ;
#80081=ADVANCED_FACE ( 'NONE', ( #19521 ), #111245, .T. ) ;
#80125=CIRCLE ( 'NONE', #225881, 0.09999999999999939493 ) ;
#80132=ORIENTED_EDGE ( 'NONE', *, *, #98257, .T. ) ;
#80139=LINE ( 'NONE', #142708, #163253 ) ;
#80141=DIRECTION ( 'NONE',  ( 0.000000000000000000, 0.5000000000000209832, 0.8660254037844264952 ) ) ;
#80148=ORIENTED_EDGE ( 'NONE', *, *, #250642, .T. ) ;
#80151=FACE_OUTER_BOUND ( 'NONE', #150141, .T. ) ;
#80152=CARTESIAN_POINT ( 'NONE',  ( -23.15000000000000213, 76.00000000001195133, -103.0231074845243171 ) ) ;
#80181=ORIENTED_EDGE ( 'NONE', *, *, #91180, .T. ) ;
#80188=CIRCLE ( 'NONE', #134371, 0.1000000000000043771 ) ;
#80208=DIRECTION ( 'NONE',  ( -1.000000000000000000, 2.952720810173289112E-16, 2.061873921506763405E-30 ) ) ;
#80226=DIRECTION ( 'NONE',  ( 0.000000000000000000, 6.982962677686266711E-15, -1.000000000000000000 ) ) ;
#80229=DIRECTION ( 'NONE',  ( 0.7071359030027593029, 0.000000000000000000, 0.7070776581709197206 ) ) ;
#80238=CARTESIAN_POINT ( 'NONE',  ( -23.15000000000000213, 64.40000000001177227, -76.45131071479988805 ) ) ;
#80247=EDGE_CURVE ( 'NONE', #30387, #216303, #215468, .T. ) ;
#80258=CIRCLE ( 'NONE', #180091, 11.74999999999999645 ) ;
#80259=AXIS2_PLACEMENT_3D ( 'NONE', #151390, #206212, #49703 ) ;
#80272=LINE ( 'NONE', #41214, #34993 ) ;
#80278=CARTESIAN_POINT ( 'NONE',  ( -20.94999999999999929, 64.35000000001171827, -69.52310748452438816 ) ) ;
#80359=DIRECTION ( 'NONE',  ( 0.000000000000000000, -1.000000000000000000, 0.000000000000000000 ) ) ;
#80362=DIRECTION ( 'NONE',  ( -0.000000000000000000, 1.000000000000000000, 6.982962677686266711E-15 ) ) ;
#80367=CARTESIAN_POINT ( 'NONE',  ( 21.07928932188134397, 69.67148334361864670, -103.1220026301787414 ) ) ;
#80378=CARTESIAN_POINT ( 'NONE',  ( 18.59999999999999787, 77.83585931145526615, -58.01866831572577610 ) ) ;
#80385=LINE ( 'NONE', #175694, #223830 ) ;
#80399=EDGE_CURVE ( 'NONE', #126928, #165593, #21779, .T. ) ;
#80426=CIRCLE ( 'NONE', #130919, 0.5000000000000004441 ) ;
#80435=CARTESIAN_POINT ( 'NONE',  ( 18.57399277249656322, 65.66887361445313331, -63.93298459182691573 ) ) ;
#80456=ORIENTED_EDGE ( 'NONE', *, *, #257622, .T. ) ;
#80469=DIRECTION ( 'NONE',  ( 1.000000000000000000, 0.000000000000000000, 0.000000000000000000 ) ) ;
#80479=DIRECTION ( 'NONE',  ( -1.000000000000000000, -0.000000000000000000, -0.000000000000000000 ) ) ;
#80484=AXIS2_PLACEMENT_3D ( 'NONE', #172738, #176558, #155727 ) ;
#80514=ORIENTED_EDGE ( 'NONE', *, *, #36101, .F. ) ;
#80529=DIRECTION ( 'NONE',  ( 0.000000000000000000, 0.000000000000000000, 1.000000000000000000 ) ) ;
#80556=ORIENTED_EDGE ( 'NONE', *, *, #51602, .T. ) ;
#80557=ADVANCED_FACE ( 'NONE', ( #225072 ), #125989, .T. ) ;
#80578=ORIENTED_EDGE ( 'NONE', *, *, #83244, .T. ) ;
#80579=CIRCLE ( 'NONE', #118025, 0.1000000000000028644 ) ;
#80591=EDGE_CURVE ( 'NONE', #10090, #200329, #149048, .T. ) ;
#80600=LINE ( 'NONE', #62358, #124242 ) ;
#80634=CARTESIAN_POINT ( 'NONE',  ( -20.85000000000000142, 76.00000000001170974, -69.52310748452431710 ) ) ;
#80661=VERTEX_POINT ( 'NONE', #74739 ) ;
#80683=CARTESIAN_POINT ( 'NONE',  ( 20.04142135623730070, 64.35000000001177511, -78.37310748452439668 ) ) ;
#80697=FACE_OUTER_BOUND ( 'NONE', #100752, .T. ) ;
#80710=AXIS2_PLACEMENT_3D ( 'NONE', #217674, #242392, #20810 ) ;
#80713=CARTESIAN_POINT ( 'NONE',  ( -23.25000000000000000, 64.35000000001203091, -114.7731074845243882 ) ) ;
#80731=CARTESIAN_POINT ( 'NONE',  ( 22.39999999999999503, 64.35000000001194564, -103.1231074845243825 ) ) ;
#80741=DIRECTION ( 'NONE',  ( 0.000000000000000000, 6.982962677686266711E-15, -1.000000000000000000 ) ) ;
#80759=VECTOR ( 'NONE', #117108, 1000.000000000000000 ) ;
#80812=AXIS2_PLACEMENT_3D ( 'NONE', #177414, #56130, #256865 ) ;
#80819=AXIS2_PLACEMENT_3D ( 'NONE', #171372, #108776, #8407 ) ;
#80834=DIRECTION ( 'NONE',  ( 0.000000000000000000, -6.547589603894034005E-15, 1.000000000000000000 ) ) ;
#80870=DIRECTION ( 'NONE',  ( 1.000000000000000000, 0.000000000000000000, 0.000000000000000000 ) ) ;
#80948=LINE ( 'NONE', #103074, #209337 ) ;
#80949=VERTEX_POINT ( 'NONE', #204895 ) ;
#80978=DIRECTION ( 'NONE',  ( 6.938893903907222067E-15, 1.000000000000000000, 6.982962677686266711E-15 ) ) ;
#81028=ORIENTED_EDGE ( 'NONE', *, *, #37037, .F. ) ;
#81039=ORIENTED_EDGE ( 'NONE', *, *, #219474, .F. ) ;
#81043=EDGE_CURVE ( 'NONE', #249207, #239900, #75692, .T. ) ;
#81061=CIRCLE ( 'NONE', #1950, 11.70000000000000284 ) ;
#81100=CARTESIAN_POINT ( 'NONE',  ( -18.50000000000000000, 66.75000000001179501, -81.87310748452438247 ) ) ;
#81109=B_SPLINE_CURVE_WITH_KNOTS ( 'NONE', 3,
 ( #100618, #240183, #201041, #22432, #101910, #241460, #88774, #170959, #10560, #148786 ),
 .UNSPECIFIED., .F., .F.,
 ( 4, 3, 3, 4 ),
 ( 0.000000000000000000, 0.0002000000000008537104, 0.001000000000082977483, 0.001967863649483339323 ),
 .UNSPECIFIED. ) ;
#81136=VECTOR ( 'NONE', #76892, 1000.000000000000000 ) ;
#81170=DIRECTION ( 'NONE',  ( 0.000000000000000000, -7.109473446599835262E-15, 1.000000000000000000 ) ) ;
#81176=CARTESIAN_POINT ( 'NONE',  ( 21.08479644141222664, 75.94144555744786373, -109.3681461422561938 ) ) ;
#81241=ORIENTED_EDGE ( 'NONE', *, *, #137390, .F. ) ;
#81255=CARTESIAN_POINT ( 'NONE',  ( -21.05000000000000071, 74.14897176987101091, -91.36919421510182815 ) ) ;
#81262=DIRECTION ( 'NONE',  ( 0.000000000000000000, 0.000000000000000000, 1.000000000000000000 ) ) ;
#81274=PLANE ( 'NONE',  #226842 ) ;
#81277=ORIENTED_EDGE ( 'NONE', *, *, #175227, .T. ) ;
#81307=AXIS2_PLACEMENT_3D ( 'NONE', #138329, #38002, #58793 ) ;
#81322=EDGE_CURVE ( 'NONE', #8981, #163251, #85908, .T. ) ;
#81325=CARTESIAN_POINT ( 'NONE',  ( 20.94999999999999929, 71.18691588786234092, -91.08158972800052311 ) ) ;
#81336=DIRECTION ( 'NONE',  ( 0.000000000000000000, 1.000000000000000000, 0.000000000000000000 ) ) ;
#81346=CIRCLE ( 'NONE', #227118, 4.150000000000001243 ) ;
#81347=FACE_OUTER_BOUND ( 'NONE', #251851, .T. ) ;
#81361=ORIENTED_EDGE ( 'NONE', *, *, #70628, .T. ) ;
#81374=SPHERICAL_SURFACE ( 'NONE', #186399, 0.1000000000000000056 ) ;
#81386=DIRECTION ( 'NONE',  ( 0.000000000000000000, -6.308085367188367561E-15, 1.000000000000000000 ) ) ;
#81405=EDGE_CURVE ( 'NONE', #61221, #146439, #220124, .T. ) ;
#81423=CARTESIAN_POINT ( 'NONE',  ( 20.85000000000000142, 77.73670573947921980, -58.00568489690056850 ) ) ;
#81434=CYLINDRICAL_SURFACE ( 'NONE', #210673, 0.1000000000000028644 ) ;
#81464=DIRECTION ( 'NONE',  ( 0.000000000000000000, 0.000000000000000000, 1.000000000000000000 ) ) ;
#81467=ORIENTED_EDGE ( 'NONE', *, *, #246527, .T. ) ;
#81484=VERTEX_POINT ( 'NONE', #53235 ) ;
#81492=AXIS2_PLACEMENT_3D ( 'NONE', #187588, #166753, #87159 ) ;
#81497=ORIENTED_EDGE ( 'NONE', *, *, #50190, .T. ) ;
#81525=ORIENTED_EDGE ( 'NONE', *, *, #246602, .T. ) ;
#81530=ORIENTED_EDGE ( 'NONE', *, *, #125508, .F. ) ;
#81532=CARTESIAN_POINT ( 'NONE',  ( -21.05000000000000071, 76.10000000001200249, -109.5637644362255543 ) ) ;
#81580=CARTESIAN_POINT ( 'NONE',  ( -20.15000000000000568, 66.70857864377455826, -90.77310748452437394 ) ) ;
#81590=CARTESIAN_POINT ( 'NONE',  ( -21.07928932188134041, 75.90110485435759813, -109.3516241409176075 ) ) ;
#81600=LINE ( 'NONE', #240718, #154269 ) ;
#81607=CARTESIAN_POINT ( 'NONE',  ( -21.05000000000000071, 70.15000000001178648, -79.65560470880227228 ) ) ;
#81639=CARTESIAN_POINT ( 'NONE',  ( 21.05000000000000071, 76.00000000001169553, -67.62310748452431142 ) ) ;
#81646=CARTESIAN_POINT ( 'NONE',  ( -23.15000000000000213, 87.65000000001172964, -72.62310748452422615 ) ) ;
#81683=DIRECTION ( 'NONE',  ( -1.000000000000000000, 0.000000000000000000, -0.000000000000000000 ) ) ;
#81687=ADVANCED_FACE ( 'NONE', ( #24394 ), #149593, .T. ) ;
#81688=DIRECTION ( 'NONE',  ( -1.000000000000000000, 0.000000000000000000, -0.000000000000000000 ) ) ;
#81707=ADVANCED_FACE ( 'NONE', ( #49047 ), #191294, .F. ) ;
#81724=CARTESIAN_POINT ( 'NONE',  ( 18.52643265882457868, 65.68026841930880266, -63.97257401318892533 ) ) ;
#81758=ORIENTED_EDGE ( 'NONE', *, *, #104557, .F. ) ;
#81765=DIRECTION ( 'NONE',  ( 0.000000000000000000, -7.026728003956683390E-15, 1.000000000000000000 ) ) ;
#81780=VERTEX_POINT ( 'NONE', #43916 ) ;
#81788=EDGE_CURVE ( 'NONE', #221948, #185034, #123458, .T. ) ;
#81801=CARTESIAN_POINT ( 'NONE',  ( 22.50000000000000000, 75.90000000001202807, -114.7731074845243029 ) ) ;
#81803=VERTEX_POINT ( 'NONE', #210692 ) ;
#81806=DIRECTION ( 'NONE',  ( 1.000000000000000000, 0.000000000000000000, 0.000000000000000000 ) ) ;
#81809=AXIS2_PLACEMENT_3D ( 'NONE', #22726, #18842, #57952 ) ;
#81810=CARTESIAN_POINT ( 'NONE',  ( -2.995603634470891112E-16, 69.35000000001180354, -81.87310748452435405 ) ) ;
#81837=ORIENTED_EDGE ( 'NONE', *, *, #112003, .T. ) ;
#81845=EDGE_CURVE ( 'NONE', #206918, #77606, #191484, .T. ) ;
#81882=ORIENTED_EDGE ( 'NONE', *, *, #220677, .F. ) ;
#81895=ORIENTED_EDGE ( 'NONE', *, *, #100693, .F. ) ;
#81912=ORIENTED_EDGE ( 'NONE', *, *, #170106, .T. ) ;
#81933=AXIS2_PLACEMENT_3D ( 'NONE', #7128, #231348, #226149 ) ;
#81941=EDGE_LOOP ( 'NONE', ( #242641, #12200, #165515, #22620 ) ) ;
#81955=DIRECTION ( 'NONE',  ( 0.000000000000000000, 0.000000000000000000, -1.000000000000000000 ) ) ;
#82005=AXIS2_PLACEMENT_3D ( 'NONE', #169296, #248802, #70182 ) ;
#82009=DIRECTION ( 'NONE',  ( 0.000000000000000000, 7.086529944415894657E-15, -1.000000000000000000 ) ) ;
#82023=CYLINDRICAL_SURFACE ( 'NONE', #13222, 0.09999999999999939493 ) ;
#82030=DIRECTION ( 'NONE',  ( -1.000000000000000000, 0.000000000000000000, -0.000000000000000000 ) ) ;
#82041=FACE_OUTER_BOUND ( 'NONE', #32350, .T. ) ;
#82046=AXIS2_PLACEMENT_3D ( 'NONE', #119684, #21859, #59666 ) ;
#82052=EDGE_CURVE ( 'NONE', #88561, #153107, #33264, .T. ) ;
#82068=VERTEX_POINT ( 'NONE', #145269 ) ;
#82069=LINE ( 'NONE', #61258, #109823 ) ;
#82100=CARTESIAN_POINT ( 'NONE',  ( -21.05000000000000071, 87.48912529308798014, -99.92310748452423752 ) ) ;
#82139=DIRECTION ( 'NONE',  ( 0.000000000000000000, 0.000000000000000000, -1.000000000000000000 ) ) ;
#82140=ORIENTED_EDGE ( 'NONE', *, *, #8333, .F. ) ;
#82156=FACE_OUTER_BOUND ( 'NONE', #48988, .T. ) ;
#82161=VERTEX_POINT ( 'NONE', #67037 ) ;
#82172=CIRCLE ( 'NONE', #98730, 0.1000000000000028644 ) ;
#82178=CARTESIAN_POINT ( 'NONE',  ( 18.49999999999999645, 77.83585931145526615, -58.01866831572577610 ) ) ;
#82186=EDGE_LOOP ( 'NONE', ( #115980, #199710, #56335, #9897 ) ) ;
#82199=VERTEX_POINT ( 'NONE', #87853 ) ;
#82239=CARTESIAN_POINT ( 'NONE',  ( 21.05000000000000071, 76.01681986839764704, -109.3305327040896913 ) ) ;
#82241=FACE_OUTER_BOUND ( 'NONE', #111781, .T. ) ;
#82244=DIRECTION ( 'NONE',  ( 0.000000000000000000, 1.000000000000000000, 0.000000000000000000 ) ) ;
#82270=( NAMED_UNIT ( * ) PLANE_ANGLE_UNIT ( ) SI_UNIT ( $, .RADIAN. ) );
#82307=CARTESIAN_POINT ( 'NONE',  ( -18.59999999999999787, 76.00000000001170974, -69.52310748452431710 ) ) ;
#82321=CYLINDRICAL_SURFACE ( 'NONE', #34421, 0.1000000000000028644 ) ;
#82366=DIRECTION ( 'NONE',  ( 1.000000000000000000, 0.000000000000000000, 0.000000000000000000 ) ) ;
#82374=AXIS2_PLACEMENT_3D ( 'NONE', #79260, #57127, #136678 ) ;
#82378=DIRECTION ( 'NONE',  ( 3.265361837132813093E-16, 1.000000000000000000, 6.982962677686266711E-15 ) ) ;
#82393=DIRECTION ( 'NONE',  ( 0.000000000000000000, 0.000000000000000000, 1.000000000000000000 ) ) ;
#82403=ORIENTED_EDGE ( 'NONE', *, *, #152471, .F. ) ;
#82409=DIRECTION ( 'NONE',  ( 0.000000000000000000, -7.056502275159894776E-15, 1.000000000000000000 ) ) ;
#82420=AXIS2_PLACEMENT_3D ( 'NONE', #137442, #158347, #257344 ) ;
#82421=DIRECTION ( 'NONE',  ( 0.000000000000000000, 6.982962677686266711E-15, -1.000000000000000000 ) ) ;
#82441=CIRCLE ( 'NONE', #228238, 0.1000000000000028644 ) ;
#82443=AXIS2_PLACEMENT_3D ( 'NONE', #233262, #31229, #92424 ) ;
#82462=CARTESIAN_POINT ( 'NONE',  ( -18.52309608778527306, 85.64247632006693323, -62.80851114335471408 ) ) ;
#82467=EDGE_CURVE ( 'NONE', #88959, #102162, #145834, .T. ) ;
#82479=EDGE_CURVE ( 'NONE', #183385, #59708, #166731, .T. ) ;
#82508=EDGE_LOOP ( 'NONE', ( #246908, #147503, #2963, #94307 ) ) ;
#82514=CARTESIAN_POINT ( 'NONE',  ( 21.05000000000000071, 70.50000000001185185, -90.61784146561124942 ) ) ;
#82517=VERTEX_POINT ( 'NONE', #141143 ) ;
#82551=FACE_OUTER_BOUND ( 'NONE', #195261, .T. ) ;
#82554=EDGE_CURVE ( 'NONE', #168580, #119060, #146016, .T. ) ;
#82574=DIRECTION ( 'NONE',  ( -0.000000000000000000, 0.1298341882519953583, 0.9915357197604862671 ) ) ;
#82614=DIRECTION ( 'NONE',  ( 1.000000000000000000, 0.000000000000000000, 0.000000000000000000 ) ) ;
#82615=AXIS2_PLACEMENT_3D ( 'NONE', #254470, #195841, #253211 ) ;
#82635=DIRECTION ( 'NONE',  ( 0.000000000000000000, -6.530723674265620862E-15, 1.000000000000000000 ) ) ;
#82640=DIRECTION ( 'NONE',  ( 0.000000000000000000, 0.9876197685951241256, 0.1568667991644932258 ) ) ;
#82666=DIRECTION ( 'NONE',  ( -0.000000000000000000, 0.1298341882519953583, 0.9915357197604862671 ) ) ;
#82673=DIRECTION ( 'NONE',  ( 2.915501640297156255E-16, 1.000000000000000000, 6.997203936713175802E-15 ) ) ;
#82692=EDGE_CURVE ( 'NONE', #199332, #23607, #35346, .T. ) ;
#82693=DIRECTION ( 'NONE',  ( 0.000000000000000000, 0.000000000000000000, -1.000000000000000000 ) ) ;
#82694=DIRECTION ( 'NONE',  ( -0.000000000000000000, 6.982962677686266711E-15, -1.000000000000000000 ) ) ;
#82696=ORIENTED_EDGE ( 'NONE', *, *, #227569, .T. ) ;
#82719=ORIENTED_EDGE ( 'NONE', *, *, #128497, .T. ) ;
#82732=AXIS2_PLACEMENT_3D ( 'NONE', #53272, #32456, #174556 ) ;
#82744=CARTESIAN_POINT ( 'NONE',  ( -20.94999999999999929, 77.13501884592184865, -61.80613060109197932 ) ) ;
#82775=VERTEX_POINT ( 'NONE', #118714 ) ;
#82785=ORIENTED_EDGE ( 'NONE', *, *, #134350, .F. ) ;
#82795=DIRECTION ( 'NONE',  ( -0.000000000000000000, -6.982962677686266711E-15, 1.000000000000000000 ) ) ;
#82835=EDGE_LOOP ( 'NONE', ( #118939, #73535 ) ) ;
#82841=VECTOR ( 'NONE', #125045, 1000.000000000000000 ) ;
#82854=ORIENTED_EDGE ( 'NONE', *, *, #243117, .T. ) ;
#82860=CARTESIAN_POINT ( 'NONE',  ( -23.25000000000000000, 87.65000000001204228, -114.7731074845242318 ) ) ;
#82904=ORIENTED_EDGE ( 'NONE', *, *, #226660, .F. ) ;
#82933=CARTESIAN_POINT ( 'NONE',  ( 21.95218792049437795, 68.79849243876529385, -103.1221359243242688 ) ) ;
#82959=EDGE_CURVE ( 'NONE', #87934, #195497, #16404, .T. ) ;
#82988=CARTESIAN_POINT ( 'NONE',  ( 23.15000000000000213, 85.50000000001188027, -93.12913836187179584 ) ) ;
#82995=FACE_OUTER_BOUND ( 'NONE', #236079, .T. ) ;
#83005=DIRECTION ( 'NONE',  ( 1.000000000000000000, 0.000000000000000000, 0.000000000000000000 ) ) ;
#83006=DIRECTION ( 'NONE',  ( 0.000000000000000000, -7.147358527629762208E-15, 1.000000000000000000 ) ) ;
#83008=CARTESIAN_POINT ( 'NONE',  ( 18.50211644919734866, 65.69792220476298894, -64.03355541284614105 ) ) ;
#83030=CIRCLE ( 'NONE', #183043, 0.09999999999999520384 ) ;
#83040=CARTESIAN_POINT ( 'NONE',  ( -21.05000000000000071, 75.96636726467835388, -109.2819246792058010 ) ) ;
#83074=CARTESIAN_POINT ( 'NONE',  ( -21.05000000000000071, 87.75000000001173817, -72.42310748452422331 ) ) ;
#83079=EDGE_CURVE ( 'NONE', #249684, #146711, #115474, .T. ) ;
#83083=CARTESIAN_POINT ( 'NONE',  ( -18.59999999999999787, 64.35000000001187459, -90.87310748452438247 ) ) ;
#83086=CARTESIAN_POINT ( 'NONE',  ( -21.05000000000000071, 77.16270174994990327, -94.92310748452430857 ) ) ;
#83087=CIRCLE ( 'NONE', #95766, 0.1000000000000000888 ) ;
#83090=DIRECTION ( 'NONE',  ( 0.000000000000000000, 1.000000000000000000, 6.982962677686266711E-15 ) ) ;
#83116=VERTEX_POINT ( 'NONE', #32120 ) ;
#83148=EDGE_CURVE ( 'NONE', #208580, #111080, #118047, .T. ) ;
#83158=CYLINDRICAL_SURFACE ( 'NONE', #101127, 0.1000000000000028644 ) ;
#83167=CARTESIAN_POINT ( 'NONE',  ( -20.96077737575346944, 64.37609936600699712, -76.38231552741797259 ) ) ;
#83173=DIRECTION ( 'NONE',  ( -0.000000000000000000, 0.1350103645451835865, 0.9908441862701605762 ) ) ;
#83183=ORIENTED_EDGE ( 'NONE', *, *, #193734, .T. ) ;
#83198=SPHERICAL_SURFACE ( 'NONE', #252671, 0.1000000000000000056 ) ;
#83202=ORIENTED_EDGE ( 'NONE', *, *, #85862, .T. ) ;
#83212=FACE_OUTER_BOUND ( 'NONE', #180358, .T. ) ;
#83219=ORIENTED_EDGE ( 'NONE', *, *, #175367, .F. ) ;
#83221=ORIENTED_EDGE ( 'NONE', *, *, #4076, .F. ) ;
#83244=EDGE_CURVE ( 'NONE', #107897, #215945, #164889, .T. ) ;
#83261=ORIENTED_EDGE ( 'NONE', *, *, #177493, .T. ) ;
#83289=LINE ( 'NONE', #145846, #112614 ) ;
#83358=CIRCLE ( 'NONE', #212585, 0.09999999999999971412 ) ;
#83398=ORIENTED_EDGE ( 'NONE', *, *, #189785, .F. ) ;
#83423=VERTEX_POINT ( 'NONE', #199878 ) ;
#83441=CARTESIAN_POINT ( 'NONE',  ( -20.54999999999999716, 85.40000000001178648, -79.41707660717668205 ) ) ;
#83445=EDGE_CURVE ( 'NONE', #108089, #118009, #16664, .T. ) ;
#83447=CARTESIAN_POINT ( 'NONE',  ( 21.05000000000000071, 87.48912529308779540, -72.42310748452423752 ) ) ;
#83461=ORIENTED_EDGE ( 'NONE', *, *, #79386, .F. ) ;
#83500=ORIENTED_EDGE ( 'NONE', *, *, #83148, .T. ) ;
#83504=ORIENTED_EDGE ( 'NONE', *, *, #164318, .F. ) ;
#83511=DIRECTION ( 'NONE',  ( -1.000000000000000000, -0.000000000000000000, -0.000000000000000000 ) ) ;
#83516=CARTESIAN_POINT ( 'NONE',  ( -18.46856557590793457, 85.47421590779836720, -95.92112124364196291 ) ) ;
#83538=EDGE_CURVE ( 'NONE', #14341, #188719, #104112, .T. ) ;
#83558=CARTESIAN_POINT ( 'NONE',  ( -23.25000000000000000, 87.75000000001193712, -103.0231074845242318 ) ) ;
#83559=FACE_OUTER_BOUND ( 'NONE', #114398, .T. ) ;
#83598=DIRECTION ( 'NONE',  ( 0.000000000000000000, 0.000000000000000000, 1.000000000000000000 ) ) ;
#83619=DIRECTION ( 'NONE',  ( 0.000000000000000000, 0.9908441862701605762, -0.1350103645451835310 ) ) ;
#83629=CARTESIAN_POINT ( 'NONE',  ( -18.50000000000000000, 66.75000000001179501, -81.67310748452437963 ) ) ;
#83638=CARTESIAN_POINT ( 'NONE',  ( 21.07094088545368038, 75.90110629745977633, -109.3432747064414343 ) ) ;
#83682=AXIS2_PLACEMENT_3D ( 'NONE', #10823, #173804, #168663 ) ;
#83684=LINE ( 'NONE', #86267, #68131 ) ;
#83714=CARTESIAN_POINT ( 'NONE',  ( -18.59999999999999787, 74.26374286841446803, -91.45445515550682103 ) ) ;
#83719=DIRECTION ( 'NONE',  ( 0.000000000000000000, 0.000000000000000000, 1.000000000000000000 ) ) ;
#83732=ORIENTED_EDGE ( 'NONE', *, *, #70060, .T. ) ;
#83743=AXIS2_PLACEMENT_3D ( 'NONE', #59728, #218814, #102702 ) ;
#83748=CIRCLE ( 'NONE', #46194, 0.1000000000000028644 ) ;
#83779=DIRECTION ( 'NONE',  ( 1.000000000000000000, 0.000000000000000000, 0.000000000000000000 ) ) ;
#83796=VERTEX_POINT ( 'NONE', #88875 ) ;
#83797=CARTESIAN_POINT ( 'NONE',  ( 22.50000000000000000, 68.20922040163857503, -103.1231074845243540 ) ) ;
#83802=EDGE_LOOP ( 'NONE', ( #122029, #134681, #152918, #24627 ) ) ;
#83813=DIRECTION ( 'NONE',  ( -1.000000000000000000, 0.000000000000000000, -0.000000000000000000 ) ) ;
#83820=CARTESIAN_POINT ( 'NONE',  ( -23.25000000000000000, 64.35000000001203091, -114.7731074845243882 ) ) ;
#83852=EDGE_LOOP ( 'NONE', ( #66435, #71318, #158794, #215833 ) ) ;
#83878=ORIENTED_EDGE ( 'NONE', *, *, #254506, .F. ) ;
#83884=ORIENTED_EDGE ( 'NONE', *, *, #251627, .T. ) ;
#83891=DIRECTION ( 'NONE',  ( 0.000000000000000000, -7.026728003956683390E-15, 1.000000000000000000 ) ) ;
#83902=CYLINDRICAL_SURFACE ( 'NONE', #43931, 12.87499999999999822 ) ;
#83903=PLANE ( 'NONE',  #58393 ) ;
#83915=TOROIDAL_SURFACE ( 'NONE', #138119, 12.97499999999999787, 0.1000000000000000056 ) ;
#83946=ADVANCED_FACE ( 'NONE', ( #204671 ), #224243, .F. ) ;
#83988=ORIENTED_EDGE ( 'NONE', *, *, #22895, .T. ) ;
#83990=PLANE ( 'NONE',  #21227 ) ;
#84021=ORIENTED_EDGE ( 'NONE', *, *, #67681, .F. ) ;
#84022=FACE_OUTER_BOUND ( 'NONE', #182173, .T. ) ;
#84046=EDGE_CURVE ( 'NONE', #141595, #130365, #33438, .T. ) ;
#84047=ORIENTED_EDGE ( 'NONE', *, *, #254426, .F. ) ;
#84052=CARTESIAN_POINT ( 'NONE',  ( -21.05000000000000071, 77.16270174994990327, -95.12310748452431142 ) ) ;
#84082=ORIENTED_EDGE ( 'NONE', *, *, #247270, .F. ) ;
#84131=EDGE_CURVE ( 'NONE', #163251, #84480, #192007, .T. ) ;
#84146=FACE_OUTER_BOUND ( 'NONE', #227279, .T. ) ;
#84190=CARTESIAN_POINT ( 'NONE',  ( 21.08198257630413508, 69.66340326599689092, -103.0957508083089635 ) ) ;
#84206=CIRCLE ( 'NONE', #180145, 0.1999999999999987899 ) ;
#84211=CYLINDRICAL_SURFACE ( 'NONE', #11599, 0.09999999999999939493 ) ;
#84224=CIRCLE ( 'NONE', #105673, 0.6000000000000033085 ) ;
#84228=CARTESIAN_POINT ( 'NONE',  ( 20.94999999999999574, 74.83729825007388570, -95.02310748452431710 ) ) ;
#84242=AXIS2_PLACEMENT_3D ( 'NONE', #49035, #9908, #69914 ) ;
#84263=ORIENTED_EDGE ( 'NONE', *, *, #181360, .T. ) ;
#84274=EDGE_CURVE ( 'NONE', #4548, #17499, #40200, .T. ) ;
#84280=CARTESIAN_POINT ( 'NONE',  ( 23.14999999999999858, 76.00000000001170974, -69.52310748452431710 ) ) ;
#84297=CARTESIAN_POINT ( 'NONE',  ( -21.05000000000000426, 76.10000000001200249, -109.5001745056490563 ) ) ;
#84305=CARTESIAN_POINT ( 'NONE',  ( -23.15000000000000213, 74.00000000001180922, -82.74772940728641402 ) ) ;
#84312=EDGE_CURVE ( 'NONE', #190582, #61048, #183606, .T. ) ;
#84313=DIRECTION ( 'NONE',  ( -0.000000000000000000, -6.982962677686266711E-15, 1.000000000000000000 ) ) ;
#84315=DIRECTION ( 'NONE',  ( -1.000000000000000000, -0.000000000000000000, -0.000000000000000000 ) ) ;
#84319=EDGE_LOOP ( 'NONE', ( #27143, #159981, #186659, #146655 ) ) ;
#84355=DIRECTION ( 'NONE',  ( -1.000000000000000000, 0.000000000000000000, -0.000000000000000000 ) ) ;
#84358=SPHERICAL_SURFACE ( 'NONE', #223846, 0.1000000000000000056 ) ;
#84367=CARTESIAN_POINT ( 'NONE',  ( -18.59999999999999787, 64.35000000001190301, -96.00830171387039513 ) ) ;
#84368=VERTEX_POINT ( 'NONE', #4858 ) ;
#84373=DIRECTION ( 'NONE',  ( 0.000000000000000000, -7.056502275159890043E-15, 1.000000000000000000 ) ) ;
#84467=ORIENTED_EDGE ( 'NONE', *, *, #72276, .F. ) ;
#84480=VERTEX_POINT ( 'NONE', #208245 ) ;
#84496=VECTOR ( 'NONE', #190227, 1000.000000000000000 ) ;
#84508=DIRECTION ( 'NONE',  ( -1.000000000000000000, 3.265361837132813093E-16, 2.280189983783949500E-30 ) ) ;
#84530=DIRECTION ( 'NONE',  ( 1.000000000000000000, -2.952720810173289112E-16, -2.061873921506763405E-30 ) ) ;
#84553=ADVANCED_FACE ( 'NONE', ( #155669 ), #150488, .T. ) ;
#84582=AXIS2_PLACEMENT_3D ( 'NONE', #196336, #80208, #37291 ) ;
#84584=EDGE_CURVE ( 'NONE', #254207, #66328, #8819, .T. ) ;
#84603=ORIENTED_EDGE ( 'NONE', *, *, #136231, .F. ) ;
#84637=LINE ( 'NONE', #1276, #150040 ) ;
#84663=EDGE_CURVE ( 'NONE', #213743, #49254, #125528, .T. ) ;
#84675=CARTESIAN_POINT ( 'NONE',  ( 23.14999999999999858, 76.00000000001168132, -65.52310748452430289 ) ) ;
#84713=CARTESIAN_POINT ( 'NONE',  ( 20.00000000000000355, 64.25000000001176659, -78.37310748452439668 ) ) ;
#84739=EDGE_CURVE ( 'NONE', #178001, #252623, #62951, .T. ) ;
#84742=ORIENTED_EDGE ( 'NONE', *, *, #47843, .T. ) ;
#84749=CARTESIAN_POINT ( 'NONE',  ( 21.05000000000000426, 69.74118280533048164, -103.0567402198579998 ) ) ;
#84767=CIRCLE ( 'NONE', #105625, 11.70000000000000284 ) ;
#84774=ADVANCED_FACE ( 'NONE', ( #43390 ), #122937, .T. ) ;
#84801=ORIENTED_EDGE ( 'NONE', *, *, #171401, .F. ) ;
#84805=CARTESIAN_POINT ( 'NONE',  ( 23.14999999999999503, 64.25000000001175238, -76.53791325517833855 ) ) ;
#84816=DIRECTION ( 'NONE',  ( 1.000000000000000000, 0.000000000000000000, 0.000000000000000000 ) ) ;
#84827=ADVANCED_FACE ( 'NONE', ( #49805 ), #150210, .T. ) ;
#84870=PLANE ( 'NONE',  #42053 ) ;
#84879=DIRECTION ( 'NONE',  ( 1.000000000000000000, 0.000000000000000000, 0.000000000000000000 ) ) ;
#84916=DIRECTION ( 'NONE',  ( -1.000000000000000000, 0.000000000000000000, -0.000000000000000000 ) ) ;
#84920=FACE_OUTER_BOUND ( 'NONE', #78975, .T. ) ;
#84931=CARTESIAN_POINT ( 'NONE',  ( 21.07928932188134397, 76.00000000001195133, -103.0231074845243171 ) ) ;
#84952=EDGE_CURVE ( 'NONE', #243292, #146605, #221191, .T. ) ;
#84989=AXIS2_PLACEMENT_3D ( 'NONE', #49549, #50803, #246461 ) ;
#85030=CARTESIAN_POINT ( 'NONE',  ( -20.94999999999999929, 77.16270174994990327, -94.92310748452430857 ) ) ;
#85031=DIRECTION ( 'NONE',  ( 0.000000000000000000, 1.000000000000000000, 6.982962677686266711E-15 ) ) ;
#85054=ORIENTED_EDGE ( 'NONE', *, *, #236624, .T. ) ;
#85062=AXIS2_PLACEMENT_3D ( 'NONE', #29597, #188636, #169116 ) ;
#85080=DIRECTION ( 'NONE',  ( 1.000000000000000000, 0.000000000000000000, 0.000000000000000000 ) ) ;
#85086=VERTEX_POINT ( 'NONE', #126326 ) ;
#85090=EDGE_LOOP ( 'NONE', ( #14864, #3991, #58893, #24277 ) ) ;
#85096=EDGE_CURVE ( 'NONE', #103624, #158615, #231877, .T. ) ;
#85097=EDGE_LOOP ( 'NONE', ( #13838, #210589, #155456, #55503 ) ) ;
#85115=CIRCLE ( 'NONE', #64310, 0.1000000000000028783 ) ;
#85134=TOROIDAL_SURFACE ( 'NONE', #189241, 11.65000000000000036, 0.1000000000000000056 ) ;
#85145=DIRECTION ( 'NONE',  ( 1.000000000000000000, -0.000000000000000000, 0.000000000000000000 ) ) ;
#85196=ADVANCED_FACE ( 'NONE', ( #14109 ), #75374, .T. ) ;
#85216=CARTESIAN_POINT ( 'NONE',  ( -21.05000000000000071, 76.00000000001195133, -103.0231074845243171 ) ) ;
#85234=ORIENTED_EDGE ( 'NONE', *, *, #3911, .F. ) ;
#85265=AXIS2_PLACEMENT_3D ( 'NONE', #194606, #215417, #155489 ) ;
#85268=ORIENTED_EDGE ( 'NONE', *, *, #60333, .T. ) ;
#85279=DIRECTION ( 'NONE',  ( 0.000000000000000000, 0.000000000000000000, 1.000000000000000000 ) ) ;
#85291=DIRECTION ( 'NONE',  ( -1.000000000000000000, -0.000000000000000000, -0.000000000000000000 ) ) ;
#85326=CIRCLE ( 'NONE', #139507, 12.87499999999999822 ) ;
#85340=VERTEX_POINT ( 'NONE', #156195 ) ;
#85342=CARTESIAN_POINT ( 'NONE',  ( -23.15000000000000213, 85.50000000001179501, -79.41707660717668205 ) ) ;
#85380=CARTESIAN_POINT ( 'NONE',  ( -21.05000000000000071, 64.25000000001176659, -76.53791325517833855 ) ) ;
#85389=DIRECTION ( 'NONE',  ( -1.000000000000000000, -0.000000000000000000, -0.000000000000000000 ) ) ;
#85393=CARTESIAN_POINT ( 'NONE',  ( -18.57399277249657032, 65.66887361445314752, -63.93298459182690863 ) ) ;
#85400=ORIENTED_EDGE ( 'NONE', *, *, #122167, .F. ) ;
#85407=DIRECTION ( 'NONE',  ( 1.000000000000000000, 0.000000000000000000, 0.000000000000000000 ) ) ;
#85451=DIRECTION ( 'NONE',  ( -1.000000000000000000, 0.000000000000000000, -0.000000000000000000 ) ) ;
#85456=DIRECTION ( 'NONE',  ( 0.000000000000000000, -0.1568667991644355497, 0.9876197685951332295 ) ) ;
#85510=ORIENTED_EDGE ( 'NONE', *, *, #246527, .F. ) ;
#85536=CYLINDRICAL_SURFACE ( 'NONE', #150500, 0.5000000000000004441 ) ;
#85538=CARTESIAN_POINT ( 'NONE',  ( -21.14999999999999858, 87.65000000001195701, -103.0231074845242318 ) ) ;
#85631=FACE_OUTER_BOUND ( 'NONE', #33474, .T. ) ;
#85646=DIRECTION ( 'NONE',  ( -1.000000000000000000, 0.000000000000000000, -0.000000000000000000 ) ) ;
#85672=ORIENTED_EDGE ( 'NONE', *, *, #20323, .T. ) ;
#85687=ORIENTED_EDGE ( 'NONE', *, *, #209547, .F. ) ;
#85690=CARTESIAN_POINT ( 'NONE',  ( -2.995603634470891112E-16, 87.75000000001180922, -81.77310748452421763 ) ) ;
#85697=DIRECTION ( 'NONE',  ( 0.000000000000000000, 0.000000000000000000, -1.000000000000000000 ) ) ;
#85729=VERTEX_POINT ( 'NONE', #22948 ) ;
#85748=ORIENTED_EDGE ( 'NONE', *, *, #218976, .T. ) ;
#85787=DIRECTION ( 'NONE',  ( -1.000000000000000000, 0.000000000000000000, 0.000000000000000000 ) ) ;
#85814=CARTESIAN_POINT ( 'NONE',  ( -21.05000000000000071, 87.65000000001192859, -100.0231074845242318 ) ) ;
#85822=ORIENTED_EDGE ( 'NONE', *, *, #221033, .T. ) ;
#85830=CARTESIAN_POINT ( 'NONE',  ( 23.15000000000000213, 87.48912529308779540, -72.52310748452423184 ) ) ;
#85835=ORIENTED_EDGE ( 'NONE', *, *, #127501, .T. ) ;
#85862=EDGE_CURVE ( 'NONE', #121241, #170796, #46319, .T. ) ;
#85908=LINE ( 'NONE', #188896, #216005 ) ;
#85923=EDGE_CURVE ( 'NONE', #256898, #51707, #91878, .T. ) ;
#85946=AXIS2_PLACEMENT_3D ( 'NONE', #112114, #191664, #9146 ) ;
#85973=DIRECTION ( 'NONE',  ( 0.000000000000000000, -7.026728003956683390E-15, 1.000000000000000000 ) ) ;
#86003=CARTESIAN_POINT ( 'NONE',  ( 19.97071067811865674, 64.27928932189311695, -78.37310748452439668 ) ) ;
#86005=AXIS2_PLACEMENT_3D ( 'NONE', #181690, #3022, #241653 ) ;
#86011=CARTESIAN_POINT ( 'NONE',  ( -20.64999999999999858, 76.00000000001169553, -67.62310748452431142 ) ) ;
#86033=CONICAL_SURFACE ( 'NONE', #102601, 4.049999999999998046, 0.7853981633974604915 ) ;
#86037=CARTESIAN_POINT ( 'NONE',  ( -18.59999999999999787, 74.73821383144687047, -94.93660852097883662 ) ) ;
#86061=ORIENTED_EDGE ( 'NONE', *, *, #89306, .F. ) ;
#86063=EDGE_LOOP ( 'NONE', ( #111822, #9484, #56275, #181991, #208982, #32719, #83884, #159444, #145259, #135704 ) ) ;
#86071=ORIENTED_EDGE ( 'NONE', *, *, #246966, .T. ) ;
#86077=ORIENTED_EDGE ( 'NONE', *, *, #231910, .F. ) ;
#86107=EDGE_CURVE ( 'NONE', #57574, #31606, #109307, .T. ) ;
#86125=CYLINDRICAL_SURFACE ( 'NONE', #99707, 0.1000000000000028644 ) ;
#86156=ORIENTED_EDGE ( 'NONE', *, *, #206744, .T. ) ;
#86213=ORIENTED_EDGE ( 'NONE', *, *, #233406, .T. ) ;
#86249=CARTESIAN_POINT ( 'NONE',  ( -18.50000000000000000, 64.35000000001203091, -114.7731074845243882 ) ) ;
#86254=ORIENTED_EDGE ( 'NONE', *, *, #83445, .F. ) ;
#86258=DIRECTION ( 'NONE',  ( -0.1538461538461484146, -0.9880948137434723000, 0.000000000000000000 ) ) ;
#86265=DIRECTION ( 'NONE',  ( 1.000000000000000000, 0.000000000000000000, 0.000000000000000000 ) ) ;
#86267=CARTESIAN_POINT ( 'NONE',  ( -18.59999999999999787, 66.75000000001185185, -90.77310748452437394 ) ) ;
#86296=CIRCLE ( 'NONE', #165633, 0.1000000000000028644 ) ;
#86300=DIRECTION ( 'NONE',  ( 0.000000000000000000, -1.000000000000000000, -6.982962677686265922E-15 ) ) ;
#86305=SPHERICAL_SURFACE ( 'NONE', #192269, 0.1000000000000000056 ) ;
#86342=ORIENTED_EDGE ( 'NONE', *, *, #144421, .F. ) ;
#86349=VERTEX_POINT ( 'NONE', #232074 ) ;
#86355=VERTEX_POINT ( 'NONE', #95108 ) ;
#86360=DIRECTION ( 'NONE',  ( 1.000000000000000000, 0.000000000000000000, 0.000000000000000000 ) ) ;
#86374=VERTEX_POINT ( 'NONE', #33904 ) ;
#86376=CARTESIAN_POINT ( 'NONE',  ( -18.59999999999999787, 74.65925378207832352, -113.2959699899454904 ) ) ;
#86383=ORIENTED_EDGE ( 'NONE', *, *, #102467, .T. ) ;
#86428=ADVANCED_FACE ( 'NONE', ( #83212 ), #126253, .F. ) ;
#86437=FACE_OUTER_BOUND ( 'NONE', #143195, .T. ) ;
#86459=CARTESIAN_POINT ( 'NONE',  ( 20.87631937322882436, 65.52850496324731466, -95.44336160994302531 ) ) ;
#86499=ORIENTED_EDGE ( 'NONE', *, *, #164318, .T. ) ;
#86500=CARTESIAN_POINT ( 'NONE',  ( 21.08804582317324261, 67.12183383291996108, -90.67310765511901138 ) ) ;
#86505=AXIS2_PLACEMENT_3D ( 'NONE', #150491, #51341, #69679 ) ;
#86510=AXIS2_PLACEMENT_3D ( 'NONE', #84305, #45241, #242151 ) ;
#86560=ORIENTED_EDGE ( 'NONE', *, *, #2498, .T. ) ;
#86562=ORIENTED_EDGE ( 'NONE', *, *, #13932, .T. ) ;
#86570=ADVANCED_FACE ( 'NONE', ( #8849 ), #109215, .T. ) ;
#86583=EDGE_CURVE ( 'NONE', #118009, #221355, #209615, .T. ) ;
#86590=EDGE_CURVE ( 'NONE', #132438, #59112, #238872, .T. ) ;
#86602=DIRECTION ( 'NONE',  ( -0.000000000000000000, -6.982962677686266711E-15, 1.000000000000000000 ) ) ;
#86616=ORIENTED_EDGE ( 'NONE', *, *, #172148, .T. ) ;
#86617=CARTESIAN_POINT ( 'NONE',  ( -20.54999999999999716, 73.60000000001184617, -89.79848556176223440 ) ) ;
#86640=ADVANCED_FACE ( 'NONE', ( #148358 ), #131353, .T. ) ;
#86669=CIRCLE ( 'NONE', #195061, 0.1000000000000028644 ) ;
#86670=EDGE_LOOP ( 'NONE', ( #125520, #112091, #211763, #128032 ) ) ;
#86681=VERTEX_POINT ( 'NONE', #37412 ) ;
#86724=EDGE_CURVE ( 'NONE', #111193, #235470, #231757, .T. ) ;
#86727=AXIS2_PLACEMENT_3D ( 'NONE', #94257, #74748, #254597 ) ;
#86773=EDGE_LOOP ( 'NONE', ( #136959, #256057, #146965, #133662 ) ) ;
#86807=CARTESIAN_POINT ( 'NONE',  ( 22.59999985501178799, 64.25013020700896504, -103.0887061543238303 ) ) ;
#86810=LINE ( 'NONE', #217653, #249425 ) ;
#86815=DIRECTION ( 'NONE',  ( 1.000000000000000000, -0.000000000000000000, 0.000000000000000000 ) ) ;
#86819=DIRECTION ( 'NONE',  ( 1.000000000000000000, 0.000000000000000000, 0.000000000000000000 ) ) ;
#86826=AXIS2_PLACEMENT_3D ( 'NONE', #5380, #26270, #164503 ) ;
#86855=CARTESIAN_POINT ( 'NONE',  ( 18.49999999999999645, 77.36242903720497566, -61.63422623660309796 ) ) ;
#86858=CARTESIAN_POINT ( 'NONE',  ( -18.59999999999999787, 77.16412189325286874, -61.60825939895269698 ) ) ;
#86872=DIRECTION ( 'NONE',  ( 0.000000000000000000, 0.000000000000000000, 1.000000000000000000 ) ) ;
#86888=CARTESIAN_POINT ( 'NONE',  ( -20.94999999999999929, 68.96868720525648655, -65.91395654629705803 ) ) ;
#86900=ORIENTED_EDGE ( 'NONE', *, *, #84739, .T. ) ;
#86901=CIRCLE ( 'NONE', #11952, 0.1000000000000028644 ) ;
#86904=CARTESIAN_POINT ( 'NONE',  ( -21.05000000000000071, 75.90220970870321082, -109.2809220950004203 ) ) ;
#86926=CARTESIAN_POINT ( 'NONE',  ( 20.95512820512820440, 67.12384868372375024, -90.87310748452436826 ) ) ;
#86964=ORIENTED_EDGE ( 'NONE', *, *, #242563, .F. ) ;
#87004=AXIS2_PLACEMENT_3D ( 'NONE', #23698, #60209, #83598 ) ;
#87005=DIRECTION ( 'NONE',  ( 0.000000000000000000, 0.3738317757009942399, -0.9274965247785252886 ) ) ;
#87011=ORIENTED_EDGE ( 'NONE', *, *, #96733, .F. ) ;
#87029=CARTESIAN_POINT ( 'NONE',  ( -21.05000000000000071, 64.40000000001175806, -76.45131071479988805 ) ) ;
#87055=TOROIDAL_SURFACE ( 'NONE', #66239, 0.9750000000000019762, 0.1000000000000000056 ) ;
#87059=EDGE_LOOP ( 'NONE', ( #148596, #26448, #178548, #242955 ) ) ;
#87067=TOROIDAL_SURFACE ( 'NONE', #32980, 11.65000000000000036, 0.1000000000000000056 ) ;
#87097=EDGE_LOOP ( 'NONE', ( #105599, #13150, #133480, #6142 ) ) ;
#87118=EDGE_CURVE ( 'NONE', #8311, #142060, #115330, .T. ) ;
#87158=CARTESIAN_POINT ( 'NONE',  ( -20.85000000000000142, 87.75000000001172396, -69.52310748452423184 ) ) ;
#87159=DIRECTION ( 'NONE',  ( 0.000000000000000000, -6.467318590049456648E-15, 1.000000000000000000 ) ) ;
#87169=DIRECTION ( 'NONE',  ( 0.000000000000000000, 0.000000000000000000, 1.000000000000000000 ) ) ;
#87185=CARTESIAN_POINT ( 'NONE',  ( -21.10257677756356642, 69.60161825747921682, -103.0480582340923092 ) ) ;
#87248=CARTESIAN_POINT ( 'NONE',  ( -18.59999999999999787, 64.35000000001203091, -114.7731074845243882 ) ) ;
#87266=TOROIDAL_SURFACE ( 'NONE', #249784, 11.65000000000000036, 0.1000000000000000056 ) ;
#87273=CIRCLE ( 'NONE', #174646, 0.6000000000000033085 ) ;
#87274=CARTESIAN_POINT ( 'NONE',  ( 21.05000000000000071, 71.00000000001180922, -81.92837350343744163 ) ) ;
#87281=LINE ( 'NONE', #7775, #243914 ) ;
#87314=DIRECTION ( 'NONE',  ( -0.000000000000000000, -1.000000000000000000, -6.982962677686266711E-15 ) ) ;
#87354=ORIENTED_EDGE ( 'NONE', *, *, #104635, .F. ) ;
#87356=AXIS2_PLACEMENT_3D ( 'NONE', #110351, #172945, #34696 ) ;
#87379=VERTEX_POINT ( 'NONE', #203856 ) ;
#87382=DIRECTION ( 'NONE',  ( 1.000000000000000000, 0.000000000000000000, 0.000000000000000000 ) ) ;
#87395=DIRECTION ( 'NONE',  ( -1.000000000000000000, -0.000000000000000000, -0.000000000000000000 ) ) ;
#87396=CARTESIAN_POINT ( 'NONE',  ( -18.50000000000000000, 102.4393534156127572, -84.88159887701665696 ) ) ;
#87410=CARTESIAN_POINT ( 'NONE',  ( 20.94999999999999929, 87.48912529308779540, -72.42310748452423752 ) ) ;
#87465=AXIS2_PLACEMENT_3D ( 'NONE', #100887, #180481, #81336 ) ;
#87483=CARTESIAN_POINT ( 'NONE',  ( -20.87600722750343252, 65.66887361445314752, -63.93298459182691573 ) ) ;
#87501=DIRECTION ( 'NONE',  ( 1.000000000000000000, 7.304098846218105085E-16, 4.217023435051676515E-16 ) ) ;
#87504=DIRECTION ( 'NONE',  ( 2.952720810173289112E-16, 1.000000000000000000, 6.982962677686266711E-15 ) ) ;
#87574=EDGE_LOOP ( 'NONE', ( #150963, #34732, #3434, #102350 ) ) ;
#87576=CARTESIAN_POINT ( 'NONE',  ( 20.99749315643147440, 64.25000000001175238, -76.53791325328415951 ) ) ;
#87587=ADVANCED_FACE ( 'NONE', ( #51179 ), #31684, .F. ) ;
#87599=ADVANCED_FACE ( 'NONE', ( #39389 ), #178905, .F. ) ;
#87612=EDGE_CURVE ( 'NONE', #132438, #226125, #58411, .T. ) ;
#87618=ADVANCED_FACE ( 'NONE', ( #100575 ), #226753, .T. ) ;
#87635=EDGE_CURVE ( 'NONE', #76480, #72649, #201810, .T. ) ;
#87662=CYLINDRICAL_SURFACE ( 'NONE', #256283, 0.1000000000000028644 ) ;
#87676=DIRECTION ( 'NONE',  ( 0.000000000000000000, 6.982962677686266711E-15, -1.000000000000000000 ) ) ;
#87679=DIRECTION ( 'NONE',  ( -0.000000000000000000, 1.000000000000000000, 7.172728831056617961E-15 ) ) ;
#87709=TOROIDAL_SURFACE ( 'NONE', #21122, 0.2000000000000000111, 0.1000000000000000056 ) ;
#87737=CARTESIAN_POINT ( 'NONE',  ( 18.49999999999997868, 85.32100840337321301, -95.78716923544641304 ) ) ;
#87781=CARTESIAN_POINT ( 'NONE',  ( -23.15000000000000213, 73.40000000001181490, -82.74772940728642823 ) ) ;
#87783=CIRCLE ( 'NONE', #225142, 0.09999999999999939493 ) ;
#87787=ORIENTED_EDGE ( 'NONE', *, *, #140070, .F. ) ;
#87789=AXIS2_PLACEMENT_3D ( 'NONE', #116352, #56342, #115056 ) ;
#87853=CARTESIAN_POINT ( 'NONE',  ( 23.24999999999999289, 70.05000000001177796, -79.82880978955917328 ) ) ;
#87867=VERTEX_POINT ( 'NONE', #31389 ) ;
#87870=VECTOR ( 'NONE', #188471, 1000.000000000000000 ) ;
#87878=AXIS2_PLACEMENT_3D ( 'NONE', #32472, #9021, #29894 ) ;
#87897=CARTESIAN_POINT ( 'NONE',  ( -22.49072729836729678, 75.94351806727840426, -114.6731157336792535 ) ) ;
#87904=ADVANCED_FACE ( 'NONE', ( #13089 ), #172194, .T. ) ;
#87934=VERTEX_POINT ( 'NONE', #76880 ) ;
#87967=ORIENTED_EDGE ( 'NONE', *, *, #124542, .F. ) ;
#87969=ORIENTED_EDGE ( 'NONE', *, *, #8165, .T. ) ;
#87970=CARTESIAN_POINT ( 'NONE',  ( -23.15000000000000213, 76.00000000001195133, -103.0231074845243171 ) ) ;
#87983=DIRECTION ( 'NONE',  ( 0.000000000000000000, -1.000000000000000000, 0.000000000000000000 ) ) ;
#87984=EDGE_CURVE ( 'NONE', #237421, #83796, #15053, .T. ) ;
#87990=EDGE_LOOP ( 'NONE', ( #40879, #25453, #146270, #177215 ) ) ;
#88029=ORIENTED_EDGE ( 'NONE', *, *, #167170, .F. ) ;
#88096=TOROIDAL_SURFACE ( 'NONE', #242237, 3.899999999999999467, 0.1000000000000000056 ) ;
#88118=ADVANCED_FACE ( 'NONE', ( #108950 ), #146779, .F. ) ;
#88135=AXIS2_PLACEMENT_3D ( 'NONE', #56041, #75658, #255502 ) ;
#88166=EDGE_LOOP ( 'NONE', ( #11884, #189243, #3989, #41862 ) ) ;
#88229=CARTESIAN_POINT ( 'NONE',  ( -18.59999999999999787, 64.35000000001187459, -90.87310748452438247 ) ) ;
#88298=EDGE_CURVE ( 'NONE', #49254, #171051, #39527, .T. ) ;
#88308=ORIENTED_EDGE ( 'NONE', *, *, #28171, .F. ) ;
#88332=CARTESIAN_POINT ( 'NONE',  ( 20.85000000000000142, 69.01799029515522932, -65.82695536626806643 ) ) ;
#88339=ADVANCED_FACE ( 'NONE', ( #21443 ), #137488, .F. ) ;
#88347=DIRECTION ( 'NONE',  ( 1.000000000000000000, 0.000000000000000000, 0.000000000000000000 ) ) ;
#88349=CIRCLE ( 'NONE', #238399, 0.1000000000000028644 ) ;
#88356=ADVANCED_FACE ( 'NONE', ( #202620 ), #239693, .T. ) ;
#88363=AXIS2_PLACEMENT_3D ( 'NONE', #180955, #84355, #4842 ) ;
#88373=ORIENTED_EDGE ( 'NONE', *, *, #225496, .T. ) ;
#88391=ORIENTED_EDGE ( 'NONE', *, *, #206301, .F. ) ;
#88406=CARTESIAN_POINT ( 'NONE',  ( 20.94999999999999929, 85.00000000001179501, -79.41707660717668205 ) ) ;
#88458=CARTESIAN_POINT ( 'NONE',  ( -22.50000000000094147, 75.89914163091340527, -114.7726746080137303 ) ) ;
#88504=EDGE_CURVE ( 'NONE', #211450, #218485, #135625, .T. ) ;
#88507=DIRECTION ( 'NONE',  ( 0.000000000000000000, -1.000000000000000000, -6.982962677686266711E-15 ) ) ;
#88510=TOROIDAL_SURFACE ( 'NONE', #176059, 0.9750000000000019762, 0.1000000000000000056 ) ;
#88516=CARTESIAN_POINT ( 'NONE',  ( -21.05000000000000071, 77.83534155023627932, -91.46795619196132066 ) ) ;
#88523=CIRCLE ( 'NONE', #196868, 2.000000000000001776 ) ;
#88527=ADVANCED_FACE ( 'NONE', ( #33024 ), #95508, .T. ) ;
#88561=VERTEX_POINT ( 'NONE', #72115 ) ;
#88585=CARTESIAN_POINT ( 'NONE',  ( 20.04142135623731136, 64.25000000001176659, -78.37310748452439668 ) ) ;
#88643=VECTOR ( 'NONE', #75269, 1000.000000000000000 ) ;
#88665=LINE ( 'NONE', #247766, #244475 ) ;
#88678=DIRECTION ( 'NONE',  ( -0.000000000000000000, 1.000000000000000000, 6.982962677686266711E-15 ) ) ;
#88684=ORIENTED_EDGE ( 'NONE', *, *, #167765, .F. ) ;
#88716=AXIS2_PLACEMENT_3D ( 'NONE', #235297, #533, #77486 ) ;
#88732=AXIS2_PLACEMENT_3D ( 'NONE', #38160, #55103, #117677 ) ;
#88760=CARTESIAN_POINT ( 'NONE',  ( -20.94999675878240808, 65.70692517833212776, -64.06446533783034170 ) ) ;
#88766=DIRECTION ( 'NONE',  ( 0.000000000000000000, 6.982962677686266711E-15, -1.000000000000000000 ) ) ;
#88769=VERTEX_POINT ( 'NONE', #156354 ) ;
#88772=EDGE_CURVE ( 'NONE', #165247, #7336, #84767, .T. ) ;
#88774=CARTESIAN_POINT ( 'NONE',  ( -21.78635804494510708, 68.96433851485876687, -103.1221125500320426 ) ) ;
#88795=EDGE_CURVE ( 'NONE', #152727, #213696, #118122, .T. ) ;
#88805=CARTESIAN_POINT ( 'NONE',  ( 21.04999999999999716, 65.31569084252679147, -95.49641069419752171 ) ) ;
#88806=ORIENTED_EDGE ( 'NONE', *, *, #133522, .T. ) ;
#88821=DIRECTION ( 'NONE',  ( 1.000000000000000000, 7.304098846218105085E-16, 4.217023435051677501E-16 ) ) ;
#88844=EDGE_CURVE ( 'NONE', #221948, #215622, #51452, .T. ) ;
#88855=CARTESIAN_POINT ( 'NONE',  ( 21.05000000000000071, 64.25000000001175238, -76.53791325517833855 ) ) ;
#88860=LINE ( 'NONE', #184125, #182185 ) ;
#88867=VERTEX_POINT ( 'NONE', #112075 ) ;
#88868=CARTESIAN_POINT ( 'NONE',  ( -18.59999999999999787, 85.32100840337318459, -95.78716923544635620 ) ) ;
#88870=ORIENTED_EDGE ( 'NONE', *, *, #192649, .T. ) ;
#88875=CARTESIAN_POINT ( 'NONE',  ( 21.05000000000000071, 65.27628289530437655, -95.35819391543677170 ) ) ;
#88907=ORIENTED_EDGE ( 'NONE', *, *, #99690, .T. ) ;
#88920=ORIENTED_EDGE ( 'NONE', *, *, #251710, .F. ) ;
#88925=B_SPLINE_CURVE_WITH_KNOTS ( 'NONE', 3,
 ( #170945, #250420, #88760, #187898, #151349, #247858, #230887, #146180, #206168, #28863, #69241, #9242, #27569, #186618, #109621, #87483, #167073, #189176, #67934 ),
 .UNSPECIFIED., .F., .F.,
 ( 4, 3, 3, 3, 3, 3, 4 ),
 ( -2.000416914659873068E-06, 0.000000000000000000, 4.714008503744566487E-05, 9.979203887777271477E-05, 0.0001372215519229485938, 0.0001635031576220933387, 0.0001900083748504131887 ),
 .UNSPECIFIED. ) ;
#88936=VERTEX_POINT ( 'NONE', #119786 ) ;
#88959=VERTEX_POINT ( 'NONE', #222691 ) ;
#88979=DIRECTION ( 'NONE',  ( 2.952720810173289112E-16, 1.000000000000000000, 7.086529944415894657E-15 ) ) ;
#89029=CARTESIAN_POINT ( 'NONE',  ( 18.49351773456776016, 85.44302569515703283, -95.83778195849694725 ) ) ;
#89048=CARTESIAN_POINT ( 'NONE',  ( 20.22516295850462598, 66.10063570456303239, -95.11304177243273728 ) ) ;
#89056=CARTESIAN_POINT ( 'NONE',  ( 21.05000000000010374, 75.98528214348843335, -109.3678308886146056 ) ) ;
#89064=CARTESIAN_POINT ( 'NONE',  ( -20.54999999999999716, 84.73084112150721126, -93.42503276553991043 ) ) ;
#89069=FACE_OUTER_BOUND ( 'NONE', #26301, .T. ) ;
#89101=DIRECTION ( 'NONE',  ( 0.000000000000000000, -1.000000000000000000, -6.982962677686265922E-15 ) ) ;
#89119=EDGE_CURVE ( 'NONE', #189189, #225321, #219009, .T. ) ;
#89124=LINE ( 'NONE', #128261, #66254 ) ;
#89184=CIRCLE ( 'NONE', #10083, 0.09999999999999520384 ) ;
#89206=VECTOR ( 'NONE', #19605, 1000.000000000000000 ) ;
#89219=DIRECTION ( 'NONE',  ( 0.000000000000000000, 0.000000000000000000, 1.000000000000000000 ) ) ;
#89241=CARTESIAN_POINT ( 'NONE',  ( 20.94999675878240808, 65.70692517833212776, -64.06446533783034170 ) ) ;
#89269=DIRECTION ( 'NONE',  ( 1.000000000000000000, 7.304098846218134667E-16, 5.100424963727256530E-30 ) ) ;
#89306=EDGE_CURVE ( 'NONE', #142842, #71479, #184955, .T. ) ;
#89307=DIRECTION ( 'NONE',  ( -4.336808689942052446E-15, 0.8660254037844445918, 0.4999999999999896194 ) ) ;
#89340=EDGE_LOOP ( 'NONE', ( #165121, #176620, #250025 ) ) ;
#89345=ORIENTED_EDGE ( 'NONE', *, *, #137705, .F. ) ;
#89353=EDGE_LOOP ( 'NONE', ( #54342, #220095, #191287, #122976 ) ) ;
#89357=EDGE_CURVE ( 'NONE', #31810, #3980, #194039, .T. ) ;
#89359=CARTESIAN_POINT ( 'NONE',  ( 21.14999999999998082, 87.75000000001193712, -103.0231074845242318 ) ) ;
#89396=DIRECTION ( 'NONE',  ( 0.000000000000000000, 0.9999631594459055250, 0.008583690987131395445 ) ) ;
#89419=CYLINDRICAL_SURFACE ( 'NONE', #102893, 0.1000000000000028644 ) ;
#89434=CARTESIAN_POINT ( 'NONE',  ( -18.50000000000000000, 64.25000000001186606, -90.87310748452439668 ) ) ;
#89439=CIRCLE ( 'NONE', #222704, 0.2000000000000057288 ) ;
#89444=CARTESIAN_POINT ( 'NONE',  ( -20.94999999999999929, 74.75000000001189449, -95.02310748452431710 ) ) ;
#89454=CARTESIAN_POINT ( 'NONE',  ( 18.41832399655377372, 85.68240326668576756, -62.86626386449687942 ) ) ;
#89470=ORIENTED_EDGE ( 'NONE', *, *, #143324, .F. ) ;
#89508=CARTESIAN_POINT ( 'NONE',  ( -23.25000000000000000, 64.25000000001170974, -69.52310748452438816 ) ) ;
#89520=ADVANCED_FACE ( 'NONE', ( #20533 ), #158768, .T. ) ;
#89571=DIRECTION ( 'NONE',  ( 1.000000000000000000, 0.000000000000000000, 0.000000000000000000 ) ) ;
#89597=DIRECTION ( 'NONE',  ( 0.000000000000000000, -5.551115123125777653E-14, 1.000000000000000000 ) ) ;
#89607=ORIENTED_EDGE ( 'NONE', *, *, #117958, .F. ) ;
#89618=EDGE_LOOP ( 'NONE', ( #148182, #68714, #206449, #78546 ) ) ;
#89644=VERTEX_POINT ( 'NONE', #189853 ) ;
#89668=ADVANCED_FACE ( 'NONE', ( #251091 ), #170340, .T. ) ;
#89683=EDGE_CURVE ( 'NONE', #224804, #204844, #201695, .T. ) ;
#89684=EDGE_LOOP ( 'NONE', ( #132044, #191975, #249343, #160498 ) ) ;
#89685=ORIENTED_EDGE ( 'NONE', *, *, #45698, .T. ) ;
#89688=CARTESIAN_POINT ( 'NONE',  ( -18.59999999999999787, 64.35000000001203091, -114.7731074845243882 ) ) ;
#89734=CIRCLE ( 'NONE', #235473, 0.1000000000000055705 ) ;
#89766=DIRECTION ( 'NONE',  ( 1.000000000000000000, 0.000000000000000000, 0.000000000000000000 ) ) ;
#89772=DIRECTION ( 'NONE',  ( 1.000000000000000000, 0.000000000000000000, 0.000000000000000000 ) ) ;
#89788=ORIENTED_EDGE ( 'NONE', *, *, #6665, .F. ) ;
#89804=CARTESIAN_POINT ( 'NONE',  ( 23.14999999999998437, 64.25000000001195133, -103.0231074845244024 ) ) ;
#89826=EDGE_CURVE ( 'NONE', #151773, #246470, #14283, .T. ) ;
#89828=ORIENTED_EDGE ( 'NONE', *, *, #208230, .T. ) ;
#89866=ORIENTED_EDGE ( 'NONE', *, *, #20351, .F. ) ;
#89868=EDGE_CURVE ( 'NONE', #50671, #224268, #104523, .T. ) ;
#89886=ORIENTED_EDGE ( 'NONE', *, *, #199612, .T. ) ;
#89906=ADVANCED_FACE ( 'NONE', ( #182840 ), #143675, .F. ) ;
#89925=ADVANCED_FACE ( 'NONE', ( #161991 ), #134660, .T. ) ;
#89929=EDGE_CURVE ( 'NONE', #11679, #66389, #101297, .T. ) ;
#89973=AXIS2_PLACEMENT_3D ( 'NONE', #202119, #242519, #226806 ) ;
#89983=AXIS2_PLACEMENT_3D ( 'NONE', #72622, #107868, #67459 ) ;
#89984=VERTEX_POINT ( 'NONE', #71866 ) ;
#89989=DIRECTION ( 'NONE',  ( 1.000000000000000000, 0.000000000000000000, 0.000000000000000000 ) ) ;
#90009=CARTESIAN_POINT ( 'NONE',  ( 19.97071067811865319, 64.27928932189311695, -78.31452884076171017 ) ) ;
#90038=ORIENTED_EDGE ( 'NONE', *, *, #242805, .F. ) ;
#90056=CARTESIAN_POINT ( 'NONE',  ( -18.40000000000000213, 85.51932773110434027, -96.05013110796491560 ) ) ;
#90102=VERTEX_POINT ( 'NONE', #97796 ) ;
#90120=AXIS2_PLACEMENT_3D ( 'NONE', #227587, #51491, #148062 ) ;
#90130=AXIS2_PLACEMENT_3D ( 'NONE', #38631, #175587, #154748 ) ;
#90134=B_SPLINE_CURVE_WITH_KNOTS ( 'NONE', 3,
 ( #221253, #179601, #178326, #137866, #199147, #83008, #160044, #140439, #122184, #81724, #119623, #904, #3495, #201707, #23097, #80435, #79176, #120921, #38796 ),
 .UNSPECIFIED., .F., .F.,
 ( 4, 3, 3, 3, 3, 3, 4 ),
 ( -2.000416914649330048E-06, 0.000000000000000000, 4.714008503747417261E-05, 9.979203887780082271E-05, 0.0001372215519229642606, 0.0001635031576221119057, 0.0001900083748504280965 ),
 .UNSPECIFIED. ) ;
#90174=SPHERICAL_SURFACE ( 'NONE', #14421, 0.1000000000000000056 ) ;
#90205=ORIENTED_EDGE ( 'NONE', *, *, #202590, .T. ) ;
#90249=AXIS2_PLACEMENT_3D ( 'NONE', #13772, #1888, #60585 ) ;
#90281=ORIENTED_EDGE ( 'NONE', *, *, #183862, .T. ) ;
#90304=CARTESIAN_POINT ( 'NONE',  ( 20.94999999999999574, 77.16270174994990327, -94.92310748452430857 ) ) ;
#90314=CYLINDRICAL_SURFACE ( 'NONE', #216267, 4.000000000000003553 ) ;
#90334=AXIS2_PLACEMENT_3D ( 'NONE', #59391, #214645, #198932 ) ;
#90341=EDGE_CURVE ( 'NONE', #255841, #167682, #247610, .T. ) ;
#90392=EDGE_LOOP ( 'NONE', ( #242700, #174962, #17394, #231908 ) ) ;
#90393=DIRECTION ( 'NONE',  ( 0.000000000000000000, -6.467318590049456648E-15, 1.000000000000000000 ) ) ;
#90412=EDGE_CURVE ( 'NONE', #168199, #152727, #193136, .T. ) ;
#90442=ORIENTED_EDGE ( 'NONE', *, *, #89357, .T. ) ;
#90443=EDGE_CURVE ( 'NONE', #109375, #152727, #131509, .T. ) ;
#90452=CARTESIAN_POINT ( 'NONE',  ( 18.59999999999999076, 61.95000000001189733, -97.50941241376342816 ) ) ;
#90459=DIRECTION ( 'NONE',  ( -1.000000000000000000, 0.000000000000000000, 0.000000000000000000 ) ) ;
#90493=DIRECTION ( 'NONE',  ( 0.000000000000000000, -6.938893903907222067E-15, 1.000000000000000000 ) ) ;
#90510=VECTOR ( 'NONE', #168535, 1000.000000000000000 ) ;
#90548=ORIENTED_EDGE ( 'NONE', *, *, #183826, .T. ) ;
#90559=ORIENTED_EDGE ( 'NONE', *, *, #127696, .T. ) ;
#90564=ORIENTED_EDGE ( 'NONE', *, *, #7938, .F. ) ;
#90664=FACE_OUTER_BOUND ( 'NONE', #145235, .T. ) ;
#90691=CARTESIAN_POINT ( 'NONE',  ( -20.94999999999999929, 77.16412189325286874, -61.60825939895269698 ) ) ;
#90753=EDGE_CURVE ( 'NONE', #22444, #20758, #66090, .T. ) ;
#90767=CARTESIAN_POINT ( 'NONE',  ( 23.24999999999999289, 64.35000000001201670, -114.7731074845243882 ) ) ;
#90774=DIRECTION ( 'NONE',  ( 0.000000000000000000, -6.982962677686266711E-15, 1.000000000000000000 ) ) ;
#90803=VECTOR ( 'NONE', #228865, 1000.000000000000000 ) ;
#90827=ORIENTED_EDGE ( 'NONE', *, *, #175726, .T. ) ;
#90846=CARTESIAN_POINT ( 'NONE',  ( -18.59999999999999787, 68.97833521811159585, -65.68954208262705663 ) ) ;
#90869=ORIENTED_EDGE ( 'NONE', *, *, #69215, .F. ) ;
#90875=CARTESIAN_POINT ( 'NONE',  ( 20.94999999999999574, 77.34908441863890971, -95.03660852097883094 ) ) ;
#90879=EDGE_CURVE ( 'NONE', #183416, #20030, #13577, .T. ) ;
#90899=B_SPLINE_CURVE_WITH_KNOTS ( 'NONE', 3,
 ( #20861, #3840, #165493, #202042, #183762, #1246, #25979, #119966 ),
 .UNSPECIFIED., .F., .F.,
 ( 4, 2, 2, 4 ),
 ( 0.000000000000000000, 9.550056980124262422E-05, 0.0001910011396024852484, 0.0003820022792049918557 ),
 .UNSPECIFIED. ) ;
#90917=ORIENTED_EDGE ( 'NONE', *, *, #179878, .F. ) ;
#90950=EDGE_CURVE ( 'NONE', #107898, #245381, #41115, .T. ) ;
#90951=ORIENTED_EDGE ( 'NONE', *, *, #70378, .T. ) ;
#90982=ADVANCED_FACE ( 'NONE', ( #220995 ), #218417, .T. ) ;
#91039=FACE_OUTER_BOUND ( 'NONE', #4673, .T. ) ;
#91045=VERTEX_POINT ( 'NONE', #59328 ) ;
#91050=CARTESIAN_POINT ( 'NONE',  ( 18.59999999999999432, 74.36282728704149747, -91.44095411905230719 ) ) ;
#91065=AXIS2_PLACEMENT_3D ( 'NONE', #211401, #151443, #53612 ) ;
#91100=CARTESIAN_POINT ( 'NONE',  ( 21.05000000000000071, 67.22371710471941242, -94.46447848938342418 ) ) ;
#91113=VERTEX_POINT ( 'NONE', #206586 ) ;
#91166=FACE_OUTER_BOUND ( 'NONE', #28147, .T. ) ;
#91179=ADVANCED_FACE ( 'NONE', ( #104873 ), #244423, .T. ) ;
#91180=EDGE_CURVE ( 'NONE', #40998, #162117, #5789, .T. ) ;
#91191=AXIS2_PLACEMENT_3D ( 'NONE', #230056, #108811, #11007 ) ;
#91239=EDGE_LOOP ( 'NONE', ( #210519, #49519, #251841, #33094 ) ) ;
#91260=CARTESIAN_POINT ( 'NONE',  ( -18.50000000000000000, 77.83534155023627932, -91.46795619196132066 ) ) ;
#91274=EDGE_CURVE ( 'NONE', #127648, #113736, #201861, .T. ) ;
#91291=VERTEX_POINT ( 'NONE', #137309 ) ;
#91310=LINE ( 'NONE', #156450, #238047 ) ;
#91313=DIRECTION ( 'NONE',  ( -1.000000000000000000, 0.000000000000000000, -0.000000000000000000 ) ) ;
#91315=FACE_OUTER_BOUND ( 'NONE', #170579, .T. ) ;
#91327=CARTESIAN_POINT ( 'NONE',  ( -20.85000000000000142, 77.36242903720497566, -61.63422623660309796 ) ) ;
#91329=CIRCLE ( 'NONE', #237057, 0.1000000000000028644 ) ;
#91349=DIRECTION ( 'NONE',  ( 0.000000000000000000, 0.000000000000000000, 1.000000000000000000 ) ) ;
#91352=DIRECTION ( 'NONE',  ( 0.000000000000000000, -0.8660254037844419273, 0.4999999999999942824 ) ) ;
#91355=ORIENTED_EDGE ( 'NONE', *, *, #1434, .T. ) ;
#91359=CARTESIAN_POINT ( 'NONE',  ( 20.94999999999999929, 70.15000000001178648, -79.65560470880227228 ) ) ;
#91367=CARTESIAN_POINT ( 'NONE',  ( -18.48550754432041288, 85.46339977857189751, -95.97431773210885808 ) ) ;
#91394=ORIENTED_EDGE ( 'NONE', *, *, #101472, .F. ) ;
#91397=CARTESIAN_POINT ( 'NONE',  ( -21.14999999999999858, 69.45934304831071415, -103.0231074845243597 ) ) ;
#91443=AXIS2_PLACEMENT_3D ( 'NONE', #55197, #214315, #56493 ) ;
#91534=EDGE_CURVE ( 'NONE', #65772, #99108, #212396, .T. ) ;
#91535=CARTESIAN_POINT ( 'NONE',  ( 21.05000000000000071, 65.43728505328341782, -95.56630537887993171 ) ) ;
#91545=ORIENTED_EDGE ( 'NONE', *, *, #114109, .T. ) ;
#91554=CYLINDRICAL_SURFACE ( 'NONE', #40037, 0.1000000000000028644 ) ;
#91556=ORIENTED_EDGE ( 'NONE', *, *, #122807, .F. ) ;
#91567=ORIENTED_EDGE ( 'NONE', *, *, #16429, .T. ) ;
#91568=DIRECTION ( 'NONE',  ( -1.000000000000000000, -0.000000000000000000, -0.000000000000000000 ) ) ;
#91571=CYLINDRICAL_SURFACE ( 'NONE', #31262, 0.09999999999999939493 ) ;
#91611=CARTESIAN_POINT ( 'NONE',  ( 18.46947024752537203, 85.50929715716800672, -96.03641803582634395 ) ) ;
#91628=EDGE_LOOP ( 'NONE', ( #139557, #224809, #82403, #19094 ) ) ;
#91633=EDGE_LOOP ( 'NONE', ( #96630, #65248 ) ) ;
#91720=FACE_OUTER_BOUND ( 'NONE', #247741, .T. ) ;
#91723=AXIS2_PLACEMENT_3D ( 'NONE', #179049, #39537, #177756 ) ;
#91728=CARTESIAN_POINT ( 'NONE',  ( 21.12802099929860944, 67.21944740978965172, -90.77491749959274614 ) ) ;
#91813=AXIS2_PLACEMENT_3D ( 'NONE', #67485, #186162, #143160 ) ;
#91874=DIRECTION ( 'NONE',  ( -0.000000000000000000, 1.000000000000000000, 6.352154140967427193E-15 ) ) ;
#91878=LINE ( 'NONE', #74917, #163493 ) ;
#91924=CARTESIAN_POINT ( 'NONE',  ( -20.05000000000000426, 66.75000000001179501, -81.87310748452438247 ) ) ;
#91930=LINE ( 'NONE', #30711, #7001 ) ;
#92009=ADVANCED_FACE ( 'NONE', ( #153422, #235464 ), #256249, .T. ) ;
#92059=VECTOR ( 'NONE', #207180, 1000.000000000000000 ) ;
#92066=CARTESIAN_POINT ( 'NONE',  ( -18.45140287520617761, 85.48607773954122990, -62.88258435783815514 ) ) ;
#92080=ADVANCED_FACE ( 'NONE', ( #243171 ), #114753, .T. ) ;
#92109=VERTEX_POINT ( 'NONE', #84052 ) ;
#92121=LINE ( 'NONE', #189950, #160567 ) ;
#92131=FACE_OUTER_BOUND ( 'NONE', #58316, .T. ) ;
#92150=ORIENTED_EDGE ( 'NONE', *, *, #142003, .T. ) ;
#92165=CARTESIAN_POINT ( 'NONE',  ( 19.99999999999998934, 64.35000000001180354, -81.77310748452438816 ) ) ;
#92170=ORIENTED_EDGE ( 'NONE', *, *, #51095, .T. ) ;
#92193=ORIENTED_EDGE ( 'NONE', *, *, #162954, .F. ) ;
#92198=CARTESIAN_POINT ( 'NONE',  ( 19.75857864376268935, 64.25000000001176659, -78.17310748452439384 ) ) ;
#92201=DIRECTION ( 'NONE',  ( -0.000000000000000000, 6.982962677686266711E-15, -1.000000000000000000 ) ) ;
#92229=ORIENTED_EDGE ( 'NONE', *, *, #51095, .F. ) ;
#92230=EDGE_CURVE ( 'NONE', #90102, #21472, #173247, .T. ) ;
#92256=ORIENTED_EDGE ( 'NONE', *, *, #134389, .T. ) ;
#92279=ORIENTED_EDGE ( 'NONE', *, *, #128039, .F. ) ;
#92284=DIRECTION ( 'NONE',  ( 0.000000000000000000, 1.000000000000000000, 6.982962677686266711E-15 ) ) ;
#92299=CARTESIAN_POINT ( 'NONE',  ( 18.49999999999999645, 74.27191306321758191, -116.1386724793565577 ) ) ;
#92348=VERTEX_POINT ( 'NONE', #255964 ) ;
#92353=AXIS2_PLACEMENT_3D ( 'NONE', #208755, #9250, #88766 ) ;
#92374=CARTESIAN_POINT ( 'NONE',  ( 18.49999999999999645, 76.00000000001170974, -69.52310748452431710 ) ) ;
#92380=FACE_OUTER_BOUND ( 'NONE', #147261, .T. ) ;
#92401=EDGE_LOOP ( 'NONE', ( #104397, #37670, #104993 ) ) ;
#92415=DIRECTION ( 'NONE',  ( 0.000000000000000000, -1.000000000000000000, -6.982962677686265922E-15 ) ) ;
#92424=DIRECTION ( 'NONE',  ( 0.000000000000000000, 0.000000000000000000, 1.000000000000000000 ) ) ;
#92496=CARTESIAN_POINT ( 'NONE',  ( -23.25000000000000000, 71.65000000001187175, -90.67310748452433700 ) ) ;
#92498=VERTEX_POINT ( 'NONE', #2969 ) ;
#92532=EDGE_CURVE ( 'NONE', #11679, #88959, #181636, .T. ) ;
#92535=DIRECTION ( 'NONE',  ( 0.000000000000000000, 0.1455152366551500653, 0.9893560106964507384 ) ) ;
#92539=CARTESIAN_POINT ( 'NONE',  ( 23.14999999999999503, 64.35000000001176090, -76.43791325517833002 ) ) ;
#92542=FACE_OUTER_BOUND ( 'NONE', #154980, .T. ) ;
#92549=AXIS2_PLACEMENT_3D ( 'NONE', #121601, #202390, #104536 ) ;
#92614=ADVANCED_FACE ( 'NONE', ( #59066 ), #39577, .F. ) ;
#92631=EDGE_CURVE ( 'NONE', #2690, #206918, #164634, .T. ) ;
#92644=CARTESIAN_POINT ( 'NONE',  ( -20.64999999999999858, 68.85000000001180354, -81.77310748452435973 ) ) ;
#92693=ORIENTED_EDGE ( 'NONE', *, *, #173421, .T. ) ;
#92756=ORIENTED_EDGE ( 'NONE', *, *, #162043, .T. ) ;
#92810=CIRCLE ( 'NONE', #71989, 0.2000000000000057288 ) ;
#92816=EDGE_LOOP ( 'NONE', ( #221059, #129050, #137602, #3846 ) ) ;
#92826=CARTESIAN_POINT ( 'NONE',  ( -18.59999999999999787, 76.00000000001165290, -61.62310748452430431 ) ) ;
#92828=VECTOR ( 'NONE', #230721, 1000.000000000000000 ) ;
#92840=DIRECTION ( 'NONE',  ( 1.000000000000000000, 0.000000000000000000, 0.000000000000000000 ) ) ;
#92873=CARTESIAN_POINT ( 'NONE',  ( -23.15000000000000213, 64.25000000001186606, -90.87310748452438247 ) ) ;
#92894=DIRECTION ( 'NONE',  ( 1.000000000000000000, 0.000000000000000000, 0.000000000000000000 ) ) ;
#92897=ORIENTED_EDGE ( 'NONE', *, *, #243016, .F. ) ;
#92903=EDGE_LOOP ( 'NONE', ( #38274, #164760, #222308, #139540, #194782 ) ) ;
#92907=CARTESIAN_POINT ( 'NONE',  ( 21.05000000000000071, 76.01454569058293487, -109.5201252709567541 ) ) ;
#92934=ORIENTED_EDGE ( 'NONE', *, *, #180379, .T. ) ;
#92950=EDGE_CURVE ( 'NONE', #23326, #167954, #107101, .T. ) ;
#92956=CARTESIAN_POINT ( 'NONE',  ( 21.09551895715278746, 65.37856267284385581, -90.78598281862467445 ) ) ;
#93000=AXIS2_PLACEMENT_3D ( 'NONE', #203798, #138658, #81262 ) ;
#93030=CIRCLE ( 'NONE', #105463, 0.1000000000000000888 ) ;
#93052=DIRECTION ( 'NONE',  ( 0.000000000000000000, 0.000000000000000000, 1.000000000000000000 ) ) ;
#93058=CARTESIAN_POINT ( 'NONE',  ( 18.49999999999998934, 65.75000000001176659, -78.27310748452438816 ) ) ;
#93065=ADVANCED_FACE ( 'NONE', ( #110530 ), #140409, .F. ) ;
#93112=DIRECTION ( 'NONE',  ( 1.000000000000000000, 0.000000000000000000, 0.000000000000000000 ) ) ;
#93133=CARTESIAN_POINT ( 'NONE',  ( -18.53317502108577486, 65.67736539654923433, -63.96251168765718376 ) ) ;
#93138=CARTESIAN_POINT ( 'NONE',  ( 23.25000000000000000, 87.48912529308779540, -72.62310748452422615 ) ) ;
#93142=CARTESIAN_POINT ( 'NONE',  ( 21.05000000000000071, 76.00000000001170974, -69.52310748452431710 ) ) ;
#93153=DIRECTION ( 'NONE',  ( -1.000000000000000000, -0.000000000000000000, -0.000000000000000000 ) ) ;
#93179=EDGE_CURVE ( 'NONE', #21614, #38211, #153118, .T. ) ;
#93180=PLANE ( 'NONE',  #124482 ) ;
#93191=DIRECTION ( 'NONE',  ( 1.000000000000000000, -0.000000000000000000, 0.000000000000000000 ) ) ;
#93195=CARTESIAN_POINT ( 'NONE',  ( -18.59999999999999787, 85.48068669529064323, -62.58199231576639932 ) ) ;
#93209=ORIENTED_EDGE ( 'NONE', *, *, #58735, .T. ) ;
#93211=CYLINDRICAL_SURFACE ( 'NONE', #36261, 0.09999999999999939493 ) ;
#93227=CARTESIAN_POINT ( 'NONE',  ( -21.05000000000000071, 74.16465844978745281, -91.46795619196133487 ) ) ;
#93229=DIRECTION ( 'NONE',  ( -1.000000000000000000, 3.265361837132813093E-16, 2.280189983783949500E-30 ) ) ;
#93236=EDGE_CURVE ( 'NONE', #46226, #23758, #194621, .T. ) ;
#93238=CARTESIAN_POINT ( 'NONE',  ( -18.59999999999999787, 74.16465844978745281, -91.46795619196133487 ) ) ;
#93263=ORIENTED_EDGE ( 'NONE', *, *, #35791, .F. ) ;
#93270=DIRECTION ( 'NONE',  ( 0.000000000000000000, -7.272083257015735086E-15, 1.000000000000000000 ) ) ;
#93284=DIRECTION ( 'NONE',  ( -1.000000000000000000, 0.000000000000000000, -0.000000000000000000 ) ) ;
#93321=CARTESIAN_POINT ( 'NONE',  ( 21.05000000000000071, 64.25000000001175238, -76.53791325517833855 ) ) ;
#93349=CARTESIAN_POINT ( 'NONE',  ( -18.49513951962168434, 85.43772502668934976, -62.74503490949511075 ) ) ;
#93370=TOROIDAL_SURFACE ( 'NONE', #105834, 0.2000000000000000111, 0.1000000000000000056 ) ;
#93428=DIRECTION ( 'NONE',  ( 0.000000000000000000, 0.000000000000000000, 1.000000000000000000 ) ) ;
#93432=CARTESIAN_POINT ( 'NONE',  ( 20.95346350065193519, 67.11282275083739535, -94.51137553748898767 ) ) ;
#93434=DIRECTION ( 'NONE',  ( 0.000000000000000000, 0.1350103645451807555, 0.9908441862701609093 ) ) ;
#93543=ORIENTED_EDGE ( 'NONE', *, *, #47757, .T. ) ;
#93545=ORIENTED_EDGE ( 'NONE', *, *, #178063, .F. ) ;
#93561=ORIENTED_EDGE ( 'NONE', *, *, #173958, .T. ) ;
#93582=TOROIDAL_SURFACE ( 'NONE', #97827, 0.2000000000000000111, 0.1000000000000000056 ) ;
#93661=ORIENTED_EDGE ( 'NONE', *, *, #184577, .F. ) ;
#93689=DIRECTION ( 'NONE',  ( 1.000000000000000000, 0.000000000000000000, 0.000000000000000000 ) ) ;
#93702=DIRECTION ( 'NONE',  ( 1.000000000000000000, 0.000000000000000000, 0.000000000000000000 ) ) ;
#93715=ORIENTED_EDGE ( 'NONE', *, *, #145570, .F. ) ;
#93727=ORIENTED_EDGE ( 'NONE', *, *, #52025, .T. ) ;
#93736=CIRCLE ( 'NONE', #239497, 0.09999999999999939493 ) ;
#93789=ORIENTED_EDGE ( 'NONE', *, *, #158900, .T. ) ;
#93833=CARTESIAN_POINT ( 'NONE',  ( -21.05000000000000071, 74.83729825007388570, -94.92310748452432279 ) ) ;
#93869=CARTESIAN_POINT ( 'NONE',  ( 18.49999999999999289, 69.15387683765909799, -65.78538121767449809 ) ) ;
#93890=CARTESIAN_POINT ( 'NONE',  ( -22.48660254037843487, 64.35000000001194564, -103.0731074845243711 ) ) ;
#93932=CARTESIAN_POINT ( 'NONE',  ( -22.39999999999999858, 68.20922040163854660, -103.0231074845243739 ) ) ;
#93943=DIRECTION ( 'NONE',  ( 1.000000000000000000, -0.000000000000000000, 0.000000000000000000 ) ) ;
#93955=DIRECTION ( 'NONE',  ( 0.000000000000000000, 0.9893560106964510714, -0.1455152366551481502 ) ) ;
#93972=CYLINDRICAL_SURFACE ( 'NONE', #3470, 0.1000000000000028644 ) ;
#93977=EDGE_LOOP ( 'NONE', ( #197702, #110081 ) ) ;
#94001=CARTESIAN_POINT ( 'NONE',  ( 21.05000000000000071, 85.00000000001179501, -79.01707660717669057 ) ) ;
#94016=ORIENTED_EDGE ( 'NONE', *, *, #111284, .F. ) ;
#94039=VECTOR ( 'NONE', #61053, 1000.000000000000114 ) ;
#94092=ORIENTED_EDGE ( 'NONE', *, *, #203929, .T. ) ;
#94137=FACE_OUTER_BOUND ( 'NONE', #162806, .T. ) ;
#94151=EDGE_LOOP ( 'NONE', ( #243469, #12014, #125379 ) ) ;
#94157=AXIS2_PLACEMENT_3D ( 'NONE', #4001, #6568, #100501 ) ;
#94191=CARTESIAN_POINT ( 'NONE',  ( 21.05000000000000071, 75.96798630682398823, -109.2819502080621277 ) ) ;
#94207=CARTESIAN_POINT ( 'NONE',  ( -21.64999999999999858, 68.65000000001180069, -81.77310748452435973 ) ) ;
#94217=CARTESIAN_POINT ( 'NONE',  ( -18.59999999999999787, 77.16412189325286874, -61.80825939895269272 ) ) ;
#94254=EDGE_CURVE ( 'NONE', #160204, #77606, #99438, .T. ) ;
#94257=CARTESIAN_POINT ( 'NONE',  ( -20.64999999999999858, 76.00000000001195133, -103.0231074845243171 ) ) ;
#94278=AXIS2_PLACEMENT_3D ( 'NONE', #126643, #165793, #83619 ) ;
#94280=FACE_OUTER_BOUND ( 'NONE', #154392, .T. ) ;
#94296=ORIENTED_EDGE ( 'NONE', *, *, #81322, .F. ) ;
#94307=ORIENTED_EDGE ( 'NONE', *, *, #144050, .F. ) ;
#94313=CARTESIAN_POINT ( 'NONE',  ( 18.59999999999999076, 64.35000000001177511, -78.17310748452437963 ) ) ;
#94339=EDGE_CURVE ( 'NONE', #254433, #233882, #112875, .T. ) ;
#94376=CIRCLE ( 'NONE', #33933, 0.1000000000000028644 ) ;
#94415=CARTESIAN_POINT ( 'NONE',  ( -18.50000324121759121, 65.70692517833214197, -64.06446533783034170 ) ) ;
#94420=VERTEX_POINT ( 'NONE', #9881 ) ;
#94422=ADVANCED_FACE ( 'NONE', ( #206808 ), #28202, .F. ) ;
#94430=EDGE_CURVE ( 'NONE', #106895, #18436, #62052, .T. ) ;
#94444=ORIENTED_EDGE ( 'NONE', *, *, #232009, .F. ) ;
#94471=DIRECTION ( 'NONE',  ( 0.000000000000000000, 0.000000000000000000, 1.000000000000000000 ) ) ;
#94524=CARTESIAN_POINT ( 'NONE',  ( 23.14999999999999858, 71.18691588786226987, -81.46462524104816794 ) ) ;
#94532=ADVANCED_FACE ( 'NONE', ( #71164 ), #169006, .F. ) ;
#94549=DIRECTION ( 'NONE',  ( 0.000000000000000000, -6.853228547068871147E-15, 1.000000000000000000 ) ) ;
#94556=FACE_OUTER_BOUND ( 'NONE', #69516, .T. ) ;
#94581=VECTOR ( 'NONE', #250081, 1000.000000000000114 ) ;
#94593=CARTESIAN_POINT ( 'NONE',  ( 18.44208962362758442, 85.55234049692009535, -62.68093442906086210 ) ) ;
#94597=LINE ( 'NONE', #34660, #218848 ) ;
#94620=AXIS2_PLACEMENT_3D ( 'NONE', #161493, #105305, #241017 ) ;
#94650=ADVANCED_FACE ( 'NONE', ( #59231 ), #81374, .T. ) ;
#94667=DIRECTION ( 'NONE',  ( 0.000000000000000000, 0.000000000000000000, 1.000000000000000000 ) ) ;
#94718=EDGE_LOOP ( 'NONE', ( #227038, #240743, #180892, #243925 ) ) ;
#94746=VERTEX_POINT ( 'NONE', #107389 ) ;
#94780=DIRECTION ( 'NONE',  ( 0.000000000000000000, 6.982962677686266711E-15, -1.000000000000000000 ) ) ;
#94794=ORIENTED_EDGE ( 'NONE', *, *, #7077, .T. ) ;
#94797=CARTESIAN_POINT ( 'NONE',  ( -23.25000000000000000, 85.00000000001179501, -78.81707660717668773 ) ) ;
#94903=LINE ( 'NONE', #253973, #41534 ) ;
#94905=CARTESIAN_POINT ( 'NONE',  ( -18.59999999999999787, 68.97833521811159585, -65.68954208262705663 ) ) ;
#94935=PRODUCT_DEFINITION_CONTEXT ( 'detailed design', #165871, 'design' ) ;
#94944=CARTESIAN_POINT ( 'NONE',  ( 21.05000000000000071, 69.58602111852350447, -102.9373083682503562 ) ) ;
#94945=ORIENTED_EDGE ( 'NONE', *, *, #62336, .T. ) ;
#94983=DIRECTION ( 'NONE',  ( -3.265361837132813093E-16, -1.000000000000000000, -7.086529944415894657E-15 ) ) ;
#94986=AXIS2_PLACEMENT_3D ( 'NONE', #90875, #93434, #34793 ) ;
#94996=EDGE_LOOP ( 'NONE', ( #194273, #45039, #240607, #33809 ) ) ;
#95066=DIRECTION ( 'NONE',  ( 1.000000000000000000, 0.000000000000000000, 0.000000000000000000 ) ) ;
#95108=CARTESIAN_POINT ( 'NONE',  ( 23.14999999999999858, 80.00000000001170974, -69.52310748452428868 ) ) ;
#95118=ORIENTED_EDGE ( 'NONE', *, *, #69830, .F. ) ;
#95125=CARTESIAN_POINT ( 'NONE',  ( 21.07189867249812210, 65.27501972991871071, -90.81065604224765764 ) ) ;
#95126=AXIS2_PLACEMENT_3D ( 'NONE', #26311, #44590, #105808 ) ;
#95139=CIRCLE ( 'NONE', #86727, 12.87499999999999822 ) ;
#95150=B_SPLINE_CURVE_WITH_KNOTS ( 'NONE', 3,
 ( #32860, #232327, #112367, #114922, #13265, #137053, #156653, #256946, #237438, #133204 ),
 .UNSPECIFIED., .F., .F.,
 ( 4, 3, 3, 4 ),
 ( 0.000000000000000000, 0.0002000000000008536833, 0.001000000000082972495, 0.001967863649483305062 ),
 .UNSPECIFIED. ) ;
#95160=CARTESIAN_POINT ( 'NONE',  ( -23.15000000000000213, 85.00000000001179501, -78.91707660717668205 ) ) ;
#95170=DIRECTION ( 'NONE',  ( 0.000000000000000000, 0.000000000000000000, -1.000000000000000000 ) ) ;
#95185=CARTESIAN_POINT ( 'NONE',  ( -20.94999999999999929, 70.10000000001193143, -92.80400771986793984 ) ) ;
#95188=CARTESIAN_POINT ( 'NONE',  ( 20.85000000000000142, 77.83585931145526615, -57.91866831572577468 ) ) ;
#95202=DIRECTION ( 'NONE',  ( -0.7071067811865475727, 0.7071067811865475727, 4.937700262164531476E-15 ) ) ;
#95214=ORIENTED_EDGE ( 'NONE', *, *, #169593, .F. ) ;
#95219=CARTESIAN_POINT ( 'NONE',  ( -21.51976009735018991, 69.08954155835274946, -103.0231074845243739 ) ) ;
#95235=CIRCLE ( 'NONE', #161902, 0.1000000000000028644 ) ;
#95269=ORIENTED_EDGE ( 'NONE', *, *, #160356, .T. ) ;
#95295=CARTESIAN_POINT ( 'NONE',  ( 20.94999999999999929, 87.65000000001172964, -72.42310748452422331 ) ) ;
#95302=CIRCLE ( 'NONE', #145354, 0.09999999999999520384 ) ;
#95337=CARTESIAN_POINT ( 'NONE',  ( 20.95263205890650582, 67.10425989211782394, -94.53359907758274971 ) ) ;
#95360=CARTESIAN_POINT ( 'NONE',  ( 20.94999999999999929, 70.15000000001192859, -92.89061026024637613 ) ) ;
#95366=ORIENTED_EDGE ( 'NONE', *, *, #15675, .T. ) ;
#95401=DIRECTION ( 'NONE',  ( 0.000000000000000000, 0.000000000000000000, 1.000000000000000000 ) ) ;
#95444=DIRECTION ( 'NONE',  ( 0.000000000000000000, -2.775557561562888827E-14, 1.000000000000000000 ) ) ;
#95465=DIRECTION ( 'NONE',  ( 0.000000000000000000, -1.000000000000000000, -6.982962677686266711E-15 ) ) ;
#95481=CARTESIAN_POINT ( 'NONE',  ( -20.64999999999999858, 68.75000000001179501, -81.87310748452436826 ) ) ;
#95489=AXIS2_PLACEMENT_3D ( 'NONE', #210887, #169232, #132642 ) ;
#95508=CYLINDRICAL_SURFACE ( 'NONE', #69022, 0.09999999999999939493 ) ;
#95515=EDGE_LOOP ( 'NONE', ( #73657, #86900, #14825, #235566, #141504, #47026, #184571, #201343, #157544, #155360, #185359, #80456 ) ) ;
#95540=DIRECTION ( 'NONE',  ( -1.000000000000000000, 0.000000000000000000, -0.000000000000000000 ) ) ;
#95546=ORIENTED_EDGE ( 'NONE', *, *, #225571, .F. ) ;
#95576=ORIENTED_EDGE ( 'NONE', *, *, #39151, .F. ) ;
#95654=FACE_OUTER_BOUND ( 'NONE', #204358, .T. ) ;
#95657=EDGE_LOOP ( 'NONE', ( #106826, #133801, #227536, #236165 ) ) ;
#95659=ORIENTED_EDGE ( 'NONE', *, *, #255330, .T. ) ;
#95665=VECTOR ( 'NONE', #130744, 999.9999999999998863 ) ;
#95678=PLANE ( 'NONE',  #161285 ) ;
#95690=CARTESIAN_POINT ( 'NONE',  ( 22.50000000000000000, 76.00000000001195133, -103.0231074845243171 ) ) ;
#95711=ADVANCED_FACE ( 'NONE', ( #151059 ), #3568, .T. ) ;
#95715=DIRECTION ( 'NONE',  ( 0.000000000000000000, -1.000000000000000000, 0.000000000000000000 ) ) ;
#95746=AXIS2_PLACEMENT_3D ( 'NONE', #123040, #242968, #162182 ) ;
#95766=AXIS2_PLACEMENT_3D ( 'NONE', #217351, #17877, #861 ) ;
#95782=DIRECTION ( 'NONE',  ( 0.000000000000000000, 0.000000000000000000, 1.000000000000000000 ) ) ;
#95808=LINE ( 'NONE', #562, #128368 ) ;
#95813=EDGE_LOOP ( 'NONE', ( #2992, #105060, #127861, #199701, #86499, #116264, #191353, #191942 ) ) ;
#95824=CARTESIAN_POINT ( 'NONE',  ( 20.94999999999999929, 85.50000000001188027, -93.12913836187179584 ) ) ;
#95828=DIRECTION ( 'NONE',  ( 0.000000000000000000, 6.982962677686266711E-15, -1.000000000000000000 ) ) ;
#95886=CARTESIAN_POINT ( 'NONE',  ( -23.15000000000000213, 64.35000000001180354, -81.67310748452439384 ) ) ;
#95919=AXIS2_PLACEMENT_3D ( 'NONE', #6479, #22222, #80870 ) ;
#95934=AXIS2_PLACEMENT_3D ( 'NONE', #189128, #224387, #164441 ) ;
#95945=ORIENTED_EDGE ( 'NONE', *, *, #188941, .T. ) ;
#95947=ADVANCED_FACE ( 'NONE', ( #219998 ), #183454, .F. ) ;
#95955=CARTESIAN_POINT ( 'NONE',  ( 20.94999999999999929, 65.27628289530427708, -81.77310748452438816 ) ) ;
#95980=DIRECTION ( 'NONE',  ( 1.000000000000000000, 0.000000000000000000, 0.000000000000000000 ) ) ;
#95985=CARTESIAN_POINT ( 'NONE',  ( -20.94999999999999929, 76.00000000001192291, -100.1231074845243256 ) ) ;
#95998=CIRCLE ( 'NONE', #16932, 0.1000000000000028644 ) ;
#96007=ADVANCED_FACE ( 'NONE', ( #199159 ), #220443, .T. ) ;
#96034=CARTESIAN_POINT ( 'NONE',  ( 22.39999999999999503, 76.00000000001200817, -110.7731074845243171 ) ) ;
#96074=ADVANCED_FACE ( 'NONE', ( #140454 ), #242123, .F. ) ;
#96127=DIRECTION ( 'NONE',  ( 0.000000000000000000, -7.147358527629766941E-15, 1.000000000000000000 ) ) ;
#96147=VERTEX_POINT ( 'NONE', #205554 ) ;
#96241=DIRECTION ( 'NONE',  ( -0.000000000000000000, -6.982962677686266711E-15, 1.000000000000000000 ) ) ;
#96242=DIRECTION ( 'NONE',  ( 0.000000000000000000, 0.000000000000000000, -1.000000000000000000 ) ) ;
#96278=CARTESIAN_POINT ( 'NONE',  ( -23.25000000000000000, 77.16412189325286874, -61.60825939895269698 ) ) ;
#96310=ORIENTED_EDGE ( 'NONE', *, *, #47559, .T. ) ;
#96314=ORIENTED_EDGE ( 'NONE', *, *, #205928, .F. ) ;
#96360=ORIENTED_EDGE ( 'NONE', *, *, #124691, .T. ) ;
#96363=CARTESIAN_POINT ( 'NONE',  ( 21.30000000000002558, 76.00000000001192291, -98.97310748452431994 ) ) ;
#96365=ORIENTED_EDGE ( 'NONE', *, *, #232777, .T. ) ;
#96367=AXIS2_PLACEMENT_3D ( 'NONE', #200832, #256895, #157897 ) ;
#96376=EDGE_LOOP ( 'NONE', ( #34830, #190505, #81241, #237824, #248976, #219571, #257596, #169425, #17180, #78922, #206770, #185103, #149915, #9384, #207889, #93543 ) ) ;
#96386=CARTESIAN_POINT ( 'NONE',  ( 21.05000000000000071, 65.27628289530434813, -90.86191719039695158 ) ) ;
#96396=VERTEX_POINT ( 'NONE', #167312 ) ;
#96407=PLANE ( 'NONE',  #897 ) ;
#96416=ORIENTED_EDGE ( 'NONE', *, *, #135373, .T. ) ;
#96438=EDGE_LOOP ( 'NONE', ( #193449, #17122, #227843, #10104 ) ) ;
#96440=CARTESIAN_POINT ( 'NONE',  ( 18.49999999999998934, 64.35000000001177511, -78.27310748452438816 ) ) ;
#96460=DIRECTION ( 'NONE',  ( 1.000000000000000000, -2.952720810173289112E-16, -2.061873921506763405E-30 ) ) ;
#96504=CARTESIAN_POINT ( 'NONE',  ( -20.94999999999999929, 64.40000000001190017, -96.09490425424884563 ) ) ;
#96528=VERTEX_POINT ( 'NONE', #82178 ) ;
#96574=AXIS2_PLACEMENT_3D ( 'NONE', #28501, #187552, #168002 ) ;
#96578=CARTESIAN_POINT ( 'NONE',  ( 20.04142135623730070, 64.25000000001179501, -81.67310748452439384 ) ) ;
#96580=DIRECTION ( 'NONE',  ( 1.000000000000000000, -2.952720810173289112E-16, -2.061873921506763405E-30 ) ) ;
#96589=ORIENTED_EDGE ( 'NONE', *, *, #35804, .F. ) ;
#96596=ORIENTED_EDGE ( 'NONE', *, *, #57755, .F. ) ;
#96610=ORIENTED_EDGE ( 'NONE', *, *, #220571, .F. ) ;
#96630=ORIENTED_EDGE ( 'NONE', *, *, #50623, .T. ) ;
#96633=EDGE_CURVE ( 'NONE', #10839, #129734, #206014, .T. ) ;
#96646=DIRECTION ( 'NONE',  ( 1.000000000000000000, 0.000000000000000000, 0.000000000000000000 ) ) ;
#96729=ORIENTED_EDGE ( 'NONE', *, *, #22188, .T. ) ;
#96733=EDGE_CURVE ( 'NONE', #86681, #224268, #174880, .T. ) ;
#96771=EDGE_CURVE ( 'NONE', #173885, #140050, #230719, .T. ) ;
#96790=EDGE_CURVE ( 'NONE', #256577, #102162, #224869, .T. ) ;
#96816=EDGE_CURVE ( 'NONE', #211450, #240371, #29125, .T. ) ;
#96852=ADVANCED_FACE ( 'NONE', ( #138002 ), #97577, .F. ) ;
#96883=CARTESIAN_POINT ( 'NONE',  ( 21.53752568617673191, 69.21319212550805844, -103.1220819457950171 ) ) ;
#96909=VERTEX_POINT ( 'NONE', #221385 ) ;
#96914=CARTESIAN_POINT ( 'NONE',  ( -20.94999999999999929, 70.15000000001192859, -92.89061026024637613 ) ) ;
#96944=CIRCLE ( 'NONE', #205104, 0.09999999999999939493 ) ;
#96945=ORIENTED_EDGE ( 'NONE', *, *, #9068, .T. ) ;
#96947=DIRECTION ( 'NONE',  ( -1.000000000000000000, -0.000000000000000000, -0.000000000000000000 ) ) ;
#96948=ORIENTED_EDGE ( 'NONE', *, *, #212283, .F. ) ;
#96955=ORIENTED_EDGE ( 'NONE', *, *, #86590, .F. ) ;
#96972=DIRECTION ( 'NONE',  ( -1.000000000000000000, 0.000000000000000000, -0.000000000000000000 ) ) ;
#96989=VECTOR ( 'NONE', #119306, 999.9999999999998863 ) ;
#97048=ORIENTED_EDGE ( 'NONE', *, *, #146914, .F. ) ;
#97065=CIRCLE ( 'NONE', #167874, 0.09999999999999799327 ) ;
#97069=CARTESIAN_POINT ( 'NONE',  ( -20.94999999999999929, 87.65000000001192859, -99.92310748452422331 ) ) ;
#97090=ORIENTED_EDGE ( 'NONE', *, *, #205819, .T. ) ;
#97118=EDGE_LOOP ( 'NONE', ( #54929, #180937 ) ) ;
#97131=DIRECTION ( 'NONE',  ( 1.000000000000000000, 0.000000000000000000, 0.000000000000000000 ) ) ;
#97137=CARTESIAN_POINT ( 'NONE',  ( -23.25000000000000000, 76.00000000001169553, -67.42310748452430857 ) ) ;
#97157=DIRECTION ( 'NONE',  ( 0.000000000000000000, 0.000000000000000000, 1.000000000000000000 ) ) ;
#97158=CARTESIAN_POINT ( 'NONE',  ( -18.46907102845853643, 85.47372736477574051, -62.84707274578772740 ) ) ;
#97166=CIRCLE ( 'NONE', #105563, 0.1000000000000028644 ) ;
#97182=CARTESIAN_POINT ( 'NONE',  ( -23.15000000000000213, 76.00000000001169553, -67.52310748452430289 ) ) ;
#97194=EDGE_CURVE ( 'NONE', #215622, #164805, #111736, .T. ) ;
#97201=DIRECTION ( 'NONE',  ( 0.000000000000000000, 6.982962677686266711E-15, -1.000000000000000000 ) ) ;
#97238=ADVANCED_FACE ( 'NONE', ( #223338 ), #5564, .F. ) ;
#97253=CARTESIAN_POINT ( 'NONE',  ( 20.95159278453404639, 67.09210366206283993, -94.53838729941513463 ) ) ;
#97264=CARTESIAN_POINT ( 'NONE',  ( 18.50000000000000711, 85.41920976342116489, -95.77533802176530742 ) ) ;
#97269=LINE ( 'NONE', #76456, #169428 ) ;
#97283=ORIENTED_EDGE ( 'NONE', *, *, #184409, .T. ) ;
#97286=( BOUNDED_SURFACE ( )  B_SPLINE_SURFACE ( 3, 2, ( 
 ( #134070, #153709, #213613 ),
 ( #196615, #233211, #114523 ),
 ( #256536, #75425, #16720 ),
 ( #113234, #14165, #94944 ),
 ( #15439, #174553, #135351 ),
 ( #214900, #57084, #157542 ) ),
 .UNSPECIFIED., .F., .F., .F. ) 
 B_SPLINE_SURFACE_WITH_KNOTS ( ( 4, 2, 4 ),
 ( 3, 3 ),
 ( 0.0001792624049599557520, 0.0003686986002124558403, 0.0005581347954649559014 ),
 ( 0.000000000000000000, 1.000000000000000000 ),
 .UNSPECIFIED. ) 
 GEOMETRIC_REPRESENTATION_ITEM ( )  RATIONAL_B_SPLINE_SURFACE ( (
 ( 1.000000000000000000, 0.9238795325112858503, 1.000000000000000000),
 ( 1.000000000000000000, 0.9229318695231540914, 1.000000000000000000),
 ( 1.000000000000000000, 0.8926288119239994545, 1.000000000000000000),
 ( 1.000000000000000000, 0.8123777807262057005, 1.000000000000000000),
 ( 1.000000000000000000, 0.7629087100938296562, 1.000000000000000000),
 ( 1.000000000000000000, 0.7071067811865966446, 1.000000000000000000) ) ) 
 REPRESENTATION_ITEM ( '' )  SURFACE ( )  );
#97294=CARTESIAN_POINT ( 'NONE',  ( -18.59999999999999787, 77.26178616857691850, -94.93660852097882241 ) ) ;
#97301=VERTEX_POINT ( 'NONE', #83797 ) ;
#97302=ORIENTED_EDGE ( 'NONE', *, *, #247710, .T. ) ;
#97304=VECTOR ( 'NONE', #127998, 1000.000000000000000 ) ;
#97333=EDGE_CURVE ( 'NONE', #86374, #248733, #125763, .T. ) ;
#97368=DIRECTION ( 'NONE',  ( 0.000000000000000000, 0.4930308989875575865, 0.8700118002898125091 ) ) ;
#97370=ORIENTED_EDGE ( 'NONE', *, *, #205141, .F. ) ;
#97394=ADVANCED_FACE ( 'NONE', ( #111109 ), #169850, .T. ) ;
#97402=LINE ( 'NONE', #235654, #146441 ) ;
#97405=VECTOR ( 'NONE', #42358, 1000.000000000000000 ) ;
#97415=ORIENTED_EDGE ( 'NONE', *, *, #114713, .T. ) ;
#97429=DIRECTION ( 'NONE',  ( -0.000000000000000000, -1.000000000000000000, -6.982962677686266711E-15 ) ) ;
#97432=CIRCLE ( 'NONE', #18363, 1.899999999999999023 ) ;
#97433=CARTESIAN_POINT ( 'NONE',  ( -23.25000000000000000, 69.06610602788535402, -65.73746165015079157 ) ) ;
#97436=ORIENTED_EDGE ( 'NONE', *, *, #163355, .F. ) ;
#97474=ORIENTED_EDGE ( 'NONE', *, *, #50886, .F. ) ;
#97485=LINE ( 'NONE', #55786, #187430 ) ;
#97509=VECTOR ( 'NONE', #185149, 1000.000000000000000 ) ;
#97529=DIRECTION ( 'NONE',  ( 3.616040088954490704E-32, 7.105427357601001859E-15, -1.000000000000000000 ) ) ;
#97546=DIRECTION ( 'NONE',  ( -1.000000000000000000, -0.000000000000000000, -0.000000000000000000 ) ) ;
#97577=CYLINDRICAL_SURFACE ( 'NONE', #179311, 0.5000000000000004441 ) ;
#97597=ORIENTED_EDGE ( 'NONE', *, *, #115285, .T. ) ;
#97626=ORIENTED_EDGE ( 'NONE', *, *, #243931, .F. ) ;
#97641=EDGE_CURVE ( 'NONE', #194138, #83796, #80948, .T. ) ;
#97650=VERTEX_POINT ( 'NONE', #120138 ) ;
#97655=VERTEX_POINT ( 'NONE', #202205 ) ;
#97665=CARTESIAN_POINT ( 'NONE',  ( -20.00857864376270001, 66.75000000001179501, -81.87310748452438247 ) ) ;
#97726=TOROIDAL_SURFACE ( 'NONE', #139432, 11.70000000000000107, 0.1000000000000000056 ) ;
#97731=DIRECTION ( 'NONE',  ( 0.000000000000000000, -6.938893903907222067E-15, 1.000000000000000000 ) ) ;
#97738=AXIS2_PLACEMENT_3D ( 'NONE', #126370, #24738, #182518 ) ;
#97749=VERTEX_POINT ( 'NONE', #204753 ) ;
#97796=CARTESIAN_POINT ( 'NONE',  ( 21.05000000000000071, 85.50000000001188027, -93.12913836187179584 ) ) ;
#97809=FACE_OUTER_BOUND ( 'NONE', #45077, .T. ) ;
#97827=AXIS2_PLACEMENT_3D ( 'NONE', #74446, #176100, #172269 ) ;
#97857=DIRECTION ( 'NONE',  ( 0.000000000000000000, -2.771150684185008344E-14, -1.000000000000000000 ) ) ;
#97866=CIRCLE ( 'NONE', #2014, 0.09999999999999939493 ) ;
#97888=STYLED_ITEM ( 'NONE', ( #22357 ), #250584 ) ;
#97983=VECTOR ( 'NONE', #143823, 1000.000000000000000 ) ;
#97989=CARTESIAN_POINT ( 'NONE',  ( 20.94999999999999929, 87.29603075034721371, -99.97520832486037534 ) ) ;
#98006=DIRECTION ( 'NONE',  ( -1.000000000000000000, 0.000000000000000000, -0.000000000000000000 ) ) ;
#98012=CARTESIAN_POINT ( 'NONE',  ( 22.44352723754029810, 75.99072290496874871, -114.6728288298730263 ) ) ;
#98024=AXIS2_PLACEMENT_3D ( 'NONE', #168929, #210577, #30683 ) ;
#98061=CARTESIAN_POINT ( 'NONE',  ( 21.13461538461538680, 65.38541703798632909, -90.67310748452437963 ) ) ;
#98165=CARTESIAN_POINT ( 'NONE',  ( -20.00857864376270001, 66.85000000001180354, -81.77310748452437394 ) ) ;
#98166=EDGE_CURVE ( 'NONE', #70373, #47548, #76239, .T. ) ;
#98180=VERTEX_POINT ( 'NONE', #66235 ) ;
#98186=DIRECTION ( 'NONE',  ( -1.000000000000000000, -0.000000000000000000, -0.000000000000000000 ) ) ;
#98190=CYLINDRICAL_SURFACE ( 'NONE', #76444, 0.1000000000000028644 ) ;
#98202=DIRECTION ( 'NONE',  ( 0.000000000000000000, 1.000000000000000000, 6.853228547068871147E-15 ) ) ;
#98257=EDGE_CURVE ( 'NONE', #208155, #255663, #184982, .T. ) ;
#98266=FACE_OUTER_BOUND ( 'NONE', #23340, .T. ) ;
#98297=CIRCLE ( 'NONE', #178035, 0.5000000000000004441 ) ;
#98330=FACE_OUTER_BOUND ( 'NONE', #177249, .T. ) ;
#98337=DIRECTION ( 'NONE',  ( 1.000000000000000000, 0.000000000000000000, 0.000000000000000000 ) ) ;
#98358=DIRECTION ( 'NONE',  ( 0.000000000000000000, 6.982962677686267499E-15, -1.000000000000000000 ) ) ;
#98397=ORIENTED_EDGE ( 'NONE', *, *, #101141, .F. ) ;
#98426=FACE_OUTER_BOUND ( 'NONE', #208003, .T. ) ;
#98459=VECTOR ( 'NONE', #224649, 1000.000000000000000 ) ;
#98463=B_SPLINE_CURVE_WITH_KNOTS ( 'NONE', 3,
 ( #69671, #47497, #172658, #252129, #250838, #87897, #187055, #108772, #149209, #27991, #50081, #151783, #248288, #127057, #190916, #231312 ),
 .UNSPECIFIED., .F., .F.,
 ( 4, 3, 3, 3, 3, 4 ),
 ( 0.000000000000000000, 2.209075297431583676E-05, 5.594258369009758524E-05, 8.979524372341978606E-05, 0.0001236472815274614761, 0.0001574990747609543624 ),
 .UNSPECIFIED. ) ;
#98472=CARTESIAN_POINT ( 'NONE',  ( -23.15000000000000213, 76.00000000001195133, -103.0231074845243171 ) ) ;
#98476=ORIENTED_EDGE ( 'NONE', *, *, #205574, .T. ) ;
#98494=DIRECTION ( 'NONE',  ( 0.000000000000000000, 0.1568667991644355497, 0.9876197685951332295 ) ) ;
#98505=DIRECTION ( 'NONE',  ( 1.000000000000000000, -0.000000000000000000, 0.000000000000000000 ) ) ;
#98524=CYLINDRICAL_SURFACE ( 'NONE', #77450, 0.1000000000000028644 ) ;
#98546=DIRECTION ( 'NONE',  ( 0.000000000000000000, -0.7397360091702802620, 0.6728971962616779878 ) ) ;
#98575=EDGE_LOOP ( 'NONE', ( #187935, #31879, #243479, #197654 ) ) ;
#98616=CARTESIAN_POINT ( 'NONE',  ( 20.94999999999999929, 76.00000000001169553, -67.52310748452430289 ) ) ;
#98649=CARTESIAN_POINT ( 'NONE',  ( -23.25000000000000000, 70.05000000001177796, -79.82880978955917328 ) ) ;
#98674=DIRECTION ( 'NONE',  ( 1.000000000000000000, 0.000000000000000000, 0.000000000000000000 ) ) ;
#98689=CIRCLE ( 'NONE', #132051, 0.1000000000000028644 ) ;
#98719=DIRECTION ( 'NONE',  ( 0.000000000000000000, -7.189901751995769991E-15, 1.000000000000000000 ) ) ;
#98725=DIRECTION ( 'NONE',  ( -0.000000000000000000, 1.000000000000000000, 8.717686153663073805E-15 ) ) ;
#98730=AXIS2_PLACEMENT_3D ( 'NONE', #125020, #246241, #25917 ) ;
#98792=VERTEX_POINT ( 'NONE', #120485 ) ;
#98821=( BOUNDED_SURFACE ( )  B_SPLINE_SURFACE ( 3, 2, ( 
 ( #251990, #128203, #13397 ),
 ( #113761, #92907, #193317 ),
 ( #189462, #108631, #172517 ),
 ( #34268, #89056, #132049 ),
 ( #14702, #53794, #94191 ),
 ( #188178, #211596, #69528 ) ),
 .UNSPECIFIED., .F., .F., .F. ) 
 B_SPLINE_SURFACE_WITH_KNOTS ( ( 4, 2, 4 ),
 ( 3, 3 ),
 ( 0.0001300404313046710908, 0.0003183318589266662135, 0.0005066232865486613090 ),
 ( 0.000000000000000000, 1.000000000000000000 ),
 .UNSPECIFIED. ) 
 GEOMETRIC_REPRESENTATION_ITEM ( )  RATIONAL_B_SPLINE_SURFACE ( (
 ( 1.000000000000000000, 0.7071067811865597852, 1.000000000000000000),
 ( 1.000000000000000000, 0.7625113560545420111, 1.000000000000000000),
 ( 1.000000000000000000, 0.8126073484681639592, 1.000000000000000000),
 ( 1.000000000000000000, 0.8923049332739299011, 1.000000000000000000),
 ( 1.000000000000000000, 0.9231914937764394979, 1.000000000000000000),
 ( 1.000000000000000000, 0.9238795325112900692, 1.000000000000000000) ) ) 
 REPRESENTATION_ITEM ( '' )  SURFACE ( )  );
#98867=CARTESIAN_POINT ( 'NONE',  ( 21.05000000000000071, 65.27628289530437655, -95.35819391543677170 ) ) ;
#98876=AXIS2_PLACEMENT_3D ( 'NONE', #49219, #251260, #170512 ) ;
#98882=ORIENTED_EDGE ( 'NONE', *, *, #66559, .T. ) ;
#98886=CARTESIAN_POINT ( 'NONE',  ( 20.85000000000000142, 64.25000000001175238, -76.30697314750248950 ) ) ;
#98928=VERTEX_POINT ( 'NONE', #4339 ) ;
#98958=VERTEX_POINT ( 'NONE', #163436 ) ;
#98979=LINE ( 'NONE', #80713, #187649 ) ;
#98988=ORIENTED_EDGE ( 'NONE', *, *, #153309, .T. ) ;
#98998=CARTESIAN_POINT ( 'NONE',  ( -18.50000000000000000, 66.65000000001180069, -81.67310748452437963 ) ) ;
#99009=CARTESIAN_POINT ( 'NONE',  ( 18.47149038651511788, 85.67145715801837014, -62.85032114978587714 ) ) ;
#99023=DIRECTION ( 'NONE',  ( 0.000000000000000000, -1.000000000000000000, -6.982962677686266711E-15 ) ) ;
#99030=CIRCLE ( 'NONE', #248920, 0.1000000000000043771 ) ;
#99043=CARTESIAN_POINT ( 'NONE',  ( -20.64999999999999858, 74.00000000001186606, -90.29848556176222019 ) ) ;
#99063=AXIS2_PLACEMENT_3D ( 'NONE', #43747, #202814, #101097 ) ;
#99090=ORIENTED_EDGE ( 'NONE', *, *, #82467, .F. ) ;
#99108=VERTEX_POINT ( 'NONE', #134243 ) ;
#99131=EDGE_CURVE ( 'NONE', #36183, #229949, #121062, .T. ) ;
#99132=CARTESIAN_POINT ( 'NONE',  ( 18.59999999999999076, 74.25000000001186606, -91.35359592662267403 ) ) ;
#99195=DIRECTION ( 'NONE',  ( 0.000000000000000000, -0.1575844902526579161, -0.9875055080513779338 ) ) ;
#99211=CARTESIAN_POINT ( 'NONE',  ( 18.60000000000000142, 85.32100840337318459, -95.78716923544635620 ) ) ;
#99220=EDGE_LOOP ( 'NONE', ( #213342, #18816, #20209, #163084 ) ) ;
#99225=DIRECTION ( 'NONE',  ( 0.000000000000000000, 6.982962677686266711E-15, -1.000000000000000000 ) ) ;
#99247=DIRECTION ( 'NONE',  ( -2.952720810173289605E-16, -1.000000000000000000, -7.086529944415894657E-15 ) ) ;
#99267=ORIENTED_EDGE ( 'NONE', *, *, #226275, .T. ) ;
#99305=ORIENTED_EDGE ( 'NONE', *, *, #21874, .F. ) ;
#99315=ORIENTED_EDGE ( 'NONE', *, *, #22188, .F. ) ;
#99354=DIRECTION ( 'NONE',  ( 0.000000000000000000, -6.982962677686266711E-15, 1.000000000000000000 ) ) ;
#99362=CARTESIAN_POINT ( 'NONE',  ( -18.50000000000000000, 85.40000000001167280, -62.64106563635157698 ) ) ;
#99388=CARTESIAN_POINT ( 'NONE',  ( 22.39999999999999858, 68.20922040163857503, -103.1231074845243540 ) ) ;
#99438=CIRCLE ( 'NONE', #245225, 0.09999999999999739653 ) ;
#99445=DIRECTION ( 'NONE',  ( -1.000000000000000000, -0.000000000000000000, -0.000000000000000000 ) ) ;
#99464=CARTESIAN_POINT ( 'NONE',  ( -18.31331870001039874, 85.53629471919262528, -62.65452879353873072 ) ) ;
#99465=CARTESIAN_POINT ( 'NONE',  ( 21.93340585972004320, 68.67585297715810100, -103.0231074845243597 ) ) ;
#99498=VECTOR ( 'NONE', #82574, 999.9999999999998863 ) ;
#99503=EDGE_LOOP ( 'NONE', ( #139236, #29990 ) ) ;
#99506=DIRECTION ( 'NONE',  ( 1.000000000000000000, -6.938893903907222067E-15, -4.845403715540888588E-29 ) ) ;
#99519=ORIENTED_EDGE ( 'NONE', *, *, #163663, .F. ) ;
#99528=ORIENTED_EDGE ( 'NONE', *, *, #79647, .F. ) ;
#99557=AXIS2_PLACEMENT_3D ( 'NONE', #141921, #140637, #63668 ) ;
#99575=DIRECTION ( 'NONE',  ( -0.000000000000000000, -1.000000000000000000, -6.982962677686266711E-15 ) ) ;
#99605=AXIS2_PLACEMENT_3D ( 'NONE', #113171, #233149, #192716 ) ;
#99630=ADVANCED_FACE ( 'NONE', ( #41298 ), #154562, .F. ) ;
#99654=DIRECTION ( 'NONE',  ( 1.000000000000000000, 0.000000000000000000, 0.000000000000000000 ) ) ;
#99664=ADVANCED_FACE ( 'NONE', ( #197767 ), #79084, .F. ) ;
#99671=ORIENTED_EDGE ( 'NONE', *, *, #9303, .F. ) ;
#99690=EDGE_CURVE ( 'NONE', #155591, #214994, #83748, .T. ) ;
#99695=VECTOR ( 'NONE', #114511, 1000.000000000000000 ) ;
#99707=AXIS2_PLACEMENT_3D ( 'NONE', #142276, #44482, #23655 ) ;
#99713=CARTESIAN_POINT ( 'NONE',  ( 18.59999999999999076, 77.25000000001189449, -95.02310748452430289 ) ) ;
#99719=EDGE_CURVE ( 'NONE', #21472, #77606, #47660, .T. ) ;
#99749=DIRECTION ( 'NONE',  ( -0.000000000000000000, -0.1298341882519953583, -0.9915357197604862671 ) ) ;
#99755=DIRECTION ( 'NONE',  ( 0.000000000000000000, 0.000000000000000000, -1.000000000000000000 ) ) ;
#99778=CIRCLE ( 'NONE', #153852, 0.1000000000000028644 ) ;
#99793=VERTEX_POINT ( 'NONE', #25567 ) ;
#99801=DIRECTION ( 'NONE',  ( 1.000000000000000000, 0.000000000000000000, 0.000000000000000000 ) ) ;
#99806=DIRECTION ( 'NONE',  ( -1.000000000000000000, 0.000000000000000000, -0.000000000000000000 ) ) ;
#99826=EDGE_LOOP ( 'NONE', ( #146692, #73279, #103214 ) ) ;
#99845=LINE ( 'NONE', #80278, #181713 ) ;
#99847=CIRCLE ( 'NONE', #137295, 0.1000000000000028644 ) ;
#99856=ORIENTED_EDGE ( 'NONE', *, *, #128117, .F. ) ;
#99911=ADVANCED_FACE ( 'NONE', ( #230166 ), #114061, .T. ) ;
#99925=CARTESIAN_POINT ( 'NONE',  ( -20.94999999999999929, 64.35000000001171827, -69.52310748452438816 ) ) ;
#99934=CARTESIAN_POINT ( 'NONE',  ( 22.42357213249528769, 68.32706761365203363, -103.1221944485259314 ) ) ;
#99949=ORIENTED_EDGE ( 'NONE', *, *, #8978, .T. ) ;
#99971=FACE_OUTER_BOUND ( 'NONE', #238725, .T. ) ;
#100012=CARTESIAN_POINT ( 'NONE',  ( 18.59999999999999076, 65.79142135624907439, -78.27310748452437394 ) ) ;
#100033=DIRECTION ( 'NONE',  ( 0.000000000000000000, 0.1350103645451946055, -0.9908441862701591329 ) ) ;
#100052=FACE_OUTER_BOUND ( 'NONE', #51499, .T. ) ;
#100082=CIRCLE ( 'NONE', #29417, 3.900000000000000799 ) ;
#100101=FACE_OUTER_BOUND ( 'NONE', #24987, .T. ) ;
#100120=ORIENTED_EDGE ( 'NONE', *, *, #55261, .T. ) ;
#100155=CIRCLE ( 'NONE', #204405, 11.74999999999999645 ) ;
#100156=CARTESIAN_POINT ( 'NONE',  ( 21.04999999999999716, 65.49746832288542464, -95.46427766744905341 ) ) ;
#100157=LINE ( 'NONE', #177194, #94039 ) ;
#100170=PLANE ( 'NONE',  #191148 ) ;
#100194=DIRECTION ( 'NONE',  ( -1.000000000000000000, -0.000000000000000000, -0.000000000000000000 ) ) ;
#100209=DIRECTION ( 'NONE',  ( 0.000000000000000000, 0.000000000000000000, 1.000000000000000000 ) ) ;
#100212=CARTESIAN_POINT ( 'NONE',  ( -21.14999999999999858, 76.10000000001198828, -109.5637644362255543 ) ) ;
#100248=ORIENTED_EDGE ( 'NONE', *, *, #200961, .F. ) ;
#100258=ADVANCED_FACE ( 'NONE', ( #30124 ), #26262, .T. ) ;
#100268=CARTESIAN_POINT ( 'NONE',  ( 23.14999999999999858, 76.00000000001170974, -69.52310748452431710 ) ) ;
#100280=EDGE_CURVE ( 'NONE', #111063, #84368, #127925, .T. ) ;
#100299=VECTOR ( 'NONE', #92284, 1000.000000000000000 ) ;
#100307=ORIENTED_EDGE ( 'NONE', *, *, #131688, .F. ) ;
#100333=FACE_OUTER_BOUND ( 'NONE', #180991, .T. ) ;
#100377=ORIENTED_EDGE ( 'NONE', *, *, #154282, .F. ) ;
#100391=DIRECTION ( 'NONE',  ( -1.000000000000000000, -0.000000000000000000, -0.000000000000000000 ) ) ;
#100401=ORIENTED_EDGE ( 'NONE', *, *, #114713, .F. ) ;
#100470=DIRECTION ( 'NONE',  ( -1.000000000000000000, 2.952720810173289112E-16, 2.061873921506763405E-30 ) ) ;
#100501=DIRECTION ( 'NONE',  ( 0.000000000000000000, -0.9908441862701605762, 0.1350103645451835310 ) ) ;
#100503=ORIENTED_EDGE ( 'NONE', *, *, #81788, .F. ) ;
#100517=DIRECTION ( 'NONE',  ( 0.000000000000000000, 0.1455152366551500653, 0.9893560106964507384 ) ) ;
#100519=CARTESIAN_POINT ( 'NONE',  ( -23.15000000000000213, 76.00000000001170974, -69.52310748452431710 ) ) ;
#100540=DIRECTION ( 'NONE',  ( 1.000000000000000000, 0.000000000000000000, 0.000000000000000000 ) ) ;
#100543=DIRECTION ( 'NONE',  ( 0.000000000000000000, 1.000000000000000000, 6.853228547068871147E-15 ) ) ;
#100557=ORIENTED_EDGE ( 'NONE', *, *, #124653, .T. ) ;
#100575=FACE_OUTER_BOUND ( 'NONE', #38782, .T. ) ;
#100588=ORIENTED_EDGE ( 'NONE', *, *, #183826, .F. ) ;
#100609=ORIENTED_EDGE ( 'NONE', *, *, #234903, .T. ) ;
#100618=CARTESIAN_POINT ( 'NONE',  ( -21.07928932188134041, 69.67148334361864670, -103.1220026301787414 ) ) ;
#100664=ORIENTED_EDGE ( 'NONE', *, *, #22618, .F. ) ;
#100668=DIRECTION ( 'NONE',  ( 0.000000000000000000, 0.000000000000000000, -1.000000000000000000 ) ) ;
#100669=EDGE_CURVE ( 'NONE', #244131, #27688, #142588, .T. ) ;
#100693=EDGE_CURVE ( 'NONE', #193738, #11451, #55091, .T. ) ;
#100704=ADVANCED_FACE ( 'NONE', ( #150701 ), #52866, .F. ) ;
#100720=CARTESIAN_POINT ( 'NONE',  ( 22.49806830649814060, 64.35011034517287953, -103.1005718008498917 ) ) ;
#100721=CARTESIAN_POINT ( 'NONE',  ( 21.07928932188134397, 75.90110485435759813, -109.3516241409176217 ) ) ;
#100732=CARTESIAN_POINT ( 'NONE',  ( -18.40000000000000213, 85.50000000001168132, -62.92291809330220786 ) ) ;
#100750=AXIS2_PLACEMENT_3D ( 'NONE', #73770, #228973, #50305 ) ;
#100752=EDGE_LOOP ( 'NONE', ( #69355, #171832, #5705, #60098 ) ) ;
#100825=EDGE_CURVE ( 'NONE', #57105, #211497, #37191, .T. ) ;
#100829=CARTESIAN_POINT ( 'NONE',  ( -23.15000000000000213, 73.40000000001204228, -114.7731074845243171 ) ) ;
#100838=EDGE_CURVE ( 'NONE', #7674, #131827, #230089, .T. ) ;
#100878=LINE ( 'NONE', #81325, #41869 ) ;
#100887=CARTESIAN_POINT ( 'NONE',  ( 23.24999999999997513, 64.35000000001176090, -76.53791325517833855 ) ) ;
#100900=CARTESIAN_POINT ( 'NONE',  ( 23.24999999999999289, 64.35000000001176090, -76.53791325517833855 ) ) ;
#100919=EDGE_CURVE ( 'NONE', #6405, #188719, #143963, .T. ) ;
#100960=ORIENTED_EDGE ( 'NONE', *, *, #39020, .T. ) ;
#101025=DIRECTION ( 'NONE',  ( -0.000000000000000000, 0.4791956752371485107, 0.8777080977375185666 ) ) ;
#101030=EDGE_LOOP ( 'NONE', ( #139572, #240893, #78678, #49544 ) ) ;
#101042=ORIENTED_EDGE ( 'NONE', *, *, #83445, .T. ) ;
#101097=DIRECTION ( 'NONE',  ( 0.000000000000000000, 0.000000000000000000, 1.000000000000000000 ) ) ;
#101120=( BOUNDED_SURFACE ( )  B_SPLINE_SURFACE ( 3, 2, ( 
 ( #9335, #169741, #88855 ),
 ( #247945, #125450, #87576 ),
 ( #245398, #249249, #66759 ),
 ( #167171, #130563, #228406 ),
 ( #229681, #185417, #31510 ),
 ( #204955, #51002, #126724 ) ),
 .UNSPECIFIED., .F., .F., .F. ) 
 B_SPLINE_SURFACE_WITH_KNOTS ( ( 4, 2, 4 ),
 ( 3, 3 ),
 ( -1.776356839400250465E-15, 0.7853981633974468357, 1.570796326794895448 ),
 ( 0.000000000000000000, 1.000000000000000000 ),
 .UNSPECIFIED. ) 
 GEOMETRIC_REPRESENTATION_ITEM ( )  RATIONAL_B_SPLINE_SURFACE ( (
 ( 1.000000000000000000, 0.5000000000000154321, 1.000000000000000000),
 ( 1.000000000000000000, 0.4993418825333872935, 1.000000000000000000),
 ( 1.000000000000000000, 0.5278258667058143283, 1.000000000000000000),
 ( 1.000000000000000000, 0.6092287576696161500, 1.000000000000000000),
 ( 1.000000000000000000, 0.6611148371778734489, 1.000000000000000000),
 ( 1.000000000000000000, 0.7071067811865597852, 1.000000000000000000) ) ) 
 REPRESENTATION_ITEM ( '' )  SURFACE ( )  );
#101127=AXIS2_PLACEMENT_3D ( 'NONE', #209239, #127144, #129708 ) ;
#101138=CARTESIAN_POINT ( 'NONE',  ( -21.08198257630413508, 75.92735667622740436, -109.3597042185393775 ) ) ;
#101141=EDGE_CURVE ( 'NONE', #7674, #158615, #1112, .T. ) ;
#101151=CARTESIAN_POINT ( 'NONE',  ( -23.25000000000000000, 84.59626168225477727, -78.97323500167452437 ) ) ;
#101167=VECTOR ( 'NONE', #21180, 1000.000000000000000 ) ;
#101178=CARTESIAN_POINT ( 'NONE',  ( 18.49999999999999289, 65.79142135624910281, -81.67310748452439384 ) ) ;
#101182=EDGE_CURVE ( 'NONE', #111080, #91045, #62849, .T. ) ;
#101192=DIRECTION ( 'NONE',  ( 0.000000000000000000, -6.982962677686266711E-15, 1.000000000000000000 ) ) ;
#101202=CARTESIAN_POINT ( 'NONE',  ( 21.07933241753356768, 69.67135405163219275, -103.1164870749436488 ) ) ;
#101249=CARTESIAN_POINT ( 'NONE',  ( 21.05000000000000071, 65.57661458509899433, -95.53105556065429482 ) ) ;
#101254=VERTEX_POINT ( 'NONE', #2858 ) ;
#101259=AXIS2_PLACEMENT_3D ( 'NONE', #12221, #188262, #112590 ) ;
#101272=CIRCLE ( 'NONE', #9557, 0.1000000000000043771 ) ;
#101284=DIRECTION ( 'NONE',  ( 0.000000000000000000, 0.000000000000000000, 1.000000000000000000 ) ) ;
#101297=CIRCLE ( 'NONE', #43104, 0.1000000000000028644 ) ;
#101309=DIRECTION ( 'NONE',  ( 0.000000000000000000, 0.000000000000000000, 1.000000000000000000 ) ) ;
#101314=TOROIDAL_SURFACE ( 'NONE', #9224, 0.4000000000000017431, 0.1000000000000000056 ) ;
#101352=ADVANCED_FACE ( 'NONE', ( #103237 ), #130514, .T. ) ;
#101368=CARTESIAN_POINT ( 'NONE',  ( -18.39999999999999858, 85.60000000001190301, -95.99103808782457747 ) ) ;
#101388=ORIENTED_EDGE ( 'NONE', *, *, #216467, .T. ) ;
#101414=EDGE_CURVE ( 'NONE', #161543, #36183, #222047, .T. ) ;
#101428=LINE ( 'NONE', #135457, #1014 ) ;
#101435=ORIENTED_EDGE ( 'NONE', *, *, #120913, .F. ) ;
#101441=ADVANCED_FACE ( 'NONE', ( #11890 ), #247009, .F. ) ;
#101444=CIRCLE ( 'NONE', #172284, 0.1000000000000028644 ) ;
#101466=VECTOR ( 'NONE', #162621, 1000.000000000000000 ) ;
#101472=EDGE_CURVE ( 'NONE', #205047, #83796, #16953, .T. ) ;
#101490=CARTESIAN_POINT ( 'NONE',  ( -20.64999999999999858, 85.00000000001179501, -79.41707660717668205 ) ) ;
#101497=CARTESIAN_POINT ( 'NONE',  ( -18.43707690579160996, 85.68240343348810484, -62.86626410711147628 ) ) ;
#101498=AXIS2_PLACEMENT_3D ( 'NONE', #50665, #170693, #71565 ) ;
#101504=EDGE_LOOP ( 'NONE', ( #175096, #213582, #202570, #233467, #17176, #2297, #8558, #231186, #14248, #170414, #185371 ) ) ;
#101560=ORIENTED_EDGE ( 'NONE', *, *, #180379, .F. ) ;
#101606=VERTEX_POINT ( 'NONE', #213908 ) ;
#101624=CARTESIAN_POINT ( 'NONE',  ( 20.95512820512820440, 67.12384868372377866, -94.46447848938342418 ) ) ;
#101626=TOROIDAL_SURFACE ( 'NONE', #189154, 3.899999999999999467, 0.1000000000000000056 ) ;
#101633=ORIENTED_EDGE ( 'NONE', *, *, #243572, .F. ) ;
#101642=CARTESIAN_POINT ( 'NONE',  ( -23.25000000000000000, 76.00000000001197975, -107.0731074845243143 ) ) ;
#101654=VERTEX_POINT ( 'NONE', #101624 ) ;
#101658=LINE ( 'NONE', #107777, #89206 ) ;
#101663=CARTESIAN_POINT ( 'NONE',  ( 21.87500000000000355, 66.25000000001179501, -81.77310748452437394 ) ) ;
#101678=EDGE_CURVE ( 'NONE', #1991, #235864, #213892, .T. ) ;
#101681=CARTESIAN_POINT ( 'NONE',  ( 21.05000000000000071, 76.00000000001168132, -65.52310748452430289 ) ) ;
#101695=DIRECTION ( 'NONE',  ( 5.421010862427554711E-16, 1.000000000000000000, 1.023556919514279895E-14 ) ) ;
#101712=ORIENTED_EDGE ( 'NONE', *, *, #205993, .F. ) ;
#101734=EDGE_CURVE ( 'NONE', #40972, #22332, #82069, .T. ) ;
#101751=AXIS2_PLACEMENT_3D ( 'NONE', #253200, #135812, #134526 ) ;
#101792=CIRCLE ( 'NONE', #26841, 0.09999999999999939493 ) ;
#101816=LINE ( 'NONE', #62729, #107588 ) ;
#101819=ORIENTED_EDGE ( 'NONE', *, *, #181399, .T. ) ;
#101820=EDGE_CURVE ( 'NONE', #127088, #5545, #48105, .T. ) ;
#101831=CARTESIAN_POINT ( 'NONE',  ( -20.85000000000000142, 77.26327546522891510, -61.62124281777789037 ) ) ;
#101883=CARTESIAN_POINT ( 'NONE',  ( -22.00356870069947135, 76.00000000001202238, -110.2773498462699564 ) ) ;
#101910=CARTESIAN_POINT ( 'NONE',  ( -21.40925344232282512, 69.34148114062149659, -103.1220576731440133 ) ) ;
#101933=DIRECTION ( 'NONE',  ( 0.000000000000000000, -7.116814260417668513E-15, 1.000000000000000000 ) ) ;
#101951=ORIENTED_EDGE ( 'NONE', *, *, #163903, .F. ) ;
#101974=VERTEX_POINT ( 'NONE', #76650 ) ;
#101997=AXIS2_PLACEMENT_3D ( 'NONE', #71633, #195438, #230703 ) ;
#102013=DIRECTION ( 'NONE',  ( 0.000000000000000000, -1.000000000000000000, -6.982962677686265922E-15 ) ) ;
#102072=CARTESIAN_POINT ( 'NONE',  ( 20.94999999999999929, 85.00000000001179501, -79.41707660717668205 ) ) ;
#102088=VERTEX_POINT ( 'NONE', #238286 ) ;
#102092=AXIS2_PLACEMENT_3D ( 'NONE', #155243, #93943, #233484 ) ;
#102119=VECTOR ( 'NONE', #252253, 1000.000000000000000 ) ;
#102125=EDGE_LOOP ( 'NONE', ( #20551, #137588, #63482, #246923 ) ) ;
#102143=EDGE_CURVE ( 'NONE', #108747, #193967, #30945, .T. ) ;
#102162=VERTEX_POINT ( 'NONE', #186026 ) ;
#102198=CARTESIAN_POINT ( 'NONE',  ( -22.32929514600008503, 75.90092432189808846, -110.6017550499008166 ) ) ;
#102311=ORIENTED_EDGE ( 'NONE', *, *, #84274, .T. ) ;
#102318=ADVANCED_FACE ( 'NONE', ( #67364 ), #146872, .F. ) ;
#102338=AXIS2_PLACEMENT_3D ( 'NONE', #106, #100470, #194494 ) ;
#102350=ORIENTED_EDGE ( 'NONE', *, *, #112382, .F. ) ;
#102384=EDGE_LOOP ( 'NONE', ( #156428, #88806, #214432, #154928 ) ) ;
#102405=CARTESIAN_POINT ( 'NONE',  ( 20.94999999999999929, 67.22371710471938400, -90.87310748452436826 ) ) ;
#102426=CARTESIAN_POINT ( 'NONE',  ( -20.94999999999999574, 64.37928932189309705, -76.39152413686537102 ) ) ;
#102444=ORIENTED_EDGE ( 'NONE', *, *, #220677, .T. ) ;
#102467=EDGE_CURVE ( 'NONE', #29920, #6405, #203689, .T. ) ;
#102601=AXIS2_PLACEMENT_3D ( 'NONE', #10792, #249410, #31667 ) ;
#102618=TOROIDAL_SURFACE ( 'NONE', #140049, 0.2000000000000000111, 0.1000000000000000056 ) ;
#102621=AXIS2_PLACEMENT_3D ( 'NONE', #219314, #18562, #120264 ) ;
#102635=EDGE_CURVE ( 'NONE', #96396, #173426, #172314, .T. ) ;
#102647=ORIENTED_EDGE ( 'NONE', *, *, #45806, .T. ) ;
#102660=ORIENTED_EDGE ( 'NONE', *, *, #215668, .T. ) ;
#102672=CARTESIAN_POINT ( 'NONE',  ( -21.14999999999999858, 64.25000000001189449, -96.23924182154622997 ) ) ;
#102678=VERTEX_POINT ( 'NONE', #74486 ) ;
#102680=AXIS2_PLACEMENT_3D ( 'NONE', #216172, #252731, #76666 ) ;
#102701=ORIENTED_EDGE ( 'NONE', *, *, #112382, .T. ) ;
#102702=DIRECTION ( 'NONE',  ( 1.000000000000000000, 0.000000000000000000, 0.000000000000000000 ) ) ;
#102711=CARTESIAN_POINT ( 'NONE',  ( -20.94999999999999929, 77.36242903720497566, -61.63422623660309796 ) ) ;
#102712=CIRCLE ( 'NONE', #231945, 0.1000000000000028644 ) ;
#102742=ORIENTED_EDGE ( 'NONE', *, *, #47559, .F. ) ;
#102769=EDGE_LOOP ( 'NONE', ( #107754, #96948, #11739, #40812 ) ) ;
#102786=ORIENTED_EDGE ( 'NONE', *, *, #40444, .T. ) ;
#102845=DIRECTION ( 'NONE',  ( 0.000000000000000000, -7.056502275159890832E-15, 1.000000000000000000 ) ) ;
#102893=AXIS2_PLACEMENT_3D ( 'NONE', #245947, #46440, #6025 ) ;
#102901=CYLINDRICAL_SURFACE ( 'NONE', #19550, 0.09999999999999939493 ) ;
#102902=CARTESIAN_POINT ( 'NONE',  ( -23.15000000000000213, 64.35000000001187459, -90.87310748452438247 ) ) ;
#102905=TOROIDAL_SURFACE ( 'NONE', #82046, 0.4000000000000003553, 0.1000000000000000056 ) ;
#102926=ORIENTED_EDGE ( 'NONE', *, *, #133395, .T. ) ;
#102946=DIRECTION ( 'NONE',  ( 0.000000000000000000, 0.000000000000000000, 1.000000000000000000 ) ) ;
#102956=ORIENTED_EDGE ( 'NONE', *, *, #77556, .T. ) ;
#102968=DIRECTION ( 'NONE',  ( 0.000000000000000000, -6.467318590049456648E-15, 1.000000000000000000 ) ) ;
#103020=LINE ( 'NONE', #83441, #184149 ) ;
#103035=ORIENTED_EDGE ( 'NONE', *, *, #145426, .T. ) ;
#103045=ORIENTED_EDGE ( 'NONE', *, *, #78493, .F. ) ;
#103061=ORIENTED_EDGE ( 'NONE', *, *, #253733, .F. ) ;
#103065=CARTESIAN_POINT ( 'NONE',  ( -23.25000000000000000, 76.00000000001195133, -103.0231074845243171 ) ) ;
#103074=CARTESIAN_POINT ( 'NONE',  ( 21.05000000000000071, 65.27628289530443340, -103.0231074845243882 ) ) ;
#103088=ORIENTED_EDGE ( 'NONE', *, *, #178913, .F. ) ;
#103105=DIRECTION ( 'NONE',  ( 1.000000000000000000, -7.304098846218163263E-16, 4.217023435051626718E-16 ) ) ;
#103107=EDGE_CURVE ( 'NONE', #200766, #255325, #230652, .T. ) ;
#103164=ORIENTED_EDGE ( 'NONE', *, *, #32463, .F. ) ;
#103197=EDGE_CURVE ( 'NONE', #9387, #96528, #156271, .T. ) ;
#103214=ORIENTED_EDGE ( 'NONE', *, *, #111204, .F. ) ;
#103231=ORIENTED_EDGE ( 'NONE', *, *, #225261, .T. ) ;
#103237=FACE_OUTER_BOUND ( 'NONE', #32311, .T. ) ;
#103269=EDGE_CURVE ( 'NONE', #222763, #44904, #148161, .T. ) ;
#103271=DIRECTION ( 'NONE',  ( -1.000000000000000000, 0.000000000000000000, 0.000000000000000000 ) ) ;
#103309=ORIENTED_EDGE ( 'NONE', *, *, #195110, .T. ) ;
#103312=FACE_OUTER_BOUND ( 'NONE', #49270, .T. ) ;
#103324=CARTESIAN_POINT ( 'NONE',  ( -18.46154800491010306, 85.48020627425367479, -62.86565664614276727 ) ) ;
#103335=VECTOR ( 'NONE', #223365, 1000.000000000000114 ) ;
#103373=CARTESIAN_POINT ( 'NONE',  ( 18.59999999999999076, 69.35000000001180354, -81.87310748452435405 ) ) ;
#103376=ORIENTED_EDGE ( 'NONE', *, *, #123892, .T. ) ;
#103453=FACE_OUTER_BOUND ( 'NONE', #82186, .T. ) ;
#103595=EDGE_LOOP ( 'NONE', ( #138460, #95366, #122528 ) ) ;
#103615=CARTESIAN_POINT ( 'NONE',  ( 20.95512820512820440, 65.37615131629998189, -90.87310748452438247 ) ) ;
#103624=VERTEX_POINT ( 'NONE', #193770 ) ;
#103693=EDGE_LOOP ( 'NONE', ( #90917, #149284, #180011, #64367 ) ) ;
#103696=DIRECTION ( 'NONE',  ( 0.000000000000000000, 0.000000000000000000, 1.000000000000000000 ) ) ;
#103706=DIRECTION ( 'NONE',  ( 0.000000000000000000, -7.086529944415894657E-15, 1.000000000000000000 ) ) ;
#103721=EDGE_LOOP ( 'NONE', ( #227828, #76486, #53675, #101951 ) ) ;
#103727=CARTESIAN_POINT ( 'NONE',  ( -21.13498764882296044, 75.99834360528066668, -109.5187256279982506 ) ) ;
#103739=CARTESIAN_POINT ( 'NONE',  ( 21.00000000000000000, 66.25000000001179501, -81.77310748452437394 ) ) ;
#103761=ORIENTED_EDGE ( 'NONE', *, *, #203072, .T. ) ;
#103768=TOROIDAL_SURFACE ( 'NONE', #70523, 0.6000000000000013101, 0.1000000000000000056 ) ;
#103775=ADVANCED_FACE ( 'NONE', ( #5817 ), #107498, .T. ) ;
#103789=CARTESIAN_POINT ( 'NONE',  ( 21.09316766718127667, 69.62984668753753681, -103.0623708868390622 ) ) ;
#103813=VERTEX_POINT ( 'NONE', #85342 ) ;
#103831=FACE_OUTER_BOUND ( 'NONE', #113047, .T. ) ;
#103855=DIRECTION ( 'NONE',  ( -0.000000000000000000, 6.982962677686266711E-15, -1.000000000000000000 ) ) ;
#103861=CARTESIAN_POINT ( 'NONE',  ( 21.05000000000000071, 76.00000000001195133, -102.9231074845243228 ) ) ;
#103865=CARTESIAN_POINT ( 'NONE',  ( 20.94999999999999929, 76.00000000001170974, -69.52310748452431710 ) ) ;
#103950=AXIS2_PLACEMENT_3D ( 'NONE', #244945, #243663, #65022 ) ;
#103953=VECTOR ( 'NONE', #199574, 1000.000000000000000 ) ;
#103961=EDGE_LOOP ( 'NONE', ( #122660, #67064, #116899, #67845 ) ) ;
#103994=CARTESIAN_POINT ( 'NONE',  ( -18.59999999999999787, 64.25000000001186606, -90.87310748452438247 ) ) ;
#104010=EDGE_CURVE ( 'NONE', #57105, #224804, #193574, .T. ) ;
#104024=ORIENTED_EDGE ( 'NONE', *, *, #172929, .F. ) ;
#104083=AXIS2_PLACEMENT_3D ( 'NONE', #55911, #213728, #252848 ) ;
#104112=CIRCLE ( 'NONE', #249875, 0.5000000000000004441 ) ;
#104134=CARTESIAN_POINT ( 'NONE',  ( -18.60000000000001208, 85.36424052760280290, -95.84285890268347430 ) ) ;
#104158=CARTESIAN_POINT ( 'NONE',  ( 18.50000000000000000, 85.40000000001165859, -62.64106563635156277 ) ) ;
#104189=CARTESIAN_POINT ( 'NONE',  ( 20.95378194480896639, 65.46508800846910958, -95.45805333637652268 ) ) ;
#104209=DIRECTION ( 'NONE',  ( 0.000000000000000000, 0.000000000000000000, 1.000000000000000000 ) ) ;
#104228=AXIS2_PLACEMENT_3D ( 'NONE', #87970, #207970, #171431 ) ;
#104230=DIRECTION ( 'NONE',  ( -1.000000000000000000, -0.000000000000000000, -0.000000000000000000 ) ) ;
#104243=DIRECTION ( 'NONE',  ( 0.000000000000000000, 6.982962677686266711E-15, -1.000000000000000000 ) ) ;
#104244=ORIENTED_EDGE ( 'NONE', *, *, #148365, .F. ) ;
#104262=CARTESIAN_POINT ( 'NONE',  ( -21.93340585972178758, 68.67585297715976367, -103.0231074845243597 ) ) ;
#104271=DIRECTION ( 'NONE',  ( 1.000000000000000000, 0.000000000000000000, 0.000000000000000000 ) ) ;
#104275=DIRECTION ( 'NONE',  ( -1.000000000000000000, 1.836970198721029934E-16, 1.282749433769087582E-30 ) ) ;
#104296=DIRECTION ( 'NONE',  ( 2.952720810173289112E-16, 1.000000000000000000, -6.088138035986627436E-46 ) ) ;
#104301=ORIENTED_EDGE ( 'NONE', *, *, #145570, .T. ) ;
#104304=CARTESIAN_POINT ( 'NONE',  ( -23.25000000000000000, 73.40000000001180069, -82.74772940728642823 ) ) ;
#104314=ORIENTED_EDGE ( 'NONE', *, *, #145944, .F. ) ;
#104333=ORIENTED_EDGE ( 'NONE', *, *, #43332, .F. ) ;
#104339=EDGE_LOOP ( 'NONE', ( #119948, #196904, #139441, #38574 ) ) ;
#104372=CIRCLE ( 'NONE', #4425, 0.09999999999999939493 ) ;
#104377=ORIENTED_EDGE ( 'NONE', *, *, #57573, .T. ) ;
#104392=AXIS2_PLACEMENT_3D ( 'NONE', #180834, #140399, #238221 ) ;
#104397=ORIENTED_EDGE ( 'NONE', *, *, #5446, .F. ) ;
#104407=DIRECTION ( 'NONE',  ( 1.000000000000000000, 0.000000000000000000, 0.000000000000000000 ) ) ;
#104500=DIRECTION ( 'NONE',  ( 0.000000000000000000, 8.896017825522085641E-15, -1.000000000000000000 ) ) ;
#104510=EDGE_CURVE ( 'NONE', #242308, #173093, #58844, .T. ) ;
#104523=LINE ( 'NONE', #86249, #122795 ) ;
#104531=CARTESIAN_POINT ( 'NONE',  ( 21.14999999999999858, 67.21339244341174890, -90.67310748452436542 ) ) ;
#104532=ORIENTED_EDGE ( 'NONE', *, *, #248577, .T. ) ;
#104536=DIRECTION ( 'NONE',  ( 0.000000000000000000, 0.000000000000000000, 1.000000000000000000 ) ) ;
#104557=EDGE_CURVE ( 'NONE', #40263, #224619, #73177, .T. ) ;
#104593=FACE_OUTER_BOUND ( 'NONE', #58877, .T. ) ;
#104630=ORIENTED_EDGE ( 'NONE', *, *, #222865, .T. ) ;
#104635=EDGE_CURVE ( 'NONE', #179506, #254110, #148143, .T. ) ;
#104654=EDGE_CURVE ( 'NONE', #223762, #171936, #236494, .T. ) ;
#104655=DIRECTION ( 'NONE',  ( 1.000000000000000000, 0.000000000000000000, 0.000000000000000000 ) ) ;
#104671=CIRCLE ( 'NONE', #192213, 0.1000000000000028644 ) ;
#104693=ADVANCED_FACE ( 'NONE', ( #60421 ), #219494, .F. ) ;
#104701=EDGE_CURVE ( 'NONE', #416, #34831, #139752, .T. ) ;
#104728=ADVANCED_FACE ( 'NONE', ( #22613 ), #27760, .F. ) ;
#104740=EDGE_CURVE ( 'NONE', #17324, #14256, #214783, .T. ) ;
#104761=DIRECTION ( 'NONE',  ( -1.000000000000000000, 0.000000000000000000, -0.000000000000000000 ) ) ;
#104778=CARTESIAN_POINT ( 'NONE',  ( 21.06086055315979522, 67.22529248505564681, -90.82078532937038062 ) ) ;
#104779=ADVANCED_FACE ( 'NONE', ( #65562 ), #198218, .T. ) ;
#104781=DIRECTION ( 'NONE',  ( 0.000000000000000000, -7.056502275159890832E-15, 1.000000000000000000 ) ) ;
#104784=ORIENTED_EDGE ( 'NONE', *, *, #244473, .F. ) ;
#104829=ORIENTED_EDGE ( 'NONE', *, *, #109358, .F. ) ;
#104857=ADVANCED_FACE ( 'NONE', ( #51108 ), #91554, .F. ) ;
#104869=LINE ( 'NONE', #164893, #136484 ) ;
#104873=FACE_OUTER_BOUND ( 'NONE', #185813, .T. ) ;
#104885=CARTESIAN_POINT ( 'NONE',  ( 20.97224591636398472, 65.37484658384822467, -90.77318157986078972 ) ) ;
#104900=CIRCLE ( 'NONE', #167337, 0.2000000000000057288 ) ;
#104905=EDGE_LOOP ( 'NONE', ( #191381, #108598, #97597, #136438 ) ) ;
#104911=DIRECTION ( 'NONE',  ( -1.000000000000000000, -0.000000000000000000, -0.000000000000000000 ) ) ;
#104914=DIRECTION ( 'NONE',  ( 1.000000000000000000, 0.000000000000000000, 0.000000000000000000 ) ) ;
#104956=CARTESIAN_POINT ( 'NONE',  ( -18.58222699835055280, 65.66799936921512426, -63.92993998886008455 ) ) ;
#104970=DIRECTION ( 'NONE',  ( 0.000000000000000000, 0.000000000000000000, 1.000000000000000000 ) ) ;
#104993=ORIENTED_EDGE ( 'NONE', *, *, #120580, .T. ) ;
#104995=CARTESIAN_POINT ( 'NONE',  ( -21.11927991906891577, 75.99091632053813328, -109.4716006030158155 ) ) ;
#105002=DIRECTION ( 'NONE',  ( 0.000000000000000000, 0.000000000000000000, 1.000000000000000000 ) ) ;
#105025=EDGE_CURVE ( 'NONE', #53997, #140889, #110921, .T. ) ;
#105027=DIRECTION ( 'NONE',  ( -1.000000000000000000, -0.000000000000000000, -0.000000000000000000 ) ) ;
#105060=ORIENTED_EDGE ( 'NONE', *, *, #229545, .T. ) ;
#105072=DIRECTION ( 'NONE',  ( 1.000000000000000000, 0.000000000000000000, 0.000000000000000000 ) ) ;
#105086=EDGE_CURVE ( 'NONE', #71706, #83423, #156745, .T. ) ;
#105118=FACE_OUTER_BOUND ( 'NONE', #85090, .T. ) ;
#105127=CARTESIAN_POINT ( 'NONE',  ( -21.44999999999999929, 68.65000000001180069, -81.87310748452436826 ) ) ;
#105145=ORIENTED_EDGE ( 'NONE', *, *, #250125, .F. ) ;
#105153=AXIS2_PLACEMENT_3D ( 'NONE', #20494, #81688, #201671 ) ;
#105184=EDGE_CURVE ( 'NONE', #225625, #242050, #144217, .T. ) ;
#105191=AXIS2_PLACEMENT_3D ( 'NONE', #57111, #257853, #15466 ) ;
#105202=ORIENTED_EDGE ( 'NONE', *, *, #22420, .F. ) ;
#105203=DIRECTION ( 'NONE',  ( 0.000000000000000000, -0.01562499999996343723, -0.9998779222360104635 ) ) ;
#105221=DIRECTION ( 'NONE',  ( -0.000000000000000000, -0.01283462868040327436, 0.9999176327611370985 ) ) ;
#105274=EDGE_CURVE ( 'NONE', #53997, #43410, #165085, .T. ) ;
#105305=DIRECTION ( 'NONE',  ( 0.000000000000000000, 1.000000000000000000, 6.982962677686266711E-15 ) ) ;
#105306=CIRCLE ( 'NONE', #71499, 0.09999999999999939493 ) ;
#105308=ORIENTED_EDGE ( 'NONE', *, *, #210428, .F. ) ;
#105311=ORIENTED_EDGE ( 'NONE', *, *, #137893, .F. ) ;
#105314=CARTESIAN_POINT ( 'NONE',  ( 21.14999999999999503, 76.10000000001203091, -114.6726782920691079 ) ) ;
#105331=DIRECTION ( 'NONE',  ( 1.000000000000000000, 0.000000000000000000, 0.000000000000000000 ) ) ;
#105373=CARTESIAN_POINT ( 'NONE',  ( 23.14999999999999858, 76.00000000001170974, -69.52310748452431710 ) ) ;
#105401=AXIS2_PLACEMENT_3D ( 'NONE', #73737, #236623, #174142 ) ;
#105414=AXIS2_PLACEMENT_3D ( 'NONE', #240227, #215507, #235087 ) ;
#105423=DIRECTION ( 'NONE',  ( -1.000000000000000000, 0.000000000000000000, -0.000000000000000000 ) ) ;
#105445=DIRECTION ( 'NONE',  ( 1.000000000000000000, 0.000000000000000000, 0.000000000000000000 ) ) ;
#105463=AXIS2_PLACEMENT_3D ( 'NONE', #24518, #244812, #87005 ) ;
#105477=EDGE_CURVE ( 'NONE', #18436, #98928, #79361, .T. ) ;
#105517=FACE_OUTER_BOUND ( 'NONE', #241201, .T. ) ;
#105548=VECTOR ( 'NONE', #136713, 1000.000000000000000 ) ;
#105550=EDGE_CURVE ( 'NONE', #245381, #21468, #77751, .T. ) ;
#105561=VECTOR ( 'NONE', #16562, 1000.000000000000000 ) ;
#105563=AXIS2_PLACEMENT_3D ( 'NONE', #257170, #158175, #16081 ) ;
#105599=ORIENTED_EDGE ( 'NONE', *, *, #204267, .T. ) ;
#105616=ORIENTED_EDGE ( 'NONE', *, *, #16963, .F. ) ;
#105621=ORIENTED_EDGE ( 'NONE', *, *, #197809, .T. ) ;
#105625=AXIS2_PLACEMENT_3D ( 'NONE', #75523, #76775, #15555 ) ;
#105633=ORIENTED_EDGE ( 'NONE', *, *, #169322, .T. ) ;
#105652=ADVANCED_FACE ( 'NONE', ( #35794 ), #233964, .F. ) ;
#105673=AXIS2_PLACEMENT_3D ( 'NONE', #9390, #10690, #129344 ) ;
#105698=CARTESIAN_POINT ( 'NONE',  ( -20.54999999999999716, 85.00000000001188027, -93.12913836187181005 ) ) ;
#105702=CARTESIAN_POINT ( 'NONE',  ( -22.39999999999999858, 64.35000000001195986, -103.1231074845243825 ) ) ;
#105755=CARTESIAN_POINT ( 'NONE',  ( 21.14999999999999503, 76.00000000001199396, -109.2731074845243171 ) ) ;
#105764=CIRCLE ( 'NONE', #205742, 0.1000000000000028644 ) ;
#105767=CARTESIAN_POINT ( 'NONE',  ( -23.15000000000000213, 64.35000000001187459, -90.87310748452438247 ) ) ;
#105793=CIRCLE ( 'NONE', #64135, 0.1000000000000026007 ) ;
#105808=DIRECTION ( 'NONE',  ( 0.000000000000000000, 0.000000000000000000, 1.000000000000000000 ) ) ;
#105816=CARTESIAN_POINT ( 'NONE',  ( -18.50000000000000711, 64.25000000001190870, -96.00830171387039513 ) ) ;
#105825=CARTESIAN_POINT ( 'NONE',  ( -18.59999999999999787, 102.4393534156127572, -84.88159887701665696 ) ) ;
#105834=AXIS2_PLACEMENT_3D ( 'NONE', #213202, #164161, #65046 ) ;
#105876=DIRECTION ( 'NONE',  ( 1.000000000000000000, 0.000000000000000000, 0.000000000000000000 ) ) ;
#105880=ORIENTED_EDGE ( 'NONE', *, *, #44691, .T. ) ;
#105938=ORIENTED_EDGE ( 'NONE', *, *, #59048, .F. ) ;
#105960=CARTESIAN_POINT ( 'NONE',  ( -20.85000000000000142, 76.00000000001170974, -69.52310748452431710 ) ) ;
#106001=DIRECTION ( 'NONE',  ( 1.000000000000000000, 0.000000000000000000, 0.000000000000000000 ) ) ;
#106007=CARTESIAN_POINT ( 'NONE',  ( 18.52165635395173027, 85.48115071129409159, -95.99826990166178575 ) ) ;
#106031=ORIENTED_EDGE ( 'NONE', *, *, #79386, .T. ) ;
#106055=DIRECTION ( 'NONE',  ( 0.000000000000000000, -1.000000000000000000, -6.352154140967427193E-15 ) ) ;
#106071=CARTESIAN_POINT ( 'NONE',  ( -23.25000000000000000, 64.25000000001203659, -114.7731074845243882 ) ) ;
#106092=DIRECTION ( 'NONE',  ( -0.000000000000000000, -6.982962677686266711E-15, 1.000000000000000000 ) ) ;
#106105=AXIS2_PLACEMENT_3D ( 'NONE', #219117, #20966, #177479 ) ;
#106133=ORIENTED_EDGE ( 'NONE', *, *, #59171, .T. ) ;
#106184=DIRECTION ( 'NONE',  ( -1.000000000000000000, 0.000000000000000000, -0.000000000000000000 ) ) ;
#106187=AXIS2_PLACEMENT_3D ( 'NONE', #143442, #106874, #166900 ) ;
#106188=ORIENTED_EDGE ( 'NONE', *, *, #73169, .F. ) ;
#106190=DIRECTION ( 'NONE',  ( -0.7071067811865475727, 0.7071067811865475727, 4.937700262164531476E-15 ) ) ;
#106215=ORIENTED_EDGE ( 'NONE', *, *, #253126, .F. ) ;
#106216=ORIENTED_EDGE ( 'NONE', *, *, #247110, .T. ) ;
#106249=CARTESIAN_POINT ( 'NONE',  ( -21.45000000000000284, 68.29142135624915966, -90.77310748452437394 ) ) ;
#106259=EDGE_CURVE ( 'NONE', #204570, #195198, #24919, .T. ) ;
#106296=FACE_OUTER_BOUND ( 'NONE', #206754, .T. ) ;
#106303=CARTESIAN_POINT ( 'NONE',  ( -21.08376601933334271, 75.93622398908212290, -109.3650547558000454 ) ) ;
#106305=ORIENTED_EDGE ( 'NONE', *, *, #199864, .F. ) ;
#106363=AXIS2_PLACEMENT_3D ( 'NONE', #184245, #68155, #182982 ) ;
#106380=CARTESIAN_POINT ( 'NONE',  ( 18.45139536634708932, 85.48608172029291552, -62.88259586671362911 ) ) ;
#106407=DIRECTION ( 'NONE',  ( 0.000000000000000000, 0.000000000000000000, 1.000000000000000000 ) ) ;
#106423=AXIS2_PLACEMENT_3D ( 'NONE', #56385, #16024, #176378 ) ;
#106444=( GEOMETRIC_REPRESENTATION_CONTEXT ( 3 ) GLOBAL_UNCERTAINTY_ASSIGNED_CONTEXT ( ( #186040 ) ) GLOBAL_UNIT_ASSIGNED_CONTEXT ( ( #58860, #82270, #241394 ) ) REPRESENTATION_CONTEXT ( 'NONE', 'WORKASPACE' ) );
#106459=AXIS2_PLACEMENT_3D ( 'NONE', #134100, #177121, #94983 ) ;
#106530=EDGE_CURVE ( 'NONE', #96909, #255325, #86669, .T. ) ;
#106532=EDGE_CURVE ( 'NONE', #86681, #3957, #25888, .T. ) ;
#106540=AXIS2_PLACEMENT_3D ( 'NONE', #69461, #148999, #228529 ) ;
#106545=CIRCLE ( 'NONE', #243939, 0.1000000000000028644 ) ;
#106556=CARTESIAN_POINT ( 'NONE',  ( 21.14999999999999858, 69.35000000001186038, -90.67310748452435121 ) ) ;
#106565=EDGE_CURVE ( 'NONE', #88561, #82161, #49098, .T. ) ;
#106631=DIRECTION ( 'NONE',  ( -1.000000000000000000, -0.000000000000000000, -0.000000000000000000 ) ) ;
#106643=CARTESIAN_POINT ( 'NONE',  ( 20.94999999999999929, 85.50000000001179501, -79.41707660717668205 ) ) ;
#106704=CARTESIAN_POINT ( 'NONE',  ( -18.43569575749025446, 85.51932773110432606, -96.05013110796488718 ) ) ;
#106752=AXIS2_PLACEMENT_3D ( 'NONE', #222360, #202828, #24216 ) ;
#106754=CARTESIAN_POINT ( 'NONE',  ( -22.60000000000094289, 75.89914163091351895, -114.7726746080137303 ) ) ;
#106762=CARTESIAN_POINT ( 'NONE',  ( 20.95539060131842746, 65.37613784235624337, -95.36937367086818540 ) ) ;
#106763=CARTESIAN_POINT ( 'NONE',  ( -21.64999999999999858, 68.75000000001186606, -90.77310748452435973 ) ) ;
#106777=DIRECTION ( 'NONE',  ( -1.000000000000000000, -0.000000000000000000, -0.000000000000000000 ) ) ;
#106781=DIRECTION ( 'NONE',  ( 0.000000000000000000, 0.000000000000000000, -1.000000000000000000 ) ) ;
#106803=DIRECTION ( 'NONE',  ( 0.000000000000000000, -1.000000000000000000, -6.982962677686265922E-15 ) ) ;
#106808=CARTESIAN_POINT ( 'NONE',  ( -23.25000000000000000, 76.00000000001197975, -107.1731074845243086 ) ) ;
#106818=CARTESIAN_POINT ( 'NONE',  ( -21.05000000000000071, 74.16465844978745281, -91.46795619196133487 ) ) ;
#106825=ORIENTED_EDGE ( 'NONE', *, *, #2498, .F. ) ;
#106826=ORIENTED_EDGE ( 'NONE', *, *, #89357, .F. ) ;
#106872=CARTESIAN_POINT ( 'NONE',  ( 19.97071067695833690, 64.27928932305343324, -78.34685405172075434 ) ) ;
#106874=DIRECTION ( 'NONE',  ( 1.000000000000000000, 0.000000000000000000, 0.000000000000000000 ) ) ;
#106894=CARTESIAN_POINT ( 'NONE',  ( -20.54999999999999716, 71.65000000001182912, -86.27310748452434552 ) ) ;
#106895=VERTEX_POINT ( 'NONE', #162527 ) ;
#106909=ORIENTED_EDGE ( 'NONE', *, *, #44323, .F. ) ;
#106913=CARTESIAN_POINT ( 'NONE',  ( -23.15000000000000213, 64.35000000001203091, -114.7731074845243882 ) ) ;
#106919=CARTESIAN_POINT ( 'NONE',  ( -21.14999999999999858, 64.35000000001195986, -102.9231074845243938 ) ) ;
#106927=ORIENTED_EDGE ( 'NONE', *, *, #88504, .F. ) ;
#106958=CARTESIAN_POINT ( 'NONE',  ( -20.94999999999999929, 77.26178616857691850, -94.93660852097882241 ) ) ;
#106979=EDGE_LOOP ( 'NONE', ( #122355, #176157, #249939, #145501 ) ) ;
#106980=AXIS2_PLACEMENT_3D ( 'NONE', #20257, #198880, #99755 ) ;
#106996=ORIENTED_EDGE ( 'NONE', *, *, #46221, .T. ) ;
#107022=AXIS2_PLACEMENT_3D ( 'NONE', #222471, #163820, #245921 ) ;
#107072=AXIS2_PLACEMENT_3D ( 'NONE', #209251, #93153, #29381 ) ;
#107085=CARTESIAN_POINT ( 'NONE',  ( -23.15000000000000213, 73.40000000001185754, -89.79848556176223440 ) ) ;
#107097=AXIS2_PLACEMENT_3D ( 'NONE', #197322, #76099, #74859 ) ;
#107101=CIRCLE ( 'NONE', #173802, 4.049999999999998046 ) ;
#107126=ORIENTED_EDGE ( 'NONE', *, *, #133471, .T. ) ;
#107127=CIRCLE ( 'NONE', #111229, 0.09999999999999938105 ) ;
#107140=ORIENTED_EDGE ( 'NONE', *, *, #129604, .F. ) ;
#107154=FACE_OUTER_BOUND ( 'NONE', #51393, .T. ) ;
#107179=EDGE_CURVE ( 'NONE', #51868, #183416, #254119, .T. ) ;
#107239=DIRECTION ( 'NONE',  ( 0.000000000000000000, 0.000000000000000000, 1.000000000000000000 ) ) ;
#107270=DIRECTION ( 'NONE',  ( -1.000000000000000000, -0.000000000000000000, -0.000000000000000000 ) ) ;
#107288=DIRECTION ( 'NONE',  ( 0.000000000000000000, -0.1350103645451974088, 0.9908441862701587999 ) ) ;
#107310=ADVANCED_FACE ( 'NONE', ( #186597 ), #224894, .T. ) ;
#107332=CARTESIAN_POINT ( 'NONE',  ( 20.84451136049770525, 65.37985808519944442, -95.52918292499884956 ) ) ;
#107353=VERTEX_POINT ( 'NONE', #240968 ) ;
#107355=DIRECTION ( 'NONE',  ( 0.000000000000000000, 6.467318590049456648E-15, -1.000000000000000000 ) ) ;
#107359=EDGE_LOOP ( 'NONE', ( #92693, #76832, #116867, #237534 ) ) ;
#107377=CIRCLE ( 'NONE', #3127, 0.1000000000000028644 ) ;
#107389=CARTESIAN_POINT ( 'NONE',  ( -21.05000000000000071, 64.40000000001177227, -76.45131071479988805 ) ) ;
#107404=SPHERICAL_SURFACE ( 'NONE', #194165, 0.1000000000000000056 ) ;
#107487=FACE_OUTER_BOUND ( 'NONE', #226173, .T. ) ;
#107491=AXIS2_PLACEMENT_3D ( 'NONE', #41743, #179961, #219058 ) ;
#107492=FACE_OUTER_BOUND ( 'NONE', #160108, .T. ) ;
#107498=CYLINDRICAL_SURFACE ( 'NONE', #69080, 0.1000000000000028644 ) ;
#107502=EDGE_LOOP ( 'NONE', ( #215898, #162179, #236774, #244169 ) ) ;
#107525=VECTOR ( 'NONE', #192604, 1000.000000000000114 ) ;
#107547=DIRECTION ( 'NONE',  ( 0.000000000000000000, -1.000000000000000000, 0.000000000000000000 ) ) ;
#107552=FACE_OUTER_BOUND ( 'NONE', #14617, .T. ) ;
#107567=EDGE_CURVE ( 'NONE', #60702, #5347, #143217, .T. ) ;
#107571=CARTESIAN_POINT ( 'NONE',  ( -23.15000000000000213, 64.25000000001185185, -90.87310748452438247 ) ) ;
#107586=AXIS2_PLACEMENT_3D ( 'NONE', #122734, #39350, #118877 ) ;
#107588=VECTOR ( 'NONE', #84816, 1000.000000000000000 ) ;
#107617=ORIENTED_EDGE ( 'NONE', *, *, #57755, .T. ) ;
#107634=EDGE_LOOP ( 'NONE', ( #221340, #193777, #209074, #204125, #59519 ) ) ;
#107643=EDGE_LOOP ( 'NONE', ( #96610, #187469, #145399, #82785 ) ) ;
#107666=AXIS2_PLACEMENT_3D ( 'NONE', #221290, #59636, #19262 ) ;
#107701=EDGE_CURVE ( 'NONE', #140050, #178561, #237752, .T. ) ;
#107705=DIRECTION ( 'NONE',  ( -2.812466655313719426E-14, -0.1350103645451835865, -0.9908441862701605762 ) ) ;
#107714=FACE_OUTER_BOUND ( 'NONE', #186396, .T. ) ;
#107718=ORIENTED_EDGE ( 'NONE', *, *, #37037, .T. ) ;
#107754=ORIENTED_EDGE ( 'NONE', *, *, #88844, .F. ) ;
#107773=CIRCLE ( 'NONE', #28723, 0.09999999999999939493 ) ;
#107777=CARTESIAN_POINT ( 'NONE',  ( 23.14999999999999858, 87.75000000001202238, -114.7731074845242318 ) ) ;
#107785=DIRECTION ( 'NONE',  ( 0.000000000000000000, 0.9908441862701605762, -0.1350103645451835310 ) ) ;
#107788=EDGE_LOOP ( 'NONE', ( #24270, #83500, #29215, #165088 ) ) ;
#107799=CIRCLE ( 'NONE', #236986, 12.97499999999999964 ) ;
#107800=LINE ( 'NONE', #89508, #125777 ) ;
#107808=ORIENTED_EDGE ( 'NONE', *, *, #252435, .T. ) ;
#107821=ORIENTED_EDGE ( 'NONE', *, *, #135742, .T. ) ;
#107859=ORIENTED_EDGE ( 'NONE', *, *, #190113, .T. ) ;
#107868=DIRECTION ( 'NONE',  ( 0.000000000000000000, -1.000000000000000000, -6.982962677686266711E-15 ) ) ;
#107897=VERTEX_POINT ( 'NONE', #101178 ) ;
#107898=VERTEX_POINT ( 'NONE', #16575 ) ;
#107900=ORIENTED_EDGE ( 'NONE', *, *, #181212, .T. ) ;
#107915=DIRECTION ( 'NONE',  ( 0.000000000000000000, 0.8660254037844420383, -0.4999999999999941713 ) ) ;
#107916=ORIENTED_EDGE ( 'NONE', *, *, #136694, .T. ) ;
#107931=ORIENTED_EDGE ( 'NONE', *, *, #55574, .T. ) ;
#107939=CARTESIAN_POINT ( 'NONE',  ( -23.15000000000000213, 76.00000000001195133, -103.0231074845243171 ) ) ;
#107941=CIRCLE ( 'NONE', #24773, 0.1000000000000028644 ) ;
#107959=VECTOR ( 'NONE', #16679, 1000.000000000000000 ) ;
#108019=EDGE_CURVE ( 'NONE', #116663, #107897, #131643, .T. ) ;
#108020=EDGE_LOOP ( 'NONE', ( #211584, #3307, #148246, #76826 ) ) ;
#108021=EDGE_CURVE ( 'NONE', #239334, #107898, #119177, .T. ) ;
#108044=CARTESIAN_POINT ( 'NONE',  ( -23.25000000000000000, 77.83585931145526615, -57.91866831572577468 ) ) ;
#108050=EDGE_CURVE ( 'NONE', #44904, #121706, #153228, .T. ) ;
#108085=AXIS2_PLACEMENT_3D ( 'NONE', #119930, #161616, #241145 ) ;
#108089=VERTEX_POINT ( 'NONE', #174085 ) ;
#108099=ORIENTED_EDGE ( 'NONE', *, *, #14984, .F. ) ;
#108101=ORIENTED_EDGE ( 'NONE', *, *, #126539, .F. ) ;
#108106=CARTESIAN_POINT ( 'NONE',  ( -23.25000000000000000, 64.25000000001195133, -103.0231074845244024 ) ) ;
#108136=ORIENTED_EDGE ( 'NONE', *, *, #181647, .F. ) ;
#108153=DIRECTION ( 'NONE',  ( 0.000000000000000000, 0.000000000000000000, 1.000000000000000000 ) ) ;
#108155=ADVANCED_FACE ( 'NONE', ( #210596, #80033, #59180 ), #37121, .F. ) ;
#108169=CARTESIAN_POINT ( 'NONE',  ( 18.59999999999997655, 76.00000000001170974, -69.52310748452431710 ) ) ;
#108201=ADVANCED_FACE ( 'NONE', ( #214436 ), #176629, .T. ) ;
#108209=EDGE_LOOP ( 'NONE', ( #182639, #3634, #247763 ) ) ;
#108231=AXIS2_PLACEMENT_3D ( 'NONE', #174227, #193749, #22516 ) ;
#108259=AXIS2_PLACEMENT_3D ( 'NONE', #28164, #30731, #26878 ) ;
#108262=AXIS2_PLACEMENT_3D ( 'NONE', #113166, #153633, #233146 ) ;
#108305=VERTEX_POINT ( 'NONE', #222118 ) ;
#108325=CIRCLE ( 'NONE', #150034, 0.1000000000000028644 ) ;
#108340=CIRCLE ( 'NONE', #79079, 0.1000000000000028644 ) ;
#108389=DIRECTION ( 'NONE',  ( 0.000000000000000000, -0.1350103645451945777, 0.9908441862701590219 ) ) ;
#108413=CARTESIAN_POINT ( 'NONE',  ( -20.94999999999999929, 76.00000000001170974, -69.52310748452431710 ) ) ;
#108453=CARTESIAN_POINT ( 'NONE',  ( 23.14999999999998437, 71.95000000001195417, -103.0231074845243455 ) ) ;
#108463=EDGE_CURVE ( 'NONE', #218126, #64641, #223570, .T. ) ;
#108482=DIRECTION ( 'NONE',  ( 0.000000000000000000, 0.000000000000000000, 1.000000000000000000 ) ) ;
#108488=AXIS2_PLACEMENT_3D ( 'NONE', #134043, #55763, #214872 ) ;
#108535=DIRECTION ( 'NONE',  ( 0.000000000000000000, -7.086529944415894657E-15, 1.000000000000000000 ) ) ;
#108580=DIRECTION ( 'NONE',  ( 0.000000000000000000, -0.9908441862701605762, -0.1350103645451835310 ) ) ;
#108598=ORIENTED_EDGE ( 'NONE', *, *, #117958, .T. ) ;
#108631=CARTESIAN_POINT ( 'NONE',  ( 21.04999999999987992, 76.01759718701998736, -109.4638783781862656 ) ) ;
#108640=CARTESIAN_POINT ( 'NONE',  ( 20.94999999999999929, 74.16465844978745281, -91.46795619196133487 ) ) ;
#108660=TOROIDAL_SURFACE ( 'NONE', #87789, 7.791421356237316687, 0.1000000000000000056 ) ;
#108712=EDGE_CURVE ( 'NONE', #86349, #158859, #119563, .T. ) ;
#108727=DIRECTION ( 'NONE',  ( 1.000000000000000000, 0.000000000000000000, 0.000000000000000000 ) ) ;
#108747=VERTEX_POINT ( 'NONE', #205812 ) ;
#108762=CARTESIAN_POINT ( 'NONE',  ( 18.49999999999999289, 65.79142135624934440, -114.7731074845243739 ) ) ;
#108772=CARTESIAN_POINT ( 'NONE',  ( -22.47886152344871036, 75.96249906115033923, -114.6730961275722507 ) ) ;
#108776=DIRECTION ( 'NONE',  ( 1.000000000000000000, 0.000000000000000000, 0.000000000000000000 ) ) ;
#108787=ORIENTED_EDGE ( 'NONE', *, *, #161133, .T. ) ;
#108804=CARTESIAN_POINT ( 'NONE',  ( 20.84999999999998721, 65.66751761918648356, -63.92826094061123143 ) ) ;
#108811=DIRECTION ( 'NONE',  ( 1.734723475976817507E-14, -6.982962677686266711E-15, 1.000000000000000000 ) ) ;
#108841=EDGE_CURVE ( 'NONE', #161481, #222763, #190115, .T. ) ;
#108847=CARTESIAN_POINT ( 'NONE',  ( -23.25000000000000000, 69.06610602788535402, -65.73746165015079157 ) ) ;
#108856=( BOUNDED_SURFACE ( )  B_SPLINE_SURFACE ( 3, 2, ( 
 ( #159067, #22119, #217707 ),
 ( #121242, #118655, #211658 ),
 ( #36567, #195627, #165472 ),
 ( #7682, #88458, #106754 ) ),
 .UNSPECIFIED., .F., .F., .F. ) 
 B_SPLINE_SURFACE_WITH_KNOTS ( ( 4, 4 ),
 ( 3, 3 ),
 ( -5.827586677109586333E-19, 0.0003124336117481331431 ),
 ( 0.000000000000000000, 1.000000000000000000 ),
 .UNSPECIFIED. ) 
 GEOMETRIC_REPRESENTATION_ITEM ( )  RATIONAL_B_SPLINE_SURFACE ( (
 ( 1.000000000000000000, 0.7040654476015839602, 1.000000000000000000),
 ( 1.000000000000000000, 0.7039193538781365334, 1.000000000000000000),
 ( 1.000000000000000000, 0.7089171279145672910, 1.000000000000000000),
 ( 1.000000000000000000, 0.7071067811865509034, 1.000000000000000000) ) ) 
 REPRESENTATION_ITEM ( '' )  SURFACE ( )  );
#108880=EDGE_CURVE ( 'NONE', #185475, #254207, #19789, .T. ) ;
#108942=DIRECTION ( 'NONE',  ( -0.000000000000000000, 1.000000000000000000, 6.982962677686266711E-15 ) ) ;
#108945=CARTESIAN_POINT ( 'NONE',  ( 22.57320508075688892, 64.25000000001193712, -103.0231074845244024 ) ) ;
#108950=FACE_OUTER_BOUND ( 'NONE', #232966, .T. ) ;
#108981=AXIS2_PLACEMENT_3D ( 'NONE', #157475, #236981, #68613 ) ;
#108983=CARTESIAN_POINT ( 'NONE',  ( 23.15000000000000213, 84.66355140188093742, -79.04720860259155302 ) ) ;
#109033=EDGE_CURVE ( 'NONE', #55246, #96147, #178656, .T. ) ;
#109041=ADVANCED_FACE ( 'NONE', ( #225043 ), #84211, .F. ) ;
#109047=VECTOR ( 'NONE', #124997, 1000.000000000000000 ) ;
#109049=ORIENTED_EDGE ( 'NONE', *, *, #162954, .T. ) ;
#109136=DIRECTION ( 'NONE',  ( 1.000000000000000000, 0.000000000000000000, 0.000000000000000000 ) ) ;
#109164=AXIS2_PLACEMENT_3D ( 'NONE', #105960, #156705, #35474 ) ;
#109172=VECTOR ( 'NONE', #95066, 1000.000000000000000 ) ;
#109190=DIRECTION ( 'NONE',  ( 0.000000000000000000, -0.008583690987162452199, 0.9999631594459053030 ) ) ;
#109193=ORIENTED_EDGE ( 'NONE', *, *, #102143, .T. ) ;
#109203=ORIENTED_EDGE ( 'NONE', *, *, #247845, .F. ) ;
#109215=CYLINDRICAL_SURFACE ( 'NONE', #55474, 0.1000000000000028644 ) ;
#109235=TOROIDAL_SURFACE ( 'NONE', #188357, 0.2000000000000000111, 0.1000000000000000056 ) ;
#109263=FACE_OUTER_BOUND ( 'NONE', #250603, .T. ) ;
#109307=CIRCLE ( 'NONE', #5238, 0.1000000000000028644 ) ;
#109308=ORIENTED_EDGE ( 'NONE', *, *, #150235, .F. ) ;
#109329=DIRECTION ( 'NONE',  ( 0.000000000000000000, 6.982962677686266711E-15, -1.000000000000000000 ) ) ;
#109331=EDGE_LOOP ( 'NONE', ( #185922, #44732, #200455, #8460, #157378, #219839 ) ) ;
#109337=DIRECTION ( 'NONE',  ( 0.000000000000000000, -6.982962677686266711E-15, 1.000000000000000000 ) ) ;
#109358=EDGE_CURVE ( 'NONE', #235470, #98958, #153089, .T. ) ;
#109362=DIRECTION ( 'NONE',  ( 0.000000000000000000, 0.000000000000000000, 1.000000000000000000 ) ) ;
#109375=VERTEX_POINT ( 'NONE', #119253 ) ;
#109419=ORIENTED_EDGE ( 'NONE', *, *, #90443, .T. ) ;
#109462=EDGE_CURVE ( 'NONE', #9387, #25250, #236597, .T. ) ;
#109468=VECTOR ( 'NONE', #235348, 1000.000000000000000 ) ;
#109522=ORIENTED_EDGE ( 'NONE', *, *, #40444, .F. ) ;
#109537=DIRECTION ( 'NONE',  ( 1.000000000000000000, -0.000000000000000000, 0.000000000000000000 ) ) ;
#109539=ORIENTED_EDGE ( 'NONE', *, *, #178742, .F. ) ;
#109546=CIRCLE ( 'NONE', #146952, 0.1999999999999987899 ) ;
#109556=DIRECTION ( 'NONE',  ( 0.000000000000000000, 0.000000000000000000, 1.000000000000000000 ) ) ;
#109607=DIRECTION ( 'NONE',  ( 0.000000000000000000, -0.7397360091702823714, 0.6728971962616756564 ) ) ;
#109617=CARTESIAN_POINT ( 'NONE',  ( 21.05000000000000071, 87.75000000001173817, -72.62310748452422615 ) ) ;
#109621=CARTESIAN_POINT ( 'NONE',  ( -20.88420186297724257, 65.66974365629646115, -63.93601455626049557 ) ) ;
#109635=DIRECTION ( 'NONE',  ( 0.000000000000000000, 0.000000000000000000, -1.000000000000000000 ) ) ;
#109690=FACE_OUTER_BOUND ( 'NONE', #83852, .T. ) ;
#109741=AXIS2_PLACEMENT_3D ( 'NONE', #213721, #35130, #232028 ) ;
#109747=CARTESIAN_POINT ( 'NONE',  ( 21.05000000000000071, 67.07338541492478612, -94.55142446530125255 ) ) ;
#109771=DIRECTION ( 'NONE',  ( 1.000000000000000000, 0.000000000000000000, 0.000000000000000000 ) ) ;
#109799=EDGE_CURVE ( 'NONE', #24108, #87934, #255827, .T. ) ;
#109807=ORIENTED_EDGE ( 'NONE', *, *, #21357, .T. ) ;
#109823=VECTOR ( 'NONE', #79514, 1000.000000000000000 ) ;
#109829=DIRECTION ( 'NONE',  ( 2.952720810173289112E-16, 1.000000000000000000, -6.088138035986627436E-46 ) ) ;
#109834=DIRECTION ( 'NONE',  ( 1.000000000000000000, 0.000000000000000000, 0.000000000000000000 ) ) ;
#109962=CARTESIAN_POINT ( 'NONE',  ( 23.14999999999999858, 64.35000000001176090, -76.53791325517833855 ) ) ;
#109967=( BOUNDED_CURVE ( )  B_SPLINE_CURVE ( 3, ( #141586, #162456, #102426, #2059 ),
 .UNSPECIFIED., .F., .F. ) 
 B_SPLINE_CURVE_WITH_KNOTS ( ( 4, 4 ),
 ( 3.141592653589793116, 4.712388980384689674 ),
 .UNSPECIFIED. ) 
 CURVE ( )  GEOMETRIC_REPRESENTATION_ITEM ( )  RATIONAL_B_SPLINE_CURVE ( ( 1.000000000000000000, 0.8047378541243649375, 0.8047378541243649375, 1.000000000000000000 ) ) 
 REPRESENTATION_ITEM ( '' )  );
#109999=AXIS2_PLACEMENT_3D ( 'NONE', #76996, #157870, #133129 ) ;
#110011=EDGE_CURVE ( 'NONE', #206437, #116798, #168384, .T. ) ;
#110049=CARTESIAN_POINT ( 'NONE',  ( -18.39999999999999858, 85.60000000001166143, -62.82291809330219223 ) ) ;
#110055=DIRECTION ( 'NONE',  ( -1.000000000000000000, 0.000000000000000000, 0.000000000000000000 ) ) ;
#110059=DIRECTION ( 'NONE',  ( -1.000000000000000000, 0.000000000000000000, 0.000000000000000000 ) ) ;
#110061=DIRECTION ( 'NONE',  ( 0.000000000000000000, -0.9908441862701605762, -0.1350103645451835310 ) ) ;
#110081=ORIENTED_EDGE ( 'NONE', *, *, #213288, .T. ) ;
#110088=VERTEX_POINT ( 'NONE', #114778 ) ;
#110093=CARTESIAN_POINT ( 'NONE',  ( 20.91682497891422798, 65.67736539654923433, -63.96251168765719797 ) ) ;
#110131=CARTESIAN_POINT ( 'NONE',  ( -18.50016250449483479, 65.70233904876991460, -64.04874109119681691 ) ) ;
#110152=DIRECTION ( 'NONE',  ( -1.000000000000000000, 0.000000000000000000, 0.000000000000000000 ) ) ;
#110154=CARTESIAN_POINT ( 'NONE',  ( -18.59999999999999787, 74.36282728704149747, -91.44095411905230719 ) ) ;
#110160=VERTEX_POINT ( 'NONE', #63788 ) ;
#110184=DIRECTION ( 'NONE',  ( 1.000000000000000000, 0.000000000000000000, 0.000000000000000000 ) ) ;
#110192=ORIENTED_EDGE ( 'NONE', *, *, #171023, .T. ) ;
#110208=ORIENTED_EDGE ( 'NONE', *, *, #201604, .F. ) ;
#110237=DIRECTION ( 'NONE',  ( 1.000000000000000000, -1.875376730785737719E-16, -1.309568571767809260E-30 ) ) ;
#110239=VERTEX_POINT ( 'NONE', #1223 ) ;
#110248=ORIENTED_EDGE ( 'NONE', *, *, #256308, .T. ) ;
#110267=DIRECTION ( 'NONE',  ( 1.000000000000000000, 0.000000000000000000, 0.000000000000000000 ) ) ;
#110276=CARTESIAN_POINT ( 'NONE',  ( 23.24999999999999645, 76.00000000001170974, -69.52310748452431710 ) ) ;
#110281=ADVANCED_FACE ( 'NONE', ( #204572 ), #37091, .T. ) ;
#110303=ORIENTED_EDGE ( 'NONE', *, *, #6665, .T. ) ;
#110351=CARTESIAN_POINT ( 'NONE',  ( -21.05000000000000071, 76.00000000001195133, -103.0231074845243171 ) ) ;
#110400=ORIENTED_EDGE ( 'NONE', *, *, #216467, .F. ) ;
#110404=AXIS2_PLACEMENT_3D ( 'NONE', #163892, #222551, #28262 ) ;
#110431=AXIS2_PLACEMENT_3D ( 'NONE', #234165, #35992, #235442 ) ;
#110455=CARTESIAN_POINT ( 'NONE',  ( -22.50000000000000000, 68.20922040163854660, -103.1231074845243540 ) ) ;
#110456=CARTESIAN_POINT ( 'NONE',  ( 20.94999999999999929, 69.45000000001186891, -90.87310748452435405 ) ) ;
#110476=DIRECTION ( 'NONE',  ( 1.000000000000000000, -0.000000000000000000, 0.000000000000000000 ) ) ;
#110521=LINE ( 'NONE', #229204, #119266 ) ;
#110530=FACE_OUTER_BOUND ( 'NONE', #21710, .T. ) ;
#110579=LINE ( 'NONE', #33666, #126609 ) ;
#110653=EDGE_CURVE ( 'NONE', #118654, #200940, #199687, .T. ) ;
#110657=ORIENTED_EDGE ( 'NONE', *, *, #75332, .T. ) ;
#110668=AXIS2_PLACEMENT_3D ( 'NONE', #8300, #224746, #69559 ) ;
#110680=CARTESIAN_POINT ( 'NONE',  ( -20.54999999999999716, 73.60000000001177511, -79.41707660717676731 ) ) ;
#110712=EDGE_CURVE ( 'NONE', #200905, #200766, #8221, .T. ) ;
#110734=LINE ( 'NONE', #149890, #25952 ) ;
#110738=CARTESIAN_POINT ( 'NONE',  ( 21.05000000000000071, 71.00000000001186606, -90.61784146561124942 ) ) ;
#110748=CIRCLE ( 'NONE', #81492, 12.87499999999999822 ) ;
#110753=DIRECTION ( 'NONE',  ( -0.000000000000000000, -6.982962677686266711E-15, 1.000000000000000000 ) ) ;
#110765=CARTESIAN_POINT ( 'NONE',  ( -23.15000000000000213, 87.65000000001172964, -72.62310748452422615 ) ) ;
#110811=EDGE_CURVE ( 'NONE', #102162, #239427, #27492, .T. ) ;
#110839=EDGE_LOOP ( 'NONE', ( #207461, #220981, #217576, #92279 ) ) ;
#110860=ORIENTED_EDGE ( 'NONE', *, *, #225296, .F. ) ;
#110864=VERTEX_POINT ( 'NONE', #75588 ) ;
#110874=ADVANCED_FACE ( 'NONE', ( #36464 ), #209952, .F. ) ;
#110887=ORIENTED_EDGE ( 'NONE', *, *, #43593, .F. ) ;
#110893=CARTESIAN_POINT ( 'NONE',  ( -22.59999999999999787, 64.25043287652255231, -103.1239658536231047 ) ) ;
#110916=CARTESIAN_POINT ( 'NONE',  ( -18.43473496883406426, 85.49495241101126908, -95.97723591229602391 ) ) ;
#110921=CIRCLE ( 'NONE', #65125, 11.64999999999999325 ) ;
#110938=AXIS2_PLACEMENT_3D ( 'NONE', #42303, #120576, #81386 ) ;
#110960=CARTESIAN_POINT ( 'NONE',  ( -18.59999999999999787, 85.50000000001185185, -90.87310748452424036 ) ) ;
#110963=CARTESIAN_POINT ( 'NONE',  ( -20.85000000000000142, 64.35000000001176090, -76.30697314750248950 ) ) ;
#110971=ADVANCED_FACE ( 'NONE', ( #94137 ), #173737, .T. ) ;
#110973=DIRECTION ( 'NONE',  ( 1.000000000000000000, 0.000000000000000000, 0.000000000000000000 ) ) ;
#110978=DIRECTION ( 'NONE',  ( 2.952720810173289112E-16, 1.000000000000000000, 6.530723674265620862E-15 ) ) ;
#110993=CARTESIAN_POINT ( 'NONE',  ( 18.52928932304161691, 65.72071067697012836, -78.34685405172071171 ) ) ;
#111008=ORIENTED_EDGE ( 'NONE', *, *, #142467, .T. ) ;
#111018=CARTESIAN_POINT ( 'NONE',  ( 21.14999999999999858, 76.00000000001200817, -109.5637644362255685 ) ) ;
#111026=AXIS2_PLACEMENT_3D ( 'NONE', #147666, #128103, #108535 ) ;
#111032=ORIENTED_EDGE ( 'NONE', *, *, #115469, .F. ) ;
#111053=EDGE_CURVE ( 'NONE', #132890, #169820, #101816, .T. ) ;
#111063=VERTEX_POINT ( 'NONE', #1453 ) ;
#111080=VERTEX_POINT ( 'NONE', #139667 ) ;
#111092=CARTESIAN_POINT ( 'NONE',  ( 21.05000000000000071, 65.37049252075090067, -95.39512808452764148 ) ) ;
#111109=FACE_OUTER_BOUND ( 'NONE', #119514, .T. ) ;
#111169=AXIS2_PLACEMENT_3D ( 'NONE', #130753, #169934, #9514 ) ;
#111171=LINE ( 'NONE', #250662, #43101 ) ;
#111193=VERTEX_POINT ( 'NONE', #87410 ) ;
#111199=ADVANCED_FACE ( 'NONE', ( #127845 ), #132547, .T. ) ;
#111200=TOROIDAL_SURFACE ( 'NONE', #81933, 12.77500000000000036, 0.1000000000000000056 ) ;
#111204=EDGE_CURVE ( 'NONE', #157067, #215622, #236758, .T. ) ;
#111206=DIRECTION ( 'NONE',  ( 0.000000000000000000, 0.000000000000000000, 1.000000000000000000 ) ) ;
#111220=FACE_OUTER_BOUND ( 'NONE', #225075, .T. ) ;
#111229=AXIS2_PLACEMENT_3D ( 'NONE', #163567, #60590, #140122 ) ;
#111245=TOROIDAL_SURFACE ( 'NONE', #128005, 11.65000000000000036, 0.1000000000000000056 ) ;
#111284=EDGE_CURVE ( 'NONE', #71686, #199332, #186919, .T. ) ;
#111290=CARTESIAN_POINT ( 'NONE',  ( 21.14999999999999858, 76.10000000001198828, -109.5637644362255543 ) ) ;
#111296=CYLINDRICAL_SURFACE ( 'NONE', #203206, 0.09999999999999939493 ) ;
#111300=ORIENTED_EDGE ( 'NONE', *, *, #249521, .F. ) ;
#111344=TOROIDAL_SURFACE ( 'NONE', #3168, 11.70000000000000639, 0.1000000000000000056 ) ;
#111349=CYLINDRICAL_SURFACE ( 'NONE', #211026, 0.09999999999999939493 ) ;
#111366=AXIS2_PLACEMENT_3D ( 'NONE', #179440, #218519, #20373 ) ;
#111377=EDGE_CURVE ( 'NONE', #194138, #248733, #183913, .T. ) ;
#111383=EDGE_LOOP ( 'NONE', ( #199470, #213794, #177731, #223251 ) ) ;
#111393=ADVANCED_FACE ( 'NONE', ( #52131 ), #175973, .F. ) ;
#111405=CARTESIAN_POINT ( 'NONE',  ( -23.25000000000000000, 85.60000000001178933, -79.41707660717668205 ) ) ;
#111411=EDGE_LOOP ( 'NONE', ( #116687, #250255, #193453, #45062, #141755, #127221, #129743, #194190 ) ) ;
#111418=VERTEX_POINT ( 'NONE', #97665 ) ;
#111433=DIRECTION ( 'NONE',  ( 1.000000000000000000, 0.000000000000000000, 0.000000000000000000 ) ) ;
#111445=( BOUNDED_SURFACE ( )  B_SPLINE_SURFACE ( 3, 2, ( 
 ( #221339, #244762, #102672 ),
 ( #186094, #124841, #161410 ),
 ( #165242, #140527, #143090 ),
 ( #184797, #204354, #2296 ),
 ( #121013, #3593, #144363 ),
 ( #222620, #162683, #203077 ) ),
 .UNSPECIFIED., .F., .F., .T. ) 
 B_SPLINE_SURFACE_WITH_KNOTS ( ( 4, 2, 4 ),
 ( 3, 3 ),
 ( 1.570796326794895448, 2.356194490192343505, 3.141592653589791784 ),
 ( 0.000000000000000000, 1.000000000000000000 ),
 .UNSPECIFIED. ) 
 GEOMETRIC_REPRESENTATION_ITEM ( )  RATIONAL_B_SPLINE_SURFACE ( (
 ( 1.000000000000000000, 0.7071067811865475727, 1.000000000000000000),
 ( 1.000000000000000000, 0.6611148371776656152, 1.000000000000000000),
 ( 1.000000000000000000, 0.6092287576699577656, 1.000000000000000000),
 ( 1.000000000000000000, 0.5278258667053233877, 1.000000000000000000),
 ( 1.000000000000000000, 0.4993418825337002098, 1.000000000000000000),
 ( 1.000000000000000000, 0.5000000000000154321, 1.000000000000000000) ) ) 
 REPRESENTATION_ITEM ( '' )  SURFACE ( )  );
#111447=ADVANCED_FACE ( 'NONE', ( #211221 ), #128633, .F. ) ;
#111459=EDGE_CURVE ( 'NONE', #80949, #56502, #107773, .T. ) ;
#111472=CARTESIAN_POINT ( 'NONE',  ( 20.02499999999999858, 66.25000000001179501, -81.77310748452437394 ) ) ;
#111484=DIRECTION ( 'NONE',  ( 0.000000000000000000, -6.938893903907222067E-15, 1.000000000000000000 ) ) ;
#111527=CARTESIAN_POINT ( 'NONE',  ( 23.24999999999999645, 79.90000000001171543, -69.52310748452428868 ) ) ;
#111551=VERTEX_POINT ( 'NONE', #19447 ) ;
#111577=CIRCLE ( 'NONE', #136486, 0.09999999999999939493 ) ;
#111597=LINE ( 'NONE', #32082, #151217 ) ;
#111610=DIRECTION ( 'NONE',  ( 0.000000000000000000, 0.000000000000000000, 1.000000000000000000 ) ) ;
#111623=ADVANCED_FACE ( 'NONE', ( #224039 ), #34539, .T. ) ;
#111627=AXIS2_PLACEMENT_3D ( 'NONE', #206535, #70909, #9611 ) ;
#111633=ORIENTED_EDGE ( 'NONE', *, *, #240741, .T. ) ;
#111639=CARTESIAN_POINT ( 'NONE',  ( -20.94999999999999929, 68.87972903831409610, -65.86354444268503983 ) ) ;
#111642=ORIENTED_EDGE ( 'NONE', *, *, #16280, .F. ) ;
#111661=ADVANCED_FACE ( 'NONE', ( #8864 ), #133607, .T. ) ;
#111684=VERTEX_POINT ( 'NONE', #93195 ) ;
#111723=DIRECTION ( 'NONE',  ( -0.000000000000000000, 1.000000000000000000, 6.982962677686266711E-15 ) ) ;
#111736=LINE ( 'NONE', #92165, #191787 ) ;
#111753=DIRECTION ( 'NONE',  ( -7.304098846218134667E-16, 1.000000000000000000, 6.982962677686266711E-15 ) ) ;
#111754=TOROIDAL_SURFACE ( 'NONE', #28404, 0.6000000000000004219, 0.1000000000000000056 ) ;
#111778=EDGE_CURVE ( 'NONE', #221237, #215945, #228781, .T. ) ;
#111781=EDGE_LOOP ( 'NONE', ( #85054, #188431, #83878, #180545 ) ) ;
#111794=ORIENTED_EDGE ( 'NONE', *, *, #152054, .T. ) ;
#111804=AXIS2_PLACEMENT_3D ( 'NONE', #237905, #21454, #197485 ) ;
#111821=AXIS2_PLACEMENT_3D ( 'NONE', #197488, #43569, #99654 ) ;
#111822=ORIENTED_EDGE ( 'NONE', *, *, #184120, .F. ) ;
#111823=AXIS2_PLACEMENT_3D ( 'NONE', #211374, #133118, #213932 ) ;
#111844=CARTESIAN_POINT ( 'NONE',  ( -23.15000000000000213, 70.05000000001177796, -79.82880978955917328 ) ) ;
#111846=FACE_OUTER_BOUND ( 'NONE', #151270, .T. ) ;
#111872=MANIFOLD_SOLID_BREP ( 'Stock-MAS-200-1', #249288 ) ;
#111891=CARTESIAN_POINT ( 'NONE',  ( -20.64999999999999858, 76.00000000001170974, -69.52310748452431710 ) ) ;
#111910=CARTESIAN_POINT ( 'NONE',  ( 21.05000000000000071, 69.45934304831071415, -102.9231074845243512 ) ) ;
#111923=DIRECTION ( 'NONE',  ( 0.000000000000000000, 0.000000000000000000, -1.000000000000000000 ) ) ;
#111933=CARTESIAN_POINT ( 'NONE',  ( 20.95420533658165141, 65.45413552525231182, -95.45560146383114386 ) ) ;
#111956=ORIENTED_EDGE ( 'NONE', *, *, #49713, .F. ) ;
#111966=CARTESIAN_POINT ( 'NONE',  ( -22.39999999999999858, 76.10085836911075319, -114.7726746080137019 ) ) ;
#111968=CARTESIAN_POINT ( 'NONE',  ( -23.15000000000000213, 71.75000000001180922, -81.77310748452433131 ) ) ;
#112003=EDGE_CURVE ( 'NONE', #227104, #190290, #112445, .T. ) ;
#112007=FACE_OUTER_BOUND ( 'NONE', #210139, .T. ) ;
#112042=EDGE_CURVE ( 'NONE', #159653, #29906, #169922, .T. ) ;
#112054=CYLINDRICAL_SURFACE ( 'NONE', #39774, 0.09999999999999939493 ) ;
#112067=EDGE_CURVE ( 'NONE', #117549, #21472, #57113, .T. ) ;
#112071=DIRECTION ( 'NONE',  ( 0.000000000000000000, 0.000000000000000000, -1.000000000000000000 ) ) ;
#112075=CARTESIAN_POINT ( 'NONE',  ( 18.60000000000000142, 85.32100840337318459, -95.78716923544635620 ) ) ;
#112091=ORIENTED_EDGE ( 'NONE', *, *, #137390, .T. ) ;
#112105=EDGE_CURVE ( 'NONE', #256577, #245252, #220583, .T. ) ;
#112114=CARTESIAN_POINT ( 'NONE',  ( -20.85000000000000142, 64.35000000001171827, -69.52310748452438816 ) ) ;
#112117=ORIENTED_EDGE ( 'NONE', *, *, #158015, .T. ) ;
#112132=EDGE_LOOP ( 'NONE', ( #179046, #58104, #78346, #192160, #188541 ) ) ;
#112153=ORIENTED_EDGE ( 'NONE', *, *, #49755, .T. ) ;
#112175=CARTESIAN_POINT ( 'NONE',  ( 22.39999999999999503, 64.25000000001195133, -103.1231074845243825 ) ) ;
#112177=DIRECTION ( 'NONE',  ( -1.000000000000000000, 7.304098846218134667E-16, 5.100424963727255829E-30 ) ) ;
#112214=CARTESIAN_POINT ( 'NONE',  ( 18.59999999999997655, 76.00000000001170974, -69.52310748452431710 ) ) ;
#112218=CARTESIAN_POINT ( 'NONE',  ( 20.94999999999999929, 76.00000000001170974, -69.52310748452431710 ) ) ;
#112239=CARTESIAN_POINT ( 'NONE',  ( 21.97500000000000497, 66.25000000001186606, -90.67310748452437963 ) ) ;
#112241=CARTESIAN_POINT ( 'NONE',  ( -21.05000000000000071, 87.39257802171739797, -72.59705706435616435 ) ) ;
#112325=ORIENTED_EDGE ( 'NONE', *, *, #115650, .T. ) ;
#112367=CARTESIAN_POINT ( 'NONE',  ( 21.17356465864818915, 75.90108875899811380, -109.4459106107660489 ) ) ;
#112382=EDGE_CURVE ( 'NONE', #16536, #232010, #133281, .T. ) ;
#112386=LINE ( 'NONE', #114944, #639 ) ;
#112404=EDGE_CURVE ( 'NONE', #129578, #96147, #175025, .T. ) ;
#112419=ADVANCED_FACE ( 'NONE', ( #150031 ), #74363, .T. ) ;
#112445=CIRCLE ( 'NONE', #120639, 0.1000000000000028644 ) ;
#112461=CARTESIAN_POINT ( 'NONE',  ( -22.59080734064477625, 64.25000000001195133, -103.0538571926214217 ) ) ;
#112482=AXIS2_PLACEMENT_3D ( 'NONE', #32544, #172054, #251544 ) ;
#112488=EDGE_LOOP ( 'NONE', ( #51765, #214372, #156358, #76065 ) ) ;
#112510=VERTEX_POINT ( 'NONE', #256754 ) ;
#112519=ORIENTED_EDGE ( 'NONE', *, *, #169063, .F. ) ;
#112541=CARTESIAN_POINT ( 'NONE',  ( -21.05000000000000071, 76.00000000001170974, -69.52310748452431710 ) ) ;
#112547=FACE_OUTER_BOUND ( 'NONE', #192893, .T. ) ;
#112550=DIRECTION ( 'NONE',  ( 0.000000000000000000, -7.116814260417668513E-15, 1.000000000000000000 ) ) ;
#112551=ADVANCED_FACE ( 'NONE', ( #172191, #138125 ), #217659, .F. ) ;
#112561=EDGE_CURVE ( 'NONE', #173885, #111551, #12678, .T. ) ;
#112590=DIRECTION ( 'NONE',  ( 0.000000000000000000, 0.000000000000000000, -1.000000000000000000 ) ) ;
#112596=ORIENTED_EDGE ( 'NONE', *, *, #167765, .T. ) ;
#112614=VECTOR ( 'NONE', #203263, 1000.000000000000000 ) ;
#112629=CARTESIAN_POINT ( 'NONE',  ( 21.05000000000000071, 64.40000000001175806, -76.45131071479988805 ) ) ;
#112633=EDGE_CURVE ( 'NONE', #245252, #88959, #83358, .T. ) ;
#112641=CARTESIAN_POINT ( 'NONE',  ( -18.49372193242234275, 85.44248452336977095, -62.75832622448970710 ) ) ;
#112654=( BOUNDED_SURFACE ( )  B_SPLINE_SURFACE ( 3, 2, ( 
 ( #516, #80031, #140019 ),
 ( #163464, #219568, #40975 ),
 ( #200027, #229859, #51185 ),
 ( #150334, #129479, #189456 ),
 ( #228585, #146443, #207745 ),
 ( #89048, #249433, #206440 ),
 ( #47345, #69520, #48638 ),
 ( #231167, #52484, #27837 ),
 ( #49928, #209009, #30389 ),
 ( #128193, #190764, #225963 ),
 ( #86459, #107332, #29138 ),
 ( #149057, #210306, #186902 ) ),
 .UNSPECIFIED., .F., .F., .F. ) 
 B_SPLINE_SURFACE_WITH_KNOTS ( ( 4, 2, 2, 2, 2, 4 ),
 ( 3, 3 ),
 ( 3.174653483277205090, 3.943930578431714018, 4.713207673586222946, 5.482484768740731873, 5.867123316317986337, 6.251761863895240801 ),
 ( 0.000000000000000000, 1.000000000000000000 ),
 .UNSPECIFIED. ) 
 GEOMETRIC_REPRESENTATION_ITEM ( )  RATIONAL_B_SPLINE_SURFACE ( (
 ( 1.000000000000000000, 0.8659465255642289083, 1.000000000000000000),
 ( 1.000000000000000000, 0.8648614068487607831, 1.000000000000000000),
 ( 1.000000000000000000, 0.8489031841324650163, 1.000000000000000000),
 ( 1.000000000000000000, 0.7927507630160894880, 1.000000000000000000),
 ( 1.000000000000000000, 0.7523013859007505744, 1.000000000000000000),
 ( 1.000000000000000000, 0.6616226951199137840, 1.000000000000000000),
 ( 1.000000000000000000, 0.6112214368721295976, 1.000000000000000000),
 ( 1.000000000000000000, 0.5507684314499833311, 1.000000000000000000),
 ( 1.000000000000000000, 0.5333267243194751428, 1.000000000000000000),
 ( 1.000000000000000000, 0.5084565446437981917, 1.000000000000000000),
 ( 1.000000000000000000, 0.5010722703481732543, 1.000000000000000000),
 ( 1.000000000000000000, 0.5001234037139490329, 1.000000000000000000) ) ) 
 REPRESENTATION_ITEM ( '' )  SURFACE ( )  );
#112681=FACE_OUTER_BOUND ( 'NONE', #56726, .T. ) ;
#112686=CARTESIAN_POINT ( 'NONE',  ( -20.94999999999999929, 74.83729825007388570, -94.92310748452432279 ) ) ;
#112700=PLANE ( 'NONE',  #81307 ) ;
#112721=DIRECTION ( 'NONE',  ( 0.000000000000000000, 0.000000000000000000, 1.000000000000000000 ) ) ;
#112728=CARTESIAN_POINT ( 'NONE',  ( -21.05000000000000071, 77.83534155023627932, -91.36795619196132634 ) ) ;
#112747=AXIS2_PLACEMENT_3D ( 'NONE', #118421, #60989, #180953 ) ;
#112760=EDGE_CURVE ( 'NONE', #215026, #12008, #175203, .T. ) ;
#112762=VERTEX_POINT ( 'NONE', #157438 ) ;
#112799=CARTESIAN_POINT ( 'NONE',  ( -20.54999999999999716, 76.00000000001169553, -67.62310748452431142 ) ) ;
#112821=CYLINDRICAL_SURFACE ( 'NONE', #145055, 0.09999999999999939493 ) ;
#112844=EDGE_LOOP ( 'NONE', ( #175690, #206581, #168607, #82904, #121070 ) ) ;
#112855=CIRCLE ( 'NONE', #142065, 4.000000000000003553 ) ;
#112875=B_SPLINE_CURVE_WITH_KNOTS ( 'NONE', 3,
 ( #213855, #56033, #54768, #196844, #19520, #99009, #256774, #159045 ),
 .UNSPECIFIED., .F., .F.,
 ( 4, 2, 2, 4 ),
 ( 0.000000000000000000, 0.0002181133598169196985, 0.0003271700397253618346, 0.0004362267196338040520 ),
 .UNSPECIFIED. ) ;
#112879=FACE_OUTER_BOUND ( 'NONE', #99220, .T. ) ;
#112885=CARTESIAN_POINT ( 'NONE',  ( 18.60000000000000142, 85.48068669529062902, -62.58199231576637089 ) ) ;
#112894=DIRECTION ( 'NONE',  ( -1.000000000000000000, 0.000000000000000000, 0.000000000000000000 ) ) ;
#112913=EDGE_CURVE ( 'NONE', #135352, #116632, #191431, .T. ) ;
#112935=FACE_OUTER_BOUND ( 'NONE', #125281, .T. ) ;
#112945=FACE_OUTER_BOUND ( 'NONE', #131186, .T. ) ;
#112958=DIRECTION ( 'NONE',  ( 1.000000000000000000, 0.000000000000000000, 0.000000000000000000 ) ) ;
#112976=ORIENTED_EDGE ( 'NONE', *, *, #147266, .F. ) ;
#113025=ORIENTED_EDGE ( 'NONE', *, *, #119500, .T. ) ;
#113038=ADVANCED_FACE ( 'NONE', ( #20476 ), #159994, .F. ) ;
#113047=EDGE_LOOP ( 'NONE', ( #46720, #219900, #135588, #1554, #23372, #27397 ) ) ;
#113050=ORIENTED_EDGE ( 'NONE', *, *, #69448, .T. ) ;
#113066=LINE ( 'NONE', #88332, #107525 ) ;
#113071=DIRECTION ( 'NONE',  ( 0.000000000000000000, -1.000000000000000000, -6.860497997771532351E-15 ) ) ;
#113130=EDGE_LOOP ( 'NONE', ( #77078, #201608, #161499, #38992 ) ) ;
#113144=CIRCLE ( 'NONE', #254739, 0.1000000000000028644 ) ;
#113159=DIRECTION ( 'NONE',  ( 0.000000000000000000, -6.467318590049456648E-15, 1.000000000000000000 ) ) ;
#113166=CARTESIAN_POINT ( 'NONE',  ( -21.05000000000000071, 76.00000000001170974, -69.52310748452431710 ) ) ;
#113171=CARTESIAN_POINT ( 'NONE',  ( 23.24999999999999289, 64.35000000001194564, -102.9231074845243938 ) ) ;
#113234=CARTESIAN_POINT ( 'NONE',  ( 21.11833042828134666, 69.55435530615672235, -103.0302079935837725 ) ) ;
#113261=CARTESIAN_POINT ( 'NONE',  ( 18.49999999999999645, 70.30054753569044124, -115.5653814410941891 ) ) ;
#113278=CARTESIAN_POINT ( 'NONE',  ( -23.25000000000000000, 77.85161776048053639, -57.91991776492063337 ) ) ;
#113319=CARTESIAN_POINT ( 'NONE',  ( 20.94999999999999929, 67.22371710471932715, -81.77310748452437394 ) ) ;
#113329=ORIENTED_EDGE ( 'NONE', *, *, #67581, .F. ) ;
#113352=DIRECTION ( 'NONE',  ( 1.000000000000000000, 0.000000000000000000, 0.000000000000000000 ) ) ;
#113370=( BOUNDED_SURFACE ( )  B_SPLINE_SURFACE ( 3, 2, ( 
 ( #69243, #70541, #90056 ),
 ( #232169, #53513, #169656 ),
 ( #110916, #190485, #250422 ),
 ( #11847, #91367, #254259 ),
 ( #177349, #75667, #217693 ),
 ( #54782, #19535, #57340 ),
 ( #237292, #256787, #39108 ),
 ( #212601, #18242, #238563 ) ),
 .UNSPECIFIED., .F., .F., .F. ) 
 B_SPLINE_SURFACE_WITH_KNOTS ( ( 4, 2, 2, 4 ),
 ( 3, 3 ),
 ( 0.0001723339234021441008, 0.0002782939632049936159, 0.0003842540030078431582, 0.0005961740826135421886 ),
 ( 0.000000000000000000, 1.000000000000000000 ),
 .UNSPECIFIED. ) 
 GEOMETRIC_REPRESENTATION_ITEM ( )  RATIONAL_B_SPLINE_SURFACE ( (
 ( 1.000000000000000000, 0.9504532311154701985, 1.000000000000000000),
 ( 1.000000000000000000, 0.9506023220711478094, 1.000000000000000000),
 ( 1.000000000000000000, 0.9395774818179351007, 1.000000000000000000),
 ( 1.000000000000000000, 0.9079328464649522035, 1.000000000000000000),
 ( 1.000000000000000000, 0.8875702416205013545, 1.000000000000000000),
 ( 1.000000000000000000, 0.8205919608041974955, 1.000000000000000000),
 ( 1.000000000000000000, 0.7666842783597154209, 1.000000000000000000),
 ( 1.000000000000000000, 0.7071067811864398811, 1.000000000000000000) ) ) 
 REPRESENTATION_ITEM ( '' )  SURFACE ( )  );
#113392=AXIS2_PLACEMENT_3D ( 'NONE', #210669, #71183, #131129 ) ;
#113399=ORIENTED_EDGE ( 'NONE', *, *, #104740, .F. ) ;
#113407=DIRECTION ( 'NONE',  ( 1.000000000000000000, 0.000000000000000000, 0.000000000000000000 ) ) ;
#113438=CARTESIAN_POINT ( 'NONE',  ( -20.85000000000000142, 69.06610602788535402, -65.73746165015079157 ) ) ;
#113459=DIRECTION ( 'NONE',  ( 0.000000000000000000, 0.000000000000000000, -1.000000000000000000 ) ) ;
#113471=EDGE_CURVE ( 'NONE', #222093, #123180, #170514, .T. ) ;
#113472=CIRCLE ( 'NONE', #1003, 4.000000000000003553 ) ;
#113500=ADVANCED_FACE ( 'NONE', ( #168375 ), #113370, .T. ) ;
#113503=AXIS2_PLACEMENT_3D ( 'NONE', #248598, #12580, #171667 ) ;
#113521=CARTESIAN_POINT ( 'NONE',  ( -21.05000000000000071, 69.69503888732695884, -103.0017219185864121 ) ) ;
#113549=VERTEX_POINT ( 'NONE', #74401 ) ;
#113580=FACE_OUTER_BOUND ( 'NONE', #209645, .T. ) ;
#113589=DIRECTION ( 'NONE',  ( 0.000000000000000000, 6.982962677686266711E-15, -1.000000000000000000 ) ) ;
#113610=AXIS2_PLACEMENT_3D ( 'NONE', #128715, #70040, #50425 ) ;
#113616=ORIENTED_EDGE ( 'NONE', *, *, #154720, .F. ) ;
#113654=ORIENTED_EDGE ( 'NONE', *, *, #43006, .T. ) ;
#113669=ORIENTED_EDGE ( 'NONE', *, *, #119500, .F. ) ;
#113699=ADVANCED_FACE ( 'NONE', ( #181182 ), #82023, .T. ) ;
#113711=CIRCLE ( 'NONE', #5348, 0.9750000000000036415 ) ;
#113716=ORIENTED_EDGE ( 'NONE', *, *, #250446, .F. ) ;
#113736=VERTEX_POINT ( 'NONE', #209714 ) ;
#113761=CARTESIAN_POINT ( 'NONE',  ( 21.13435531349814767, 76.00000000001199396, -109.5168285481162940 ) ) ;
#113778=DIRECTION ( 'NONE',  ( 0.000000000000000000, 6.982962677686267499E-15, -1.000000000000000000 ) ) ;
#113809=FACE_OUTER_BOUND ( 'NONE', #235059, .T. ) ;
#113829=TOROIDAL_SURFACE ( 'NONE', #105414, 0.2000000000000000111, 0.1000000000000000056 ) ;
#113847=AXIS2_PLACEMENT_3D ( 'NONE', #102072, #202488, #117806 ) ;
#113902=VERTEX_POINT ( 'NONE', #16659 ) ;
#113910=CARTESIAN_POINT ( 'NONE',  ( 21.05000000000000071, 87.48912529308798014, -100.1231074845242262 ) ) ;
#113944=CARTESIAN_POINT ( 'NONE',  ( 20.86777300164945004, 65.66799936921512426, -63.92993998886009877 ) ) ;
#113961=CARTESIAN_POINT ( 'NONE',  ( 18.39999999999999858, 85.50000000001166711, -62.60844914155458696 ) ) ;
#113980=EDGE_CURVE ( 'NONE', #59112, #168899, #252672, .T. ) ;
#113985=CARTESIAN_POINT ( 'NONE',  ( -20.85000000000000142, 77.83585931145526615, -58.01866831572577610 ) ) ;
#114030=CARTESIAN_POINT ( 'NONE',  ( 20.12500000000000000, 66.25000000001189449, -94.91133620241009794 ) ) ;
#114034=CARTESIAN_POINT ( 'NONE',  ( 23.14999999999999858, 64.40000000001175806, -76.45131071479988805 ) ) ;
#114047=ORIENTED_EDGE ( 'NONE', *, *, #31543, .F. ) ;
#114061=CYLINDRICAL_SURFACE ( 'NONE', #254642, 0.1000000000000028644 ) ;
#114069=DIRECTION ( 'NONE',  ( 1.000000000000000000, 0.000000000000000000, -0.000000000000000000 ) ) ;
#114071=DIRECTION ( 'NONE',  ( 1.000000000000000000, 0.000000000000000000, 0.000000000000000000 ) ) ;
#114073=DIRECTION ( 'NONE',  ( 0.000000000000000000, -1.000000000000000000, -3.469446951953515108E-14 ) ) ;
#114086=ORIENTED_EDGE ( 'NONE', *, *, #193872, .T. ) ;
#114095=ORIENTED_EDGE ( 'NONE', *, *, #172282, .F. ) ;
#114109=EDGE_CURVE ( 'NONE', #183416, #97655, #202974, .T. ) ;
#114123=CARTESIAN_POINT ( 'NONE',  ( -18.59999999999999787, 68.97833521811159585, -65.68954208262705663 ) ) ;
#114132=AXIS2_PLACEMENT_3D ( 'NONE', #183261, #58143, #158581 ) ;
#114149=ORIENTED_EDGE ( 'NONE', *, *, #27094, .T. ) ;
#114153=ORIENTED_EDGE ( 'NONE', *, *, #86724, .T. ) ;
#114156=DIRECTION ( 'NONE',  ( 0.000000000000000000, -6.982962677686266711E-15, 1.000000000000000000 ) ) ;
#114174=ORIENTED_EDGE ( 'NONE', *, *, #246306, .T. ) ;
#114201=AXIS2_PLACEMENT_3D ( 'NONE', #159404, #155578, #178996 ) ;
#114248=DIRECTION ( 'NONE',  ( -1.000000000000000000, 0.000000000000000000, 0.000000000000000000 ) ) ;
#114256=EDGE_CURVE ( 'NONE', #188719, #227881, #226363, .T. ) ;
#114286=ADVANCED_FACE ( 'NONE', ( #105118 ), #246786, .F. ) ;
#114328=EDGE_LOOP ( 'NONE', ( #68125, #101042, #61426 ) ) ;
#114342=ORIENTED_EDGE ( 'NONE', *, *, #22415, .T. ) ;
#114352=CARTESIAN_POINT ( 'NONE',  ( -23.15000000000000213, 87.48912529308779540, -72.62310748452422615 ) ) ;
#114364=CARTESIAN_POINT ( 'NONE',  ( -23.25000000000000000, 76.00000000001170974, -69.52310748452431710 ) ) ;
#114375=DIRECTION ( 'NONE',  ( 1.000000000000000000, 0.000000000000000000, 0.000000000000000000 ) ) ;
#114398=EDGE_LOOP ( 'NONE', ( #40476, #163772, #41003, #217823 ) ) ;
#114400=ORIENTED_EDGE ( 'NONE', *, *, #59596, .F. ) ;
#114432=AXIS2_PLACEMENT_3D ( 'NONE', #149471, #33394, #111610 ) ;
#114483=CIRCLE ( 'NONE', #177239, 1.899999999999999023 ) ;
#114489=DIRECTION ( 'NONE',  ( -1.000000000000000000, 0.000000000000000000, -0.000000000000000000 ) ) ;
#114491=EDGE_CURVE ( 'NONE', #156829, #126928, #117346, .T. ) ;
#114511=DIRECTION ( 'NONE',  ( -0.000000000000000000, 6.982962677686266711E-15, -1.000000000000000000 ) ) ;
#114523=CARTESIAN_POINT ( 'NONE',  ( 21.05000000000000071, 69.74115287693277310, -103.0548658375798965 ) ) ;
#114547=VERTEX_POINT ( 'NONE', #134423 ) ;
#114552=VERTEX_POINT ( 'NONE', #96578 ) ;
#114573=CARTESIAN_POINT ( 'NONE',  ( -20.85000000000000142, 77.83585931145526615, -57.91866831572577468 ) ) ;
#114605=CARTESIAN_POINT ( 'NONE',  ( -23.15000000000000213, 76.00000000001179501, -82.39810748452430289 ) ) ;
#114628=ORIENTED_EDGE ( 'NONE', *, *, #82052, .T. ) ;
#114688=CARTESIAN_POINT ( 'NONE',  ( 21.05563370358598263, 65.27576964416535077, -90.84001666856131862 ) ) ;
#114696=AXIS2_PLACEMENT_3D ( 'NONE', #158780, #217418, #101284 ) ;
#114706=FACE_OUTER_BOUND ( 'NONE', #122179, .T. ) ;
#114713=EDGE_CURVE ( 'NONE', #170518, #20030, #122608, .T. ) ;
#114753=TOROIDAL_SURFACE ( 'NONE', #2293, 0.2000000000000000111, 0.1000000000000000056 ) ;
#114778=CARTESIAN_POINT ( 'NONE',  ( -22.59999999999999787, 75.89914163091332000, -114.7726746080137019 ) ) ;
#114786=CARTESIAN_POINT ( 'NONE',  ( -22.16821283564876666, 68.44102665923117002, -103.0231074845243739 ) ) ;
#114796=AXIS2_PLACEMENT_3D ( 'NONE', #156716, #61434, #58833 ) ;
#114799=DIRECTION ( 'NONE',  ( -1.000000000000000000, -3.469446951953635015E-14, -2.422701857770461054E-28 ) ) ;
#114825=CARTESIAN_POINT ( 'NONE',  ( -18.50000000000000000, 68.97833521811159585, -65.68954208262705663 ) ) ;
#114830=CYLINDRICAL_SURFACE ( 'NONE', #111823, 0.1000000000000052097 ) ;
#114836=ORIENTED_EDGE ( 'NONE', *, *, #180026, .F. ) ;
#114888=AXIS2_PLACEMENT_3D ( 'NONE', #23781, #58987, #159420 ) ;
#114900=CARTESIAN_POINT ( 'NONE',  ( -20.94999999999999929, 87.65000000001172964, -72.62310748452422615 ) ) ;
#114908=B_SPLINE_CURVE_WITH_KNOTS ( 'NONE', 3,
 ( #246239, #106704, #208416, #164144, #147125, #184978, #104134, #222800 ),
 .UNSPECIFIED., .F., .F.,
 ( 4, 2, 2, 4 ),
 ( 0.000000000000000000, 0.0001049670497869896891, 0.0002099340995739793782, 0.0004198681991480113403 ),
 .UNSPECIFIED. ) ;
#114922=CARTESIAN_POINT ( 'NONE',  ( 21.22070241538126467, 75.90108096947696481, -109.4930537573939375 ) ) ;
#114923=ORIENTED_EDGE ( 'NONE', *, *, #225296, .T. ) ;
#114925=TOROIDAL_SURFACE ( 'NONE', #239837, 12.97499999999999609, 0.1000000000000000056 ) ;
#114941=EDGE_CURVE ( 'NONE', #44131, #242050, #11648, .T. ) ;
#114944=CARTESIAN_POINT ( 'NONE',  ( -18.50000000000000000, 72.08710075277841156, -91.54128451151336776 ) ) ;
#114975=CARTESIAN_POINT ( 'NONE',  ( -20.64999999999999858, 74.00000000001186606, -89.79848556176222019 ) ) ;
#114978=LINE ( 'NONE', #175003, #33608 ) ;
#115011=CARTESIAN_POINT ( 'NONE',  ( -22.59999999999999787, 64.25043287652255231, -103.1239658536231047 ) ) ;
#115028=CARTESIAN_POINT ( 'NONE',  ( 18.39999999999999858, 85.51932773110434027, -96.05013110796491560 ) ) ;
#115037=AXIS2_PLACEMENT_3D ( 'NONE', #19863, #240191, #195937 ) ;
#115056=DIRECTION ( 'NONE',  ( 0.000000000000000000, -7.034366652768107165E-15, 1.000000000000000000 ) ) ;
#115100=ORIENTED_EDGE ( 'NONE', *, *, #236842, .T. ) ;
#115146=CARTESIAN_POINT ( 'NONE',  ( 21.11747605621531321, 67.22129199451896397, -90.77854431473458874 ) ) ;
#115179=AXIS2_PLACEMENT_3D ( 'NONE', #136861, #183375, #195579 ) ;
#115201=DIRECTION ( 'NONE',  ( 0.000000000000000000, 6.982962677686266711E-15, -1.000000000000000000 ) ) ;
#115213=DIRECTION ( 'NONE',  ( 0.000000000000000000, -1.000000000000000000, -6.982962677686266711E-15 ) ) ;
#115257=ORIENTED_EDGE ( 'NONE', *, *, #190113, .F. ) ;
#115285=EDGE_CURVE ( 'NONE', #69698, #125644, #213850, .T. ) ;
#115297=DIRECTION ( 'NONE',  ( 0.000000000000000000, 0.000000000000000000, 1.000000000000000000 ) ) ;
#115321=CARTESIAN_POINT ( 'NONE',  ( -18.50000000000000000, 77.16412189325286874, -61.60825939895269698 ) ) ;
#115330=LINE ( 'NONE', #171494, #209842 ) ;
#115363=DIRECTION ( 'NONE',  ( 0.000000000000000000, 0.9999176327611370985, -0.01283462868041289687 ) ) ;
#115373=CARTESIAN_POINT ( 'NONE',  ( -21.05000000000000071, 76.00000000001192291, -100.1231074845243256 ) ) ;
#115379=CARTESIAN_POINT ( 'NONE',  ( -21.44999999999999929, 68.75000000001179501, -81.77310748452435973 ) ) ;
#115383=DIRECTION ( 'NONE',  ( 4.377807931758639578E-15, -0.2605042016806606298, -0.9654727137038736640 ) ) ;
#115387=CARTESIAN_POINT ( 'NONE',  ( -21.14999999999999858, 87.65000000001195701, -103.0231074845242318 ) ) ;
#115405=DIRECTION ( 'NONE',  ( 1.000000000000000000, 0.000000000000000000, 0.000000000000000000 ) ) ;
#115420=AXIS2_PLACEMENT_3D ( 'NONE', #53923, #176461, #255917 ) ;
#115454=CARTESIAN_POINT ( 'NONE',  ( -21.05000000000000071, 76.00000000001195133, -103.0231074845243171 ) ) ;
#115469=EDGE_CURVE ( 'NONE', #254425, #64641, #246716, .T. ) ;
#115474=LINE ( 'NONE', #213285, #150319 ) ;
#115502=ORIENTED_EDGE ( 'NONE', *, *, #76755, .F. ) ;
#115512=DIRECTION ( 'NONE',  ( 0.000000000000000000, 0.000000000000000000, 1.000000000000000000 ) ) ;
#115532=CARTESIAN_POINT ( 'NONE',  ( -20.94999999999999929, 77.83534155023627932, -91.46795619196130644 ) ) ;
#115560=CYLINDRICAL_SURFACE ( 'NONE', #136237, 0.1000000000000028644 ) ;
#115587=CARTESIAN_POINT ( 'NONE',  ( 20.46382478191414833, 67.09862044130927927, -94.47737938964125703 ) ) ;
#115588=EDGE_CURVE ( 'NONE', #6826, #209310, #84224, .T. ) ;
#115603=AXIS2_PLACEMENT_3D ( 'NONE', #71913, #211411, #172333 ) ;
#115623=EDGE_CURVE ( 'NONE', #123658, #182622, #238985, .T. ) ;
#115624=CARTESIAN_POINT ( 'NONE',  ( 20.04142135623731136, 64.25000000001176659, -78.25595019699900945 ) ) ;
#115650=EDGE_CURVE ( 'NONE', #181805, #154400, #209359, .T. ) ;
#115686=EDGE_CURVE ( 'NONE', #192857, #209005, #95150, .T. ) ;
#115694=AXIS2_PLACEMENT_3D ( 'NONE', #105825, #167147, #163275 ) ;
#115704=LINE ( 'NONE', #120866, #257296 ) ;
#115705=CARTESIAN_POINT ( 'NONE',  ( -21.37071067811865532, 67.92928932189313684, -81.77310748452435973 ) ) ;
#115747=AXIS2_PLACEMENT_3D ( 'NONE', #200664, #239795, #63706 ) ;
#115750=ORIENTED_EDGE ( 'NONE', *, *, #57573, .F. ) ;
#115758=DIRECTION ( 'NONE',  ( -1.000000000000000000, 3.265361837132813093E-16, 2.280189983783949500E-30 ) ) ;
#115760=LINE ( 'NONE', #195327, #107959 ) ;
#115819=CARTESIAN_POINT ( 'NONE',  ( 18.52928932188133970, 65.72071067813043044, -78.27310748452438816 ) ) ;
#115861=CARTESIAN_POINT ( 'NONE',  ( 22.57856590037848576, 76.00412833007638369, -114.7731659471998000 ) ) ;
#115900=DIRECTION ( 'NONE',  ( 1.000000000000000000, 0.000000000000000000, 0.000000000000000000 ) ) ;
#115927=LINE ( 'NONE', #38965, #109172 ) ;
#115962=EDGE_CURVE ( 'NONE', #178561, #74222, #71653, .T. ) ;
#115970=FACE_OUTER_BOUND ( 'NONE', #89353, .T. ) ;
#115977=DIRECTION ( 'NONE',  ( 1.000000000000000000, 0.000000000000000000, 0.000000000000000000 ) ) ;
#115980=ORIENTED_EDGE ( 'NONE', *, *, #110811, .F. ) ;
#115982=DIRECTION ( 'NONE',  ( 0.000000000000000000, 7.109473446599835262E-15, -1.000000000000000000 ) ) ;
#115984=DIRECTION ( 'NONE',  ( 0.000000000000000000, 0.000000000000000000, 1.000000000000000000 ) ) ;
#115987=CARTESIAN_POINT ( 'NONE',  ( 21.08750232978087524, 65.27513661400170975, -90.79424931152482259 ) ) ;
#116029=CARTESIAN_POINT ( 'NONE',  ( 20.04142135623730070, 64.35000000001201670, -114.7731074845243882 ) ) ;
#116059=CARTESIAN_POINT ( 'NONE',  ( 23.14999999999999858, 70.40000000001180069, -81.92837350343744163 ) ) ;
#116080=DIRECTION ( 'NONE',  ( 0.000000000000000000, 8.783410004945854632E-15, -1.000000000000000000 ) ) ;
#116106=DIRECTION ( 'NONE',  ( 0.000000000000000000, 0.1455152366551500653, 0.9893560106964507384 ) ) ;
#116124=DIRECTION ( 'NONE',  ( -0.000000000000000000, -0.8660254037844377084, -0.5000000000000016653 ) ) ;
#116131=CIRCLE ( 'NONE', #211987, 0.09999999999999939493 ) ;
#116139=CARTESIAN_POINT ( 'NONE',  ( 18.49999999999999289, 65.50857864377447015, -78.27310748452438816 ) ) ;
#116147=ORIENTED_EDGE ( 'NONE', *, *, #201196, .T. ) ;
#116159=AXIS2_PLACEMENT_3D ( 'NONE', #120596, #121873, #55749 ) ;
#116168=CARTESIAN_POINT ( 'NONE',  ( -21.05000000000000071, 74.83729825007388570, -95.12310748452432563 ) ) ;
#116215=TOROIDAL_SURFACE ( 'NONE', #91065, 0.2000000000000000111, 0.1000000000000000056 ) ;
#116226=ORIENTED_EDGE ( 'NONE', *, *, #110653, .F. ) ;
#116230=DIRECTION ( 'NONE',  ( 0.000000000000000000, 6.467318590049456648E-15, -1.000000000000000000 ) ) ;
#116247=VERTEX_POINT ( 'NONE', #144410 ) ;
#116249=CARTESIAN_POINT ( 'NONE',  ( 18.54116936837188589, 85.46356419838433283, -95.97456499363596549 ) ) ;
#116264=ORIENTED_EDGE ( 'NONE', *, *, #210708, .T. ) ;
#116300=EDGE_CURVE ( 'NONE', #88769, #167256, #93030, .T. ) ;
#116340=DIRECTION ( 'NONE',  ( 0.000000000000000000, 0.9887567792719329507, 0.1495327102803732933 ) ) ;
#116352=CARTESIAN_POINT ( 'NONE',  ( 22.39999999999999858, 76.00000000001195133, -103.0231074845243171 ) ) ;
#116412=AXIS2_PLACEMENT_3D ( 'NONE', #43904, #891, #62191 ) ;
#116429=CARTESIAN_POINT ( 'NONE',  ( -22.39999999999999858, 76.10085836911075319, -114.7726746080137019 ) ) ;
#116464=CYLINDRICAL_SURFACE ( 'NONE', #163248, 4.049999999999998046 ) ;
#116497=CARTESIAN_POINT ( 'NONE',  ( 22.00356870143220078, 68.74575763754050683, -103.0231074845243597 ) ) ;
#116506=DIRECTION ( 'NONE',  ( 0.000000000000000000, -6.982962677686266711E-15, 1.000000000000000000 ) ) ;
#116508=DIRECTION ( 'NONE',  ( 0.000000000000000000, 0.000000000000000000, 1.000000000000000000 ) ) ;
#116512=TOROIDAL_SURFACE ( 'NONE', #16571, 0.2000000000000000111, 0.1000000000000000056 ) ;
#116529=ORIENTED_EDGE ( 'NONE', *, *, #243049, .F. ) ;
#116536=CIRCLE ( 'NONE', #74871, 0.09999999999999520384 ) ;
#116593=ORIENTED_EDGE ( 'NONE', *, *, #1853, .F. ) ;
#116598=EDGE_CURVE ( 'NONE', #4968, #66389, #80272, .T. ) ;
#116632=VERTEX_POINT ( 'NONE', #46301 ) ;
#116639=VERTEX_POINT ( 'NONE', #146671 ) ;
#116642=FACE_OUTER_BOUND ( 'NONE', #53382, .T. ) ;
#116648=CARTESIAN_POINT ( 'NONE',  ( -20.64999999999999858, 68.85000000001186038, -90.67310748452435121 ) ) ;
#116652=DIRECTION ( 'NONE',  ( 0.000000000000000000, 0.01283462868040226822, 0.9999176327611370985 ) ) ;
#116663=VERTEX_POINT ( 'NONE', #222354 ) ;
#116682=AXIS2_PLACEMENT_3D ( 'NONE', #52513, #171244, #106055 ) ;
#116686=DIRECTION ( 'NONE',  ( 0.000000000000000000, -1.000000000000000000, -7.272083257015735086E-15 ) ) ;
#116687=ORIENTED_EDGE ( 'NONE', *, *, #184577, .T. ) ;
#116697=EDGE_CURVE ( 'NONE', #247315, #253910, #72382, .T. ) ;
#116702=CARTESIAN_POINT ( 'NONE',  ( -20.94999999999999929, 76.00000000001168132, -65.52310748452430289 ) ) ;
#116718=DIRECTION ( 'NONE',  ( -0.000000000000000000, 1.000000000000000000, 6.982962677686266711E-15 ) ) ;
#116735=DIRECTION ( 'NONE',  ( -1.000000000000000000, 0.000000000000000000, 0.000000000000000000 ) ) ;
#116754=AXIS2_PLACEMENT_3D ( 'NONE', #64296, #83813, #214697 ) ;
#116774=DIRECTION ( 'NONE',  ( 1.000000000000000000, 0.000000000000000000, 0.000000000000000000 ) ) ;
#116798=VERTEX_POINT ( 'NONE', #93138 ) ;
#116821=DIRECTION ( 'NONE',  ( 0.000000000000000000, 6.982962677686266711E-15, -1.000000000000000000 ) ) ;
#116867=ORIENTED_EDGE ( 'NONE', *, *, #58101, .T. ) ;
#116873=CARTESIAN_POINT ( 'NONE',  ( 18.50000000000000000, 85.40000000001190017, -95.72584772486095517 ) ) ;
#116899=ORIENTED_EDGE ( 'NONE', *, *, #86107, .F. ) ;
#116928=CARTESIAN_POINT ( 'NONE',  ( -21.05000000000000071, 76.00000000001195133, -103.0231074845243171 ) ) ;
#116938=CYLINDRICAL_SURFACE ( 'NONE', #194429, 0.1000000000000052097 ) ;
#116964=LINE ( 'NONE', #17845, #247856 ) ;
#116979=ORIENTED_EDGE ( 'NONE', *, *, #128117, .T. ) ;
#116999=ORIENTED_EDGE ( 'NONE', *, *, #100669, .T. ) ;
#117040=CIRCLE ( 'NONE', #83682, 0.1000000000000028644 ) ;
#117058=TOROIDAL_SURFACE ( 'NONE', #46122, 0.4000000000000009104, 0.1000000000000000056 ) ;
#117108=DIRECTION ( 'NONE',  ( 0.000000000000000000, 6.982962677686266711E-15, -1.000000000000000000 ) ) ;
#117111=LINE ( 'NONE', #157559, #7064 ) ;
#117125=CARTESIAN_POINT ( 'NONE',  ( -23.15000000000000213, 76.00000000001197975, -107.1731074845243086 ) ) ;
#117138=CIRCLE ( 'NONE', #208731, 0.1000000000000021427 ) ;
#117147=EDGE_CURVE ( 'NONE', #220516, #1991, #197432, .T. ) ;
#117154=CARTESIAN_POINT ( 'NONE',  ( 20.85000000000000142, 76.00000000001170974, -69.52310748452431710 ) ) ;
#117160=EDGE_LOOP ( 'NONE', ( #253193, #239443, #97626, #88907 ) ) ;
#117187=LINE ( 'NONE', #18073, #34629 ) ;
#117189=ORIENTED_EDGE ( 'NONE', *, *, #76367, .T. ) ;
#117198=DIRECTION ( 'NONE',  ( 0.000000000000000000, 6.982962677686266711E-15, -1.000000000000000000 ) ) ;
#117224=B_SPLINE_CURVE_WITH_KNOTS ( 'NONE', 3,
 ( #86904, #83040, #127341, #8677, #84297, #184732 ),
 .UNSPECIFIED., .F., .F.,
 ( 4, 2, 4 ),
 ( 0.000000000000000000, 0.0001891491689349559776, 0.0003782983378699119551 ),
 .UNSPECIFIED. ) ;
#117226=CIRCLE ( 'NONE', #217149, 0.09999999999999938105 ) ;
#117282=EDGE_LOOP ( 'NONE', ( #114628, #191613, #8337, #248704 ) ) ;
#117331=CARTESIAN_POINT ( 'NONE',  ( 19.75857864376268935, 64.35000000001177511, -78.27310748452438816 ) ) ;
#117344=DIRECTION ( 'NONE',  ( -1.000000000000000000, -0.000000000000000000, -0.000000000000000000 ) ) ;
#117346=B_SPLINE_CURVE_WITH_KNOTS ( 'NONE', 3,
 ( #78852, #60580, #158445, #237941 ),
 .UNSPECIFIED., .F., .F.,
 ( 4, 4 ),
 ( 0.000000000000000000, 0.001767853679387133359 ),
 .UNSPECIFIED. ) ;
#117368=CARTESIAN_POINT ( 'NONE',  ( -21.59142135623730852, 68.15000000001180069, -81.87310748452436826 ) ) ;
#117407=DIRECTION ( 'NONE',  ( 1.000000000000000000, 0.000000000000000000, 0.000000000000000000 ) ) ;
#117410=CARTESIAN_POINT ( 'NONE',  ( 21.14999999999999503, 87.65000000001202807, -114.7731074845242318 ) ) ;
#117507=ORIENTED_EDGE ( 'NONE', *, *, #204317, .F. ) ;
#117549=VERTEX_POINT ( 'NONE', #27142 ) ;
#117552=DIRECTION ( 'NONE',  ( -3.265361837132813093E-16, -1.000000000000000000, -6.938893903907229955E-15 ) ) ;
#117561=ORIENTED_EDGE ( 'NONE', *, *, #158461, .F. ) ;
#117570=AXIS2_PLACEMENT_3D ( 'NONE', #135774, #215322, #17151 ) ;
#117573=DIRECTION ( 'NONE',  ( 1.000000000000000000, -2.952720810173289112E-16, -2.061873921506763405E-30 ) ) ;
#117578=SURFACE_SIDE_STYLE ('',( #236238 ) ) ;
#117608=CARTESIAN_POINT ( 'NONE',  ( 22.47110162079220785, 75.97120258720933350, -114.6730434212086465 ) ) ;
#117614=EDGE_CURVE ( 'NONE', #113549, #31606, #37700, .T. ) ;
#117659=DIRECTION ( 'NONE',  ( 0.000000000000000000, 1.000000000000000000, 6.982962677686266711E-15 ) ) ;
#117661=CARTESIAN_POINT ( 'NONE',  ( 21.08804281139606829, 65.37816569817070445, -90.67310751714592243 ) ) ;
#117677=DIRECTION ( 'NONE',  ( 0.000000000000000000, -6.938893903907222067E-15, 1.000000000000000000 ) ) ;
#117706=CARTESIAN_POINT ( 'NONE',  ( 21.05281448260627641, 67.22398984147423562, -90.84954957271294518 ) ) ;
#117768=CARTESIAN_POINT ( 'NONE',  ( -18.47130263965443220, 85.47115558597558049, -62.83970271904723859 ) ) ;
#117779=CARTESIAN_POINT ( 'NONE',  ( 23.14999999999999503, 64.25000000001202238, -114.7731074845243882 ) ) ;
#117796=ORIENTED_EDGE ( 'NONE', *, *, #73763, .T. ) ;
#117806=DIRECTION ( 'NONE',  ( 0.000000000000000000, 0.000000000000000000, 1.000000000000000000 ) ) ;
#117809=DIRECTION ( 'NONE',  ( 0.000000000000000000, -0.008583690987135041833, 0.9999631594459055250 ) ) ;
#117882=AXIS2_PLACEMENT_3D ( 'NONE', #5691, #205189, #69569 ) ;
#117943=EDGE_LOOP ( 'NONE', ( #115100, #100664, #134590, #251702 ) ) ;
#117958=EDGE_CURVE ( 'NONE', #37771, #69698, #242831, .T. ) ;
#117990=DIRECTION ( 'NONE',  ( 0.000000000000000000, 0.8777080977375072424, -0.4791956752371691608 ) ) ;
#118009=VERTEX_POINT ( 'NONE', #79880 ) ;
#118014=LINE ( 'NONE', #196264, #40710 ) ;
#118025=AXIS2_PLACEMENT_3D ( 'NONE', #146313, #85031, #241571 ) ;
#118027=ORIENTED_EDGE ( 'NONE', *, *, #4037, .F. ) ;
#118029=DIRECTION ( 'NONE',  ( -0.000000000000000000, 0.4791956752371485107, 0.8777080977375185666 ) ) ;
#118047=LINE ( 'NONE', #39828, #54616 ) ;
#118079=ADVANCED_FACE ( 'NONE', ( #168491 ), #164597, .T. ) ;
#118091=ORIENTED_EDGE ( 'NONE', *, *, #193872, .F. ) ;
#118108=CARTESIAN_POINT ( 'NONE',  ( -20.85000000000000142, 77.14957036958736580, -61.70719500002233815 ) ) ;
#118122=CIRCLE ( 'NONE', #109741, 0.09999999999999939493 ) ;
#118135=FACE_OUTER_BOUND ( 'NONE', #67414, .T. ) ;
#118146=CARTESIAN_POINT ( 'NONE',  ( 20.94999999999999574, 67.07338541492480033, -94.55142446530125255 ) ) ;
#118157=CARTESIAN_POINT ( 'NONE',  ( 18.46858270002952551, 85.47420267472247701, -95.92108554982041824 ) ) ;
#118185=DIRECTION ( 'NONE',  ( 2.952720810173289112E-16, 1.000000000000000000, 6.530723674265620862E-15 ) ) ;
#118219=VECTOR ( 'NONE', #124015, 1000.000000000000000 ) ;
#118220=EDGE_LOOP ( 'NONE', ( #242206, #182995, #129955, #10665 ) ) ;
#118233=AXIS2_PLACEMENT_3D ( 'NONE', #213321, #231634, #52971 ) ;
#118253=ORIENTED_EDGE ( 'NONE', *, *, #116697, .F. ) ;
#118266=ORIENTED_EDGE ( 'NONE', *, *, #55261, .F. ) ;
#118287=ORIENTED_EDGE ( 'NONE', *, *, #212836, .F. ) ;
#118294=SPHERICAL_SURFACE ( 'NONE', #229606, 0.1000000000000000056 ) ;
#118296=DIRECTION ( 'NONE',  ( -3.265361837132813093E-16, -1.000000000000000000, 7.445645354460596589E-46 ) ) ;
#118309=ORIENTED_EDGE ( 'NONE', *, *, #34428, .T. ) ;
#118336=CARTESIAN_POINT ( 'NONE',  ( -21.05000000000000071, 74.16465844978745281, -91.36795619196134055 ) ) ;
#118339=DIRECTION ( 'NONE',  ( -2.978066053179066272E-16, -1.000000000000000000, -8.338584948901384773E-15 ) ) ;
#118345=ADVANCED_FACE ( 'NONE', ( #106296 ), #62396, .T. ) ;
#118365=DIRECTION ( 'NONE',  ( -1.000000000000000000, -0.000000000000000000, 0.000000000000000000 ) ) ;
#118390=ORIENTED_EDGE ( 'NONE', *, *, #88772, .F. ) ;
#118399=CARTESIAN_POINT ( 'NONE',  ( -20.85000000000000142, 77.16412189325286874, -61.60825939895269698 ) ) ;
#118409=VERTEX_POINT ( 'NONE', #52753 ) ;
#118410=LINE ( 'NONE', #195396, #39153 ) ;
#118421=CARTESIAN_POINT ( 'NONE',  ( -20.85000000000000142, 87.65000000001171543, -69.52310748452423184 ) ) ;
#118447=AXIS2_PLACEMENT_3D ( 'NONE', #78246, #140804, #237341 ) ;
#118449=VECTOR ( 'NONE', #185737, 1000.000000000000000 ) ;
#118453=VECTOR ( 'NONE', #187597, 1000.000000000000000 ) ;
#118567=ORIENTED_EDGE ( 'NONE', *, *, #65238, .T. ) ;
#118591=ORIENTED_EDGE ( 'NONE', *, *, #195745, .F. ) ;
#118596=LINE ( 'NONE', #198107, #23018 ) ;
#118603=DIRECTION ( 'NONE',  ( 0.000000000000000000, -6.982962677686266711E-15, 1.000000000000000000 ) ) ;
#118604=EDGE_CURVE ( 'NONE', #174346, #252190, #56584, .T. ) ;
#118625=B_SPLINE_CURVE_WITH_KNOTS ( 'NONE', 3,
 ( #64120, #61555, #124107, #206198 ),
 .UNSPECIFIED., .F., .F.,
 ( 4, 4 ),
 ( 3.469446951953614189E-18, 0.0001058379652594568606 ),
 .UNSPECIFIED. ) ;
#118654=VERTEX_POINT ( 'NONE', #202550 ) ;
#118655=CARTESIAN_POINT ( 'NONE',  ( -22.45354308602371063, 75.99999978013372015, -114.7735403749838525 ) ) ;
#118658=CIRCLE ( 'NONE', #164442, 0.1000000000000021289 ) ;
#118665=CARTESIAN_POINT ( 'NONE',  ( -21.05000000000000071, 76.00000000001195133, -103.0231074845243171 ) ) ;
#118699=CARTESIAN_POINT ( 'NONE',  ( -18.59999999999999787, 61.95000000001191154, -97.50941241376341395 ) ) ;
#118703=ORIENTED_EDGE ( 'NONE', *, *, #35244, .F. ) ;
#118711=CARTESIAN_POINT ( 'NONE',  ( -22.50000000000000000, 76.00000000001195133, -103.0231074845243171 ) ) ;
#118714=CARTESIAN_POINT ( 'NONE',  ( -20.85000000000000142, 68.92903212821283887, -65.77654326265606244 ) ) ;
#118758=DIRECTION ( 'NONE',  ( 0.000000000000000000, 0.000000000000000000, 1.000000000000000000 ) ) ;
#118800=FACE_OUTER_BOUND ( 'NONE', #242444, .T. ) ;
#118850=EDGE_CURVE ( 'NONE', #204044, #81484, #12085, .T. ) ;
#118862=CARTESIAN_POINT ( 'NONE',  ( 23.14999999999999503, 69.35000000001180354, -81.87310748452435405 ) ) ;
#118877=DIRECTION ( 'NONE',  ( -1.000000000000000000, 0.000000000000000000, 0.000000000000000000 ) ) ;
#118891=EDGE_CURVE ( 'NONE', #51868, #129578, #194580, .T. ) ;
#118914=EDGE_CURVE ( 'NONE', #227881, #151730, #45853, .T. ) ;
#118927=CARTESIAN_POINT ( 'NONE',  ( -22.00411653889220176, 75.90096189422511941, -110.2765503521648185 ) ) ;
#118928=EDGE_CURVE ( 'NONE', #101974, #200905, #58299, .T. ) ;
#118931=CARTESIAN_POINT ( 'NONE',  ( -23.24999999999999645, 85.60000000001166143, -62.92291809330219365 ) ) ;
#118939=ORIENTED_EDGE ( 'NONE', *, *, #173872, .T. ) ;
#118962=CARTESIAN_POINT ( 'NONE',  ( 21.06280952165520759, 65.37286769941019315, -90.81905359774572162 ) ) ;
#119021=AXIS2_PLACEMENT_3D ( 'NONE', #159354, #60223, #21137 ) ;
#119060=VERTEX_POINT ( 'NONE', #121466 ) ;
#119083=CARTESIAN_POINT ( 'NONE',  ( -22.47071067811865319, 76.00000000001195133, -103.0231074845243171 ) ) ;
#119123=FACE_OUTER_BOUND ( 'NONE', #87059, .T. ) ;
#119177=CIRCLE ( 'NONE', #90120, 0.09999999999999939493 ) ;
#119188=EDGE_CURVE ( 'NONE', #37642, #211497, #208551, .T. ) ;
#119253=CARTESIAN_POINT ( 'NONE',  ( 22.57320508075687115, 64.25000000001195133, -103.0231074845244024 ) ) ;
#119261=CYLINDRICAL_SURFACE ( 'NONE', #55046, 11.80000000000000426 ) ;
#119263=AXIS2_PLACEMENT_3D ( 'NONE', #62109, #4671, #123366 ) ;
#119265=AXIS2_PLACEMENT_3D ( 'NONE', #242488, #100391, #102968 ) ;
#119266=VECTOR ( 'NONE', #131370, 1000.000000000000000 ) ;
#119290=SPHERICAL_SURFACE ( 'NONE', #234872, 0.1000000000000000056 ) ;
#119299=AXIS2_PLACEMENT_3D ( 'NONE', #57540, #174990, #95401 ) ;
#119306=DIRECTION ( 'NONE',  ( -0.000000000000000000, -0.8660254037844420383, 0.4999999999999943379 ) ) ;
#119324=CARTESIAN_POINT ( 'NONE',  ( 20.94999999999999929, 71.14953271029217774, -81.55737489352601699 ) ) ;
#119435=ORIENTED_EDGE ( 'NONE', *, *, #250632, .F. ) ;
#119500=EDGE_CURVE ( 'NONE', #86355, #226147, #112855, .T. ) ;
#119510=CIRCLE ( 'NONE', #73729, 0.1000000000000028644 ) ;
#119514=EDGE_LOOP ( 'NONE', ( #74564, #174285, #75765, #244293 ) ) ;
#119538=CARTESIAN_POINT ( 'NONE',  ( -20.00857864376270001, 66.85000000001186038, -90.67310748452436542 ) ) ;
#119549=CARTESIAN_POINT ( 'NONE',  ( -20.94999999999999929, 87.41227409416143246, -72.42310748452423752 ) ) ;
#119563=CIRCLE ( 'NONE', #227866, 0.1000000000000028644 ) ;
#119582=ORIENTED_EDGE ( 'NONE', *, *, #208543, .T. ) ;
#119584=FACE_OUTER_BOUND ( 'NONE', #185231, .T. ) ;
#119623=CARTESIAN_POINT ( 'NONE',  ( 18.53317502108576420, 65.67736539654922012, -63.96251168765718376 ) ) ;
#119636=CIRCLE ( 'NONE', #248819, 4.150000000000001243 ) ;
#119666=CARTESIAN_POINT ( 'NONE',  ( 20.94999999999999929, 85.40000000001188596, -93.12913836187179584 ) ) ;
#119682=CIRCLE ( 'NONE', #169613, 0.1000000000000028644 ) ;
#119684=CARTESIAN_POINT ( 'NONE',  ( -20.64999999999999858, 85.00000000001179501, -79.41707660717668205 ) ) ;
#119723=EDGE_CURVE ( 'NONE', #168580, #14237, #117138, .T. ) ;
#119786=CARTESIAN_POINT ( 'NONE',  ( 22.39999999999999503, 76.00000000001200817, -110.8138870828976934 ) ) ;
#119830=DIRECTION ( 'NONE',  ( 1.000000000000000000, 0.000000000000000000, 0.000000000000000000 ) ) ;
#119840=ORIENTED_EDGE ( 'NONE', *, *, #257625, .F. ) ;
#119879=FACE_OUTER_BOUND ( 'NONE', #66557, .T. ) ;
#119886=AXIS2_PLACEMENT_3D ( 'NONE', #201366, #38442, #240497 ) ;
#119896=CIRCLE ( 'NONE', #65683, 0.09999999999999520384 ) ;
#119917=CARTESIAN_POINT ( 'NONE',  ( -18.59999999999999787, 64.35000000001190301, -96.00830171387039513 ) ) ;
#119929=ORIENTED_EDGE ( 'NONE', *, *, #238694, .T. ) ;
#119930=CARTESIAN_POINT ( 'NONE',  ( 20.94999999999999574, 77.83534155023627932, -91.46795619196132066 ) ) ;
#119933=EDGE_LOOP ( 'NONE', ( #169246, #213083, #188268, #133744 ) ) ;
#119934=PLANE ( 'NONE',  #163385 ) ;
#119948=ORIENTED_EDGE ( 'NONE', *, *, #214977, .T. ) ;
#119957=CARTESIAN_POINT ( 'NONE',  ( 18.52928932188134326, 65.72071067813041623, -78.31452884076169596 ) ) ;
#119966=CARTESIAN_POINT ( 'NONE',  ( -21.05000000000000071, 69.45934304831071415, -102.9231074845243512 ) ) ;
#119994=DIRECTION ( 'NONE',  ( 0.000000000000000000, 0.9908441862701605762, -0.1350103645451835310 ) ) ;
#120037=CIRCLE ( 'NONE', #111627, 0.1999999999999987899 ) ;
#120056=EDGE_CURVE ( 'NONE', #201690, #255841, #251008, .T. ) ;
#120099=ORIENTED_EDGE ( 'NONE', *, *, #90950, .F. ) ;
#120113=CARTESIAN_POINT ( 'NONE',  ( -18.50000000000000000, 64.35000000001180354, -81.67310748452439384 ) ) ;
#120124=EDGE_LOOP ( 'NONE', ( #150239, #150192, #50530, #155595 ) ) ;
#120138=CARTESIAN_POINT ( 'NONE',  ( -23.15000000000000213, 71.75000000001180922, -81.87310748452433984 ) ) ;
#120143=ORIENTED_EDGE ( 'NONE', *, *, #56179, .T. ) ;
#120160=CARTESIAN_POINT ( 'NONE',  ( 21.05000000000000071, 76.10000000001198828, -109.5637644362255543 ) ) ;
#120165=CARTESIAN_POINT ( 'NONE',  ( 23.24999999999999645, 71.00000000001180922, -81.92837350343744163 ) ) ;
#120216=CARTESIAN_POINT ( 'NONE',  ( 22.48508240969612615, 75.95372358549511205, -114.6731182160978761 ) ) ;
#120225=DIRECTION ( 'NONE',  ( 0.000000000000000000, 0.000000000000000000, -1.000000000000000000 ) ) ;
#120226=AXIS2_PLACEMENT_3D ( 'NONE', #201203, #141234, #83779 ) ;
#120236=CARTESIAN_POINT ( 'NONE',  ( -21.53752568622130781, 75.90102553874135083, -109.8099153590727894 ) ) ;
#120251=CARTESIAN_POINT ( 'NONE',  ( -18.50000000000000000, 74.16465844978745281, -91.46795619196133487 ) ) ;
#120255=AXIS2_PLACEMENT_3D ( 'NONE', #14583, #231060, #234899 ) ;
#120264=DIRECTION ( 'NONE',  ( 0.000000000000000000, 0.000000000000000000, 1.000000000000000000 ) ) ;
#120286=DIRECTION ( 'NONE',  ( -1.000000000000000000, -0.000000000000000000, -0.000000000000000000 ) ) ;
#120313=CARTESIAN_POINT ( 'NONE',  ( -22.60000000000080789, 75.95218301954666629, -114.7731299156770461 ) ) ;
#120358=CYLINDRICAL_SURFACE ( 'NONE', #139447, 0.1000000000000028644 ) ;
#120368=EDGE_CURVE ( 'NONE', #232638, #146711, #209084, .T. ) ;
#120380=CARTESIAN_POINT ( 'NONE',  ( 21.07016717456946253, 69.67905916191168103, -103.0231074845243455 ) ) ;
#120417=VERTEX_POINT ( 'NONE', #136875 ) ;
#120430=CARTESIAN_POINT ( 'NONE',  ( 21.05000000000000071, 84.66355140188105111, -93.49900636645693908 ) ) ;
#120433=VERTEX_POINT ( 'NONE', #95185 ) ;
#120443=CIRCLE ( 'NONE', #70551, 0.2000000000000057288 ) ;
#120455=DIRECTION ( 'NONE',  ( -3.265361837132813093E-16, -1.000000000000000000, -6.982962677686266711E-15 ) ) ;
#120472=CIRCLE ( 'NONE', #237151, 12.87499999999999822 ) ;
#120485=CARTESIAN_POINT ( 'NONE',  ( 23.14999999999998437, 76.00000000001192291, -98.97310748452431994 ) ) ;
#120552=AXIS2_PLACEMENT_3D ( 'NONE', #197542, #127008, #26646 ) ;
#120566=DIRECTION ( 'NONE',  ( 0.000000000000000000, 0.000000000000000000, -1.000000000000000000 ) ) ;
#120576=DIRECTION ( 'NONE',  ( 1.000000000000000000, 0.000000000000000000, 0.000000000000000000 ) ) ;
#120577=AXIS2_PLACEMENT_3D ( 'NONE', #55577, #98546, #176873 ) ;
#120580=EDGE_CURVE ( 'NONE', #278, #180772, #163299, .T. ) ;
#120595=CARTESIAN_POINT ( 'NONE',  ( -20.64999999999999858, 85.00000000001179501, -79.01707660717669057 ) ) ;
#120596=CARTESIAN_POINT ( 'NONE',  ( 23.14999999999999503, 64.35000000001201670, -114.7731074845243882 ) ) ;
#120639=AXIS2_PLACEMENT_3D ( 'NONE', #192031, #246830, #32979 ) ;
#120651=DIRECTION ( 'NONE',  ( -0.000000000000000000, -6.982962677686266711E-15, 1.000000000000000000 ) ) ;
#120661=VERTEX_POINT ( 'NONE', #87158 ) ;
#120685=EDGE_CURVE ( 'NONE', #70872, #9918, #151009, .T. ) ;
#120701=ADVANCED_FACE ( 'NONE', ( #187586 ), #234181, .F. ) ;
#120708=CARTESIAN_POINT ( 'NONE',  ( -21.05000000000000071, 74.75000000001189449, -95.02310748452431710 ) ) ;
#120731=ORIENTED_EDGE ( 'NONE', *, *, #54954, .T. ) ;
#120762=CARTESIAN_POINT ( 'NONE',  ( -21.45000000000000284, 68.29142135624910281, -81.77310748452435973 ) ) ;
#120803=CARTESIAN_POINT ( 'NONE',  ( -21.06715728752538652, 64.25000000001190870, -96.00830171387038092 ) ) ;
#120833=AXIS2_PLACEMENT_3D ( 'NONE', #10794, #169913, #249412 ) ;
#120839=DIRECTION ( 'NONE',  ( -0.000000000000000000, -6.982962677686266711E-15, 1.000000000000000000 ) ) ;
#120849=CARTESIAN_POINT ( 'NONE',  ( 21.09813707148777340, 69.61493789427544243, -103.0544589840538663 ) ) ;
#120866=CARTESIAN_POINT ( 'NONE',  ( -21.05000000000000071, 74.16465844978745281, -91.36795619196134055 ) ) ;
#120879=DIRECTION ( 'NONE',  ( 1.000000000000000000, 0.000000000000000000, 0.000000000000000000 ) ) ;
#120883=CARTESIAN_POINT ( 'NONE',  ( -20.94999999999999929, 87.48912529308779540, -72.42310748452423752 ) ) ;
#120894=DIRECTION ( 'NONE',  ( 1.000000000000000000, 0.000000000000000000, 0.000000000000000000 ) ) ;
#120900=EDGE_LOOP ( 'NONE', ( #46664, #105621, #155330, #222871, #129108 ) ) ;
#120911=AXIS2_PLACEMENT_3D ( 'NONE', #46882, #163017, #220417 ) ;
#120913=EDGE_CURVE ( 'NONE', #194507, #240371, #125853, .T. ) ;
#120921=CARTESIAN_POINT ( 'NONE',  ( 18.59117750673696179, 65.66751761918648356, -63.92826094061123143 ) ) ;
#120946=LINE ( 'NONE', #183464, #101466 ) ;
#120999=DIRECTION ( 'NONE',  ( 0.000000000000000000, 6.982962677686266711E-15, -1.000000000000000000 ) ) ;
#121013=CARTESIAN_POINT ( 'NONE',  ( -20.97625342178413277, 64.39999999919203333, -96.09490425472216657 ) ) ;
#121062=CIRCLE ( 'NONE', #162738, 0.1000000000000028644 ) ;
#121066=VERTEX_POINT ( 'NONE', #108983 ) ;
#121070=ORIENTED_EDGE ( 'NONE', *, *, #235639, .F. ) ;
#121108=DIRECTION ( 'NONE',  ( 1.000000000000000000, 0.000000000000000000, 0.000000000000000000 ) ) ;
#121130=CARTESIAN_POINT ( 'NONE',  ( -20.64999999999999858, 76.00000000001186606, -90.14810748452431710 ) ) ;
#121139=EDGE_CURVE ( 'NONE', #125280, #225321, #193675, .T. ) ;
#121172=CIRCLE ( 'NONE', #112747, 0.09999999999999939493 ) ;
#121189=CARTESIAN_POINT ( 'NONE',  ( 21.05000000000000071, 87.29603075034701476, -72.57100664418810254 ) ) ;
#121215=ADVANCED_FACE ( 'NONE', ( #94556 ), #230225, .T. ) ;
#121218=CARTESIAN_POINT ( 'NONE',  ( -18.59999999999999787, 77.73670573947921980, -58.00568489690056850 ) ) ;
#121221=CARTESIAN_POINT ( 'NONE',  ( -20.00857864376270001, 66.75000000001185185, -90.67310748452436542 ) ) ;
#121223=CARTESIAN_POINT ( 'NONE',  ( 21.05000000000000071, 87.48912529308779540, -72.62310748452422615 ) ) ;
#121237=EDGE_CURVE ( 'NONE', #167682, #174804, #17898, .T. ) ;
#121241=VERTEX_POINT ( 'NONE', #197507 ) ;
#121242=CARTESIAN_POINT ( 'NONE',  ( -22.45437739390953169, 76.00000000001203659, -114.6726782961207505 ) ) ;
#121270=ORIENTED_EDGE ( 'NONE', *, *, #247845, .T. ) ;
#121272=CARTESIAN_POINT ( 'NONE',  ( 18.49999999999996803, 68.92903212821283887, -65.77654326265606244 ) ) ;
#121291=DIRECTION ( 'NONE',  ( 0.000000000000000000, -0.4999999999999689138, 0.8660254037844565822 ) ) ;
#121308=VECTOR ( 'NONE', #86602, 1000.000000000000000 ) ;
#121330=DIRECTION ( 'NONE',  ( 0.000000000000000000, 0.000000000000000000, 1.000000000000000000 ) ) ;
#121331=CARTESIAN_POINT ( 'NONE',  ( 20.94999999999999929, 76.00000000001185185, -90.04810748452430857 ) ) ;
#121342=CARTESIAN_POINT ( 'NONE',  ( 18.59999999999999076, 69.55000000001187743, -93.00608031408432907 ) ) ;
#121427=ORIENTED_EDGE ( 'NONE', *, *, #172148, .F. ) ;
#121466=CARTESIAN_POINT ( 'NONE',  ( -23.25000000000000000, 87.48912529308779540, -72.62310748452422615 ) ) ;
#121468=AXIS2_PLACEMENT_3D ( 'NONE', #250137, #211012, #111923 ) ;
#121472=CARTESIAN_POINT ( 'NONE',  ( -23.15000000000000213, 71.65000000001180069, -81.77310748452433131 ) ) ;
#121488=VECTOR ( 'NONE', #51177, 1000.000000000000000 ) ;
#121502=DIRECTION ( 'NONE',  ( 1.000000000000000000, -3.265361837132813093E-16, -2.280189983783949500E-30 ) ) ;
#121527=ORIENTED_EDGE ( 'NONE', *, *, #7938, .T. ) ;
#121601=CARTESIAN_POINT ( 'NONE',  ( 20.94999999999999574, 74.75000000001189449, -95.12310748452432563 ) ) ;
#121612=EDGE_CURVE ( 'NONE', #188436, #120661, #159392, .T. ) ;
#121620=FACE_OUTER_BOUND ( 'NONE', #31568, .T. ) ;
#121636=CARTESIAN_POINT ( 'NONE',  ( 21.09610168723072832, 75.96641049312049176, -109.4020631997490796 ) ) ;
#121644=ORIENTED_EDGE ( 'NONE', *, *, #1853, .T. ) ;
#121655=CIRCLE ( 'NONE', #163169, 0.1000000000000028644 ) ;
#121670=AXIS2_PLACEMENT_3D ( 'NONE', #86858, #169030, #208140 ) ;
#121694=ORIENTED_EDGE ( 'NONE', *, *, #143138, .F. ) ;
#121706=VERTEX_POINT ( 'NONE', #180586 ) ;
#121782=AXIS2_PLACEMENT_3D ( 'NONE', #110276, #34627, #11191 ) ;
#121803=ORIENTED_EDGE ( 'NONE', *, *, #108019, .T. ) ;
#121809=DIRECTION ( 'NONE',  ( 0.000000000000000000, 6.982962677686266711E-15, -1.000000000000000000 ) ) ;
#121816=CARTESIAN_POINT ( 'NONE',  ( -21.76363531954647357, 75.90099812571254745, -110.0360440323960631 ) ) ;
#121817=ORIENTED_EDGE ( 'NONE', *, *, #3911, .T. ) ;
#121828=CIRCLE ( 'NONE', #105191, 11.64999999999999325 ) ;
#121873=DIRECTION ( 'NONE',  ( 0.000000000000000000, -6.982962677686266711E-15, 1.000000000000000000 ) ) ;
#121892=LINE ( 'NONE', #99713, #8384 ) ;
#121903=CARTESIAN_POINT ( 'NONE',  ( -20.54999999999999716, 73.50000000001180922, -82.74772940728642823 ) ) ;
#121920=ORIENTED_EDGE ( 'NONE', *, *, #111377, .F. ) ;
#121976=AXIS2_PLACEMENT_3D ( 'NONE', #58125, #56833, #235495 ) ;
#121982=CARTESIAN_POINT ( 'NONE',  ( -21.05000000000000071, 76.08579911628599746, -109.4370863660127497 ) ) ;
#122018=EDGE_CURVE ( 'NONE', #85340, #14237, #209127, .T. ) ;
#122029=ORIENTED_EDGE ( 'NONE', *, *, #137616, .T. ) ;
#122056=CIRCLE ( 'NONE', #234285, 0.09999999999999939493 ) ;
#122057=CARTESIAN_POINT ( 'NONE',  ( 18.49999999999999289, 64.35000000001171827, -69.52310748452438816 ) ) ;
#122074=AXIS2_PLACEMENT_3D ( 'NONE', #95955, #116821, #254974 ) ;
#122144=CARTESIAN_POINT ( 'NONE',  ( 21.05000000000000071, 74.83729825007388570, -94.92310748452432279 ) ) ;
#122167=EDGE_CURVE ( 'NONE', #79511, #70872, #244092, .T. ) ;
#122179=EDGE_LOOP ( 'NONE', ( #47274, #196487, #240180, #26133 ) ) ;
#122184=CARTESIAN_POINT ( 'NONE',  ( 18.51697539158856642, 65.68434038414336840, -63.98668807260654745 ) ) ;
#122190=TOROIDAL_SURFACE ( 'NONE', #159786, 11.70000000000000107, 0.1000000000000000056 ) ;
#122201=DIRECTION ( 'NONE',  ( 1.000000000000000000, 0.000000000000000000, 0.000000000000000000 ) ) ;
#122210=ADVANCED_FACE ( 'NONE', ( #121620 ), #208832, .F. ) ;
#122239=CIRCLE ( 'NONE', #205410, 0.1000000000000028644 ) ;
#122243=CIRCLE ( 'NONE', #9801, 2.000000000000001776 ) ;
#122252=CARTESIAN_POINT ( 'NONE',  ( 20.85000000000000142, 76.00000000001170974, -69.52310748452431710 ) ) ;
#122301=DIRECTION ( 'NONE',  ( 1.000000000000000000, 0.000000000000000000, -0.000000000000000000 ) ) ;
#122305=ORIENTED_EDGE ( 'NONE', *, *, #201297, .F. ) ;
#122324=DIRECTION ( 'NONE',  ( 1.000000000000000000, 0.000000000000000000, 0.000000000000000000 ) ) ;
#122355=ORIENTED_EDGE ( 'NONE', *, *, #46765, .T. ) ;
#122356=ORIENTED_EDGE ( 'NONE', *, *, #208734, .F. ) ;
#122373=CONICAL_SURFACE ( 'NONE', #209677, 4.299999999999956302, 0.7853981633974466137 ) ;
#122380=ORIENTED_EDGE ( 'NONE', *, *, #157507, .F. ) ;
#122411=CARTESIAN_POINT ( 'NONE',  ( 18.59999999999999787, 77.83534155023627932, -91.46795619196132066 ) ) ;
#122423=DIRECTION ( 'NONE',  ( 1.000000000000000000, -1.836970198721029934E-16, -1.601412966608202925E-30 ) ) ;
#122482=EDGE_LOOP ( 'NONE', ( #22964, #108099, #159908, #36324 ) ) ;
#122494=EDGE_LOOP ( 'NONE', ( #190929, #231045, #204310, #227791, #144926, #36122, #232256, #142837, #157084, #44130 ) ) ;
#122507=DIRECTION ( 'NONE',  ( 1.000000000000000000, -2.952720810173289112E-16, -2.061873921506763405E-30 ) ) ;
#122528=ORIENTED_EDGE ( 'NONE', *, *, #101414, .T. ) ;
#122548=FACE_OUTER_BOUND ( 'NONE', #192892, .T. ) ;
#122556=ORIENTED_EDGE ( 'NONE', *, *, #160420, .F. ) ;
#122608=LINE ( 'NONE', #242531, #196910 ) ;
#122618=ADVANCED_FACE ( 'NONE', ( #220394 ), #15132, .F. ) ;
#122622=DIRECTION ( 'NONE',  ( -1.000000000000000000, 2.952720810173289112E-16, 2.061873921506763405E-30 ) ) ;
#122624=CIRCLE ( 'NONE', #147547, 0.1000000000000028644 ) ;
#122634=AXIS2_PLACEMENT_3D ( 'NONE', #174139, #234057, #66984 ) ;
#122654=ORIENTED_EDGE ( 'NONE', *, *, #89119, .T. ) ;
#122660=ORIENTED_EDGE ( 'NONE', *, *, #51312, .T. ) ;
#122690=ORIENTED_EDGE ( 'NONE', *, *, #204784, .F. ) ;
#122704=ORIENTED_EDGE ( 'NONE', *, *, #71366, .F. ) ;
#122711=DIRECTION ( 'NONE',  ( 0.000000000000000000, 0.9893560106964510714, -0.1455152366551481502 ) ) ;
#122725=ORIENTED_EDGE ( 'NONE', *, *, #198067, .F. ) ;
#122732=CARTESIAN_POINT ( 'NONE',  ( 21.05000000000000071, 76.10000000001198828, -109.5637644362255543 ) ) ;
#122733=DIRECTION ( 'NONE',  ( -1.836970198721029934E-16, -1.000000000000000000, -6.982962677686266711E-15 ) ) ;
#122734=CARTESIAN_POINT ( 'NONE',  ( -18.59999999999999787, 64.35000000001190301, -96.00830171387039513 ) ) ;
#122746=EDGE_LOOP ( 'NONE', ( #179364, #211112, #60050, #28714 ) ) ;
#122767=EDGE_CURVE ( 'NONE', #167954, #13968, #201788, .T. ) ;
#122795=VECTOR ( 'NONE', #163263, 1000.000000000000000 ) ;
#122807=EDGE_CURVE ( 'NONE', #120433, #140343, #197924, .T. ) ;
#122826=CARTESIAN_POINT ( 'NONE',  ( 21.46681500597710013, 76.00000000001200817, -109.8806186439539516 ) ) ;
#122832=EDGE_CURVE ( 'NONE', #28459, #141595, #54570, .T. ) ;
#122930=ORIENTED_EDGE ( 'NONE', *, *, #109358, .T. ) ;
#122937=SPHERICAL_SURFACE ( 'NONE', #50478, 0.1000000000000000056 ) ;
#122945=ORIENTED_EDGE ( 'NONE', *, *, #107567, .T. ) ;
#122946=CIRCLE ( 'NONE', #143770, 0.09999999999999938105 ) ;
#122956=ADVANCED_FACE ( 'NONE', ( #128359 ), #125770, .T. ) ;
#122958=DIRECTION ( 'NONE',  ( 1.000000000000000000, -2.952720810173289112E-16, -2.061873921506763405E-30 ) ) ;
#122976=ORIENTED_EDGE ( 'NONE', *, *, #146611, .F. ) ;
#122994=ADVANCED_FACE ( 'NONE', ( #147925 ), #48806, .T. ) ;
#123040=CARTESIAN_POINT ( 'NONE',  ( -22.50000000000000000, 76.00000000001195133, -103.0231074845243171 ) ) ;
#123049=( NAMED_UNIT ( * ) PLANE_ANGLE_UNIT ( ) SI_UNIT ( $, .RADIAN. ) );
#123075=PLANE ( 'NONE',  #217710 ) ;
#123096=CARTESIAN_POINT ( 'NONE',  ( -21.53551880898957904, 75.90103026544032616, -109.8079052459406597 ) ) ;
#123108=ADVANCED_FACE ( 'NONE', ( #9679 ), #133484, .T. ) ;
#123109=CARTESIAN_POINT ( 'NONE',  ( 21.09546886439534674, 67.12144688699692097, -90.78601363396897739 ) ) ;
#123125=CARTESIAN_POINT ( 'NONE',  ( -18.59999999999999787, 77.25000000001165290, -61.72262673010922640 ) ) ;
#123142=ADVANCED_FACE ( 'NONE', ( #254667 ), #147249, .T. ) ;
#123149=CARTESIAN_POINT ( 'NONE',  ( -22.57320508075687115, 64.25000000001195133, -103.0231074845244024 ) ) ;
#123180=VERTEX_POINT ( 'NONE', #76071 ) ;
#123200=FACE_OUTER_BOUND ( 'NONE', #146488, .T. ) ;
#123208=DIRECTION ( 'NONE',  ( 1.000000000000000000, 0.000000000000000000, 0.000000000000000000 ) ) ;
#123213=ADVANCED_FACE ( 'NONE', ( #40838 ), #61595, .F. ) ;
#123215=DIRECTION ( 'NONE',  ( 1.000000000000000000, 0.000000000000000000, 0.000000000000000000 ) ) ;
#123236=EDGE_CURVE ( 'NONE', #147354, #169820, #80579, .T. ) ;
#123240=ORIENTED_EDGE ( 'NONE', *, *, #57217, .F. ) ;
#123254=VECTOR ( 'NONE', #153837, 1000.000000000000000 ) ;
#123263=CARTESIAN_POINT ( 'NONE',  ( -21.05000000000000426, 76.01771943332086323, -109.4641921729955243 ) ) ;
#123267=ADVANCED_FACE ( 'NONE', ( #104593 ), #42111, .T. ) ;
#123307=FACE_OUTER_BOUND ( 'NONE', #203360, .T. ) ;
#123323=CARTESIAN_POINT ( 'NONE',  ( 18.59999999999999076, 70.05000000001193428, -92.71740517948948934 ) ) ;
#123366=DIRECTION ( 'NONE',  ( -0.7071067811865127117, -0.7071067811865821007, 0.000000000000000000 ) ) ;
#123385=DIRECTION ( 'NONE',  ( 0.000000000000000000, 0.000000000000000000, -1.000000000000000000 ) ) ;
#123388=CARTESIAN_POINT ( 'NONE',  ( 21.11927991906888025, 69.55150688152053817, -103.0321911639982488 ) ) ;
#123426=CARTESIAN_POINT ( 'NONE',  ( 21.05000000000000071, 64.35000000001186038, -90.87310748452438247 ) ) ;
#123433=CARTESIAN_POINT ( 'NONE',  ( 21.14999999999999503, 76.10000000001203091, -114.6726782920691079 ) ) ;
#123458=LINE ( 'NONE', #24377, #4006 ) ;
#123503=AXIS2_PLACEMENT_3D ( 'NONE', #236626, #43582, #180529 ) ;
#123506=CYLINDRICAL_SURFACE ( 'NONE', #226104, 0.8750000000000007772 ) ;
#123619=DIRECTION ( 'NONE',  ( -0.000000000000000000, 1.000000000000000000, 6.982962677686266711E-15 ) ) ;
#123625=CARTESIAN_POINT ( 'NONE',  ( -20.87155475150660777, 64.25000000001175238, -76.42752095536712886 ) ) ;
#123642=EDGE_LOOP ( 'NONE', ( #122654, #245785, #80181, #179406 ) ) ;
#123658=VERTEX_POINT ( 'NONE', #26091 ) ;
#123690=VERTEX_POINT ( 'NONE', #44372 ) ;
#123705=VERTEX_POINT ( 'NONE', #104304 ) ;
#123725=EDGE_CURVE ( 'NONE', #75286, #57574, #142167, .T. ) ;
#123753=ORIENTED_EDGE ( 'NONE', *, *, #8605, .F. ) ;
#123788=ORIENTED_EDGE ( 'NONE', *, *, #226660, .T. ) ;
#123838=EDGE_CURVE ( 'NONE', #138100, #21468, #72624, .T. ) ;
#123839=ORIENTED_EDGE ( 'NONE', *, *, #50197, .F. ) ;
#123859=CARTESIAN_POINT ( 'NONE',  ( -22.47071067811865319, 68.27992525551387359, -103.1221999392269595 ) ) ;
#123867=AXIS2_PLACEMENT_3D ( 'NONE', #10497, #112177, #13077 ) ;
#123874=DIRECTION ( 'NONE',  ( 1.000000000000000000, 0.000000000000000000, 0.000000000000000000 ) ) ;
#123892=EDGE_CURVE ( 'NONE', #77493, #81484, #101792, .T. ) ;
#123896=CYLINDRICAL_SURFACE ( 'NONE', #106187, 0.5000000000000004441 ) ;
#123936=DIRECTION ( 'NONE',  ( 0.000000000000000000, -7.056502275159894776E-15, 1.000000000000000000 ) ) ;
#123951=DIRECTION ( 'NONE',  ( 1.000000000000000000, 0.000000000000000000, 0.000000000000000000 ) ) ;
#123958=ORIENTED_EDGE ( 'NONE', *, *, #137688, .T. ) ;
#123990=LINE ( 'NONE', #242628, #244432 ) ;
#124015=DIRECTION ( 'NONE',  ( 1.000000000000000000, 0.000000000000000000, 0.000000000000000000 ) ) ;
#124037=ADVANCED_FACE ( 'NONE', ( #180999 ), #20647, .T. ) ;
#124049=ADVANCED_FACE ( 'NONE', ( #222657, #140561 ), #44043, .T. ) ;
#124071=ORIENTED_EDGE ( 'NONE', *, *, #157656, .F. ) ;
#124091=DIRECTION ( 'NONE',  ( 0.000000000000000000, 0.000000000000000000, -1.000000000000000000 ) ) ;
#124098=CARTESIAN_POINT ( 'NONE',  ( 18.59999999999999432, 77.26178616857691850, -94.93660852097882241 ) ) ;
#124107=CARTESIAN_POINT ( 'NONE',  ( 22.59999999999999432, 64.25012875563544412, -103.0885370755380706 ) ) ;
#124166=EDGE_CURVE ( 'NONE', #76960, #221695, #239383, .T. ) ;
#124175=ADVANCED_FACE ( 'NONE', ( #47873 ), #235269, .F. ) ;
#124191=DIRECTION ( 'NONE',  ( 1.000000000000000000, -2.952720810173289112E-16, -2.061873921506763405E-30 ) ) ;
#124204=AXIS2_PLACEMENT_3D ( 'NONE', #181786, #162241, #226005 ) ;
#124210=ORIENTED_EDGE ( 'NONE', *, *, #126003, .T. ) ;
#124242=VECTOR ( 'NONE', #157645, 1000.000000000000000 ) ;
#124274=ORIENTED_EDGE ( 'NONE', *, *, #193888, .T. ) ;
#124279=CIRCLE ( 'NONE', #32730, 0.09999999999999939493 ) ;
#124315=DIRECTION ( 'NONE',  ( 0.000000000000000000, 0.9915357197604804940, -0.1298341882520397950 ) ) ;
#124327=CARTESIAN_POINT ( 'NONE',  ( -18.50000000000000000, 76.00000000001195133, -103.0231074845243171 ) ) ;
#124332=SURFACE_STYLE_USAGE ( .BOTH. , #61781 ) ;
#124353=AXIS2_PLACEMENT_3D ( 'NONE', #38062, #117573, #100543 ) ;
#124356=FACE_OUTER_BOUND ( 'NONE', #217172, .T. ) ;
#124357=CIRCLE ( 'NONE', #149315, 0.1000000000000028644 ) ;
#124358=AXIS2_PLACEMENT_3D ( 'NONE', #46989, #88678, #229512 ) ;
#124396=FACE_OUTER_BOUND ( 'NONE', #122494, .T. ) ;
#124448=EDGE_LOOP ( 'NONE', ( #52354, #111956, #125747, #132101 ) ) ;
#124474=ORIENTED_EDGE ( 'NONE', *, *, #169635, .F. ) ;
#124477=EDGE_CURVE ( 'NONE', #18466, #102678, #114483, .T. ) ;
#124480=AXIS2_PLACEMENT_3D ( 'NONE', #221777, #122733, #243928 ) ;
#124482=AXIS2_PLACEMENT_3D ( 'NONE', #210572, #31959, #247111 ) ;
#124494=CARTESIAN_POINT ( 'NONE',  ( -20.64999999999999858, 74.00000000001180922, -82.74772940728641402 ) ) ;
#124510=CARTESIAN_POINT ( 'NONE',  ( 20.94999999999999929, 87.48912529308779540, -72.62310748452422615 ) ) ;
#124513=CIRCLE ( 'NONE', #241047, 0.1000000000000052097 ) ;
#124542=EDGE_CURVE ( 'NONE', #74828, #64641, #185404, .T. ) ;
#124559=CARTESIAN_POINT ( 'NONE',  ( -21.11833042828134666, 75.99289949095258123, -109.4687521783795319 ) ) ;
#124607=EDGE_LOOP ( 'NONE', ( #18446, #195607, #109203, #37751 ) ) ;
#124615=CARTESIAN_POINT ( 'NONE',  ( -21.08621493067320429, 75.94380516053594476, -109.3724017756962468 ) ) ;
#124624=CARTESIAN_POINT ( 'NONE',  ( -18.59999999999999787, 77.16412189325286874, -61.60825939895269698 ) ) ;
#124645=LINE ( 'NONE', #2105, #10160 ) ;
#124653=EDGE_CURVE ( 'NONE', #84368, #4548, #64769, .T. ) ;
#124683=CARTESIAN_POINT ( 'NONE',  ( 18.50000000000000000, 85.50000000001202238, -114.7731074845242460 ) ) ;
#124691=EDGE_CURVE ( 'NONE', #70872, #154309, #23106, .T. ) ;
#124715=ADVANCED_FACE ( 'NONE', ( #72299 ), #112700, .T. ) ;
#124767=CARTESIAN_POINT ( 'NONE',  ( -21.05000000000000071, 76.00000000001179501, -81.22310748452430573 ) ) ;
#124810=DIRECTION ( 'NONE',  ( 0.000000000000000000, -0.9908441862701605762, -0.1350103645451835310 ) ) ;
#124813=AXIS2_PLACEMENT_3D ( 'NONE', #12517, #15072, #153332 ) ;
#124823=DIRECTION ( 'NONE',  ( -1.000000000000000000, -0.000000000000000000, -0.000000000000000000 ) ) ;
#124841=CARTESIAN_POINT ( 'NONE',  ( -21.03571358705830718, 64.25000000001189449, -96.19800066246598647 ) ) ;
#124877=ORIENTED_EDGE ( 'NONE', *, *, #236007, .F. ) ;
#124919=DIRECTION ( 'NONE',  ( 0.000000000000000000, 0.000000000000000000, 1.000000000000000000 ) ) ;
#124923=EDGE_LOOP ( 'NONE', ( #144723, #62239, #229446, #86562 ) ) ;
#124944=VECTOR ( 'NONE', #189015, 1000.000000000000000 ) ;
#124952=ORIENTED_EDGE ( 'NONE', *, *, #213233, .F. ) ;
#124977=DIRECTION ( 'NONE',  ( -1.000000000000000000, -0.000000000000000000, -0.000000000000000000 ) ) ;
#124985=VERTEX_POINT ( 'NONE', #172083 ) ;
#124997=DIRECTION ( 'NONE',  ( -0.000000000000000000, 6.982962677686266711E-15, -1.000000000000000000 ) ) ;
#125020=CARTESIAN_POINT ( 'NONE',  ( -20.85000000000000142, 68.97833521811159585, -65.88954208262707368 ) ) ;
#125045=DIRECTION ( 'NONE',  ( -1.000000000000000000, -0.000000000000000000, -0.000000000000000000 ) ) ;
#125060=ORIENTED_EDGE ( 'NONE', *, *, #29642, .F. ) ;
#125072=CARTESIAN_POINT ( 'NONE',  ( 23.24999999999999645, 76.00000000001195133, -103.0231074845243171 ) ) ;
#125103=CIRCLE ( 'NONE', #216667, 0.2000000000000057288 ) ;
#125104=ORIENTED_EDGE ( 'NONE', *, *, #214066, .F. ) ;
#125117=DIRECTION ( 'NONE',  ( 0.000000000000000000, 0.4930308989875575865, 0.8700118002898125091 ) ) ;
#125119=EDGE_LOOP ( 'NONE', ( #38031, #247457, #162374, #49300 ) ) ;
#125153=SPHERICAL_SURFACE ( 'NONE', #26737, 0.1000000000000000056 ) ;
#125183=CARTESIAN_POINT ( 'NONE',  ( 18.59999999999999076, 69.45000000001181206, -81.77310748452434552 ) ) ;
#125194=CIRCLE ( 'NONE', #12789, 0.1000000000000028644 ) ;
#125212=CARTESIAN_POINT ( 'NONE',  ( 21.05000000000000426, 69.58617371119899531, -102.9373665474909672 ) ) ;
#125273=CARTESIAN_POINT ( 'NONE',  ( -21.05000000000000071, 87.65000000001172964, -72.42310748452422331 ) ) ;
#125280=VERTEX_POINT ( 'NONE', #176377 ) ;
#125281=EDGE_LOOP ( 'NONE', ( #126742, #148351, #68536, #95576 ) ) ;
#125292=AXIS2_PLACEMENT_3D ( 'NONE', #73953, #128768, #50474 ) ;
#125299=DIRECTION ( 'NONE',  ( 1.000000000000000000, -3.265361837132813093E-16, -2.280189983783949500E-30 ) ) ;
#125308=ADVANCED_FACE ( 'NONE', ( #1551 ), #41999, .T. ) ;
#125330=DIRECTION ( 'NONE',  ( -3.265361837132813093E-16, -1.000000000000000000, -6.982962677686266711E-15 ) ) ;
#125345=ORIENTED_EDGE ( 'NONE', *, *, #134389, .F. ) ;
#125350=CARTESIAN_POINT ( 'NONE',  ( -21.05000000000000071, 70.10000000001177511, -79.74220724918070857 ) ) ;
#125379=ORIENTED_EDGE ( 'NONE', *, *, #15101, .T. ) ;
#125402=VERTEX_POINT ( 'NONE', #124098 ) ;
#125415=CARTESIAN_POINT ( 'NONE',  ( 20.94999999999999929, 76.00000000001195133, -103.0231074845243171 ) ) ;
#125423=ORIENTED_EDGE ( 'NONE', *, *, #100693, .T. ) ;
#125450=CARTESIAN_POINT ( 'NONE',  ( 21.05315837410544688, 64.25000000001173817, -76.36475148275641800 ) ) ;
#125452=CIRCLE ( 'NONE', #141999, 0.09999999999999489853 ) ;
#125466=DIRECTION ( 'NONE',  ( 0.000000000000000000, -1.000000000000000000, 0.000000000000000000 ) ) ;
#125480=DIRECTION ( 'NONE',  ( -1.000000000000000000, -0.000000000000000000, -0.000000000000000000 ) ) ;
#125495=EDGE_LOOP ( 'NONE', ( #228333, #95118, #204645, #156889 ) ) ;
#125508=EDGE_CURVE ( 'NONE', #224268, #223315, #48384, .T. ) ;
#125518=EDGE_LOOP ( 'NONE', ( #132910, #114149, #36902, #107126 ) ) ;
#125520=ORIENTED_EDGE ( 'NONE', *, *, #35791, .T. ) ;
#125528=CIRCLE ( 'NONE', #246146, 7.720710678118678061 ) ;
#125531=VERTEX_POINT ( 'NONE', #34010 ) ;
#125583=DIRECTION ( 'NONE',  ( 1.000000000000000000, -2.952720810173289112E-16, -2.061873921506763405E-30 ) ) ;
#125604=DIRECTION ( 'NONE',  ( 0.000000000000000000, -2.609498562153145121E-14, 1.000000000000000000 ) ) ;
#125621=EDGE_CURVE ( 'NONE', #77073, #20758, #185948, .T. ) ;
#125629=CARTESIAN_POINT ( 'NONE',  ( 18.59999999999999787, 87.75000000001179501, -81.67310748452422331 ) ) ;
#125644=VERTEX_POINT ( 'NONE', #138181 ) ;
#125652=CARTESIAN_POINT ( 'NONE',  ( 21.14999999999999503, 64.35000000001194564, -103.0231074845244024 ) ) ;
#125661=EDGE_CURVE ( 'NONE', #120433, #223762, #256618, .T. ) ;
#125697=FACE_OUTER_BOUND ( 'NONE', #107359, .T. ) ;
#125736=ADVANCED_FACE ( 'NONE', ( #29518 ), #102901, .T. ) ;
#125738=VECTOR ( 'NONE', #165145, 1000.000000000000000 ) ;
#125747=ORIENTED_EDGE ( 'NONE', *, *, #175227, .F. ) ;
#125763=CIRCLE ( 'NONE', #13353, 0.9750000000000036415 ) ;
#125770=CYLINDRICAL_SURFACE ( 'NONE', #72246, 0.09999999999999939493 ) ;
#125771=CIRCLE ( 'NONE', #59109, 0.5000000000000004441 ) ;
#125777=VECTOR ( 'NONE', #149522, 1000.000000000000000 ) ;
#125804=EDGE_CURVE ( 'NONE', #170796, #8311, #188552, .T. ) ;
#125814=DIRECTION ( 'NONE',  ( 0.000000000000000000, 0.7397360091702792628, -0.6728971962616790981 ) ) ;
#125820=CARTESIAN_POINT ( 'NONE',  ( -21.13422380239058995, 76.00000000001200817, -109.5164339993299620 ) ) ;
#125828=ORIENTED_EDGE ( 'NONE', *, *, #56155, .T. ) ;
#125829=DIRECTION ( 'NONE',  ( -1.000000000000000000, -7.304098846218134667E-16, -5.311601492717084346E-30 ) ) ;
#125838=CYLINDRICAL_SURFACE ( 'NONE', #165753, 0.09999999999999939493 ) ;
#125846=CARTESIAN_POINT ( 'NONE',  ( -18.50000000000000000, 64.35000000001187459, -90.87310748452438247 ) ) ;
#125853=CIRCLE ( 'NONE', #105153, 7.900000000000003908 ) ;
#125873=EDGE_LOOP ( 'NONE', ( #94794, #21139, #248048, #44299 ) ) ;
#125904=ORIENTED_EDGE ( 'NONE', *, *, #184144, .T. ) ;
#125963=DIRECTION ( 'NONE',  ( -1.000000000000000000, -0.000000000000000000, -0.000000000000000000 ) ) ;
#125967=VECTOR ( 'NONE', #228904, 1000.000000000000000 ) ;
#125989=CYLINDRICAL_SURFACE ( 'NONE', #257295, 0.1000000000000028644 ) ;
#125995=CARTESIAN_POINT ( 'NONE',  ( 23.14999999999999858, 76.00000000001170974, -69.52310748452431710 ) ) ;
#126003=EDGE_CURVE ( 'NONE', #110160, #19541, #202697, .T. ) ;
#126082=EDGE_CURVE ( 'NONE', #78455, #47226, #177997, .T. ) ;
#126124=DIRECTION ( 'NONE',  ( 1.000000000000000000, 0.000000000000000000, 0.000000000000000000 ) ) ;
#126167=CARTESIAN_POINT ( 'NONE',  ( -20.99780126800921565, 64.39461131213516865, -76.43575491281889356 ) ) ;
#126224=ORIENTED_EDGE ( 'NONE', *, *, #171401, .T. ) ;
#126253=TOROIDAL_SURFACE ( 'NONE', #1343, 11.70000000000000462, 0.1000000000000000056 ) ;
#126295=CARTESIAN_POINT ( 'NONE',  ( -18.59999999999999787, 77.86671491006917734, -91.27043223824227880 ) ) ;
#126306=AXIS2_PLACEMENT_3D ( 'NONE', #189085, #213780, #92535 ) ;
#126311=AXIS2_PLACEMENT_3D ( 'NONE', #44229, #99023, #238560 ) ;
#126326=CARTESIAN_POINT ( 'NONE',  ( -21.05000000000000071, 87.48912529308798014, -100.1231074845242262 ) ) ;
#126369=ORIENTED_EDGE ( 'NONE', *, *, #150197, .T. ) ;
#126370=CARTESIAN_POINT ( 'NONE',  ( -20.85000000000000142, 77.83585931145526615, -58.01866831572577610 ) ) ;
#126422=DIRECTION ( 'NONE',  ( 1.000000000000000000, 0.000000000000000000, 0.000000000000000000 ) ) ;
#126452=AXIS2_PLACEMENT_3D ( 'NONE', #40970, #219563, #61790 ) ;
#126456=EDGE_CURVE ( 'NONE', #151773, #110239, #147540, .T. ) ;
#126482=CARTESIAN_POINT ( 'NONE',  ( -18.59999999999999787, 76.00000000001195133, -103.0231074845243171 ) ) ;
#126483=VECTOR ( 'NONE', #145928, 1000.000000000000000 ) ;
#126484=DIRECTION ( 'NONE',  ( 0.000000000000000000, -0.9887567792719351711, 0.1495327102803594987 ) ) ;
#126539=EDGE_CURVE ( 'NONE', #182622, #196101, #150129, .T. ) ;
#126586=CARTESIAN_POINT ( 'NONE',  ( 18.59999999999999432, 74.26374286841446803, -91.45445515550682103 ) ) ;
#126609=VECTOR ( 'NONE', #12793, 1000.000000000000000 ) ;
#126610=CARTESIAN_POINT ( 'NONE',  ( -21.05000000000000071, 62.00000000001175238, -74.95020001490686923 ) ) ;
#126643=CARTESIAN_POINT ( 'NONE',  ( -20.94999999999999929, 76.25610579210417939, -103.0580039261966050 ) ) ;
#126646=EDGE_CURVE ( 'NONE', #154058, #77073, #238630, .T. ) ;
#126648=DIRECTION ( 'NONE',  ( 0.000000000000000000, -1.000000000000000000, 0.000000000000000000 ) ) ;
#126652=DIRECTION ( 'NONE',  ( 1.000000000000000000, -3.265361837132813093E-16, -2.280189983783949500E-30 ) ) ;
#126672=ORIENTED_EDGE ( 'NONE', *, *, #202215, .F. ) ;
#126686=DIRECTION ( 'NONE',  ( -1.000000000000000000, 0.000000000000000000, -0.000000000000000000 ) ) ;
#126719=ORIENTED_EDGE ( 'NONE', *, *, #96633, .T. ) ;
#126724=CARTESIAN_POINT ( 'NONE',  ( 20.85000000000000142, 64.25000000001175238, -76.30697314750248950 ) ) ;
#126741=SPHERICAL_SURFACE ( 'NONE', #21206, 0.1000000000000000056 ) ;
#126742=ORIENTED_EDGE ( 'NONE', *, *, #111204, .T. ) ;
#126746=EDGE_CURVE ( 'NONE', #114547, #140343, #119896, .T. ) ;
#126752=DIRECTION ( 'NONE',  ( 0.000000000000000000, -1.000000000000000000, -6.982962677686265922E-15 ) ) ;
#126757=EDGE_CURVE ( 'NONE', #5184, #127256, #36508, .T. ) ;
#126760=CARTESIAN_POINT ( 'NONE',  ( -2.995603634470891112E-16, 87.75000000001178080, -78.27310748452423184 ) ) ;
#126766=AXIS2_PLACEMENT_3D ( 'NONE', #6184, #182280, #220117 ) ;
#126784=EDGE_LOOP ( 'NONE', ( #213672, #208532, #212937, #257583 ) ) ;
#126785=CARTESIAN_POINT ( 'NONE',  ( 20.94999999999999574, 74.14897176987101091, -91.36919421510182815 ) ) ;
#126807=EDGE_CURVE ( 'NONE', #227300, #187280, #74106, .T. ) ;
#126811=CARTESIAN_POINT ( 'NONE',  ( 21.05000000000000071, 69.35000000001186038, -90.87310748452435405 ) ) ;
#126854=ADVANCED_FACE ( 'NONE', ( #122548 ), #23467, .F. ) ;
#126862=ORIENTED_EDGE ( 'NONE', *, *, #3321, .T. ) ;
#126928=VERTEX_POINT ( 'NONE', #128959 ) ;
#126935=DIRECTION ( 'NONE',  ( -1.000000000000000000, 0.000000000000000000, 0.000000000000000000 ) ) ;
#126985=CYLINDRICAL_SURFACE ( 'NONE', #179144, 4.000000000000003553 ) ;
#127004=ORIENTED_EDGE ( 'NONE', *, *, #56616, .F. ) ;
#127008=DIRECTION ( 'NONE',  ( 0.000000000000000000, -0.2605042016806740079, 0.9654727137038698892 ) ) ;
#127017=CARTESIAN_POINT ( 'NONE',  ( 21.05000000000000071, 76.00000000001185185, -90.04810748452430857 ) ) ;
#127024=LINE ( 'NONE', #90452, #229489 ) ;
#127057=CARTESIAN_POINT ( 'NONE',  ( -22.42253884134832020, 75.99806764887672728, -114.6727131818727372 ) ) ;
#127060=AXIS2_PLACEMENT_3D ( 'NONE', #62635, #163032, #65186 ) ;
#127062=VECTOR ( 'NONE', #96241, 1000.000000000000000 ) ;
#127070=ORIENTED_EDGE ( 'NONE', *, *, #19474, .T. ) ;
#127076=AXIS2_PLACEMENT_3D ( 'NONE', #143998, #220967, #24093 ) ;
#127086=DIRECTION ( 'NONE',  ( 0.7071067811865474617, -0.7071067811865474617, -4.937700262164531476E-15 ) ) ;
#127088=VERTEX_POINT ( 'NONE', #119666 ) ;
#127091=CARTESIAN_POINT ( 'NONE',  ( 18.59999999999999787, 77.26327546522891510, -61.62124281777789037 ) ) ;
#127131=EDGE_CURVE ( 'NONE', #148851, #14237, #45504, .T. ) ;
#127144=DIRECTION ( 'NONE',  ( 1.000000000000000000, 7.304098846218133681E-16, 5.100424963727255128E-30 ) ) ;
#127156=CARTESIAN_POINT ( 'NONE',  ( -21.05000000000000071, 74.83729825007388570, -95.02310748452431710 ) ) ;
#127165=FACE_OUTER_BOUND ( 'NONE', #129937, .T. ) ;
#127172=EDGE_CURVE ( 'NONE', #178769, #251279, #187348, .T. ) ;
#127173=VERTEX_POINT ( 'NONE', #25691 ) ;
#127197=CARTESIAN_POINT ( 'NONE',  ( 18.59999999999999787, 74.13328508995456900, -91.27043223824230722 ) ) ;
#127215=CIRCLE ( 'NONE', #14822, 0.1000000000000028644 ) ;
#127221=ORIENTED_EDGE ( 'NONE', *, *, #82479, .T. ) ;
#127229=DIRECTION ( 'NONE',  ( 0.000000000000000000, 0.9915357197604862671, -0.1298341882519953583 ) ) ;
#127254=CARTESIAN_POINT ( 'NONE',  ( 18.46905048506369695, 85.47374425739408821, -62.84712119226885818 ) ) ;
#127256=VERTEX_POINT ( 'NONE', #66093 ) ;
#127276=FACE_OUTER_BOUND ( 'NONE', #52835, .T. ) ;
#127339=ADVANCED_FACE ( 'NONE', ( #29572, #191209 ), #188603, .T. ) ;
#127341=CARTESIAN_POINT ( 'NONE',  ( -21.05000000000000426, 76.02103547655211457, -109.3275633064719869 ) ) ;
#127343=AXIS2_PLACEMENT_3D ( 'NONE', #132139, #254625, #193415 ) ;
#127355=DIRECTION ( 'NONE',  ( 0.000000000000000000, -0.1350103645451557199, -0.9908441862701644620 ) ) ;
#127368=ADVANCED_FACE ( 'NONE', ( #2914 ), #221945, .T. ) ;
#127371=CARTESIAN_POINT ( 'NONE',  ( -23.25000000000000000, 74.08971962618008433, -90.39173962932538586 ) ) ;
#127383=DIRECTION ( 'NONE',  ( -0.000000000000000000, 1.000000000000000000, 6.352154140967427193E-15 ) ) ;
#127394=CARTESIAN_POINT ( 'NONE',  ( -23.15000000000000213, 76.00000000001186606, -90.14810748452431710 ) ) ;
#127424=EDGE_LOOP ( 'NONE', ( #241722, #172586, #243988, #30243 ) ) ;
#127435=CARTESIAN_POINT ( 'NONE',  ( -21.05000000000000071, 76.00000000001168132, -65.42310748452432279 ) ) ;
#127458=CARTESIAN_POINT ( 'NONE',  ( -18.50000000000000000, 77.83585931145526615, -58.01866831572577610 ) ) ;
#127501=EDGE_CURVE ( 'NONE', #2887, #1640, #88860, .T. ) ;
#127512=DIRECTION ( 'NONE',  ( 1.000000000000000000, 0.000000000000000000, 0.000000000000000000 ) ) ;
#127573=CARTESIAN_POINT ( 'NONE',  ( 21.14999999999999858, 69.45934304831071415, -102.9231074845243512 ) ) ;
#127599=ORIENTED_EDGE ( 'NONE', *, *, #94339, .F. ) ;
#127648=VERTEX_POINT ( 'NONE', #108453 ) ;
#127649=VERTEX_POINT ( 'NONE', #5468 ) ;
#127675=CARTESIAN_POINT ( 'NONE',  ( -20.54999999999999716, 85.00000000001179501, -79.41707660717668205 ) ) ;
#127696=EDGE_CURVE ( 'NONE', #88936, #111063, #236041, .T. ) ;
#127716=DIRECTION ( 'NONE',  ( 1.000000000000000000, 0.000000000000000000, 0.000000000000000000 ) ) ;
#127719=DIRECTION ( 'NONE',  ( 1.000000000000000000, 0.000000000000000000, 0.000000000000000000 ) ) ;
#127728=ORIENTED_EDGE ( 'NONE', *, *, #185169, .F. ) ;
#127759=EDGE_LOOP ( 'NONE', ( #193756, #92756, #164860, #175280 ) ) ;
#127766=VERTEX_POINT ( 'NONE', #121331 ) ;
#127824=AXIS2_PLACEMENT_3D ( 'NONE', #152938, #134596, #215439 ) ;
#127826=AXIS2_PLACEMENT_3D ( 'NONE', #225003, #242019, #221162 ) ;
#127845=FACE_OUTER_BOUND ( 'NONE', #125518, .T. ) ;
#127857=LINE ( 'NONE', #33936, #28662 ) ;
#127861=ORIENTED_EDGE ( 'NONE', *, *, #40824, .T. ) ;
#127885=VECTOR ( 'NONE', #82694, 1000.000000000000000 ) ;
#127886=DIRECTION ( 'NONE',  ( 1.000000000000000000, 0.000000000000000000, 0.000000000000000000 ) ) ;
#127925=LINE ( 'NONE', #105755, #200698 ) ;
#127932=DIRECTION ( 'NONE',  ( 0.000000000000000000, 1.000000000000000000, 6.608470384673536824E-15 ) ) ;
#127965=CARTESIAN_POINT ( 'NONE',  ( 21.05000000000000426, 65.43724016256084042, -95.56629352660579002 ) ) ;
#127979=CARTESIAN_POINT ( 'NONE',  ( -18.50000000000000000, 64.35000000001171827, -69.52310748452438816 ) ) ;
#127986=ORIENTED_EDGE ( 'NONE', *, *, #242687, .F. ) ;
#127998=DIRECTION ( 'NONE',  ( -0.000000000000000000, 1.000000000000000000, 8.717686153663073805E-15 ) ) ;
#128005=AXIS2_PLACEMENT_3D ( 'NONE', #22091, #2491, #82009 ) ;
#128007=AXIS2_PLACEMENT_3D ( 'NONE', #88406, #23360, #39392 ) ;
#128009=EDGE_CURVE ( 'NONE', #121706, #218126, #252774, .T. ) ;
#128021=ADVANCED_FACE ( 'NONE', ( #100101 ), #218778, .F. ) ;
#128032=ORIENTED_EDGE ( 'NONE', *, *, #214573, .T. ) ;
#128039=EDGE_CURVE ( 'NONE', #201306, #159653, #186463, .T. ) ;
#128059=CIRCLE ( 'NONE', #244738, 0.2000000000000057288 ) ;
#128073=ORIENTED_EDGE ( 'NONE', *, *, #23133, .F. ) ;
#128077=ORIENTED_EDGE ( 'NONE', *, *, #57563, .T. ) ;
#128103=DIRECTION ( 'NONE',  ( 1.000000000000000000, 0.000000000000000000, 0.000000000000000000 ) ) ;
#128117=EDGE_CURVE ( 'NONE', #164178, #11451, #165625, .T. ) ;
#128124=ORIENTED_EDGE ( 'NONE', *, *, #1434, .F. ) ;
#128138=CARTESIAN_POINT ( 'NONE',  ( -23.15000000000000213, 76.00000000001170974, -69.52310748452431710 ) ) ;
#128173=CARTESIAN_POINT ( 'NONE',  ( 21.05000000000000071, 87.65000000001192859, -100.1231074845242262 ) ) ;
#128174=CARTESIAN_POINT ( 'NONE',  ( 18.50000000000000355, 85.42145614550825883, -95.78112540050472035 ) ) ;
#128191=VERTEX_POINT ( 'NONE', #46555 ) ;
#128193=CARTESIAN_POINT ( 'NONE',  ( 20.77766267348356166, 65.55095760939289562, -95.43039856864687920 ) ) ;
#128203=CARTESIAN_POINT ( 'NONE',  ( 21.04999999999999716, 76.00000000001199396, -109.5637644362255685 ) ) ;
#128243=FACE_OUTER_BOUND ( 'NONE', #46565, .T. ) ;
#128261=CARTESIAN_POINT ( 'NONE',  ( -21.14999999999999858, 64.25000000001190870, -96.29697684846520644 ) ) ;
#128264=( BOUNDED_CURVE ( )  B_SPLINE_CURVE ( 3, ( #96504, #193077, #57383, #14456 ),
 .UNSPECIFIED., .F., .F. ) 
 B_SPLINE_CURVE_WITH_KNOTS ( ( 4, 4 ),
 ( 3.141592653589793116, 4.712388980384689674 ),
 .UNSPECIFIED. ) 
 CURVE ( )  GEOMETRIC_REPRESENTATION_ITEM ( )  RATIONAL_B_SPLINE_CURVE ( ( 1.000000000000000000, 0.8047378541243649375, 0.8047378541243649375, 1.000000000000000000 ) ) 
 REPRESENTATION_ITEM ( '' )  );
#128286=ADVANCED_FACE ( 'NONE', ( #203074 ), #84358, .T. ) ;
#128316=AXIS2_PLACEMENT_3D ( 'NONE', #179192, #77461, #138708 ) ;
#128358=CARTESIAN_POINT ( 'NONE',  ( 18.49999999999999645, 77.83534155023627932, -91.46795619196132066 ) ) ;
#128359=FACE_OUTER_BOUND ( 'NONE', #36760, .T. ) ;
#128368=VECTOR ( 'NONE', #136204, 1000.000000000000000 ) ;
#128378=DIRECTION ( 'NONE',  ( 0.000000000000000000, 7.147358527629766941E-15, -1.000000000000000000 ) ) ;
#128396=ORIENTED_EDGE ( 'NONE', *, *, #90753, .F. ) ;
#128412=CARTESIAN_POINT ( 'NONE',  ( -18.50000000000000000, 64.25000000001203659, -114.7731074845243882 ) ) ;
#128414=CARTESIAN_POINT ( 'NONE',  ( 21.14999999999999858, 69.35000000001186038, -90.77310748452435973 ) ) ;
#128421=AXIS2_PLACEMENT_3D ( 'NONE', #76070, #231322, #136019 ) ;
#128426=EDGE_CURVE ( 'NONE', #131339, #109375, #219958, .T. ) ;
#128459=DIRECTION ( 'NONE',  ( 0.000000000000000000, 6.982962677686266711E-15, -1.000000000000000000 ) ) ;
#128465=DIRECTION ( 'NONE',  ( 1.441126678808781001E-14, -0.9876197685951241256, -0.1568667991644932258 ) ) ;
#128469=CARTESIAN_POINT ( 'NONE',  ( -20.64999999999999858, 74.00000000001180922, -82.74772940728641402 ) ) ;
#128497=EDGE_CURVE ( 'NONE', #231923, #227300, #136733, .T. ) ;
#128498=VECTOR ( 'NONE', #159656, 1000.000000000000000 ) ;
#128527=ORIENTED_EDGE ( 'NONE', *, *, #44323, .T. ) ;
#128536=CARTESIAN_POINT ( 'NONE',  ( 18.49505816908824940, 85.43787255322283158, -62.74545028285337622 ) ) ;
#128567=VECTOR ( 'NONE', #27509, 1000.000000000000000 ) ;
#128573=AXIS2_PLACEMENT_3D ( 'NONE', #150603, #128465, #209277 ) ;
#128595=CIRCLE ( 'NONE', #78509, 6.329289321881370611 ) ;
#128600=CARTESIAN_POINT ( 'NONE',  ( 20.84999999999998721, 87.75000000001172396, -69.52310748452423184 ) ) ;
#128633=TOROIDAL_SURFACE ( 'NONE', #7840, 12.97499999999999609, 0.1000000000000000056 ) ;
#128667=DIRECTION ( 'NONE',  ( 0.000000000000000000, 0.000000000000000000, -1.000000000000000000 ) ) ;
#128676=AXIS2_PLACEMENT_3D ( 'NONE', #200442, #180884, #63479 ) ;
#128681=AXIS2_PLACEMENT_3D ( 'NONE', #72377, #54069, #111484 ) ;
#128685=DIRECTION ( 'NONE',  ( 0.000000000000000000, 7.116814260417668513E-15, -1.000000000000000000 ) ) ;
#128696=EDGE_LOOP ( 'NONE', ( #173668, #155786, #14064, #158283 ) ) ;
#128699=ORIENTED_EDGE ( 'NONE', *, *, #233851, .T. ) ;
#128707=DIRECTION ( 'NONE',  ( 0.000000000000000000, -7.026728003956683390E-15, 1.000000000000000000 ) ) ;
#128715=CARTESIAN_POINT ( 'NONE',  ( 20.94999999999999929, 85.00000000001179501, -79.41707660717668205 ) ) ;
#128724=B_SPLINE_CURVE_WITH_KNOTS ( 'NONE', 3,
 ( #43676, #164904, #202736, #104885, #24130, #103615 ),
 .UNSPECIFIED., .F., .F.,
 ( 4, 2, 4 ),
 ( 0.000000000000000000, 0.0001497467027049214044, 0.0002994934054098428089 ),
 .UNSPECIFIED. ) ;
#128737=ORIENTED_EDGE ( 'NONE', *, *, #168902, .T. ) ;
#128742=EDGE_CURVE ( 'NONE', #64319, #194507, #186837, .T. ) ;
#128762=CARTESIAN_POINT ( 'NONE',  ( -20.85000000106584750, 64.25000000001175238, -76.36760282805070688 ) ) ;
#128768=DIRECTION ( 'NONE',  ( -0.000000000000000000, 0.9875055080513808203, -0.1575844902526395142 ) ) ;
#128782=DIRECTION ( 'NONE',  ( -3.787827842127534447E-15, -0.7397360091702729346, -0.6728971962616859814 ) ) ;
#128799=AXIS2_PLACEMENT_3D ( 'NONE', #93238, #150659, #210628 ) ;
#128810=DIRECTION ( 'NONE',  ( 0.000000000000000000, 6.982962677686266711E-15, -1.000000000000000000 ) ) ;
#128903=EDGE_CURVE ( 'NONE', #91045, #249684, #228530, .T. ) ;
#128906=ADVANCED_FACE ( 'NONE', ( #42150 ), #22584, .F. ) ;
#128953=CARTESIAN_POINT ( 'NONE',  ( 23.14999999999999503, 64.25000000001179501, -81.67310748452439384 ) ) ;
#128959=CARTESIAN_POINT ( 'NONE',  ( -22.39999999999999858, 76.00000000001200817, -110.8138870828977218 ) ) ;
#129012=CARTESIAN_POINT ( 'NONE',  ( -23.15000000000000213, 85.00000000001188027, -93.62913836187181005 ) ) ;
#129021=AXIS2_PLACEMENT_3D ( 'NONE', #233986, #239134, #74953 ) ;
#129047=EDGE_LOOP ( 'NONE', ( #239208, #101388, #217744 ) ) ;
#129050=ORIENTED_EDGE ( 'NONE', *, *, #86107, .T. ) ;
#129106=CIRCLE ( 'NONE', #16692, 0.1000000000000028644 ) ;
#129108=ORIENTED_EDGE ( 'NONE', *, *, #186153, .F. ) ;
#129117=CARTESIAN_POINT ( 'NONE',  ( 20.94999999999999574, 74.26374286841446803, -91.45445515550682103 ) ) ;
#129128=VERTEX_POINT ( 'NONE', #32883 ) ;
#129152=ORIENTED_EDGE ( 'NONE', *, *, #46746, .F. ) ;
#129158=DIRECTION ( 'NONE',  ( -0.000000000000000000, 6.982962677686266711E-15, -1.000000000000000000 ) ) ;
#129168=CARTESIAN_POINT ( 'NONE',  ( -20.94999999999999929, 68.97833521811159585, -65.88954208262707368 ) ) ;
#129173=ADVANCED_FACE ( 'NONE', ( #130650 ), #29629, .F. ) ;
#129183=CARTESIAN_POINT ( 'NONE',  ( -22.50000000000000000, 64.35012909624775546, -103.1056273753973613 ) ) ;
#129190=AXIS2_PLACEMENT_3D ( 'NONE', #39069, #176019, #118603 ) ;
#129286=CIRCLE ( 'NONE', #233363, 0.1000000000000028783 ) ;
#129303=ORIENTED_EDGE ( 'NONE', *, *, #90879, .F. ) ;
#129312=( BOUNDED_SURFACE ( )  B_SPLINE_SURFACE ( 3, 2, ( 
 ( #47391, #162244, #142639 ),
 ( #86500, #183082, #65684 ),
 ( #166114, #123109, #181789 ),
 ( #6992, #3124, #104778 ),
 ( #61846, #21453, #241752 ),
 ( #202627, #4418, #184342 ) ),
 .UNSPECIFIED., .F., .F., .F. ) 
 B_SPLINE_SURFACE_WITH_KNOTS ( ( 4, 2, 4 ),
 ( 3, 3 ),
 ( 0.0001381104793128061785, 0.0002947094729387726578, 0.0004513084665647390829 ),
 ( 0.000000000000000000, 1.000000000000000000 ),
 .UNSPECIFIED. ) 
 GEOMETRIC_REPRESENTATION_ITEM ( )  RATIONAL_B_SPLINE_SURFACE ( (
 ( 1.000000000000000000, 0.7071067811865985320, 1.000000000000000000),
 ( 1.000000000000000000, 0.6919563088098532599, 1.000000000000000000),
 ( 1.000000000000000000, 0.6959445945717439574, 1.000000000000000000),
 ( 1.000000000000000000, 0.7137882985313119821, 1.000000000000000000),
 ( 1.000000000000000000, 0.7257496306096471450, 1.000000000000000000),
 ( 1.000000000000000000, 0.7250110520819876836, 1.000000000000000000) ) ) 
 REPRESENTATION_ITEM ( '' )  SURFACE ( )  );
#129322=CIRCLE ( 'NONE', #4408, 0.5000000000000004441 ) ;
#129324=FACE_OUTER_BOUND ( 'NONE', #164204, .T. ) ;
#129330=ORIENTED_EDGE ( 'NONE', *, *, #206571, .F. ) ;
#129344=DIRECTION ( 'NONE',  ( 0.000000000000000000, 0.000000000000000000, 1.000000000000000000 ) ) ;
#129411=DIRECTION ( 'NONE',  ( 0.000000000000000000, -6.938893903907222067E-15, 1.000000000000000000 ) ) ;
#129450=ORIENTED_EDGE ( 'NONE', *, *, #101182, .F. ) ;
#129455=CARTESIAN_POINT ( 'NONE',  ( 18.48536876927948924, 85.46352724987913518, -95.97448921944113920 ) ) ;
#129473=EDGE_CURVE ( 'NONE', #59214, #233299, #174196, .T. ) ;
#129479=CARTESIAN_POINT ( 'NONE',  ( 20.22894356738409272, 66.72150177717416852, -94.75458457828102610 ) ) ;
#129506=VERTEX_POINT ( 'NONE', #135133 ) ;
#129520=DIRECTION ( 'NONE',  ( 0.000000000000000000, 0.000000000000000000, 1.000000000000000000 ) ) ;
#129523=CARTESIAN_POINT ( 'NONE',  ( -22.47071067811865319, 75.90090754530939421, -110.7431822290223806 ) ) ;
#129525=DIRECTION ( 'NONE',  ( 1.000000000000000000, 0.000000000000000000, 0.000000000000000000 ) ) ;
#129578=VERTEX_POINT ( 'NONE', #192566 ) ;
#129579=DIRECTION ( 'NONE',  ( 1.000000000000000000, 0.000000000000000000, 0.000000000000000000 ) ) ;
#129604=EDGE_CURVE ( 'NONE', #173093, #50671, #53918, .T. ) ;
#129626=CARTESIAN_POINT ( 'NONE',  ( 20.85000000000000142, 64.35000000001170406, -69.52310748452438816 ) ) ;
#129632=CARTESIAN_POINT ( 'NONE',  ( -20.64999999999999858, 76.00000000001170974, -69.52310748452431710 ) ) ;
#129638=DIRECTION ( 'NONE',  ( 1.000000000000000000, 0.000000000000000000, 0.000000000000000000 ) ) ;
#129662=CARTESIAN_POINT ( 'NONE',  ( 20.88420186297724257, 65.66974365629646115, -63.93601455626049557 ) ) ;
#129670=EDGE_CURVE ( 'NONE', #206540, #35640, #45040, .T. ) ;
#129675=ORIENTED_EDGE ( 'NONE', *, *, #44030, .T. ) ;
#129676=DIRECTION ( 'NONE',  ( 0.000000000000000000, -7.487053152578127080E-15, 1.000000000000000000 ) ) ;
#129688=ADVANCED_FACE ( 'NONE', ( #198976 ), #74233, .F. ) ;
#129708=DIRECTION ( 'NONE',  ( 0.000000000000000000, -1.000000000000000000, 0.000000000000000000 ) ) ;
#129720=DIRECTION ( 'NONE',  ( 0.000000000000000000, -1.000000000000000000, 0.000000000000000000 ) ) ;
#129734=VERTEX_POINT ( 'NONE', #188400 ) ;
#129740=ADVANCED_FACE ( 'NONE', ( #207987 ), #185831, .T. ) ;
#129743=ORIENTED_EDGE ( 'NONE', *, *, #172929, .T. ) ;
#129810=DIRECTION ( 'NONE',  ( 1.000000000000000000, 0.000000000000000000, 0.000000000000000000 ) ) ;
#129819=VERTEX_POINT ( 'NONE', #125846 ) ;
#129822=ORIENTED_EDGE ( 'NONE', *, *, #218386, .T. ) ;
#129843=CARTESIAN_POINT ( 'NONE',  ( -20.94999999999999929, 76.00000000001170974, -69.52310748452431710 ) ) ;
#129863=CARTESIAN_POINT ( 'NONE',  ( 18.43466021071409955, 85.49419069046821562, -62.90604592439652265 ) ) ;
#129868=DIRECTION ( 'NONE',  ( 1.000000000000000000, 0.000000000000000000, 0.000000000000000000 ) ) ;
#129937=EDGE_LOOP ( 'NONE', ( #201840, #204153, #56496, #89788 ) ) ;
#129941=ORIENTED_EDGE ( 'NONE', *, *, #112105, .F. ) ;
#129943=CARTESIAN_POINT ( 'NONE',  ( -20.54999999999999716, 66.65000000001187175, -90.77310748452437394 ) ) ;
#129951=CARTESIAN_POINT ( 'NONE',  ( -23.15000000000000213, 71.85000000001186038, -90.67310748452433700 ) ) ;
#129955=ORIENTED_EDGE ( 'NONE', *, *, #9068, .F. ) ;
#130055=LINE ( 'NONE', #250019, #173904 ) ;
#130133=CARTESIAN_POINT ( 'NONE',  ( -21.55000000000000426, 68.25000000001185185, -90.67310748452436542 ) ) ;
#130183=ORIENTED_EDGE ( 'NONE', *, *, #111778, .T. ) ;
#130213=CIRCLE ( 'NONE', #34406, 7.900000000000003908 ) ;
#130235=TOROIDAL_SURFACE ( 'NONE', #88716, 0.2000000000000000111, 0.1000000000000000056 ) ;
#130240=CARTESIAN_POINT ( 'NONE',  ( 20.94999999999999929, 77.16270174994990327, -95.12310748452431142 ) ) ;
#130252=AXIS2_PLACEMENT_3D ( 'NONE', #226433, #8699, #170393 ) ;
#130255=CARTESIAN_POINT ( 'NONE',  ( 20.94999999999999574, 76.00000000001195133, -103.0231074845243171 ) ) ;
#130263=ORIENTED_EDGE ( 'NONE', *, *, #23451, .T. ) ;
#130272=CARTESIAN_POINT ( 'NONE',  ( 22.59999999999999432, 75.95218160930723172, -114.7731299035715296 ) ) ;
#130276=ORIENTED_EDGE ( 'NONE', *, *, #58546, .F. ) ;
#130283=CARTESIAN_POINT ( 'NONE',  ( 22.39999999999999503, 75.90000000001199965, -110.8138870828976934 ) ) ;
#130290=DIRECTION ( 'NONE',  ( 0.000000000000000000, -6.982962677686266711E-15, 1.000000000000000000 ) ) ;
#130291=DIRECTION ( 'NONE',  ( 1.000000000000000000, -2.952720810173289112E-16, -2.061873921506763405E-30 ) ) ;
#130360=ORIENTED_EDGE ( 'NONE', *, *, #168915, .F. ) ;
#130365=VERTEX_POINT ( 'NONE', #212814 ) ;
#130421=DIRECTION ( 'NONE',  ( -1.000000000000000000, 0.000000000000000000, 0.000000000000000000 ) ) ;
#130424=FACE_OUTER_BOUND ( 'NONE', #104905, .T. ) ;
#130436=CARTESIAN_POINT ( 'NONE',  ( 20.94999999999999574, 77.36087058720393372, -94.95010955743333625 ) ) ;
#130441=AXIS2_PLACEMENT_3D ( 'NONE', #203464, #126484, #143476 ) ;
#130506=LINE ( 'NONE', #71849, #145139 ) ;
#130511=DIRECTION ( 'NONE',  ( 0.000000000000000000, -1.000000000000000000, -6.982962677686266711E-15 ) ) ;
#130514=CYLINDRICAL_SURFACE ( 'NONE', #13794, 0.1000000000000028644 ) ;
#130530=CYLINDRICAL_SURFACE ( 'NONE', #74852, 12.87499999999999822 ) ;
#130563=CARTESIAN_POINT ( 'NONE',  ( 20.99551997958380056, 64.25000000001175238, -76.37144834683515171 ) ) ;
#130578=LINE ( 'NONE', #63213, #255608 ) ;
#130601=EDGE_CURVE ( 'NONE', #181805, #159653, #91329, .T. ) ;
#130650=FACE_OUTER_BOUND ( 'NONE', #141000, .T. ) ;
#130695=ORIENTED_EDGE ( 'NONE', *, *, #125661, .T. ) ;
#130716=ADVANCED_FACE ( 'NONE', ( #54705 ), #134230, .T. ) ;
#130725=CARTESIAN_POINT ( 'NONE',  ( -22.50000000000000000, 76.00000000001195133, -103.1231074845243114 ) ) ;
#130728=DIRECTION ( 'NONE',  ( -0.000000000000000000, 0.1298341882520009927, 0.9915357197604854900 ) ) ;
#130733=CARTESIAN_POINT ( 'NONE',  ( 18.54147908293617064, 85.46326165794005192, -95.97415858776851394 ) ) ;
#130744=DIRECTION ( 'NONE',  ( 0.000000000000000000, -0.1298341882519953583, -0.9915357197604862671 ) ) ;
#130753=CARTESIAN_POINT ( 'NONE',  ( -21.59142135623730852, 68.15000000001187175, -90.67310748452436542 ) ) ;
#130790=ORIENTED_EDGE ( 'NONE', *, *, #223282, .T. ) ;
#130803=ORIENTED_EDGE ( 'NONE', *, *, #70226, .T. ) ;
#130824=EDGE_CURVE ( 'NONE', #204044, #253445, #19441, .T. ) ;
#130848=EDGE_LOOP ( 'NONE', ( #60603, #183201, #132179, #179462 ) ) ;
#130858=FACE_BOUND ( 'NONE', #64080, .T. ) ;
#130876=CARTESIAN_POINT ( 'NONE',  ( 18.49999999999999645, 76.00000000001195133, -103.0231074845243171 ) ) ;
#130911=CYLINDRICAL_SURFACE ( 'NONE', #159978, 0.09999999999999939493 ) ;
#130919=AXIS2_PLACEMENT_3D ( 'NONE', #257463, #215806, #78863 ) ;
#130927=( BOUNDED_CURVE ( )  B_SPLINE_CURVE ( 3, ( #114030, #174065, #171489, #151916 ),
 .UNSPECIFIED., .F., .F. ) 
 B_SPLINE_CURVE_WITH_KNOTS ( ( 4, 4 ),
 ( 4.712388980384689674, 6.231880751915386263 ),
 .UNSPECIFIED. ) 
 CURVE ( )  GEOMETRIC_REPRESENTATION_ITEM ( )  RATIONAL_B_SPLINE_CURVE ( ( 1.000000000000000000, 0.8166740347213228279, 0.8166740347213228279, 1.000000000000000000 ) ) 
 REPRESENTATION_ITEM ( '' )  );
#130929=ADVANCED_FACE ( 'NONE', ( #168932 ), #145639, .T. ) ;
#130949=CARTESIAN_POINT ( 'NONE',  ( 20.94983749550516450, 65.70233904876990039, -64.04874109119681691 ) ) ;
#130984=CARTESIAN_POINT ( 'NONE',  ( -18.52643265882458579, 65.68026841930881687, -63.97257401318892533 ) ) ;
#130985=ORIENTED_EDGE ( 'NONE', *, *, #153653, .F. ) ;
#131020=ORIENTED_EDGE ( 'NONE', *, *, #171576, .T. ) ;
#131111=CARTESIAN_POINT ( 'NONE',  ( -22.39999999999999858, 68.20922040163854660, -103.0231074845243739 ) ) ;
#131115=DIRECTION ( 'NONE',  ( -1.000000000000000000, 2.952720810173289112E-16, 2.061873921506763405E-30 ) ) ;
#131129=DIRECTION ( 'NONE',  ( 0.000000000000000000, -0.1495327102803078179, 0.9887567792719429427 ) ) ;
#131166=AXIS2_PLACEMENT_3D ( 'NONE', #110963, #245350, #225754 ) ;
#131186=EDGE_LOOP ( 'NONE', ( #155548, #165827, #19634, #190403 ) ) ;
#131199=ORIENTED_EDGE ( 'NONE', *, *, #212941, .F. ) ;
#131207=ADVANCED_FACE ( 'NONE', ( #3062 ), #49975, .T. ) ;
#131212=DIRECTION ( 'NONE',  ( 2.952720810173289112E-16, 1.000000000000000000, 6.982962677686266711E-15 ) ) ;
#131270=DIRECTION ( 'NONE',  ( 0.000000000000000000, -6.982962677686266711E-15, 1.000000000000000000 ) ) ;
#131278=CARTESIAN_POINT ( 'NONE',  ( -20.54999999999999716, 74.05981308412400210, -90.19398827347099257 ) ) ;
#131307=FACE_OUTER_BOUND ( 'NONE', #145264, .T. ) ;
#131323=CIRCLE ( 'NONE', #214709, 0.2000000000000057288 ) ;
#131339=VERTEX_POINT ( 'NONE', #30371 ) ;
#131351=CARTESIAN_POINT ( 'NONE',  ( -18.50000000000000000, 77.16412189325286874, -61.80825939895269272 ) ) ;
#131353=SPHERICAL_SURFACE ( 'NONE', #213923, 0.1000000000000000056 ) ;
#131369=ADVANCED_FACE ( 'NONE', ( #86437 ), #235984, .T. ) ;
#131370=DIRECTION ( 'NONE',  ( -1.000000000000000000, 0.000000000000000000, -0.000000000000000000 ) ) ;
#131396=CARTESIAN_POINT ( 'NONE',  ( 20.94999999999999929, 76.00000000001170974, -69.52310748452431710 ) ) ;
#131440=AXIS2_PLACEMENT_3D ( 'NONE', #130255, #235774, #196645 ) ;
#131442=ORIENTED_EDGE ( 'NONE', *, *, #251710, .T. ) ;
#131457=LINE ( 'NONE', #171909, #179735 ) ;
#131480=DIRECTION ( 'NONE',  ( 0.000000000000000000, 6.577889128801591149E-15, -1.000000000000000000 ) ) ;
#131489=VERTEX_POINT ( 'NONE', #234984 ) ;
#131509=LINE ( 'NONE', #108106, #126483 ) ;
#131533=DIRECTION ( 'NONE',  ( 0.000000000000000000, -1.000000000000000000, -6.982962677686266711E-15 ) ) ;
#131584=AXIS2_PLACEMENT_3D ( 'NONE', #77406, #40904, #197370 ) ;
#131639=ORIENTED_EDGE ( 'NONE', *, *, #116598, .F. ) ;
#131643=CIRCLE ( 'NONE', #156806, 0.1000000000000028644 ) ;
#131678=CARTESIAN_POINT ( 'NONE',  ( -20.54999999999999716, 68.85000000001180354, -81.87310748452436826 ) ) ;
#131688=EDGE_CURVE ( 'NONE', #224619, #167256, #237613, .T. ) ;
#131715=FACE_OUTER_BOUND ( 'NONE', #120900, .T. ) ;
#131751=CARTESIAN_POINT ( 'NONE',  ( 18.59999999999999076, 69.45000000001181206, -81.87310748452435405 ) ) ;
#131752=ORIENTED_EDGE ( 'NONE', *, *, #22415, .F. ) ;
#131757=CARTESIAN_POINT ( 'NONE',  ( 23.24999999999999645, 73.90000000001170122, -69.52310748452431710 ) ) ;
#131797=CARTESIAN_POINT ( 'NONE',  ( -21.05000000000000071, 69.58633726514277384, -102.9375146211624497 ) ) ;
#131813=CARTESIAN_POINT ( 'NONE',  ( -20.64999999999999858, 76.00000000001170974, -69.52310748452431710 ) ) ;
#131823=FACE_OUTER_BOUND ( 'NONE', #23226, .T. ) ;
#131827=VERTEX_POINT ( 'NONE', #190435 ) ;
#131834=CARTESIAN_POINT ( 'NONE',  ( 18.49999999999999289, 65.55993210786641612, -78.25598973563684524 ) ) ;
#131878=ADVANCED_FACE ( 'NONE', ( #59857 ), #37905, .T. ) ;
#131895=CARTESIAN_POINT ( 'NONE',  ( 18.59999999999999076, 69.55000000001187743, -93.00608031408432907 ) ) ;
#131902=DIRECTION ( 'NONE',  ( 1.000000000000000000, -2.952720810173289112E-16, -2.061873921506763405E-30 ) ) ;
#131915=EDGE_CURVE ( 'NONE', #2887, #3181, #46238, .T. ) ;
#131923=ORIENTED_EDGE ( 'NONE', *, *, #129473, .F. ) ;
#131940=ORIENTED_EDGE ( 'NONE', *, *, #28964, .T. ) ;
#131963=CIRCLE ( 'NONE', #140325, 0.09999999999999939493 ) ;
#131992=ORIENTED_EDGE ( 'NONE', *, *, #37492, .T. ) ;
#132016=SPHERICAL_SURFACE ( 'NONE', #52740, 0.1000000000000000056 ) ;
#132032=CARTESIAN_POINT ( 'NONE',  ( -20.54999999999999716, 85.00000000001179501, -79.41707660717668205 ) ) ;
#132034=ORIENTED_EDGE ( 'NONE', *, *, #176301, .F. ) ;
#132035=VECTOR ( 'NONE', #70082, 1000.000000000000114 ) ;
#132040=ORIENTED_EDGE ( 'NONE', *, *, #165648, .F. ) ;
#132044=ORIENTED_EDGE ( 'NONE', *, *, #24282, .T. ) ;
#132049=CARTESIAN_POINT ( 'NONE',  ( 21.05000000000000071, 76.02138556594995578, -109.3280685972088691 ) ) ;
#132051=AXIS2_PLACEMENT_3D ( 'NONE', #70423, #71689, #190351 ) ;
#132101=ORIENTED_EDGE ( 'NONE', *, *, #238694, .F. ) ;
#132117=ORIENTED_EDGE ( 'NONE', *, *, #84046, .F. ) ;
#132126=CARTESIAN_POINT ( 'NONE',  ( 21.00000000000000000, 66.25000000001186606, -90.67310748452437963 ) ) ;
#132139=CARTESIAN_POINT ( 'NONE',  ( -23.25000000000000000, 85.00000000001179501, -79.41707660717668205 ) ) ;
#132152=ORIENTED_EDGE ( 'NONE', *, *, #132614, .F. ) ;
#132157=CIRCLE ( 'NONE', #186331, 0.09999999999999799327 ) ;
#132179=ORIENTED_EDGE ( 'NONE', *, *, #82692, .T. ) ;
#132184=EDGE_LOOP ( 'NONE', ( #104630, #187579, #122945, #108787 ) ) ;
#132234=CARTESIAN_POINT ( 'NONE',  ( 20.93302460841142931, 65.68434038414338261, -63.98668807260656166 ) ) ;
#132274=FACE_OUTER_BOUND ( 'NONE', #169664, .T. ) ;
#132279=CARTESIAN_POINT ( 'NONE',  ( 18.50000000000000000, 85.50000000001189449, -95.99103808782457747 ) ) ;
#132300=FACE_OUTER_BOUND ( 'NONE', #169216, .T. ) ;
#132339=ORIENTED_EDGE ( 'NONE', *, *, #145280, .F. ) ;
#132416=DIRECTION ( 'NONE',  ( 0.000000000000000000, -1.000000000000000000, -6.982962677686266711E-15 ) ) ;
#132438=VERTEX_POINT ( 'NONE', #229978 ) ;
#132446=CARTESIAN_POINT ( 'NONE',  ( 18.58725287972292506, 85.56662691070313542, -62.70060267875840765 ) ) ;
#132462=CARTESIAN_POINT ( 'NONE',  ( -21.05000000000000071, 76.00000000001189449, -95.12310748452431142 ) ) ;
#132469=ORIENTED_EDGE ( 'NONE', *, *, #220901, .F. ) ;
#132470=AXIS2_PLACEMENT_3D ( 'NONE', #188213, #25304, #49981 ) ;
#132481=DIRECTION ( 'NONE',  ( -3.265361837132813093E-16, -1.000000000000000000, -6.982962677686266711E-15 ) ) ;
#132547=TOROIDAL_SURFACE ( 'NONE', #70219, 0.2000000000000000111, 0.1000000000000000056 ) ;
#132606=AXIS2_PLACEMENT_3D ( 'NONE', #126482, #48227, #228163 ) ;
#132614=EDGE_CURVE ( 'NONE', #170796, #183504, #242233, .T. ) ;
#132620=CARTESIAN_POINT ( 'NONE',  ( -18.59999999999999787, 77.83534155023627932, -91.46795619196132066 ) ) ;
#132642=DIRECTION ( 'NONE',  ( 0.000000000000000000, -0.1350103645451945777, 0.9908441862701590219 ) ) ;
#132652=DIRECTION ( 'NONE',  ( 0.000000000000000000, 0.8700118002898393765, -0.4930308989875104575 ) ) ;
#132672=ORIENTED_EDGE ( 'NONE', *, *, #103197, .F. ) ;
#132679=CARTESIAN_POINT ( 'NONE',  ( 21.05000000000000071, 85.00000000001179501, -79.41707660717668205 ) ) ;
#132683=DIRECTION ( 'NONE',  ( 0.000000000000000000, 0.1455152366551500653, 0.9893560106964507384 ) ) ;
#132723=AXIS2_PLACEMENT_3D ( 'NONE', #69035, #127716, #28660 ) ;
#132762=CARTESIAN_POINT ( 'NONE',  ( -23.25000000000000000, 76.10085836911075319, -114.7726746080137019 ) ) ;
#132793=AXIS2_PLACEMENT_3D ( 'NONE', #68511, #7229, #168937 ) ;
#132830=DIRECTION ( 'NONE',  ( 1.000000000000000000, 0.000000000000000000, 0.000000000000000000 ) ) ;
#132858=CIRCLE ( 'NONE', #82732, 12.77499999999999503 ) ;
#132886=CARTESIAN_POINT ( 'NONE',  ( 18.50000000000000000, 85.40000000001190017, -95.72584772486095517 ) ) ;
#132890=VERTEX_POINT ( 'NONE', #199558 ) ;
#132910=ORIENTED_EDGE ( 'NONE', *, *, #227, .T. ) ;
#132932=AXIS2_PLACEMENT_3D ( 'NONE', #226586, #106631, #8847 ) ;
#132944=DIRECTION ( 'NONE',  ( 0.000000000000000000, -1.000000000000000000, -6.982962677686265922E-15 ) ) ;
#133031=CARTESIAN_POINT ( 'NONE',  ( -20.64999999999999858, 68.85000000001186038, -90.77310748452435973 ) ) ;
#133035=CIRCLE ( 'NONE', #108085, 0.1000000000000028644 ) ;
#133038=CARTESIAN_POINT ( 'NONE',  ( -22.57320508075687115, 64.25000000001193712, -103.0231074845243739 ) ) ;
#133054=ORIENTED_EDGE ( 'NONE', *, *, #43489, .T. ) ;
#133066=CARTESIAN_POINT ( 'NONE',  ( 23.25000000000000000, 87.75000000001173817, -72.62310748452422615 ) ) ;
#133071=DIRECTION ( 'NONE',  ( 0.000000000000000000, -1.000000000000000000, -6.982962677686266711E-15 ) ) ;
#133090=CARTESIAN_POINT ( 'NONE',  ( -21.09107601085561257, 69.63612202465176892, -103.0624146492415178 ) ) ;
#133102=VECTOR ( 'NONE', #116735, 1000.000000000000000 ) ;
#133118=DIRECTION ( 'NONE',  ( 0.000000000000000000, 0.1350103645451945777, -0.9908441862701591329 ) ) ;
#133129=DIRECTION ( 'NONE',  ( 0.000000000000000000, 0.000000000000000000, 1.000000000000000000 ) ) ;
#133178=AXIS2_PLACEMENT_3D ( 'NONE', #198563, #194750, #179048 ) ;
#133204=CARTESIAN_POINT ( 'NONE',  ( 22.47071067811865319, 75.90090754530939421, -110.7431822290223522 ) ) ;
#133208=CARTESIAN_POINT ( 'NONE',  ( -20.54999999999999716, 76.00000000001170974, -69.52310748452431710 ) ) ;
#133214=CIRCLE ( 'NONE', #166554, 0.5000000000000004441 ) ;
#133233=VECTOR ( 'NONE', #187337, 1000.000000000000000 ) ;
#133254=AXIS2_PLACEMENT_3D ( 'NONE', #59640, #197893, #36285 ) ;
#133261=CARTESIAN_POINT ( 'NONE',  ( 20.84999999999998721, 64.25000000001170974, -69.52310748452438816 ) ) ;
#133281=CIRCLE ( 'NONE', #141642, 0.1000000000000055705 ) ;
#133312=ADVANCED_FACE ( 'NONE', ( #139214 ), #254043, .F. ) ;
#133336=AXIS2_PLACEMENT_3D ( 'NONE', #51753, #251249, #10087 ) ;
#133340=VECTOR ( 'NONE', #34221, 1000.000000000000000 ) ;
#133362=CARTESIAN_POINT ( 'NONE',  ( -23.25000000000000000, 76.00000000001168132, -65.62310748452431142 ) ) ;
#133395=EDGE_CURVE ( 'NONE', #128191, #194795, #121828, .T. ) ;
#133471=EDGE_CURVE ( 'NONE', #188436, #173426, #192743, .T. ) ;
#133472=CARTESIAN_POINT ( 'NONE',  ( 20.99999999999997868, 76.00000000001195133, -103.0231074845243171 ) ) ;
#133480=ORIENTED_EDGE ( 'NONE', *, *, #83538, .T. ) ;
#133482=FACE_OUTER_BOUND ( 'NONE', #6250, .T. ) ;
#133484=CYLINDRICAL_SURFACE ( 'NONE', #159731, 0.1000000000000052097 ) ;
#133496=EDGE_CURVE ( 'NONE', #154400, #50342, #80258, .T. ) ;
#133501=CARTESIAN_POINT ( 'NONE',  ( -23.15000000000000213, 85.00000000001188027, -93.12913836187181005 ) ) ;
#133522=EDGE_CURVE ( 'NONE', #67031, #20238, #67643, .T. ) ;
#133545=FACE_OUTER_BOUND ( 'NONE', #235054, .T. ) ;
#133558=ADVANCED_FACE ( 'NONE', ( #49117 ), #171678, .T. ) ;
#133565=CIRCLE ( 'NONE', #294, 0.2000000000000057288 ) ;
#133578=CIRCLE ( 'NONE', #241900, 11.89999999999999325 ) ;
#133580=DIRECTION ( 'NONE',  ( 0.000000000000000000, 6.982962677686266711E-15, -1.000000000000000000 ) ) ;
#133607=CYLINDRICAL_SURFACE ( 'NONE', #24803, 0.09999999999999939493 ) ;
#133630=AXIS2_PLACEMENT_3D ( 'NONE', #43052, #65163, #245095 ) ;
#133641=ADVANCED_FACE ( 'NONE', ( #135057 ), #217654, .T. ) ;
#133661=ORIENTED_EDGE ( 'NONE', *, *, #118604, .T. ) ;
#133662=ORIENTED_EDGE ( 'NONE', *, *, #198126, .F. ) ;
#133683=DIRECTION ( 'NONE',  ( 0.000000000000000000, 8.326672684688666480E-14, 1.000000000000000000 ) ) ;
#133722=CARTESIAN_POINT ( 'NONE',  ( 18.41815437325352178, 85.49870985315310179, -62.91916164572214143 ) ) ;
#133744=ORIENTED_EDGE ( 'NONE', *, *, #163797, .T. ) ;
#133801=ORIENTED_EDGE ( 'NONE', *, *, #221241, .F. ) ;
#133808=DIRECTION ( 'NONE',  ( 1.000000000000000000, 0.000000000000000000, 0.000000000000000000 ) ) ;
#133812=CIRCLE ( 'NONE', #13054, 0.1000000000000028644 ) ;
#133816=EDGE_CURVE ( 'NONE', #226125, #208704, #101272, .T. ) ;
#133920=ORIENTED_EDGE ( 'NONE', *, *, #246893, .T. ) ;
#133921=ADVANCED_FACE ( 'NONE', ( #129324 ), #38004, .F. ) ;
#133967=ORIENTED_EDGE ( 'NONE', *, *, #188411, .F. ) ;
#133975=ADVANCED_FACE ( 'NONE', ( #148902 ), #228444, .T. ) ;
#134005=AXIS2_PLACEMENT_3D ( 'NONE', #70493, #125299, #150015 ) ;
#134043=CARTESIAN_POINT ( 'NONE',  ( -20.64999999999999858, 68.85000000001180354, -81.87310748452436826 ) ) ;
#134070=CARTESIAN_POINT ( 'NONE',  ( 21.07928932188134397, 69.67148334361864670, -103.1220026301787414 ) ) ;
#134075=ORIENTED_EDGE ( 'NONE', *, *, #61616, .T. ) ;
#134100=CARTESIAN_POINT ( 'NONE',  ( 18.59999999999999076, 76.00000000001170974, -69.52310748452431710 ) ) ;
#134119=ORIENTED_EDGE ( 'NONE', *, *, #46221, .F. ) ;
#134132=ORIENTED_EDGE ( 'NONE', *, *, #136231, .T. ) ;
#134137=CARTESIAN_POINT ( 'NONE',  ( 21.05000000000000071, 85.50000000001179501, -79.41707660717668205 ) ) ;
#134157=DIRECTION ( 'NONE',  ( 1.000000000000000000, 0.000000000000000000, 0.000000000000000000 ) ) ;
#134168=DIRECTION ( 'NONE',  ( 2.557131231893037478E-16, 0.8660254037844420383, -0.4999999999999943379 ) ) ;
#134199=ORIENTED_EDGE ( 'NONE', *, *, #96790, .F. ) ;
#134230=PLANE ( 'NONE',  #45522 ) ;
#134231=CYLINDRICAL_SURFACE ( 'NONE', #44895, 0.09999999999999520384 ) ;
#134243=CARTESIAN_POINT ( 'NONE',  ( -18.59999999999999787, 77.85161776048053639, -57.91991776492063337 ) ) ;
#134271=CYLINDRICAL_SURFACE ( 'NONE', #136979, 0.09999999999999939493 ) ;
#134280=CARTESIAN_POINT ( 'NONE',  ( -23.15000000000000213, 64.25000000001179501, -81.67310748452440805 ) ) ;
#134286=EDGE_CURVE ( 'NONE', #187280, #131489, #103020, .T. ) ;
#134348=ORIENTED_EDGE ( 'NONE', *, *, #67528, .F. ) ;
#134350=EDGE_CURVE ( 'NONE', #42984, #224632, #110734, .T. ) ;
#134360=ORIENTED_EDGE ( 'NONE', *, *, #60783, .T. ) ;
#134361=CARTESIAN_POINT ( 'NONE',  ( 23.24999999999997513, 64.25000000001175238, -76.53791325517833855 ) ) ;
#134371=AXIS2_PLACEMENT_3D ( 'NONE', #244568, #65945, #145466 ) ;
#134389=EDGE_CURVE ( 'NONE', #65545, #110864, #204981, .T. ) ;
#134398=DIRECTION ( 'NONE',  ( 0.000000000000000000, -1.000000000000000000, 0.000000000000000000 ) ) ;
#134423=CARTESIAN_POINT ( 'NONE',  ( -18.50000000000000000, 70.05000000001193428, -92.71740517948948934 ) ) ;
#134462=ORIENTED_EDGE ( 'NONE', *, *, #122767, .F. ) ;
#134510=CIRCLE ( 'NONE', #251036, 0.1000000000000052097 ) ;
#134526=DIRECTION ( 'NONE',  ( 0.000000000000000000, -7.056502275159890832E-15, 1.000000000000000000 ) ) ;
#134577=DIRECTION ( 'NONE',  ( 0.000000000000000000, -6.982962677686266711E-15, 1.000000000000000000 ) ) ;
#134590=ORIENTED_EDGE ( 'NONE', *, *, #181399, .F. ) ;
#134596=DIRECTION ( 'NONE',  ( 1.000000000000000000, -0.000000000000000000, 0.000000000000000000 ) ) ;
#134660=TOROIDAL_SURFACE ( 'NONE', #135233, 4.149999999999999467, 0.1000000000000000056 ) ;
#134681=ORIENTED_EDGE ( 'NONE', *, *, #105477, .F. ) ;
#134706=VERTEX_POINT ( 'NONE', #166579 ) ;
#134747=CARTESIAN_POINT ( 'NONE',  ( -18.59999999999999787, 64.25000000001203659, -114.7731074845243882 ) ) ;
#134758=ORIENTED_EDGE ( 'NONE', *, *, #58773, .T. ) ;
#134772=EDGE_CURVE ( 'NONE', #118409, #82068, #38783, .T. ) ;
#134789=VERTEX_POINT ( 'NONE', #208259 ) ;
#134817=CARTESIAN_POINT ( 'NONE',  ( 23.14999999999999858, 76.00000000001170974, -69.52310748452431710 ) ) ;
#134858=CARTESIAN_POINT ( 'NONE',  ( 22.50000000000000000, 68.25000000001193712, -103.1231074845243540 ) ) ;
#134931=DIRECTION ( 'NONE',  ( -1.000000000000000000, 2.952720810173289112E-16, 2.061873921506763405E-30 ) ) ;
#134949=AXIS2_PLACEMENT_3D ( 'NONE', #250514, #247946, #229682 ) ;
#134950=EDGE_CURVE ( 'NONE', #110239, #278, #55299, .T. ) ;
#134961=EDGE_CURVE ( 'NONE', #195497, #223676, #154716, .T. ) ;
#134989=CARTESIAN_POINT ( 'NONE',  ( 18.48413544395646113, 85.66430403363939661, -62.84000249148589745 ) ) ;
#135026=CARTESIAN_POINT ( 'NONE',  ( -21.05000000000000071, 87.29603075034721371, -99.97520832486037534 ) ) ;
#135029=DIRECTION ( 'NONE',  ( 1.000000000000000000, 0.000000000000000000, 0.000000000000000000 ) ) ;
#135057=FACE_OUTER_BOUND ( 'NONE', #160434, .T. ) ;
#135061=ADVANCED_FACE ( 'NONE', ( #22904 ), #189545, .T. ) ;
#135071=ORIENTED_EDGE ( 'NONE', *, *, #211283, .F. ) ;
#135095=LINE ( 'NONE', #239353, #35456 ) ;
#135113=ORIENTED_EDGE ( 'NONE', *, *, #246306, .F. ) ;
#135119=CARTESIAN_POINT ( 'NONE',  ( 20.95392731769792150, 67.11693852082312617, -94.50087950495306188 ) ) ;
#135121=AXIS2_PLACEMENT_3D ( 'NONE', #110738, #11664, #212429 ) ;
#135124=ORIENTED_EDGE ( 'NONE', *, *, #135771, .F. ) ;
#135133=CARTESIAN_POINT ( 'NONE',  ( -21.05000000000000071, 70.15000000001192859, -92.89061026024637613 ) ) ;
#135160=DIRECTION ( 'NONE',  ( 0.000000000000000000, 0.000000000000000000, 1.000000000000000000 ) ) ;
#135178=ORIENTED_EDGE ( 'NONE', *, *, #127172, .F. ) ;
#135190=CARTESIAN_POINT ( 'NONE',  ( 20.94999999999999929, 76.00000000001173817, -72.42310748452430857 ) ) ;
#135233=AXIS2_PLACEMENT_3D ( 'NONE', #73166, #31473, #110978 ) ;
#135267=ORIENTED_EDGE ( 'NONE', *, *, #66709, .T. ) ;
#135277=CARTESIAN_POINT ( 'NONE',  ( -20.94999999999999929, 76.00000000001173817, -73.62310748452429721 ) ) ;
#135290=ADVANCED_FACE ( 'NONE', ( #139935 ), #1345, .T. ) ;
#135294=AXIS2_PLACEMENT_3D ( 'NONE', #36526, #22081, #216406 ) ;
#135309=DIRECTION ( 'NONE',  ( -0.000000000000000000, -1.000000000000000000, -6.982962677686266711E-15 ) ) ;
#135351=CARTESIAN_POINT ( 'NONE',  ( 21.05000000000000071, 69.52244781751849700, -102.9231075192248142 ) ) ;
#135352=VERTEX_POINT ( 'NONE', #198642 ) ;
#135371=ORIENTED_EDGE ( 'NONE', *, *, #58745, .F. ) ;
#135373=EDGE_CURVE ( 'NONE', #10090, #29906, #234583, .T. ) ;
#135382=DIRECTION ( 'NONE',  ( -1.000000000000000000, 0.000000000000000000, -0.000000000000000000 ) ) ;
#135392=CARTESIAN_POINT ( 'NONE',  ( -21.52071067811865746, 68.22071067813045886, -81.77310748452435973 ) ) ;
#135408=( BOUNDED_SURFACE ( )  B_SPLINE_SURFACE ( 3, 2, ( 
 ( #91397, #189215, #31455 ),
 ( #10582, #34025, #170979 ),
 ( #9284, #52242, #131797 ),
 ( #133090, #212635, #113521 ),
 ( #168414, #148808, #228342 ),
 ( #186195, #167940, #147044 ) ),
 .UNSPECIFIED., .F., .F., .F. ) 
 B_SPLINE_SURFACE_WITH_KNOTS ( ( 4, 2, 4 ),
 ( 3, 3 ),
 ( 0.0001300404313046710908, 0.0003183318589266775434, 0.0005066232865486839688 ),
 ( 0.000000000000000000, 1.000000000000000000 ),
 .UNSPECIFIED. ) 
 GEOMETRIC_REPRESENTATION_ITEM ( )  RATIONAL_B_SPLINE_SURFACE ( (
 ( 1.000000000000000000, 0.7071067811865966446, 1.000000000000000000),
 ( 1.000000000000000000, 0.7625113560540166535, 1.000000000000000000),
 ( 1.000000000000000000, 0.8126073484687468262, 1.000000000000000000),
 ( 1.000000000000000000, 0.8923049332733752337, 1.000000000000000000),
 ( 1.000000000000000000, 0.9231914937768672669, 1.000000000000000000),
 ( 1.000000000000000000, 0.9238795325112946211, 1.000000000000000000) ) ) 
 REPRESENTATION_ITEM ( '' )  SURFACE ( )  );
#135410=DIRECTION ( 'NONE',  ( 1.000000000000000000, 0.000000000000000000, 0.000000000000000000 ) ) ;
#135443=CARTESIAN_POINT ( 'NONE',  ( -18.59999999999999787, 77.16412189325286874, -61.60825939895269698 ) ) ;
#135457=CARTESIAN_POINT ( 'NONE',  ( -20.54999999999999716, 73.50000000001180922, -82.74772940728642823 ) ) ;
#135461=DIRECTION ( 'NONE',  ( -7.304098846218134667E-16, 1.000000000000000000, 6.982962677686267499E-15 ) ) ;
#135463=DIRECTION ( 'NONE',  ( -2.602085213965226419E-14, -6.982962677686266711E-15, 1.000000000000000000 ) ) ;
#135467=FACE_OUTER_BOUND ( 'NONE', #54962, .T. ) ;
#135472=SPHERICAL_SURFACE ( 'NONE', #232027, 0.1000000000000000056 ) ;
#135494=AXIS2_PLACEMENT_3D ( 'NONE', #106249, #227493, #107547 ) ;
#135522=TOROIDAL_SURFACE ( 'NONE', #106459, 11.65000000000000036, 0.1000000000000000056 ) ;
#135570=EDGE_LOOP ( 'NONE', ( #129822, #252205 ) ) ;
#135571=FACE_OUTER_BOUND ( 'NONE', #148127, .T. ) ;
#135588=ORIENTED_EDGE ( 'NONE', *, *, #197169, .T. ) ;
#135607=EDGE_CURVE ( 'NONE', #35640, #254886, #209844, .T. ) ;
#135625=CIRCLE ( 'NONE', #15418, 0.1000000000000028644 ) ;
#135642=CARTESIAN_POINT ( 'NONE',  ( 20.85000000000000142, 77.13501884592184865, -61.80613060109197932 ) ) ;
#135662=ORIENTED_EDGE ( 'NONE', *, *, #272, .F. ) ;
#135666=ORIENTED_EDGE ( 'NONE', *, *, #80247, .F. ) ;
#135704=ORIENTED_EDGE ( 'NONE', *, *, #139781, .T. ) ;
#135742=EDGE_CURVE ( 'NONE', #48831, #6502, #213924, .T. ) ;
#135771=EDGE_CURVE ( 'NONE', #216625, #74147, #3655, .T. ) ;
#135774=CARTESIAN_POINT ( 'NONE',  ( 20.94999999999999929, 70.50000000001180922, -81.92837350343744163 ) ) ;
#135781=EDGE_LOOP ( 'NONE', ( #185905, #137717, #81882, #251054 ) ) ;
#135791=AXIS2_PLACEMENT_3D ( 'NONE', #10073, #28396, #89597 ) ;
#135796=ORIENTED_EDGE ( 'NONE', *, *, #142649, .T. ) ;
#135812=DIRECTION ( 'NONE',  ( -1.000000000000000000, -0.000000000000000000, -0.000000000000000000 ) ) ;
#135879=AXIS2_PLACEMENT_3D ( 'NONE', #209486, #206927, #128685 ) ;
#135905=ADVANCED_FACE ( 'NONE', ( #256189 ), #214116, .T. ) ;
#135912=CIRCLE ( 'NONE', #160890, 4.049999999999998046 ) ;
#135919=DIRECTION ( 'NONE',  ( 0.000000000000000000, 1.000000000000000000, 6.982962677686266711E-15 ) ) ;
#135922=CARTESIAN_POINT ( 'NONE',  ( 21.05000000000000071, 65.27628288308574156, -90.84686788338628105 ) ) ;
#135932=LINE ( 'NONE', #175131, #17675 ) ;
#135957=FACE_OUTER_BOUND ( 'NONE', #31283, .T. ) ;
#135959=FACE_OUTER_BOUND ( 'NONE', #144193, .T. ) ;
#135967=ORIENTED_EDGE ( 'NONE', *, *, #222237, .T. ) ;
#135996=DIRECTION ( 'NONE',  ( 1.000000000000000000, -3.265361837132813093E-16, -2.280189983783949500E-30 ) ) ;
#136011=CARTESIAN_POINT ( 'NONE',  ( 22.48660254037844197, 64.35000000001194564, -103.0731074845243853 ) ) ;
#136019=DIRECTION ( 'NONE',  ( 0.000000000000000000, -0.5000000000000209832, 0.8660254037844264952 ) ) ;
#136086=ORIENTED_EDGE ( 'NONE', *, *, #150197, .F. ) ;
#136101=LINE ( 'NONE', #257307, #139681 ) ;
#136107=EDGE_CURVE ( 'NONE', #108305, #61048, #22588, .T. ) ;
#136120=CIRCLE ( 'NONE', #173639, 0.1000000000000028644 ) ;
#136125=CARTESIAN_POINT ( 'NONE',  ( -20.54999999999999716, 76.00000000001169553, -67.52310748452430289 ) ) ;
#136126=DIRECTION ( 'NONE',  ( 0.000000000000000000, 1.000000000000000000, 0.000000000000000000 ) ) ;
#136142=DIRECTION ( 'NONE',  ( 0.000000000000000000, 0.000000000000000000, 1.000000000000000000 ) ) ;
#136157=DIRECTION ( 'NONE',  ( 1.000000000000000000, 0.000000000000000000, 0.000000000000000000 ) ) ;
#136204=DIRECTION ( 'NONE',  ( 1.000000000000000000, 0.000000000000000000, 0.000000000000000000 ) ) ;
#136231=EDGE_CURVE ( 'NONE', #101606, #195198, #27062, .T. ) ;
#136237=AXIS2_PLACEMENT_3D ( 'NONE', #95985, #238071, #77702 ) ;
#136257=ORIENTED_EDGE ( 'NONE', *, *, #115686, .T. ) ;
#136266=DIRECTION ( 'NONE',  ( 1.000000000000000000, 0.000000000000000000, 0.000000000000000000 ) ) ;
#136293=EDGE_LOOP ( 'NONE', ( #253998, #1802, #192972 ) ) ;
#136328=AXIS2_PLACEMENT_3D ( 'NONE', #173190, #32380, #209700 ) ;
#136346=CIRCLE ( 'NONE', #23980, 0.1000000000000028644 ) ;
#136360=FACE_OUTER_BOUND ( 'NONE', #8362, .T. ) ;
#136387=LINE ( 'NONE', #154733, #69348 ) ;
#136413=VECTOR ( 'NONE', #125829, 1000.000000000000000 ) ;
#136414=ORIENTED_EDGE ( 'NONE', *, *, #207751, .F. ) ;
#136438=ORIENTED_EDGE ( 'NONE', *, *, #247646, .F. ) ;
#136482=VERTEX_POINT ( 'NONE', #180903 ) ;
#136484=VECTOR ( 'NONE', #244418, 1000.000000000000000 ) ;
#136486=AXIS2_PLACEMENT_3D ( 'NONE', #12694, #252544, #233020 ) ;
#136489=ORIENTED_EDGE ( 'NONE', *, *, #37492, .F. ) ;
#136505=ORIENTED_EDGE ( 'NONE', *, *, #150368, .T. ) ;
#136513=ADVANCED_FACE ( 'NONE', ( #179634 ), #64457, .T. ) ;
#136520=ORIENTED_EDGE ( 'NONE', *, *, #138319, .T. ) ;
#136529=DIRECTION ( 'NONE',  ( 0.000000000000000000, 0.000000000000000000, 1.000000000000000000 ) ) ;
#136560=ORIENTED_EDGE ( 'NONE', *, *, #173175, .T. ) ;
#136562=DIRECTION ( 'NONE',  ( 2.952720810173289112E-16, 1.000000000000000000, 6.308085367188367561E-15 ) ) ;
#136664=DIRECTION ( 'NONE',  ( 0.000000000000000000, -1.000000000000000000, -6.860497997771532351E-15 ) ) ;
#136678=DIRECTION ( 'NONE',  ( 0.000000000000000000, -7.147358527629762208E-15, 1.000000000000000000 ) ) ;
#136694=EDGE_CURVE ( 'NONE', #212250, #20048, #117224, .T. ) ;
#136698=CYLINDRICAL_SURFACE ( 'NONE', #247624, 0.09999999999999939493 ) ;
#136706=EDGE_LOOP ( 'NONE', ( #102311, #34178, #257416, #226177, #155190, #242871, #72197, #204792, #91394, #98882, #140563, #146861, #111633, #16184, #193423, #76606, #85748, #107718, #106909, #233582, #144638, #242832, #157979, #55963, #177409, #167962, #210069 ) ) ;
#136713=DIRECTION ( 'NONE',  ( -0.000000000000000000, 1.000000000000000000, 6.352154140967427193E-15 ) ) ;
#136727=CARTESIAN_POINT ( 'NONE',  ( -20.64999999999999858, 71.75000000001186606, -90.77310748452434552 ) ) ;
#136733=CIRCLE ( 'NONE', #132470, 0.3999999999999975797 ) ;
#136767=DIRECTION ( 'NONE',  ( 0.000000000000000000, -1.000000000000000000, 0.000000000000000000 ) ) ;
#136808=CARTESIAN_POINT ( 'NONE',  ( 21.12769345151713196, 65.28071232307129890, -90.77562713832689667 ) ) ;
#136814=EDGE_LOOP ( 'NONE', ( #103231, #160471, #214358, #59381 ) ) ;
#136847=CARTESIAN_POINT ( 'NONE',  ( -18.59999999999999787, 74.14897176987101091, -91.36919421510182815 ) ) ;
#136861=CARTESIAN_POINT ( 'NONE',  ( 20.94999999999999929, 65.27628289530437655, -95.35819391543677170 ) ) ;
#136875=CARTESIAN_POINT ( 'NONE',  ( 23.24999999999999289, 69.55000000001186322, -90.67310748452435121 ) ) ;
#136893=DIRECTION ( 'NONE',  ( 0.000000000000000000, 1.000000000000000000, 0.000000000000000000 ) ) ;
#136899=ORIENTED_EDGE ( 'NONE', *, *, #118914, .T. ) ;
#136924=DIRECTION ( 'NONE',  ( -3.469446951953515108E-14, 1.000000000000000000, 0.000000000000000000 ) ) ;
#136959=ORIENTED_EDGE ( 'NONE', *, *, #23549, .T. ) ;
#136972=VERTEX_POINT ( 'NONE', #60320 ) ;
#136979=AXIS2_PLACEMENT_3D ( 'NONE', #116029, #255469, #213829 ) ;
#136986=DIRECTION ( 'NONE',  ( 0.000000000000000000, 0.000000000000000000, 1.000000000000000000 ) ) ;
#137053=CARTESIAN_POINT ( 'NONE',  ( 21.59780538579342135, 75.90102133041401089, -109.8701980144675616 ) ) ;
#137084=ADVANCED_FACE ( 'NONE', ( #146277 ), #101120, .T. ) ;
#137123=FACE_OUTER_BOUND ( 'NONE', #135570, .T. ) ;
#137127=CARTESIAN_POINT ( 'NONE',  ( 23.14999999999999503, 64.35000000001178933, -81.67310748452439384 ) ) ;
#137148=LINE ( 'NONE', #60165, #195625 ) ;
#137203=EDGE_CURVE ( 'NONE', #118409, #16439, #181362, .T. ) ;
#137223=CARTESIAN_POINT ( 'NONE',  ( 21.09793522318408066, 65.27537548979908877, -90.78381661354731591 ) ) ;
#137224=DIRECTION ( 'NONE',  ( 0.000000000000000000, -7.172728831056617961E-15, 1.000000000000000000 ) ) ;
#137227=VECTOR ( 'NONE', #28827, 1000.000000000000000 ) ;
#137257=DIRECTION ( 'NONE',  ( 4.239556034732056743E-17, 0.1298341882519953860, 0.9915357197604862671 ) ) ;
#137269=CARTESIAN_POINT ( 'NONE',  ( 21.05000000000000071, 76.00000000001173817, -73.62310748452429721 ) ) ;
#137280=CIRCLE ( 'NONE', #233176, 0.1000000000000028644 ) ;
#137295=AXIS2_PLACEMENT_3D ( 'NONE', #182571, #123874, #140863 ) ;
#137303=DIRECTION ( 'NONE',  ( 1.000000000000000000, 0.000000000000000000, 0.000000000000000000 ) ) ;
#137309=CARTESIAN_POINT ( 'NONE',  ( -23.15000000000000213, 87.48912529308779540, -72.52310748452423184 ) ) ;
#137331=ORIENTED_EDGE ( 'NONE', *, *, #14933, .T. ) ;
#137374=ORIENTED_EDGE ( 'NONE', *, *, #127131, .F. ) ;
#137380=EDGE_LOOP ( 'NONE', ( #162770, #24434, #199505, #84467 ) ) ;
#137390=EDGE_CURVE ( 'NONE', #190614, #98928, #84206, .T. ) ;
#137442=CARTESIAN_POINT ( 'NONE',  ( 20.94999999999999574, 87.48912529308798014, -99.92310748452423752 ) ) ;
#137462=DIRECTION ( 'NONE',  ( 0.000000000000000000, -1.000000000000000000, -6.982962677686265922E-15 ) ) ;
#137488=CYLINDRICAL_SURFACE ( 'NONE', #81809, 0.5000000000000004441 ) ;
#137513=CARTESIAN_POINT ( 'NONE',  ( -18.59999999999999787, 77.83534155023627932, -91.46795619196132066 ) ) ;
#137528=CARTESIAN_POINT ( 'NONE',  ( 23.14999999999998437, 76.00000000001195133, -103.0231074845243171 ) ) ;
#137588=ORIENTED_EDGE ( 'NONE', *, *, #242838, .T. ) ;
#137602=ORIENTED_EDGE ( 'NONE', *, *, #117614, .F. ) ;
#137616=EDGE_CURVE ( 'NONE', #192382, #98928, #205043, .T. ) ;
#137659=TOROIDAL_SURFACE ( 'NONE', #171067, 0.6000000000000013101, 0.1000000000000000056 ) ;
#137688=EDGE_CURVE ( 'NONE', #112762, #226125, #216201, .T. ) ;
#137705=EDGE_CURVE ( 'NONE', #225321, #22313, #80125, .T. ) ;
#137717=ORIENTED_EDGE ( 'NONE', *, *, #137203, .T. ) ;
#137751=CARTESIAN_POINT ( 'NONE',  ( -21.14999999999999503, 64.25000000001190870, -96.10396023856559111 ) ) ;
#137754=AXIS2_PLACEMENT_3D ( 'NONE', #79938, #18719, #57824 ) ;
#137779=CIRCLE ( 'NONE', #87878, 0.09999999999999939493 ) ;
#137828=ADVANCED_FACE ( 'NONE', ( #8725 ), #255267, .T. ) ;
#137829=CARTESIAN_POINT ( 'NONE',  ( 18.59999999999999432, 77.16270174994990327, -94.92310748452430857 ) ) ;
#137843=DIRECTION ( 'NONE',  ( 0.000000000000000000, 0.000000000000000000, 1.000000000000000000 ) ) ;
#137866=CARTESIAN_POINT ( 'NONE',  ( 18.50000972452444969, 65.70673848566940478, -64.06382523348294455 ) ) ;
#137886=EDGE_CURVE ( 'NONE', #225625, #170631, #208222, .T. ) ;
#137893=EDGE_CURVE ( 'NONE', #221695, #38211, #92810, .T. ) ;
#137917=CARTESIAN_POINT ( 'NONE',  ( 20.84999999999998721, 65.66751761918648356, -63.92826094061123143 ) ) ;
#137918=CARTESIAN_POINT ( 'NONE',  ( -21.14999999999999858, 64.35000000001195986, -103.0231074845244024 ) ) ;
#137982=ORIENTED_EDGE ( 'NONE', *, *, #134961, .T. ) ;
#138002=FACE_OUTER_BOUND ( 'NONE', #87097, .T. ) ;
#138006=EDGE_CURVE ( 'NONE', #35640, #25250, #159799, .T. ) ;
#138021=ORIENTED_EDGE ( 'NONE', *, *, #188635, .T. ) ;
#138030=PLANE ( 'NONE',  #184983 ) ;
#138037=DIRECTION ( 'NONE',  ( 0.000000000000000000, -6.608470384673536824E-15, 1.000000000000000000 ) ) ;
#138051=ADVANCED_FACE ( 'NONE', ( #180638, #39865 ), #158527, .F. ) ;
#138067=DIRECTION ( 'NONE',  ( 0.000000000000000000, -7.056502275159890043E-15, 1.000000000000000000 ) ) ;
#138100=VERTEX_POINT ( 'NONE', #41148 ) ;
#138113=ORIENTED_EDGE ( 'NONE', *, *, #142003, .F. ) ;
#138119=AXIS2_PLACEMENT_3D ( 'NONE', #2020, #22915, #144100 ) ;
#138125=FACE_OUTER_BOUND ( 'NONE', #136706, .T. ) ;
#138135=DIRECTION ( 'NONE',  ( -3.265361837132813093E-16, -1.000000000000000000, -6.982962677686266711E-15 ) ) ;
#138164=EDGE_LOOP ( 'NONE', ( #189996, #159144, #60784, #256417 ) ) ;
#138181=CARTESIAN_POINT ( 'NONE',  ( -23.15000000000000213, 84.66355140188105111, -93.49900636645693908 ) ) ;
#138228=ORIENTED_EDGE ( 'NONE', *, *, #138962, .T. ) ;
#138229=PLANE ( 'NONE',  #49220 ) ;
#138319=EDGE_CURVE ( 'NONE', #185475, #83116, #122239, .T. ) ;
#138329=CARTESIAN_POINT ( 'NONE',  ( -20.94999999999999929, 61.95000000001175522, -75.03680255528533394 ) ) ;
#138373=DIRECTION ( 'NONE',  ( 0.000000000000000000, -6.467318590049456648E-15, 1.000000000000000000 ) ) ;
#138376=FACE_OUTER_BOUND ( 'NONE', #163649, .T. ) ;
#138447=ORIENTED_EDGE ( 'NONE', *, *, #174886, .T. ) ;
#138460=ORIENTED_EDGE ( 'NONE', *, *, #99131, .T. ) ;
#138523=ORIENTED_EDGE ( 'NONE', *, *, #184480, .T. ) ;
#138532=DIRECTION ( 'NONE',  ( 0.000000000000000000, -1.000000000000000000, -6.860497997771531562E-15 ) ) ;
#138537=CARTESIAN_POINT ( 'NONE',  ( 22.50000000000000000, 64.35042919246716053, -103.1231074845243825 ) ) ;
#138570=AXIS2_PLACEMENT_3D ( 'NONE', #177943, #224431, #257403 ) ;
#138577=VECTOR ( 'NONE', #78931, 999.9999999999998863 ) ;
#138594=DIRECTION ( 'NONE',  ( 0.000000000000000000, -1.000000000000000000, -6.982962677686267499E-15 ) ) ;
#138602=DIRECTION ( 'NONE',  ( 1.000000000000000000, 0.000000000000000000, 0.000000000000000000 ) ) ;
#138611=DIRECTION ( 'NONE',  ( -0.000000000000000000, -0.1350103645451718737, 0.9908441862701622416 ) ) ;
#138645=DIRECTION ( 'NONE',  ( 0.000000000000000000, -6.608470384673536824E-15, 1.000000000000000000 ) ) ;
#138658=DIRECTION ( 'NONE',  ( 0.000000000000000000, 1.000000000000000000, 6.352154140967427193E-15 ) ) ;
#138677=ORIENTED_EDGE ( 'NONE', *, *, #175080, .T. ) ;
#138688=DIRECTION ( 'NONE',  ( 1.000000000000000000, 0.000000000000000000, 0.000000000000000000 ) ) ;
#138692=DIRECTION ( 'NONE',  ( 0.000000000000000000, 1.000000000000000000, 0.000000000000000000 ) ) ;
#138693=ORIENTED_EDGE ( 'NONE', *, *, #143849, .F. ) ;
#138700=VECTOR ( 'NONE', #168105, 1000.000000000000000 ) ;
#138708=DIRECTION ( 'NONE',  ( 1.000000000000000000, 0.000000000000000000, 0.000000000000000000 ) ) ;
#138709=DIRECTION ( 'NONE',  ( -1.000000000000000000, -4.163336342344362270E-13, 0.000000000000000000 ) ) ;
#138749=DIRECTION ( 'NONE',  ( 0.000000000000000000, -7.086529944415894657E-15, 1.000000000000000000 ) ) ;
#138775=DIRECTION ( 'NONE',  ( 1.000000000000000000, 0.000000000000000000, 0.000000000000000000 ) ) ;
#138841=DIRECTION ( 'NONE',  ( 1.000000000000000000, 0.000000000000000000, 0.000000000000000000 ) ) ;
#138843=CARTESIAN_POINT ( 'NONE',  ( -22.50000000000000000, 64.35000000001197407, -103.0231074845244024 ) ) ;
#138860=CARTESIAN_POINT ( 'NONE',  ( -20.85000000000000142, 77.25000000001165290, -61.72262673010921930 ) ) ;
#138962=EDGE_CURVE ( 'NONE', #97650, #167682, #168450, .T. ) ;
#138964=EDGE_CURVE ( 'NONE', #75696, #87867, #180294, .T. ) ;
#138966=ORIENTED_EDGE ( 'NONE', *, *, #160448, .F. ) ;
#138976=CIRCLE ( 'NONE', #5718, 0.09999999999999939493 ) ;
#138979=CIRCLE ( 'NONE', #214040, 0.09999999999999939493 ) ;
#139022=CARTESIAN_POINT ( 'NONE',  ( 20.94999999999999929, 76.00000000001170974, -69.52310748452431710 ) ) ;
#139052=LINE ( 'NONE', #59520, #41641 ) ;
#139067=AXIS2_PLACEMENT_3D ( 'NONE', #222978, #191263, #44370 ) ;
#139177=ORIENTED_EDGE ( 'NONE', *, *, #101734, .F. ) ;
#139205=DIRECTION ( 'NONE',  ( -0.7070776581708965169, 0.7071359030027827286, 4.937903618720407826E-15 ) ) ;
#139214=FACE_OUTER_BOUND ( 'NONE', #181599, .T. ) ;
#139230=EDGE_CURVE ( 'NONE', #151730, #237924, #122624, .T. ) ;
#139236=ORIENTED_EDGE ( 'NONE', *, *, #257903, .T. ) ;
#139245=FACE_OUTER_BOUND ( 'NONE', #203682, .T. ) ;
#139283=ORIENTED_EDGE ( 'NONE', *, *, #130601, .F. ) ;
#139308=CARTESIAN_POINT ( 'NONE',  ( 20.84999999999999787, 64.25000000001175238, -76.44225473048308572 ) ) ;
#139321=ORIENTED_EDGE ( 'NONE', *, *, #191581, .F. ) ;
#139341=CARTESIAN_POINT ( 'NONE',  ( 20.94999999999999929, 77.83585931145526615, -58.01866831572577610 ) ) ;
#139365=CIRCLE ( 'NONE', #218468, 0.1000000000000017680 ) ;
#139370=LINE ( 'NONE', #241085, #190685 ) ;
#139372=DIRECTION ( 'NONE',  ( 0.000000000000000000, 0.000000000000000000, -1.000000000000000000 ) ) ;
#139391=ORIENTED_EDGE ( 'NONE', *, *, #15675, .F. ) ;
#139415=MECHANICAL_DESIGN_GEOMETRIC_PRESENTATION_REPRESENTATION('',(#97888),#106444);
#139416=CARTESIAN_POINT ( 'NONE',  ( 19.97071067811864609, 64.27928932189311695, -78.37310748452439668 ) ) ;
#139432=AXIS2_PLACEMENT_3D ( 'NONE', #75398, #53238, #170671 ) ;
#139441=ORIENTED_EDGE ( 'NONE', *, *, #142453, .F. ) ;
#139447=AXIS2_PLACEMENT_3D ( 'NONE', #163308, #81170, #125466 ) ;
#139455=CIRCLE ( 'NONE', #206114, 11.80000000000000426 ) ;
#139499=EDGE_CURVE ( 'NONE', #127649, #141595, #205389, .T. ) ;
#139507=AXIS2_PLACEMENT_3D ( 'NONE', #46047, #106001, #168631 ) ;
#139522=AXIS2_PLACEMENT_3D ( 'NONE', #214916, #132830, #72880 ) ;
#139524=CYLINDRICAL_SURFACE ( 'NONE', #107491, 0.09999999999999939493 ) ;
#139530=CIRCLE ( 'NONE', #102092, 11.64999999999999325 ) ;
#139540=ORIENTED_EDGE ( 'NONE', *, *, #100669, .F. ) ;
#139557=ORIENTED_EDGE ( 'NONE', *, *, #183465, .F. ) ;
#139572=ORIENTED_EDGE ( 'NONE', *, *, #2902, .F. ) ;
#139585=AXIS2_PLACEMENT_3D ( 'NONE', #6624, #245254, #9197 ) ;
#139604=AXIS2_PLACEMENT_3D ( 'NONE', #194206, #217569, #138037 ) ;
#139631=CIRCLE ( 'NONE', #214654, 0.1000000000000043771 ) ;
#139635=FACE_OUTER_BOUND ( 'NONE', #235304, .T. ) ;
#139647=ADVANCED_FACE ( 'NONE', ( #119123 ), #1387, .T. ) ;
#139667=CARTESIAN_POINT ( 'NONE',  ( 18.59999999999999432, 74.83729825007388570, -95.02310748452431710 ) ) ;
#139681=VECTOR ( 'NONE', #218211, 1000.000000000000000 ) ;
#139689=( NAMED_UNIT ( * ) SI_UNIT ( $, .STERADIAN. ) SOLID_ANGLE_UNIT ( ) );
#139733=DIRECTION ( 'NONE',  ( 0.000000000000000000, 0.000000000000000000, 1.000000000000000000 ) ) ;
#139735=CARTESIAN_POINT ( 'NONE',  ( -21.93340585899446182, 76.00000000001200817, -110.3472545066445178 ) ) ;
#139738=DIRECTION ( 'NONE',  ( 1.000000000000000000, 0.000000000000000000, 0.000000000000000000 ) ) ;
#139752=CIRCLE ( 'NONE', #56537, 0.1000000000000009492 ) ;
#139781=EDGE_CURVE ( 'NONE', #185034, #27505, #174847, .T. ) ;
#139803=ORIENTED_EDGE ( 'NONE', *, *, #33527, .F. ) ;
#139808=FACE_OUTER_BOUND ( 'NONE', #153505, .T. ) ;
#139825=PLANE ( 'NONE',  #114888 ) ;
#139828=ORIENTED_EDGE ( 'NONE', *, *, #130824, .T. ) ;
#139835=EDGE_LOOP ( 'NONE', ( #75662, #17693, #113399, #23394 ) ) ;
#139845=ORIENTED_EDGE ( 'NONE', *, *, #201137, .T. ) ;
#139870=DIRECTION ( 'NONE',  ( 0.000000000000000000, -0.3738317757008748909, -0.9274965247785733613 ) ) ;
#139882=CARTESIAN_POINT ( 'NONE',  ( -18.43459694179559349, 85.49421012500970107, -62.90610228186317698 ) ) ;
#139923=ORIENTED_EDGE ( 'NONE', *, *, #119723, .F. ) ;
#139935=FACE_OUTER_BOUND ( 'NONE', #231263, .T. ) ;
#139947=DIRECTION ( 'NONE',  ( 1.000000000000000000, 0.000000000000000000, 0.000000000000000000 ) ) ;
#139993=VECTOR ( 'NONE', #160035, 1000.000000000000000 ) ;
#140019=CARTESIAN_POINT ( 'NONE',  ( 20.97107704358301916, 67.12452184799060717, -94.46413425513512152 ) ) ;
#140049=AXIS2_PLACEMENT_3D ( 'NONE', #256131, #93270, #116686 ) ;
#140050=VERTEX_POINT ( 'NONE', #31515 ) ;
#140070=EDGE_CURVE ( 'NONE', #57915, #143626, #217686, .T. ) ;
#140088=LINE ( 'NONE', #60558, #54969 ) ;
#140122=DIRECTION ( 'NONE',  ( 0.000000000000000000, 0.1568667991644355497, 0.9876197685951332295 ) ) ;
#140174=DIRECTION ( 'NONE',  ( 0.7071359030027419834, 0.000000000000000000, -0.7070776581709371511 ) ) ;
#140184=CARTESIAN_POINT ( 'NONE',  ( -20.94999999999999929, 74.16465844978745281, -91.46795619196133487 ) ) ;
#140201=AXIS2_PLACEMENT_3D ( 'NONE', #59072, #138611, #13576 ) ;
#140220=AXIS2_PLACEMENT_3D ( 'NONE', #141313, #157041, #198713 ) ;
#140302=ADVANCED_FACE ( 'NONE', ( #22209 ), #125153, .F. ) ;
#140325=AXIS2_PLACEMENT_3D ( 'NONE', #2709, #178832, #242612 ) ;
#140343=VERTEX_POINT ( 'NONE', #169446 ) ;
#140361=CARTESIAN_POINT ( 'NONE',  ( 22.32929514600007792, 68.42135243463546601, -103.1221831626382794 ) ) ;
#140363=CARTESIAN_POINT ( 'NONE',  ( 21.12757541349815682, 69.52661942876049750, -103.0282687003341096 ) ) ;
#140364=AXIS2_PLACEMENT_3D ( 'NONE', #250845, #58734, #118758 ) ;
#140387=CARTESIAN_POINT ( 'NONE',  ( -20.94999999999999929, 64.40000000001190017, -96.09490425424884563 ) ) ;
#140399=DIRECTION ( 'NONE',  ( 1.000000000000000000, 0.000000000000000000, 0.000000000000000000 ) ) ;
#140409=TOROIDAL_SURFACE ( 'NONE', #40509, 0.4000000000000005773, 0.1000000000000000056 ) ;
#140416=EDGE_LOOP ( 'NONE', ( #59953, #61222, #112976, #81467 ) ) ;
#140438=ADVANCED_FACE ( 'NONE', ( #52002 ), #211099, .F. ) ;
#140439=CARTESIAN_POINT ( 'NONE',  ( 18.51024323315077069, 65.68895814178219439, -64.00265578621379348 ) ) ;
#140446=DIRECTION ( 'NONE',  ( 0.000000000000000000, -6.652207440891584540E-15, 1.000000000000000000 ) ) ;
#140454=FACE_OUTER_BOUND ( 'NONE', #95657, .T. ) ;
#140494=DIRECTION ( 'NONE',  ( -1.000000000000000000, -0.000000000000000000, -0.000000000000000000 ) ) ;
#140511=AXIS2_PLACEMENT_3D ( 'NONE', #195499, #58502, #136767 ) ;
#140527=CARTESIAN_POINT ( 'NONE',  ( -21.00448002041605733, 64.25000000001189449, -96.17476662221315564 ) ) ;
#140528=TOROIDAL_SURFACE ( 'NONE', #198801, 11.65000000000000036, 0.1000000000000000056 ) ;
#140540=CIRCLE ( 'NONE', #115603, 0.1000000000000028783 ) ;
#140561=FACE_OUTER_BOUND ( 'NONE', #31940, .T. ) ;
#140563=ORIENTED_EDGE ( 'NONE', *, *, #113471, .F. ) ;
#140589=DIRECTION ( 'NONE',  ( 0.000000000000000000, -6.547589603894048205E-15, 1.000000000000000000 ) ) ;
#140598=DIRECTION ( 'NONE',  ( 6.938893903907030216E-14, 0.000000000000000000, -1.000000000000000000 ) ) ;
#140604=DIRECTION ( 'NONE',  ( -1.000000000000000000, 0.000000000000000000, -0.000000000000000000 ) ) ;
#140637=DIRECTION ( 'NONE',  ( 0.000000000000000000, -6.982962677686266711E-15, 1.000000000000000000 ) ) ;
#140647=ORIENTED_EDGE ( 'NONE', *, *, #34925, .F. ) ;
#140688=CARTESIAN_POINT ( 'NONE',  ( -20.54999999999999716, 71.65000000001180069, -81.87310748452433984 ) ) ;
#140707=VECTOR ( 'NONE', #61276, 1000.000000000000000 ) ;
#140718=AXIS2_PLACEMENT_3D ( 'NONE', #56641, #157083, #80053 ) ;
#140751=CARTESIAN_POINT ( 'NONE',  ( 23.14999999999998437, 80.05000000001194849, -103.0231074845242887 ) ) ;
#140770=VECTOR ( 'NONE', #244894, 1000.000000000000000 ) ;
#140784=EDGE_CURVE ( 'NONE', #8311, #92109, #31233, .T. ) ;
#140793=ORIENTED_EDGE ( 'NONE', *, *, #144395, .T. ) ;
#140804=DIRECTION ( 'NONE',  ( 0.000000000000000000, -6.982962677686266711E-15, 1.000000000000000000 ) ) ;
#140824=AXIS2_PLACEMENT_3D ( 'NONE', #82100, #117407, #61286 ) ;
#140863=DIRECTION ( 'NONE',  ( 0.000000000000000000, 0.000000000000000000, 1.000000000000000000 ) ) ;
#140867=CARTESIAN_POINT ( 'NONE',  ( 23.15000000000000213, 87.48912529308779540, -72.62310748452422615 ) ) ;
#140889=VERTEX_POINT ( 'NONE', #199905 ) ;
#140911=ORIENTED_EDGE ( 'NONE', *, *, #135742, .F. ) ;
#140940=EDGE_CURVE ( 'NONE', #152727, #154309, #36992, .T. ) ;
#140995=AXIS2_PLACEMENT_3D ( 'NONE', #217667, #216405, #36525 ) ;
#141000=EDGE_LOOP ( 'NONE', ( #61063, #171823, #32275, #232637 ) ) ;
#141076=LINE ( 'NONE', #142342, #23871 ) ;
#141086=CARTESIAN_POINT ( 'NONE',  ( 21.14999999999999858, 64.25000000001193712, -102.9231074845243938 ) ) ;
#141096=CARTESIAN_POINT ( 'NONE',  ( 22.00356870070003978, 76.00000000000741807, -110.2773498462693595 ) ) ;
#141121=TOROIDAL_SURFACE ( 'NONE', #41170, 11.65000000000000036, 0.1000000000000000056 ) ;
#141124=CIRCLE ( 'NONE', #62003, 0.09999999999999939493 ) ;
#141143=CARTESIAN_POINT ( 'NONE',  ( -23.25000000000000000, 74.08971962618002749, -82.15447533972326255 ) ) ;
#141180=CARTESIAN_POINT ( 'NONE',  ( 23.14999999999999147, 71.85000000001194564, -103.0231074845243455 ) ) ;
#141229=CARTESIAN_POINT ( 'NONE',  ( -18.59999999999999787, 64.35000000001187459, -90.77310748452440237 ) ) ;
#141234=DIRECTION ( 'NONE',  ( 1.734723475976817507E-14, 1.000000000000000000, 6.982962677686266711E-15 ) ) ;
#141268=FACE_OUTER_BOUND ( 'NONE', #48635, .T. ) ;
#141270=AXIS2_PLACEMENT_3D ( 'NONE', #240849, #219988, #98719 ) ;
#141276=CARTESIAN_POINT ( 'NONE',  ( -18.59999999999999787, 68.97833521811159585, -65.78954208262706516 ) ) ;
#141304=CARTESIAN_POINT ( 'NONE',  ( -18.59999999999999787, 70.65875701002036635, -112.8297576910123752 ) ) ;
#141313=CARTESIAN_POINT ( 'NONE',  ( 22.39999999999999503, 64.35000000001194564, -103.1231074845243825 ) ) ;
#141396=CARTESIAN_POINT ( 'NONE',  ( 18.49999999999999645, 77.16270174994990327, -94.92310748452430857 ) ) ;
#141414=FACE_OUTER_BOUND ( 'NONE', #73320, .T. ) ;
#141427=VECTOR ( 'NONE', #254494, 1000.000000000000114 ) ;
#141447=CARTESIAN_POINT ( 'NONE',  ( 20.94999999999997442, 77.26327546522891510, -61.62124281777789037 ) ) ;
#141474=DIRECTION ( 'NONE',  ( 0.000000000000000000, 0.000000000000000000, 1.000000000000000000 ) ) ;
#141493=ORIENTED_EDGE ( 'NONE', *, *, #204326, .T. ) ;
#141504=ORIENTED_EDGE ( 'NONE', *, *, #69228, .F. ) ;
#141507=AXIS2_PLACEMENT_3D ( 'NONE', #52070, #135461, #74260 ) ;
#141512=FACE_OUTER_BOUND ( 'NONE', #29019, .T. ) ;
#141564=ADVANCED_FACE ( 'NONE', ( #32539 ), #112054, .F. ) ;
#141565=EDGE_CURVE ( 'NONE', #40828, #99793, #74234, .T. ) ;
#141586=CARTESIAN_POINT ( 'NONE',  ( -21.05000000000000071, 64.40000000001177227, -76.45131071479988805 ) ) ;
#141595=VERTEX_POINT ( 'NONE', #114605 ) ;
#141623=CIRCLE ( 'NONE', #145705, 0.1000000000000028644 ) ;
#141642=AXIS2_PLACEMENT_3D ( 'NONE', #91327, #71780, #151313 ) ;
#141681=VECTOR ( 'NONE', #243661, 1000.000000000000114 ) ;
#141683=CARTESIAN_POINT ( 'NONE',  ( -22.59999999999999787, 76.00000000001195133, -103.0231074845243171 ) ) ;
#141742=AXIS2_PLACEMENT_3D ( 'NONE', #158742, #219965, #137843 ) ;
#141755=ORIENTED_EDGE ( 'NONE', *, *, #209772, .T. ) ;
#141800=AXIS2_PLACEMENT_3D ( 'NONE', #60216, #238870, #163194 ) ;
#141878=FACE_OUTER_BOUND ( 'NONE', #234667, .T. ) ;
#141890=FACE_OUTER_BOUND ( 'NONE', #17307, .T. ) ;
#141921=CARTESIAN_POINT ( 'NONE',  ( 23.14999999999999503, 64.35000000001201670, -114.7731074845243882 ) ) ;
#141925=EDGE_CURVE ( 'NONE', #11996, #45676, #229111, .T. ) ;
#141972=DIRECTION ( 'NONE',  ( 0.000000000000000000, 0.000000000000000000, 1.000000000000000000 ) ) ;
#141999=AXIS2_PLACEMENT_3D ( 'NONE', #60339, #237712, #139870 ) ;
#142003=EDGE_CURVE ( 'NONE', #56502, #255841, #39944, .T. ) ;
#142004=ORIENTED_EDGE ( 'NONE', *, *, #253693, .T. ) ;
#142018=FACE_OUTER_BOUND ( 'NONE', #15892, .T. ) ;
#142023=DIRECTION ( 'NONE',  ( 1.000000000000000000, 0.000000000000000000, 0.000000000000000000 ) ) ;
#142024=EDGE_LOOP ( 'NONE', ( #10696, #216583, #97090, #70912 ) ) ;
#142027=CIRCLE ( 'NONE', #29633, 0.5000000000000004441 ) ;
#142045=SPHERICAL_SURFACE ( 'NONE', #228599, 0.1000000000000000056 ) ;
#142060=VERTEX_POINT ( 'NONE', #198957 ) ;
#142065=AXIS2_PLACEMENT_3D ( 'NONE', #105373, #8886, #209651 ) ;
#142074=EDGE_CURVE ( 'NONE', #253445, #103813, #136387, .T. ) ;
#142083=AXIS2_PLACEMENT_3D ( 'NONE', #13263, #204576, #25959 ) ;
#142088=CYLINDRICAL_SURFACE ( 'NONE', #190944, 0.09999999999999939493 ) ;
#142093=EDGE_CURVE ( 'NONE', #143626, #101654, #157231, .T. ) ;
#142100=EDGE_LOOP ( 'NONE', ( #71380, #251555, #229294, #17631 ) ) ;
#142116=ORIENTED_EDGE ( 'NONE', *, *, #47162, .F. ) ;
#142141=DIRECTION ( 'NONE',  ( 0.000000000000000000, 0.000000000000000000, -1.000000000000000000 ) ) ;
#142167=LINE ( 'NONE', #200862, #97509 ) ;
#142188=ADVANCED_FACE ( 'NONE', ( #246748 ), #219152, .T. ) ;
#142204=DIRECTION ( 'NONE',  ( 0.000000000000000000, -6.982962677686266711E-15, 1.000000000000000000 ) ) ;
#142213=EDGE_CURVE ( 'NONE', #147420, #190547, #202600, .T. ) ;
#142232=DIRECTION ( 'NONE',  ( 0.000000000000000000, 0.000000000000000000, 1.000000000000000000 ) ) ;
#142233=DIRECTION ( 'NONE',  ( 0.000000000000000000, -7.086529944415894657E-15, 1.000000000000000000 ) ) ;
#142237=CARTESIAN_POINT ( 'NONE',  ( -18.50000000000000000, 85.40000000001191438, -95.72584772486095517 ) ) ;
#142276=CARTESIAN_POINT ( 'NONE',  ( -21.05000000000000071, 77.83534155023627932, -91.46795619196132066 ) ) ;
#142278=ORIENTED_EDGE ( 'NONE', *, *, #214573, .F. ) ;
#142312=CARTESIAN_POINT ( 'NONE',  ( -21.07094088545368749, 75.90110629745977633, -109.3432747064414343 ) ) ;
#142342=CARTESIAN_POINT ( 'NONE',  ( -18.59999999999999787, 69.01799029515524353, -65.82695536626808064 ) ) ;
#142361=CARTESIAN_POINT ( 'NONE',  ( 22.47071067811864964, 75.90090754530939421, -110.7431822290223522 ) ) ;
#142452=DIRECTION ( 'NONE',  ( 3.616040088954490704E-32, 7.105427357601001859E-15, -1.000000000000000000 ) ) ;
#142453=EDGE_CURVE ( 'NONE', #129734, #178561, #2860, .T. ) ;
#142455=ORIENTED_EDGE ( 'NONE', *, *, #217599, .T. ) ;
#142467=EDGE_CURVE ( 'NONE', #51672, #13968, #36218, .T. ) ;
#142473=ORIENTED_EDGE ( 'NONE', *, *, #178780, .T. ) ;
#142507=ORIENTED_EDGE ( 'NONE', *, *, #75035, .F. ) ;
#142511=ORIENTED_EDGE ( 'NONE', *, *, #41768, .T. ) ;
#142515=ORIENTED_EDGE ( 'NONE', *, *, #115686, .F. ) ;
#142521=DIRECTION ( 'NONE',  ( 0.000000000000000000, 0.000000000000000000, 1.000000000000000000 ) ) ;
#142551=VERTEX_POINT ( 'NONE', #6552 ) ;
#142588=CIRCLE ( 'NONE', #113392, 0.1000000000000045158 ) ;
#142617=EDGE_LOOP ( 'NONE', ( #34350, #152165, #223601, #6555 ) ) ;
#142635=VECTOR ( 'NONE', #192372, 1000.000000000000000 ) ;
#142636=AXIS2_PLACEMENT_3D ( 'NONE', #71281, #127383, #189927 ) ;
#142639=CARTESIAN_POINT ( 'NONE',  ( 21.14999999999999858, 67.21339244341174890, -90.77310748452437394 ) ) ;
#142649=EDGE_CURVE ( 'NONE', #91045, #125402, #98689, .T. ) ;
#142650=LINE ( 'NONE', #183098, #250268 ) ;
#142672=AXIS2_PLACEMENT_3D ( 'NONE', #163409, #180401, #60430 ) ;
#142708=CARTESIAN_POINT ( 'NONE',  ( 20.94999999999999929, 65.61821452928772658, -64.01526212064021593 ) ) ;
#142716=CIRCLE ( 'NONE', #88732, 2.000000000000001776 ) ;
#142720=ORIENTED_EDGE ( 'NONE', *, *, #46402, .T. ) ;
#142722=ADVANCED_FACE ( 'NONE', ( #13005 ), #135472, .T. ) ;
#142728=CIRCLE ( 'NONE', #188540, 0.1000000000000028644 ) ;
#142803=ORIENTED_EDGE ( 'NONE', *, *, #117147, .T. ) ;
#142820=VERTEX_POINT ( 'NONE', #58497 ) ;
#142830=CARTESIAN_POINT ( 'NONE',  ( -23.25000000000000000, 76.00000000001170974, -69.52310748452431710 ) ) ;
#142837=ORIENTED_EDGE ( 'NONE', *, *, #103107, .T. ) ;
#142838=AXIS2_PLACEMENT_3D ( 'NONE', #33202, #214362, #189667 ) ;
#142842=VERTEX_POINT ( 'NONE', #234587 ) ;
#142857=CARTESIAN_POINT ( 'NONE',  ( -21.08035267497491816, 75.91731137523596828, -109.3548143243073554 ) ) ;
#142862=EDGE_LOOP ( 'NONE', ( #251531, #20906, #86964, #222434 ) ) ;
#142883=ORIENTED_EDGE ( 'NONE', *, *, #57563, .F. ) ;
#142902=AXIS2_PLACEMENT_3D ( 'NONE', #232946, #54267, #133808 ) ;
#142919=DIRECTION ( 'NONE',  ( 0.000000000000000000, 0.000000000000000000, 1.000000000000000000 ) ) ;
#142933=DIRECTION ( 'NONE',  ( 0.000000000000000000, 0.000000000000000000, 1.000000000000000000 ) ) ;
#142938=CARTESIAN_POINT ( 'NONE',  ( -21.05000000000000071, 69.45934304831071415, -102.9231074845243512 ) ) ;
#142964=DIRECTION ( 'NONE',  ( 1.000000000000000000, 0.000000000000000000, 0.000000000000000000 ) ) ;
#143010=EDGE_CURVE ( 'NONE', #223315, #57574, #202964, .T. ) ;
#143020=DIRECTION ( 'NONE',  ( 0.000000000000000000, -7.147358527629766941E-15, 1.000000000000000000 ) ) ;
#143025=ADVANCED_FACE ( 'NONE', ( #8821 ), #73956, .T. ) ;
#143076=AXIS2_PLACEMENT_3D ( 'NONE', #53965, #233891, #158249 ) ;
#143090=CARTESIAN_POINT ( 'NONE',  ( -21.12844524849339223, 64.25000000001189449, -96.11869401368159060 ) ) ;
#143122=CARTESIAN_POINT ( 'NONE',  ( 18.59999999999999432, 77.73625713160926409, -91.45445515550680682 ) ) ;
#143133=EDGE_LOOP ( 'NONE', ( #170456, #177542, #77007, #145467 ) ) ;
#143135=CARTESIAN_POINT ( 'NONE',  ( -20.54999999999999716, 74.00000000001186606, -89.79848556176222019 ) ) ;
#143138=EDGE_CURVE ( 'NONE', #80064, #3980, #161296, .T. ) ;
#143159=EDGE_CURVE ( 'NONE', #215983, #5545, #111577, .T. ) ;
#143160=DIRECTION ( 'NONE',  ( 0.000000000000000000, -6.467318590049456648E-15, 1.000000000000000000 ) ) ;
#143163=VERTEX_POINT ( 'NONE', #97294 ) ;
#143192=DIRECTION ( 'NONE',  ( 0.000000000000000000, -1.000000000000000000, -6.982962677686265922E-15 ) ) ;
#143195=EDGE_LOOP ( 'NONE', ( #200031, #99305, #187012, #218253 ) ) ;
#143196=CIRCLE ( 'NONE', #176550, 0.09999999999999939493 ) ;
#143214=LINE ( 'NONE', #106643, #231508 ) ;
#143217=LINE ( 'NONE', #207062, #204416 ) ;
#143229=EDGE_LOOP ( 'NONE', ( #62407, #13781, #233520, #118591 ) ) ;
#143232=CARTESIAN_POINT ( 'NONE',  ( 18.49999999999999645, 77.13501884592184865, -61.80613060109197932 ) ) ;
#143233=TOROIDAL_SURFACE ( 'NONE', #9960, 3.899999999999999467, 0.1000000000000000056 ) ;
#143280=ADVANCED_FACE ( 'NONE', ( #38651 ), #207275, .T. ) ;
#143322=DIRECTION ( 'NONE',  ( 1.000000000000000000, 0.000000000000000000, 0.000000000000000000 ) ) ;
#143324=EDGE_CURVE ( 'NONE', #178566, #194138, #239422, .T. ) ;
#143329=DIRECTION ( 'NONE',  ( 0.000000000000000000, -6.982962677686266711E-15, 1.000000000000000000 ) ) ;
#143351=VECTOR ( 'NONE', #42075, 1000.000000000000000 ) ;
#143393=DIRECTION ( 'NONE',  ( 1.000000000000000000, 0.000000000000000000, 0.000000000000000000 ) ) ;
#143442=CARTESIAN_POINT ( 'NONE',  ( 20.94999999999999929, 71.00000000001186606, -90.61784146561124942 ) ) ;
#143443=DIRECTION ( 'NONE',  ( -0.000000000000000000, 7.109473446599835262E-15, -1.000000000000000000 ) ) ;
#143476=DIRECTION ( 'NONE',  ( 0.000000000000000000, -0.1495327102803078179, -0.9887567792719429427 ) ) ;
#143488=ORIENTED_EDGE ( 'NONE', *, *, #220571, .T. ) ;
#143493=CARTESIAN_POINT ( 'NONE',  ( -20.64999999999999858, 71.65000000001187175, -90.67310748452433700 ) ) ;
#143514=FACE_OUTER_BOUND ( 'NONE', #237977, .T. ) ;
#143519=VECTOR ( 'NONE', #67054, 1000.000000000000000 ) ;
#143538=ORIENTED_EDGE ( 'NONE', *, *, #2562, .F. ) ;
#143540=VECTOR ( 'NONE', #6551, 1000.000000000000000 ) ;
#143590=ADVANCED_FACE ( 'NONE', ( #160826 ), #178424, .T. ) ;
#143598=AXIS2_PLACEMENT_3D ( 'NONE', #79269, #237089, #158857 ) ;
#143626=VERTEX_POINT ( 'NONE', #50769 ) ;
#143635=DIRECTION ( 'NONE',  ( -0.000000000000000000, 1.000000000000000000, 6.982962677686266711E-15 ) ) ;
#143643=CIRCLE ( 'NONE', #131166, 0.09999999999999939493 ) ;
#143657=ORIENTED_EDGE ( 'NONE', *, *, #68339, .F. ) ;
#143675=CYLINDRICAL_SURFACE ( 'NONE', #163904, 0.1000000000000028644 ) ;
#143690=CYLINDRICAL_SURFACE ( 'NONE', #92549, 0.1000000000000028644 ) ;
#143693=ORIENTED_EDGE ( 'NONE', *, *, #2902, .T. ) ;
#143700=DIRECTION ( 'NONE',  ( 1.000000000000000000, 0.000000000000000000, 0.000000000000000000 ) ) ;
#143731=DIRECTION ( 'NONE',  ( -1.000000000000000000, 0.000000000000000000, -0.000000000000000000 ) ) ;
#143743=ORIENTED_EDGE ( 'NONE', *, *, #151533, .F. ) ;
#143770=AXIS2_PLACEMENT_3D ( 'NONE', #115532, #195103, #98494 ) ;
#143773=CARTESIAN_POINT ( 'NONE',  ( -18.39999999999999858, 85.68240343348806221, -62.86626410711144786 ) ) ;
#143807=ORIENTED_EDGE ( 'NONE', *, *, #152507, .F. ) ;
#143823=DIRECTION ( 'NONE',  ( 0.000000000000000000, -6.982962677686266711E-15, 1.000000000000000000 ) ) ;
#143832=ORIENTED_EDGE ( 'NONE', *, *, #70547, .F. ) ;
#143849=EDGE_CURVE ( 'NONE', #81803, #116247, #80600, .T. ) ;
#143891=ADVANCED_FACE ( 'NONE', ( #63630 ), #111754, .T. ) ;
#143931=AXIS2_PLACEMENT_3D ( 'NONE', #212600, #200404, #120894 ) ;
#143941=CYLINDRICAL_SURFACE ( 'NONE', #171247, 0.09999999999999939493 ) ;
#143963=LINE ( 'NONE', #184374, #246835 ) ;
#143985=FACE_OUTER_BOUND ( 'NONE', #70352, .T. ) ;
#143993=DIRECTION ( 'NONE',  ( 4.408576920032447355E-17, 0.1350103645451807555, 0.9908441862701610203 ) ) ;
#143998=CARTESIAN_POINT ( 'NONE',  ( 20.85000000000000142, 64.35000000001176090, -76.30697314750248950 ) ) ;
#144014=EDGE_CURVE ( 'NONE', #94420, #206437, #145721, .T. ) ;
#144020=CARTESIAN_POINT ( 'NONE',  ( -21.05000000000000071, 87.39257802171759693, -99.94915790469229933 ) ) ;
#144035=ORIENTED_EDGE ( 'NONE', *, *, #112913, .T. ) ;
#144050=EDGE_CURVE ( 'NONE', #18900, #221237, #225248, .T. ) ;
#144100=DIRECTION ( 'NONE',  ( 0.000000000000000000, -7.429790795770647916E-15, 1.000000000000000000 ) ) ;
#144110=ORIENTED_EDGE ( 'NONE', *, *, #91274, .T. ) ;
#144163=DIRECTION ( 'NONE',  ( 0.000000000000000000, -1.000000000000000000, 0.000000000000000000 ) ) ;
#144179=ORIENTED_EDGE ( 'NONE', *, *, #187175, .F. ) ;
#144193=EDGE_LOOP ( 'NONE', ( #79557, #118309, #209948, #17012 ) ) ;
#144213=CARTESIAN_POINT ( 'NONE',  ( 22.49533356619862801, 64.34999999370783996, -103.0882300648471528 ) ) ;
#144217=CIRCLE ( 'NONE', #94157, 0.1000000000000052097 ) ;
#144231=AXIS2_PLACEMENT_3D ( 'NONE', #1238, #198172, #255526 ) ;
#144239=ORIENTED_EDGE ( 'NONE', *, *, #124691, .F. ) ;
#144298=CARTESIAN_POINT ( 'NONE',  ( 21.05000000000000071, 87.65000000001172964, -72.62310748452422615 ) ) ;
#144306=ADVANCED_FACE ( 'NONE', ( #215962 ), #19060, .T. ) ;
#144363=CARTESIAN_POINT ( 'NONE',  ( -21.00250684356851849, 64.25000000001189449, -96.00830171576455996 ) ) ;
#144382=CARTESIAN_POINT ( 'NONE',  ( -23.15000000000000213, 64.35000000001176090, -76.53791325517833855 ) ) ;
#144395=EDGE_CURVE ( 'NONE', #193967, #98958, #236440, .T. ) ;
#144404=ORIENTED_EDGE ( 'NONE', *, *, #200419, .T. ) ;
#144410=CARTESIAN_POINT ( 'NONE',  ( 23.24999999999999289, 64.35000000001186038, -90.87310748452438247 ) ) ;
#144421=EDGE_CURVE ( 'NONE', #136972, #11015, #253506, .T. ) ;
#144424=DIRECTION ( 'NONE',  ( 0.000000000000000000, -6.982962677686266711E-15, 1.000000000000000000 ) ) ;
#144431=EDGE_LOOP ( 'NONE', ( #145489, #118027, #45894, #9852 ) ) ;
#144449=ORIENTED_EDGE ( 'NONE', *, *, #91180, .F. ) ;
#144458=FACE_OUTER_BOUND ( 'NONE', #159011, .T. ) ;
#144468=EDGE_CURVE ( 'NONE', #154309, #55514, #153180, .T. ) ;
#144478=DIRECTION ( 'NONE',  ( 1.000000000000000000, 7.304098846218133681E-16, 4.639676173203992654E-30 ) ) ;
#144485=ORIENTED_EDGE ( 'NONE', *, *, #14869, .T. ) ;
#144491=CIRCLE ( 'NONE', #140201, 0.1000000000000052097 ) ;
#144520=LINE ( 'NONE', #68873, #5009 ) ;
#144565=DIRECTION ( 'NONE',  ( 1.000000000000000000, 0.000000000000000000, 0.000000000000000000 ) ) ;
#144591=CARTESIAN_POINT ( 'NONE',  ( 20.94999999999999929, 76.00000000001169553, -67.62310748452431142 ) ) ;
#144621=FACE_OUTER_BOUND ( 'NONE', #31551, .T. ) ;
#144634=EDGE_CURVE ( 'NONE', #195387, #221355, #11618, .T. ) ;
#144638=ORIENTED_EDGE ( 'NONE', *, *, #247899, .F. ) ;
#144679=CARTESIAN_POINT ( 'NONE',  ( -22.00356870143215460, 68.74575763754053526, -103.0231074845243455 ) ) ;
#144693=CARTESIAN_POINT ( 'NONE',  ( 21.51976009735019346, 69.08954155835274946, -103.0231074845243739 ) ) ;
#144707=CARTESIAN_POINT ( 'NONE',  ( -18.59999999999999787, 76.00000000001170974, -69.52310748452431710 ) ) ;
#144722=CARTESIAN_POINT ( 'NONE',  ( 23.24999999999999289, 64.35000000001194564, -103.0231074845244024 ) ) ;
#144723=ORIENTED_EDGE ( 'NONE', *, *, #65238, .F. ) ;
#144727=AXIS2_PLACEMENT_3D ( 'NONE', #61177, #217660, #102845 ) ;
#144739=EDGE_LOOP ( 'NONE', ( #116529, #8824, #172921, #201682 ) ) ;
#144746=CARTESIAN_POINT ( 'NONE',  ( 21.05000000000000071, 69.74218538953583391, -103.1208977758331571 ) ) ;
#144749=FACE_OUTER_BOUND ( 'NONE', #88166, .T. ) ;
#144755=ORIENTED_EDGE ( 'NONE', *, *, #241631, .T. ) ;
#144761=EDGE_CURVE ( 'NONE', #25415, #162117, #64308, .T. ) ;
#144801=DIRECTION ( 'NONE',  ( 0.000000000000000000, 1.000000000000000000, 6.982962677686266711E-15 ) ) ;
#144883=CARTESIAN_POINT ( 'NONE',  ( -21.05000000000000071, 76.10000000001203091, -114.6731074845243086 ) ) ;
#144890=LINE ( 'NONE', #125350, #77302 ) ;
#144910=DIRECTION ( 'NONE',  ( -0.000000000000000000, 0.8660254037844377084, 0.5000000000000016653 ) ) ;
#144926=ORIENTED_EDGE ( 'NONE', *, *, #170366, .T. ) ;
#144933=EDGE_LOOP ( 'NONE', ( #72260, #118287, #7035, #256612 ) ) ;
#145007=AXIS2_PLACEMENT_3D ( 'NONE', #120762, #211836, #166318 ) ;
#145026=CARTESIAN_POINT ( 'NONE',  ( -20.54999999999999716, 76.00000000001170974, -69.52310748452431710 ) ) ;
#145055=AXIS2_PLACEMENT_3D ( 'NONE', #176663, #234040, #253594 ) ;
#145085=DIRECTION ( 'NONE',  ( 0.000000000000000000, -0.1350103645451807555, -0.9908441862701610203 ) ) ;
#145113=DIRECTION ( 'NONE',  ( 0.000000000000000000, -6.982962677686266711E-15, 1.000000000000000000 ) ) ;
#145124=ORIENTED_EDGE ( 'NONE', *, *, #195117, .F. ) ;
#145136=FACE_OUTER_BOUND ( 'NONE', #125873, .T. ) ;
#145139=VECTOR ( 'NONE', #230923, 1000.000000000000000 ) ;
#145235=EDGE_LOOP ( 'NONE', ( #161649, #190606, #89866, #198592 ) ) ;
#145249=ADVANCED_FACE ( 'NONE', ( #92542 ), #229510, .F. ) ;
#145259=ORIENTED_EDGE ( 'NONE', *, *, #81788, .T. ) ;
#145264=EDGE_LOOP ( 'NONE', ( #19792, #194609, #4922, #145566, #50800, #229080, #168181, #98476, #172952 ) ) ;
#145269=CARTESIAN_POINT ( 'NONE',  ( 20.94999999999999929, 84.73084112150711178, -79.12118220350858167 ) ) ;
#145280=EDGE_CURVE ( 'NONE', #39117, #153564, #232575, .T. ) ;
#145314=DIRECTION ( 'NONE',  ( 0.000000000000000000, -1.000000000000000000, -6.982962677686265922E-15 ) ) ;
#145315=DIRECTION ( 'NONE',  ( -1.000000000000000000, -0.000000000000000000, -0.000000000000000000 ) ) ;
#145354=AXIS2_PLACEMENT_3D ( 'NONE', #231881, #53220, #234410 ) ;
#145355=CARTESIAN_POINT ( 'NONE',  ( 21.05000000000000071, 85.00000000001188027, -93.12913836187181005 ) ) ;
#145393=ORIENTED_EDGE ( 'NONE', *, *, #93236, .F. ) ;
#145399=ORIENTED_EDGE ( 'NONE', *, *, #39818, .F. ) ;
#145416=LINE ( 'NONE', #132279, #194287 ) ;
#145425=ORIENTED_EDGE ( 'NONE', *, *, #53676, .F. ) ;
#145426=EDGE_CURVE ( 'NONE', #188436, #51707, #245205, .T. ) ;
#145442=CARTESIAN_POINT ( 'NONE',  ( -21.08134388332232589, 75.92418108250502939, -109.3577880650422856 ) ) ;
#145449=FACE_OUTER_BOUND ( 'NONE', #44378, .T. ) ;
#145456=DIRECTION ( 'NONE',  ( 0.000000000000000000, -6.982962677686267499E-15, 1.000000000000000000 ) ) ;
#145458=FACE_OUTER_BOUND ( 'NONE', #140416, .T. ) ;
#145466=DIRECTION ( 'NONE',  ( 0.000000000000000000, -0.008583690987162452199, -0.9999631594459053030 ) ) ;
#145467=ORIENTED_EDGE ( 'NONE', *, *, #89683, .F. ) ;
#145489=ORIENTED_EDGE ( 'NONE', *, *, #43189, .T. ) ;
#145501=ORIENTED_EDGE ( 'NONE', *, *, #242512, .F. ) ;
#145566=ORIENTED_EDGE ( 'NONE', *, *, #149297, .T. ) ;
#145570=EDGE_CURVE ( 'NONE', #174346, #249207, #203690, .T. ) ;
#145589=ORIENTED_EDGE ( 'NONE', *, *, #244249, .T. ) ;
#145591=CARTESIAN_POINT ( 'NONE',  ( 23.25000000000000000, 69.45000000001186891, -90.67310748452435121 ) ) ;
#145639=TOROIDAL_SURFACE ( 'NONE', #187365, 11.65000000000000036, 0.1000000000000000056 ) ;
#145649=DIRECTION ( 'NONE',  ( -1.000000000000000000, 0.000000000000000000, 0.000000000000000000 ) ) ;
#145663=ORIENTED_EDGE ( 'NONE', *, *, #76367, .F. ) ;
#145696=AXIS2_PLACEMENT_3D ( 'NONE', #24447, #23164, #124810 ) ;
#145705=AXIS2_PLACEMENT_3D ( 'NONE', #29877, #88507, #109362 ) ;
#145721=LINE ( 'NONE', #10078, #194610 ) ;
#145733=FACE_OUTER_BOUND ( 'NONE', #164901, .T. ) ;
#145746=VERTEX_POINT ( 'NONE', #37108 ) ;
#145760=FACE_OUTER_BOUND ( 'NONE', #82508, .T. ) ;
#145770=DIRECTION ( 'NONE',  ( 0.000000000000000000, 0.000000000000000000, 1.000000000000000000 ) ) ;
#145791=SHAPE_REPRESENTATION_RELATIONSHIP ( 'NONE' , 'NONE' ,  #178537, #250584 ) ;
#145792=AXIS2_PLACEMENT_3D ( 'NONE', #195859, #58862, #95444 ) ;
#145834=CIRCLE ( 'NONE', #20976, 11.79999999999999716 ) ;
#145846=CARTESIAN_POINT ( 'NONE',  ( 21.14999999999999858, 87.75000000001186606, -90.77310748452423184 ) ) ;
#145879=ORIENTED_EDGE ( 'NONE', *, *, #138964, .F. ) ;
#145911=VERTEX_POINT ( 'NONE', #223404 ) ;
#145928=DIRECTION ( 'NONE',  ( 1.000000000000000000, 0.000000000000000000, 0.000000000000000000 ) ) ;
#145944=EDGE_CURVE ( 'NONE', #10839, #40972, #99778, .T. ) ;
#145983=CARTESIAN_POINT ( 'NONE',  ( 21.14999999999999858, 69.45934304831071415, -103.0231074845243597 ) ) ;
#146004=CARTESIAN_POINT ( 'NONE',  ( 19.75857864376268935, 64.25000000001176659, -78.27310748452438816 ) ) ;
#146016=CIRCLE ( 'NONE', #250089, 11.90000000000000036 ) ;
#146042=ORIENTED_EDGE ( 'NONE', *, *, #224924, .T. ) ;
#146049=VERTEX_POINT ( 'NONE', #77183 ) ;
#146066=AXIS2_PLACEMENT_3D ( 'NONE', #247840, #207445, #91349 ) ;
#146105=DIRECTION ( 'NONE',  ( 0.000000000000000000, 7.056502275159890832E-15, -1.000000000000000000 ) ) ;
#146134=CARTESIAN_POINT ( 'NONE',  ( 19.88284271247461987, 64.30857864377446731, -78.27310748452438816 ) ) ;
#146144=DIRECTION ( 'NONE',  ( -0.000000000000000000, -0.1350103645451835865, -0.9908441862701606873 ) ) ;
#146171=ORIENTED_EDGE ( 'NONE', *, *, #201604, .T. ) ;
#146180=CARTESIAN_POINT ( 'NONE',  ( -20.93975676684922504, 65.68895814178220860, -64.00265578621380769 ) ) ;
#146209=FACE_OUTER_BOUND ( 'NONE', #163290, .T. ) ;
#146236=EDGE_CURVE ( 'NONE', #23326, #154058, #221810, .T. ) ;
#146237=LINE ( 'NONE', #206227, #12484 ) ;
#146238=CARTESIAN_POINT ( 'NONE',  ( -20.94999999999999929, 64.35000000001190301, -96.00830171387039513 ) ) ;
#146252=CARTESIAN_POINT ( 'NONE',  ( 18.53691006697109955, 65.69784844286137115, -78.32090876722591588 ) ) ;
#146253=DIRECTION ( 'NONE',  ( 0.000000000000000000, -6.997203936713171069E-15, 1.000000000000000000 ) ) ;
#146264=FACE_OUTER_BOUND ( 'NONE', #81941, .T. ) ;
#146266=EDGE_LOOP ( 'NONE', ( #54310, #26035, #196726, #135662 ) ) ;
#146270=ORIENTED_EDGE ( 'NONE', *, *, #126757, .F. ) ;
#146277=FACE_OUTER_BOUND ( 'NONE', #11388, .T. ) ;
#146313=CARTESIAN_POINT ( 'NONE',  ( 23.14999999999999503, 69.35000000001180354, -81.67310748452436542 ) ) ;
#146325=ORIENTED_EDGE ( 'NONE', *, *, #108841, .F. ) ;
#146331=DIRECTION ( 'NONE',  ( 1.000000000000000000, 0.000000000000000000, 0.000000000000000000 ) ) ;
#146360=ORIENTED_EDGE ( 'NONE', *, *, #27657, .F. ) ;
#146382=AXIS2_PLACEMENT_3D ( 'NONE', #60893, #20516, #218676 ) ;
#146433=AXIS2_PLACEMENT_3D ( 'NONE', #255268, #140494, #58375 ) ;
#146439=VERTEX_POINT ( 'NONE', #129168 ) ;
#146441=VECTOR ( 'NONE', #20490, 1000.000000000000114 ) ;
#146443=CARTESIAN_POINT ( 'NONE',  ( 20.13684514580104334, 66.50414460725923504, -94.88007579883958442 ) ) ;
#146488=EDGE_LOOP ( 'NONE', ( #174980, #175175, #55053, #49701 ) ) ;
#146500=ORIENTED_EDGE ( 'NONE', *, *, #114491, .F. ) ;
#146529=ORIENTED_EDGE ( 'NONE', *, *, #32269, .F. ) ;
#146554=ORIENTED_EDGE ( 'NONE', *, *, #71366, .T. ) ;
#146576=LINE ( 'NONE', #144020, #118449 ) ;
#146605=VERTEX_POINT ( 'NONE', #23367 ) ;
#146611=EDGE_CURVE ( 'NONE', #164805, #116663, #164140, .T. ) ;
#146628=ORIENTED_EDGE ( 'NONE', *, *, #221981, .T. ) ;
#146655=ORIENTED_EDGE ( 'NONE', *, *, #233382, .F. ) ;
#146660=ORIENTED_EDGE ( 'NONE', *, *, #28495, .F. ) ;
#146671=CARTESIAN_POINT ( 'NONE',  ( 20.94999999999999574, 87.65000000001192859, -100.0231074845242318 ) ) ;
#146676=EDGE_LOOP ( 'NONE', ( #102444, #95659, #121527, #41550 ) ) ;
#146692=ORIENTED_EDGE ( 'NONE', *, *, #35300, .T. ) ;
#146698=ORIENTED_EDGE ( 'NONE', *, *, #105550, .T. ) ;
#146711=VERTEX_POINT ( 'NONE', #204526 ) ;
#146727=FACE_OUTER_BOUND ( 'NONE', #244805, .T. ) ;
#146755=PLANE ( 'NONE',  #1140 ) ;
#146760=FACE_OUTER_BOUND ( 'NONE', #173771, .T. ) ;
#146779=PLANE ( 'NONE',  #181813 ) ;
#146786=AXIS2_PLACEMENT_3D ( 'NONE', #209809, #120999, #59683 ) ;
#146831=DIRECTION ( 'NONE',  ( 0.000000000000000000, 1.000000000000000000, 6.938893903907222067E-15 ) ) ;
#146833=CYLINDRICAL_SURFACE ( 'NONE', #25028, 11.80000000000000426 ) ;
#146849=FACE_OUTER_BOUND ( 'NONE', #182210, .T. ) ;
#146861=ORIENTED_EDGE ( 'NONE', *, *, #54873, .T. ) ;
#146862=FACE_OUTER_BOUND ( 'NONE', #99826, .T. ) ;
#146872=PLANE ( 'NONE',  #243276 ) ;
#146877=ADVANCED_FACE ( 'NONE', ( #181953 ), #64558, .F. ) ;
#146914=EDGE_CURVE ( 'NONE', #251279, #125644, #220795, .T. ) ;
#146918=ORIENTED_EDGE ( 'NONE', *, *, #167375, .F. ) ;
#146929=DIRECTION ( 'NONE',  ( 1.000000000000000000, 0.000000000000000000, 0.000000000000000000 ) ) ;
#146952=AXIS2_PLACEMENT_3D ( 'NONE', #35481, #74614, #92840 ) ;
#146965=ORIENTED_EDGE ( 'NONE', *, *, #77801, .F. ) ;
#146985=ORIENTED_EDGE ( 'NONE', *, *, #161025, .F. ) ;
#147013=CARTESIAN_POINT ( 'NONE',  ( -21.02374657821586013, 64.39999999919189122, -76.45131071432655290 ) ) ;
#147036=EDGE_CURVE ( 'NONE', #206570, #231923, #41948, .T. ) ;
#147044=CARTESIAN_POINT ( 'NONE',  ( -21.05000000000000071, 69.74218538953043378, -103.1208977758335834 ) ) ;
#147054=DIRECTION ( 'NONE',  ( -0.000000000000000000, -6.982962677686266711E-15, 1.000000000000000000 ) ) ;
#147059=LINE ( 'NONE', #67535, #198311 ) ;
#147087=ORIENTED_EDGE ( 'NONE', *, *, #146914, .T. ) ;
#147125=CARTESIAN_POINT ( 'NONE',  ( -18.54118089899631983, 85.46353763186000663, -95.97452988665611429 ) ) ;
#147129=ORIENTED_EDGE ( 'NONE', *, *, #183154, .F. ) ;
#147152=CYLINDRICAL_SURFACE ( 'NONE', #167694, 0.1000000000000028644 ) ;
#147157=DIRECTION ( 'NONE',  ( 0.000000000000000000, -0.8660254037844468122, -0.4999999999999859557 ) ) ;
#147225=DIRECTION ( 'NONE',  ( 4.026293107431335996E-15, 0.8700118002898393765, -0.4930308989875104575 ) ) ;
#147249=TOROIDAL_SURFACE ( 'NONE', #55629, 0.6000000000000004219, 0.1000000000000000056 ) ;
#147261=EDGE_LOOP ( 'NONE', ( #76472, #48531, #152194, #79397 ) ) ;
#147266=EDGE_CURVE ( 'NONE', #190040, #127766, #175236, .T. ) ;
#147316=ORIENTED_EDGE ( 'NONE', *, *, #236349, .T. ) ;
#147326=ORIENTED_EDGE ( 'NONE', *, *, #162538, .F. ) ;
#147331=CARTESIAN_POINT ( 'NONE',  ( -23.15000000000000213, 76.00000000001170974, -69.52310748452431710 ) ) ;
#147354=VERTEX_POINT ( 'NONE', #222936 ) ;
#147363=VERTEX_POINT ( 'NONE', #101681 ) ;
#147366=ADVANCED_FACE ( 'NONE', ( #2606 ), #241245, .T. ) ;
#147395=DIRECTION ( 'NONE',  ( 0.000000000000000000, 0.000000000000000000, 1.000000000000000000 ) ) ;
#147420=VERTEX_POINT ( 'NONE', #61309 ) ;
#147457=TOROIDAL_SURFACE ( 'NONE', #151587, 0.2000000000000000111, 0.1000000000000000056 ) ;
#147479=ORIENTED_EDGE ( 'NONE', *, *, #111459, .F. ) ;
#147481=DIRECTION ( 'NONE',  ( -0.000000000000000000, 6.982962677686266711E-15, -1.000000000000000000 ) ) ;
#147496=DIRECTION ( 'NONE',  ( -0.000000000000000000, 1.000000000000000000, 6.982962677686266711E-15 ) ) ;
#147503=ORIENTED_EDGE ( 'NONE', *, *, #63254, .F. ) ;
#147509=ORIENTED_EDGE ( 'NONE', *, *, #227022, .F. ) ;
#147520=ORIENTED_EDGE ( 'NONE', *, *, #188941, .F. ) ;
#147522=CARTESIAN_POINT ( 'NONE',  ( 23.14999999999999503, 64.35000000001176090, -76.53791325517833855 ) ) ;
#147540=LINE ( 'NONE', #105816, #57301 ) ;
#147547=AXIS2_PLACEMENT_3D ( 'NONE', #256285, #38598, #42441 ) ;
#147549=FACE_OUTER_BOUND ( 'NONE', #87990, .T. ) ;
#147563=CARTESIAN_POINT ( 'NONE',  ( -20.94999999999999929, 87.75000000001173817, -72.62310748452422615 ) ) ;
#147567=CIRCLE ( 'NONE', #185161, 0.09999999999999939493 ) ;
#147577=DIRECTION ( 'NONE',  ( 0.000000000000000000, 6.982962677686266711E-15, -1.000000000000000000 ) ) ;
#147594=ADVANCED_FACE ( 'NONE', ( #149852 ), #152322, .F. ) ;
#147599=ORIENTED_EDGE ( 'NONE', *, *, #180026, .T. ) ;
#147618=ORIENTED_EDGE ( 'NONE', *, *, #45698, .F. ) ;
#147627=ADVANCED_FACE ( 'NONE', ( #178407 ), #135522, .T. ) ;
#147666=CARTESIAN_POINT ( 'NONE',  ( 22.60000000000000142, 76.00000000001195133, -103.0231074845243171 ) ) ;
#147684=ORIENTED_EDGE ( 'NONE', *, *, #167428, .T. ) ;
#147808=CARTESIAN_POINT ( 'NONE',  ( 18.59999999999999076, 69.35000000001180354, -81.87310748452435405 ) ) ;
#147888=EDGE_CURVE ( 'NONE', #61221, #153341, #231583, .T. ) ;
#147925=FACE_OUTER_BOUND ( 'NONE', #123642, .T. ) ;
#147951=ORIENTED_EDGE ( 'NONE', *, *, #233641, .T. ) ;
#147977=FACE_OUTER_BOUND ( 'NONE', #202504, .T. ) ;
#147978=EDGE_LOOP ( 'NONE', ( #31263, #222033, #118567, #167634 ) ) ;
#147984=LINE ( 'NONE', #108847, #47842 ) ;
#147985=AXIS2_PLACEMENT_3D ( 'NONE', #216606, #177523, #151850 ) ;
#148009=ORIENTED_EDGE ( 'NONE', *, *, #105025, .T. ) ;
#148035=EDGE_LOOP ( 'NONE', ( #136520, #83461, #195778, #110860 ) ) ;
#148061=CARTESIAN_POINT ( 'NONE',  ( 20.85000000000000142, 76.00000000001170974, -69.52310748452431710 ) ) ;
#148062=DIRECTION ( 'NONE',  ( 1.000000000000000000, 0.000000000000000000, 0.000000000000000000 ) ) ;
#148090=FACE_OUTER_BOUND ( 'NONE', #87574, .T. ) ;
#148115=CIRCLE ( 'NONE', #156529, 0.09999999999999939493 ) ;
#148118=ORIENTED_EDGE ( 'NONE', *, *, #3460, .F. ) ;
#148127=EDGE_LOOP ( 'NONE', ( #221070, #97283, #71244, #70008 ) ) ;
#148138=FACE_OUTER_BOUND ( 'NONE', #130848, .T. ) ;
#148143=CIRCLE ( 'NONE', #52453, 0.1000000000000028644 ) ;
#148161=CIRCLE ( 'NONE', #27408, 0.1000000000000026007 ) ;
#148182=ORIENTED_EDGE ( 'NONE', *, *, #34867, .F. ) ;
#148227=DIRECTION ( 'NONE',  ( 0.000000000000000000, -0.9998779222360097974, 0.01562500000000363945 ) ) ;
#148243=ORIENTED_EDGE ( 'NONE', *, *, #243572, .T. ) ;
#148246=ORIENTED_EDGE ( 'NONE', *, *, #143159, .T. ) ;
#148276=CARTESIAN_POINT ( 'NONE',  ( 21.05000000000000071, 76.00000000001170974, -69.52310748452431710 ) ) ;
#148335=DIRECTION ( 'NONE',  ( 0.000000000000000000, 6.982962677686266711E-15, -1.000000000000000000 ) ) ;
#148348=FACE_OUTER_BOUND ( 'NONE', #142024, .T. ) ;
#148351=ORIENTED_EDGE ( 'NONE', *, *, #246424, .F. ) ;
#148358=FACE_OUTER_BOUND ( 'NONE', #129047, .T. ) ;
#148365=EDGE_CURVE ( 'NONE', #229799, #171759, #250864, .T. ) ;
#148388=VECTOR ( 'NONE', #66418, 1000.000000000000000 ) ;
#148409=CYLINDRICAL_SURFACE ( 'NONE', #167537, 0.09999999999999976963 ) ;
#148424=EDGE_CURVE ( 'NONE', #112510, #46212, #231776, .T. ) ;
#148446=CARTESIAN_POINT ( 'NONE',  ( 21.05000000000000071, 76.00000000001195133, -103.0231074845243171 ) ) ;
#148450=VECTOR ( 'NONE', #146331, 1000.000000000000000 ) ;
#148456=VERTEX_POINT ( 'NONE', #242870 ) ;
#148462=ORIENTED_EDGE ( 'NONE', *, *, #58773, .F. ) ;
#148478=CARTESIAN_POINT ( 'NONE',  ( 20.95576188350343116, 65.39101945504849311, -95.41187376177008161 ) ) ;
#148482=LINE ( 'NONE', #8965, #92059 ) ;
#148523=ORIENTED_EDGE ( 'NONE', *, *, #222718, .T. ) ;
#148536=DIRECTION ( 'NONE',  ( -1.000000000000000000, 0.000000000000000000, 0.000000000000000000 ) ) ;
#148538=AXIS2_PLACEMENT_3D ( 'NONE', #152948, #233744, #74701 ) ;
#148570=EDGE_LOOP ( 'NONE', ( #70731, #252165, #110400, #37247 ) ) ;
#148596=ORIENTED_EDGE ( 'NONE', *, *, #168309, .T. ) ;
#148626=ORIENTED_EDGE ( 'NONE', *, *, #167423, .F. ) ;
#148693=CARTESIAN_POINT ( 'NONE',  ( -21.14999999999999858, 69.45934304831071415, -103.0231074845243597 ) ) ;
#148694=DIRECTION ( 'NONE',  ( 0.000000000000000000, -7.056502275159890832E-15, 1.000000000000000000 ) ) ;
#148705=CIRCLE ( 'NONE', #36277, 11.70000000000000284 ) ;
#148746=DIRECTION ( 'NONE',  ( -1.000000000000000000, 0.000000000000000000, -0.000000000000000000 ) ) ;
#148752=CARTESIAN_POINT ( 'NONE',  ( -22.50000000000000000, 64.35042919246716053, -103.1231074845243825 ) ) ;
#148786=CARTESIAN_POINT ( 'NONE',  ( -22.47071067811865319, 68.27992525551387359, -103.1221999392269737 ) ) ;
#148801=DIRECTION ( 'NONE',  ( 0.000000000000000000, 7.086529944415894657E-15, -1.000000000000000000 ) ) ;
#148808=CARTESIAN_POINT ( 'NONE',  ( -21.04999999999999716, 69.69982018209508112, -103.0745903664065395 ) ) ;
#148818=AXIS2_PLACEMENT_3D ( 'NONE', #81639, #80362, #62125 ) ;
#148827=ORIENTED_EDGE ( 'NONE', *, *, #247899, .T. ) ;
#148851=VERTEX_POINT ( 'NONE', #174310 ) ;
#148874=ADVANCED_FACE ( 'NONE', ( #118135 ), #115560, .F. ) ;
#148880=ORIENTED_EDGE ( 'NONE', *, *, #179746, .F. ) ;
#148902=FACE_OUTER_BOUND ( 'NONE', #122482, .T. ) ;
#148980=VECTOR ( 'NONE', #166694, 1000.000000000000114 ) ;
#148984=B_SPLINE_CURVE_WITH_KNOTS ( 'NONE', 3,
 ( #187763, #166936, #125212, #223003, #84749, #144746 ),
 .UNSPECIFIED., .F., .F.,
 ( 4, 2, 4 ),
 ( 0.000000000000000000, 0.0001895189928937412213, 0.0003790379857874824425 ),
 .UNSPECIFIED. ) ;
#148999=DIRECTION ( 'NONE',  ( 1.000000000000000000, 0.000000000000000000, 0.000000000000000000 ) ) ;
#149037=CARTESIAN_POINT ( 'NONE',  ( 18.59999999999999787, 85.32100840337319880, -95.78716923544638462 ) ) ;
#149048=CIRCLE ( 'NONE', #178078, 7.800000000000001599 ) ;
#149057=CARTESIAN_POINT ( 'NONE',  ( 20.97565083910961548, 65.52538259873308846, -95.44516430793582629 ) ) ;
#149062=AXIS2_PLACEMENT_3D ( 'NONE', #158847, #97529, #239649 ) ;
#149095=CIRCLE ( 'NONE', #119886, 12.97499999999999964 ) ;
#149098=CARTESIAN_POINT ( 'NONE',  ( -23.25000000000000000, 77.83585931145526615, -58.01866831572577610 ) ) ;
#149112=DIRECTION ( 'NONE',  ( 1.000000000000000000, 0.000000000000000000, 0.000000000000000000 ) ) ;
#149143=ORIENTED_EDGE ( 'NONE', *, *, #41375, .T. ) ;
#149209=CARTESIAN_POINT ( 'NONE',  ( -22.47120815636973745, 75.97109617810814086, -114.6730394732778109 ) ) ;
#149227=AXIS2_PLACEMENT_3D ( 'NONE', #22938, #179436, #62049 ) ;
#149243=ORIENTED_EDGE ( 'NONE', *, *, #153643, .F. ) ;
#149260=ADVANCED_FACE ( 'NONE', ( #147977 ), #9736, .F. ) ;
#149284=ORIENTED_EDGE ( 'NONE', *, *, #239019, .F. ) ;
#149297=EDGE_CURVE ( 'NONE', #16537, #78455, #72304, .T. ) ;
#149315=AXIS2_PLACEMENT_3D ( 'NONE', #112239, #49676, #54800 ) ;
#149320=VECTOR ( 'NONE', #72332, 1000.000000000000000 ) ;
#149353=AXIS2_PLACEMENT_3D ( 'NONE', #211030, #191493, #166797 ) ;
#149432=AXIS2_PLACEMENT_3D ( 'NONE', #56526, #14886, #156969 ) ;
#149442=ORIENTED_EDGE ( 'NONE', *, *, #88298, .F. ) ;
#149471=CARTESIAN_POINT ( 'NONE',  ( 21.05000000000000071, 87.48912529308798014, -99.92310748452423752 ) ) ;
#149522=DIRECTION ( 'NONE',  ( 1.000000000000000000, 0.000000000000000000, 0.000000000000000000 ) ) ;
#149555=LINE ( 'NONE', #129943, #19444 ) ;
#149565=ORIENTED_EDGE ( 'NONE', *, *, #234516, .F. ) ;
#149573=DIRECTION ( 'NONE',  ( -1.000000000000000000, 0.000000000000000000, -0.000000000000000000 ) ) ;
#149593=TOROIDAL_SURFACE ( 'NONE', #70509, 11.89999999999999858, 0.1000000000000000056 ) ;
#149699=CARTESIAN_POINT ( 'NONE',  ( 18.59999999999999076, 64.35000000001177511, -78.27310748452438816 ) ) ;
#149713=EDGE_CURVE ( 'NONE', #204570, #158859, #78176, .T. ) ;
#149731=DIRECTION ( 'NONE',  ( -2.952720810173289112E-16, -1.000000000000000000, -6.982962677686266711E-15 ) ) ;
#149741=DIRECTION ( 'NONE',  ( 0.000000000000000000, 7.056502275159890832E-15, -1.000000000000000000 ) ) ;
#149745=DIRECTION ( 'NONE',  ( 1.000000000000000000, 0.000000000000000000, 0.000000000000000000 ) ) ;
#149773=FACE_OUTER_BOUND ( 'NONE', #2710, .T. ) ;
#149797=CARTESIAN_POINT ( 'NONE',  ( -20.64999999999999858, 71.65000000001187175, -90.77310748452434552 ) ) ;
#149825=ORIENTED_EDGE ( 'NONE', *, *, #213636, .F. ) ;
#149852=FACE_OUTER_BOUND ( 'NONE', #85097, .T. ) ;
#149890=CARTESIAN_POINT ( 'NONE',  ( 18.59999999999999076, 65.75000000001176659, -78.27310748452438816 ) ) ;
#149915=ORIENTED_EDGE ( 'NONE', *, *, #160148, .T. ) ;
#149926=CYLINDRICAL_SURFACE ( 'NONE', #246744, 0.09999999999999520384 ) ;
#149933=DIRECTION ( 'NONE',  ( 0.000000000000000000, 0.000000000000000000, 1.000000000000000000 ) ) ;
#150015=DIRECTION ( 'NONE',  ( -2.952720810173289605E-16, -1.000000000000000000, -7.086529944415894657E-15 ) ) ;
#150031=FACE_OUTER_BOUND ( 'NONE', #160721, .T. ) ;
#150034=AXIS2_PLACEMENT_3D ( 'NONE', #24721, #185043, #45537 ) ;
#150040=VECTOR ( 'NONE', #40465, 999.9999999999998863 ) ;
#150041=CARTESIAN_POINT ( 'NONE',  ( -22.59999985501179154, 64.25013020700896504, -103.0887061543239582 ) ) ;
#150071=CARTESIAN_POINT ( 'NONE',  ( -23.15000000000000213, 76.00000000001170974, -69.52310748452431710 ) ) ;
#150080=AXIS2_PLACEMENT_3D ( 'NONE', #169786, #131902, #15841 ) ;
#150086=FACE_OUTER_BOUND ( 'NONE', #132184, .T. ) ;
#150090=ADVANCED_FACE ( 'NONE', ( #55932 ), #32587, .T. ) ;
#150129=LINE ( 'NONE', #11903, #53223 ) ;
#150141=EDGE_LOOP ( 'NONE', ( #247184, #205673 ) ) ;
#150174=CARTESIAN_POINT ( 'NONE',  ( -20.85000000000000142, 77.83585931145526615, -58.01866831572577610 ) ) ;
#150189=CARTESIAN_POINT ( 'NONE',  ( 21.05000000000000071, 67.18479819544494092, -94.60256998784034010 ) ) ;
#150190=EDGE_LOOP ( 'NONE', ( #64527, #233014, #1698, #127728, #151496 ) ) ;
#150192=ORIENTED_EDGE ( 'NONE', *, *, #46402, .F. ) ;
#150197=EDGE_CURVE ( 'NONE', #182384, #184113, #252955, .T. ) ;
#150210=CYLINDRICAL_SURFACE ( 'NONE', #158869, 0.09999999999999939493 ) ;
#150235=EDGE_CURVE ( 'NONE', #216303, #229799, #40619, .T. ) ;
#150239=ORIENTED_EDGE ( 'NONE', *, *, #53569, .T. ) ;
#150306=DIRECTION ( 'NONE',  ( -1.000000000000000000, 2.952720810173289112E-16, 2.061873921506763405E-30 ) ) ;
#150319=VECTOR ( 'NONE', #132481, 1000.000000000000000 ) ;
#150333=ORIENTED_EDGE ( 'NONE', *, *, #120685, .F. ) ;
#150334=CARTESIAN_POINT ( 'NONE',  ( 20.30466543256828160, 66.69576306075641980, -94.76944483313239687 ) ) ;
#150368=EDGE_CURVE ( 'NONE', #187906, #168580, #64932, .T. ) ;
#150461=AXIS2_PLACEMENT_3D ( 'NONE', #4683, #820, #19132 ) ;
#150488=TOROIDAL_SURFACE ( 'NONE', #200366, 2.100000000000002309, 0.1000000000000000056 ) ;
#150491=CARTESIAN_POINT ( 'NONE',  ( -18.59999999999999787, 77.16270174994990327, -94.92310748452430857 ) ) ;
#150500=AXIS2_PLACEMENT_3D ( 'NONE', #244639, #81683, #243359 ) ;
#150536=FACE_OUTER_BOUND ( 'NONE', #229275, .T. ) ;
#150555=CARTESIAN_POINT ( 'NONE',  ( -18.50000000000000000, 65.70711192142347556, -64.06510546851220056 ) ) ;
#150603=CARTESIAN_POINT ( 'NONE',  ( -20.94999999999999929, 74.16465844978745281, -91.46795619196133487 ) ) ;
#150625=ORIENTED_EDGE ( 'NONE', *, *, #159691, .T. ) ;
#150630=DIRECTION ( 'NONE',  ( -0.000000000000000000, -6.982962677686266711E-15, 1.000000000000000000 ) ) ;
#150659=DIRECTION ( 'NONE',  ( -1.000000000000000000, 0.000000000000000000, -0.000000000000000000 ) ) ;
#150683=CARTESIAN_POINT ( 'NONE',  ( 20.94999999999999574, 77.83534155023627932, -91.36795619196132634 ) ) ;
#150687=FACE_OUTER_BOUND ( 'NONE', #9186, .T. ) ;
#150692=CIRCLE ( 'NONE', #121670, 0.1000000000000028644 ) ;
#150700=LINE ( 'NONE', #49025, #233874 ) ;
#150701=FACE_OUTER_BOUND ( 'NONE', #222776, .T. ) ;
#150715=AXIS2_PLACEMENT_3D ( 'NONE', #67395, #50372, #247304 ) ;
#150720=AXIS2_PLACEMENT_3D ( 'NONE', #248841, #152325, #70224 ) ;
#150733=DIRECTION ( 'NONE',  ( 0.000000000000000000, 0.000000000000000000, 1.000000000000000000 ) ) ;
#150782=CYLINDRICAL_SURFACE ( 'NONE', #113503, 0.1000000000000028644 ) ;
#150784=CYLINDRICAL_SURFACE ( 'NONE', #150715, 0.1000000000000028644 ) ;
#150844=EDGE_CURVE ( 'NONE', #183504, #39117, #3136, .T. ) ;
#150911=EDGE_LOOP ( 'NONE', ( #31444, #196284, #172648, #145879, #134360, #15104, #159683, #187484, #197121, #255531, #114153, #186083, #181681, #76528 ) ) ;
#150927=AXIS2_PLACEMENT_3D ( 'NONE', #95360, #157948, #197008 ) ;
#150934=ADVANCED_FACE ( 'NONE', ( #235049 ), #56380, .F. ) ;
#150963=ORIENTED_EDGE ( 'NONE', *, *, #38387, .T. ) ;
#151009=LINE ( 'NONE', #28537, #200881 ) ;
#151013=AXIS2_PLACEMENT_3D ( 'NONE', #148446, #149745, #208432 ) ;
#151049=CARTESIAN_POINT ( 'NONE',  ( 20.95568717954149562, 65.39800594612007956, -95.42059911625572965 ) ) ;
#151059=FACE_OUTER_BOUND ( 'NONE', #94718, .T. ) ;
#151071=CIRCLE ( 'NONE', #76043, 11.90000000000000746 ) ;
#151076=CIRCLE ( 'NONE', #200959, 0.1000000000000028644 ) ;
#151139=CARTESIAN_POINT ( 'NONE',  ( -20.64999999999999858, 76.00000000001195133, -103.0231074845243171 ) ) ;
#151143=CARTESIAN_POINT ( 'NONE',  ( 18.49999999999999645, 74.36282728704149747, -91.44095411905230719 ) ) ;
#151155=ADVANCED_FACE ( 'NONE', ( #150086 ), #251729, .T. ) ;
#151156=CYLINDRICAL_SURFACE ( 'NONE', #122074, 0.09999999999999939493 ) ;
#151177=AXIS2_PLACEMENT_3D ( 'NONE', #39473, #155571, #235081 ) ;
#151217=VECTOR ( 'NONE', #17611, 1000.000000000000000 ) ;
#151245=ORIENTED_EDGE ( 'NONE', *, *, #67027, .F. ) ;
#151270=EDGE_LOOP ( 'NONE', ( #161857, #208338, #92193, #110657 ) ) ;
#151313=DIRECTION ( 'NONE',  ( 0.000000000000000000, 0.9915357197604892647, -0.1298341882519715440 ) ) ;
#151335=CIRCLE ( 'NONE', #159697, 0.1000000000000028644 ) ;
#151337=EDGE_CURVE ( 'NONE', #221237, #224632, #63091, .T. ) ;
#151349=CARTESIAN_POINT ( 'NONE',  ( -20.94983749550516450, 65.70233904876990039, -64.04874109119681691 ) ) ;
#151373=ORIENTED_EDGE ( 'NONE', *, *, #189785, .T. ) ;
#151390=CARTESIAN_POINT ( 'NONE',  ( -21.64999999999999858, 68.65000000001180069, -81.87310748452436826 ) ) ;
#151396=CIRCLE ( 'NONE', #85265, 0.09999999999999939493 ) ;
#151420=CARTESIAN_POINT ( 'NONE',  ( 18.49999999999999289, 65.62657994473217116, -78.25731935989797705 ) ) ;
#151424=CARTESIAN_POINT ( 'NONE',  ( 21.05000000000000071, 87.75000000001190870, -100.1231074845242262 ) ) ;
#151443=DIRECTION ( 'NONE',  ( 1.000000000000000000, -3.265361837132813093E-16, -2.280189983783949500E-30 ) ) ;
#151471=EDGE_CURVE ( 'NONE', #57915, #237421, #69049, .T. ) ;
#151482=CARTESIAN_POINT ( 'NONE',  ( 20.95429402530583829, 67.12380584890971136, -94.50002078658648941 ) ) ;
#151496=ORIENTED_EDGE ( 'NONE', *, *, #147888, .F. ) ;
#151529=CARTESIAN_POINT ( 'NONE',  ( -20.94999999999999929, 74.73821383144687047, -94.93660852097883662 ) ) ;
#151533=EDGE_CURVE ( 'NONE', #2887, #80661, #11931, .T. ) ;
#151542=CARTESIAN_POINT ( 'NONE',  ( 18.49999999999999645, 74.16465844978745281, -91.46795619196133487 ) ) ;
#151564=ORIENTED_EDGE ( 'NONE', *, *, #243291, .F. ) ;
#151568=CARTESIAN_POINT ( 'NONE',  ( 18.49999999999998934, 69.45000000001181206, -81.87310748452435405 ) ) ;
#151575=EDGE_CURVE ( 'NONE', #125531, #153341, #211825, .T. ) ;
#151587=AXIS2_PLACEMENT_3D ( 'NONE', #201774, #162669, #242185 ) ;
#151611=CARTESIAN_POINT ( 'NONE',  ( -18.59999999999999787, 77.36242903720497566, -61.63422623660309796 ) ) ;
#151612=DIRECTION ( 'NONE',  ( 0.000000000000000000, -0.9999631594459053030, -0.008583690987162452199 ) ) ;
#151613=AXIS2_PLACEMENT_3D ( 'NONE', #144707, #40534, #239987 ) ;
#151642=EDGE_LOOP ( 'NONE', ( #173159, #36803, #130790, #195461 ) ) ;
#151646=ADVANCED_FACE ( 'NONE', ( #141414 ), #220941, .T. ) ;
#151653=LINE ( 'NONE', #13405, #162511 ) ;
#151691=DIRECTION ( 'NONE',  ( 0.000000000000000000, 6.938893903907222067E-15, -1.000000000000000000 ) ) ;
#151702=CARTESIAN_POINT ( 'NONE',  ( 21.05000000000000071, 71.00000000001180922, -81.92837350343744163 ) ) ;
#151719=AXIS2_PLACEMENT_3D ( 'NONE', #167285, #49865, #88979 ) ;
#151726=DIRECTION ( 'NONE',  ( 1.000000000000000000, 0.000000000000000000, 0.000000000000000000 ) ) ;
#151730=VERTEX_POINT ( 'NONE', #248231 ) ;
#151734=ORIENTED_EDGE ( 'NONE', *, *, #144634, .F. ) ;
#151761=EDGE_CURVE ( 'NONE', #160189, #155916, #249429, .T. ) ;
#151773=VERTEX_POINT ( 'NONE', #222213 ) ;
#151783=CARTESIAN_POINT ( 'NONE',  ( -22.44366136229477249, 75.99065843052596847, -114.6728260419982206 ) ) ;
#151791=CARTESIAN_POINT ( 'NONE',  ( -18.59999994787167310, 85.52363768977346581, -62.64065794975200419 ) ) ;
#151812=LINE ( 'NONE', #8432, #55386 ) ;
#151829=CARTESIAN_POINT ( 'NONE',  ( 21.87500000000000355, 66.25000000001185185, -90.67310748452437963 ) ) ;
#151839=AXIS2_PLACEMENT_3D ( 'NONE', #60282, #158160, #198521 ) ;
#151847=ADVANCED_FACE ( 'NONE', ( #94280 ), #166237, .F. ) ;
#151850=DIRECTION ( 'NONE',  ( 0.000000000000000000, 0.000000000000000000, 1.000000000000000000 ) ) ;
#151851=EDGE_LOOP ( 'NONE', ( #183456, #148523, #4592, #105880 ) ) ;
#151860=CARTESIAN_POINT ( 'NONE',  ( -18.50000972452446035, 65.70673848566957531, -64.06382523348288771 ) ) ;
#151881=CARTESIAN_POINT ( 'NONE',  ( -20.94999999999999929, 76.00000000001170974, -69.52310748452431710 ) ) ;
#151916=CARTESIAN_POINT ( 'NONE',  ( 20.95512820512820440, 65.37615131630001031, -95.35819391543677170 ) ) ;
#151960=CARTESIAN_POINT ( 'NONE',  ( -23.25000000000000000, 64.35000000001180354, -81.77310748452438816 ) ) ;
#151995=DIRECTION ( 'NONE',  ( 0.000000000000000000, -7.056502275159894776E-15, 1.000000000000000000 ) ) ;
#152009=DIRECTION ( 'NONE',  ( 0.000000000000000000, 0.000000000000000000, -1.000000000000000000 ) ) ;
#152034=DIRECTION ( 'NONE',  ( -0.000000000000000000, 1.000000000000000000, 6.982962677686266711E-15 ) ) ;
#152035=CARTESIAN_POINT ( 'NONE',  ( 18.52326479938722059, 85.64236444492716771, -62.80835007111859625 ) ) ;
#152040=DIRECTION ( 'NONE',  ( 0.000000000000000000, -6.982962677686266711E-15, 1.000000000000000000 ) ) ;
#152054=EDGE_CURVE ( 'NONE', #20503, #182622, #220661, .T. ) ;
#152084=DIRECTION ( 'NONE',  ( 1.000000000000000000, -2.952720810173289112E-16, -2.061873921506763405E-30 ) ) ;
#152086=EDGE_LOOP ( 'NONE', ( #253761, #10390, #118091 ) ) ;
#152113=VERTEX_POINT ( 'NONE', #64155 ) ;
#152165=ORIENTED_EDGE ( 'NONE', *, *, #120056, .F. ) ;
#152176=DIRECTION ( 'NONE',  ( 0.000000000000000000, -7.109473446599835262E-15, 1.000000000000000000 ) ) ;
#152188=VECTOR ( 'NONE', #14203, 1000.000000000000000 ) ;
#152194=ORIENTED_EDGE ( 'NONE', *, *, #43189, .F. ) ;
#152198=ORIENTED_EDGE ( 'NONE', *, *, #188614, .F. ) ;
#152204=CIRCLE ( 'NONE', #106363, 0.1000000000000028644 ) ;
#152242=LINE ( 'NONE', #192630, #34710 ) ;
#152289=ORIENTED_EDGE ( 'NONE', *, *, #23133, .T. ) ;
#152322=TOROIDAL_SURFACE ( 'NONE', #131440, 11.70000000000000639, 0.1000000000000000056 ) ;
#152325=DIRECTION ( 'NONE',  ( -1.000000000000000000, 0.000000000000000000, -0.000000000000000000 ) ) ;
#152328=CARTESIAN_POINT ( 'NONE',  ( 20.94999999999999929, 67.12338541492479749, -94.63802700567968884 ) ) ;
#152355=CARTESIAN_POINT ( 'NONE',  ( 20.95545211741311320, 65.41358668846794444, -95.43696062493610555 ) ) ;
#152366=FACE_OUTER_BOUND ( 'NONE', #177115, .T. ) ;
#152386=CIRCLE ( 'NONE', #73286, 0.1000000000000028644 ) ;
#152394=AXIS2_PLACEMENT_3D ( 'NONE', #149098, #206487, #129520 ) ;
#152444=FACE_OUTER_BOUND ( 'NONE', #204114, .T. ) ;
#152471=EDGE_CURVE ( 'NONE', #140343, #180772, #76977, .T. ) ;
#152484=CARTESIAN_POINT ( 'NONE',  ( -20.64999999999999858, 68.75000000001185185, -90.77310748452435973 ) ) ;
#152502=DIRECTION ( 'NONE',  ( 0.000000000000000000, 0.8660254037844378194, 0.5000000000000016653 ) ) ;
#152507=EDGE_CURVE ( 'NONE', #127256, #206286, #208278, .T. ) ;
#152527=CARTESIAN_POINT ( 'NONE',  ( 18.59999999999999432, 77.83585931145526615, -58.01866831572577610 ) ) ;
#152552=DIRECTION ( 'NONE',  ( -0.7071067811865475727, 0.7071067811865475727, 4.937700262164531476E-15 ) ) ;
#152599=CIRCLE ( 'NONE', #106752, 12.77499999999999503 ) ;
#152653=EDGE_LOOP ( 'NONE', ( #208663, #51033, #56987, #14403 ) ) ;
#152684=ORIENTED_EDGE ( 'NONE', *, *, #53676, .T. ) ;
#152717=ORIENTED_EDGE ( 'NONE', *, *, #153644, .F. ) ;
#152722=EDGE_CURVE ( 'NONE', #170796, #153564, #141623, .T. ) ;
#152727=VERTEX_POINT ( 'NONE', #89804 ) ;
#152731=EDGE_LOOP ( 'NONE', ( #154276, #138693, #2273, #150333 ) ) ;
#152742=AXIS2_PLACEMENT_3D ( 'NONE', #238040, #196349, #195099 ) ;
#152778=VERTEX_POINT ( 'NONE', #154956 ) ;
#152780=EDGE_CURVE ( 'NONE', #97301, #112762, #170727, .T. ) ;
#152785=EDGE_CURVE ( 'NONE', #113902, #156829, #97485, .T. ) ;
#152833=DIRECTION ( 'NONE',  ( -1.000000000000000000, 3.265361837132813093E-16, 2.280189983783949500E-30 ) ) ;
#152848=ORIENTED_EDGE ( 'NONE', *, *, #174193, .F. ) ;
#152889=ORIENTED_EDGE ( 'NONE', *, *, #105550, .F. ) ;
#152903=CARTESIAN_POINT ( 'NONE',  ( -20.95000000000000284, 64.35000000001176090, -76.53791325517833855 ) ) ;
#152906=CARTESIAN_POINT ( 'NONE',  ( 20.94999999999999929, 84.66355140188093742, -79.04720860259155302 ) ) ;
#152917=B_SPLINE_CURVE_WITH_KNOTS ( 'NONE', 3,
 ( #218119, #237711, #100720, #77330, #16116, #257215, #136011 ),
 .UNSPECIFIED., .F., .F.,
 ( 4, 3, 4 ),
 ( 0.000000000000000000, 3.357501770814779694E-05, 5.199112466348563400E-05 ),
 .UNSPECIFIED. ) ;
#152918=ORIENTED_EDGE ( 'NONE', *, *, #94430, .F. ) ;
#152938=CARTESIAN_POINT ( 'NONE',  ( -18.59999999999999787, 74.16465844978745281, -91.46795619196133487 ) ) ;
#152941=CARTESIAN_POINT ( 'NONE',  ( -20.85000000000000142, 65.66751761918648356, -63.92826094061121722 ) ) ;
#152948=CARTESIAN_POINT ( 'NONE',  ( -18.59999999999999787, 64.35000000001171827, -69.52310748452438816 ) ) ;
#153028=CARTESIAN_POINT ( 'NONE',  ( 21.13920837816993270, 67.21675294989194072, -90.77310748452437394 ) ) ;
#153051=AXIS2_PLACEMENT_3D ( 'NONE', #107939, #88347, #153537 ) ;
#153064=EDGE_CURVE ( 'NONE', #178566, #55514, #104372, .T. ) ;
#153078=DIRECTION ( 'NONE',  ( 1.000000000000000000, 0.000000000000000000, 0.000000000000000000 ) ) ;
#153089=CIRCLE ( 'NONE', #219664, 0.09999999999999939493 ) ;
#153091=CARTESIAN_POINT ( 'NONE',  ( -18.58744394320951443, 85.56638515456009486, -62.70025943064806739 ) ) ;
#153107=VERTEX_POINT ( 'NONE', #135026 ) ;
#153116=DIRECTION ( 'NONE',  ( 0.000000000000000000, -1.000000000000000000, -6.982962677686266711E-15 ) ) ;
#153118=CIRCLE ( 'NONE', #173973, 0.09999999999999939493 ) ;
#153130=CARTESIAN_POINT ( 'NONE',  ( 23.15000000000000213, 85.00000000001179501, -79.41707660717668205 ) ) ;
#153180=LINE ( 'NONE', #14926, #253018 ) ;
#153188=DIRECTION ( 'NONE',  ( 1.000000000000000000, 0.000000000000000000, 0.000000000000000000 ) ) ;
#153228=LINE ( 'NONE', #91924, #169289 ) ;
#153232=DIRECTION ( 'NONE',  ( 0.000000000000000000, 6.982962677686266711E-15, -1.000000000000000000 ) ) ;
#153268=EDGE_CURVE ( 'NONE', #16439, #215983, #75391, .T. ) ;
#153306=DIRECTION ( 'NONE',  ( 0.000000000000000000, 0.000000000000000000, -1.000000000000000000 ) ) ;
#153309=EDGE_CURVE ( 'NONE', #103813, #81484, #200173, .T. ) ;
#153331=CARTESIAN_POINT ( 'NONE',  ( 22.39999999999999503, 75.90000000001199965, -109.2731074845243171 ) ) ;
#153332=DIRECTION ( 'NONE',  ( 2.694716079187273439E-16, 1.000000000000000000, 6.467318590049456648E-15 ) ) ;
#153338=LINE ( 'NONE', #172905, #185273 ) ;
#153341=VERTEX_POINT ( 'NONE', #82744 ) ;
#153352=ADVANCED_FACE ( 'NONE', ( #123200 ), #117058, .F. ) ;
#153355=DIRECTION ( 'NONE',  ( 0.000000000000000000, -6.454785026890510900E-15, 1.000000000000000000 ) ) ;
#153376=LINE ( 'NONE', #55470, #215704 ) ;
#153422=FACE_BOUND ( 'NONE', #91633, .T. ) ;
#153442=CARTESIAN_POINT ( 'NONE',  ( -20.85000000000000142, 64.25000000001176659, -76.36470817442145176 ) ) ;
#153475=EDGE_LOOP ( 'NONE', ( #249059, #51365, #147520, #240368, #166462 ) ) ;
#153505=EDGE_LOOP ( 'NONE', ( #237377, #204117, #6128, #5747 ) ) ;
#153513=CARTESIAN_POINT ( 'NONE',  ( 0.000000000000000000, 0.000000000000000000, 0.000000000000000000 ) ) ;
#153537=DIRECTION ( 'NONE',  ( 0.000000000000000000, -7.086529944415894657E-15, 1.000000000000000000 ) ) ;
#153549=ORIENTED_EDGE ( 'NONE', *, *, #144761, .T. ) ;
#153558=ORIENTED_EDGE ( 'NONE', *, *, #22618, .T. ) ;
#153564=VERTEX_POINT ( 'NONE', #116168 ) ;
#153573=DIRECTION ( 'NONE',  ( 0.000000000000000000, 0.9893560106964510714, -0.1455152366551481502 ) ) ;
#153633=DIRECTION ( 'NONE',  ( -1.000000000000000000, 0.000000000000000000, -0.000000000000000000 ) ) ;
#153641=ORIENTED_EDGE ( 'NONE', *, *, #58654, .F. ) ;
#153643=EDGE_CURVE ( 'NONE', #25415, #131827, #162876, .T. ) ;
#153644=EDGE_CURVE ( 'NONE', #171759, #232638, #237388, .T. ) ;
#153653=EDGE_CURVE ( 'NONE', #171995, #103813, #183875, .T. ) ;
#153662=DIRECTION ( 'NONE',  ( -0.000000000000000000, -1.000000000000000000, -6.982962677686266711E-15 ) ) ;
#153688=AXIS2_PLACEMENT_3D ( 'NONE', #62494, #80741, #166428 ) ;
#153699=CARTESIAN_POINT ( 'NONE',  ( -20.94999999999999929, 87.65000000001192859, -100.1231074845242262 ) ) ;
#153709=CARTESIAN_POINT ( 'NONE',  ( 21.05000000000000071, 69.70076908992504627, -103.1215449845243626 ) ) ;
#153755=CARTESIAN_POINT ( 'NONE',  ( 20.94999999999999574, 87.75000000001190870, -99.92310748452422331 ) ) ;
#153763=( BOUNDED_CURVE ( )  B_SPLINE_CURVE ( 3, ( #98886, #139308, #40265, #20692 ),
 .UNSPECIFIED., .F., .F. ) 
 B_SPLINE_CURVE_WITH_KNOTS ( ( 4, 4 ),
 ( 4.712388980384690562, 6.283185307179586232 ),
 .UNSPECIFIED. ) 
 CURVE ( )  GEOMETRIC_REPRESENTATION_ITEM ( )  RATIONAL_B_SPLINE_CURVE ( ( 1.000000000000000000, 0.8047378541243652705, 0.8047378541243652705, 1.000000000000000000 ) ) 
 REPRESENTATION_ITEM ( '' )  );
#153786=CARTESIAN_POINT ( 'NONE',  ( -21.05000000000000071, 85.51932773110434027, -96.05013110796491560 ) ) ;
#153836=ORIENTED_EDGE ( 'NONE', *, *, #227569, .F. ) ;
#153837=DIRECTION ( 'NONE',  ( -0.000000000000000000, 6.982962677686266711E-15, -1.000000000000000000 ) ) ;
#153852=AXIS2_PLACEMENT_3D ( 'NONE', #154212, #95465, #211574 ) ;
#153871=CARTESIAN_POINT ( 'NONE',  ( 21.05933563467872105, 65.27547528793053289, -90.82945973556843455 ) ) ;
#153898=CARTESIAN_POINT ( 'NONE',  ( -23.15000000000000213, 76.00000000001197975, -107.0731074845243143 ) ) ;
#153926=DIRECTION ( 'NONE',  ( 0.000000000000000000, -7.026728003956683390E-15, 1.000000000000000000 ) ) ;
#153928=CIRCLE ( 'NONE', #103950, 0.09999999999999939493 ) ;
#153963=CARTESIAN_POINT ( 'NONE',  ( 23.24999999999999645, 72.10000000001170406, -69.52310748452433131 ) ) ;
#154046=TOROIDAL_SURFACE ( 'NONE', #141507, 0.2000000000000000111, 0.1000000000000000056 ) ;
#154058=VERTEX_POINT ( 'NONE', #183524 ) ;
#154075=CARTESIAN_POINT ( 'NONE',  ( 20.95512820512820085, 67.12384868372377866, -94.46447848938342418 ) ) ;
#154093=ORIENTED_EDGE ( 'NONE', *, *, #165763, .F. ) ;
#154101=DIRECTION ( 'NONE',  ( -1.000000000000000000, 0.000000000000000000, -0.000000000000000000 ) ) ;
#154118=DIRECTION ( 'NONE',  ( 0.000000000000000000, 0.8660254037844377084, 0.5000000000000015543 ) ) ;
#154147=CARTESIAN_POINT ( 'NONE',  ( -18.41353343127311248, 85.50000000001190870, -95.99103808782456326 ) ) ;
#154185=EDGE_CURVE ( 'NONE', #125531, #8374, #113144, .T. ) ;
#154212=CARTESIAN_POINT ( 'NONE',  ( -20.64999999999999858, 71.65000000001180069, -81.87310748452433984 ) ) ;
#154269=VECTOR ( 'NONE', #200306, 1000.000000000000000 ) ;
#154276=ORIENTED_EDGE ( 'NONE', *, *, #205141, .T. ) ;
#154282=EDGE_CURVE ( 'NONE', #254425, #92348, #104900, .T. ) ;
#154303=ADVANCED_FACE ( 'NONE', ( #174274 ), #236746, .T. ) ;
#154309=VERTEX_POINT ( 'NONE', #37300 ) ;
#154347=TOROIDAL_SURFACE ( 'NONE', #166801, 0.2000000000000000111, 0.1000000000000000056 ) ;
#154354=CIRCLE ( 'NONE', #37622, 0.2000000000000057288 ) ;
#154377=FACE_OUTER_BOUND ( 'NONE', #253167, .T. ) ;
#154392=EDGE_LOOP ( 'NONE', ( #72599, #38298, #25390, #54121 ) ) ;
#154400=VERTEX_POINT ( 'NONE', #249482 ) ;
#154480=ORIENTED_EDGE ( 'NONE', *, *, #148424, .T. ) ;
#154485=CARTESIAN_POINT ( 'NONE',  ( -18.59999999999999787, 74.75000000001189449, -95.02310748452431710 ) ) ;
#154500=DIRECTION ( 'NONE',  ( 1.000000000000000000, 0.000000000000000000, 0.000000000000000000 ) ) ;
#154512=ORIENTED_EDGE ( 'NONE', *, *, #121139, .F. ) ;
#154533=FACE_OUTER_BOUND ( 'NONE', #144933, .T. ) ;
#154543=DIRECTION ( 'NONE',  ( 1.000000000000000000, 0.000000000000000000, 0.000000000000000000 ) ) ;
#154555=EDGE_CURVE ( 'NONE', #71706, #206437, #250857, .T. ) ;
#154562=TOROIDAL_SURFACE ( 'NONE', #150461, 11.70000000000000462, 0.1000000000000000056 ) ;
#154571=CARTESIAN_POINT ( 'NONE',  ( -23.25000000000000000, 76.00000000001195133, -103.0231074845243171 ) ) ;
#154612=CARTESIAN_POINT ( 'NONE',  ( 18.50000000000000355, 85.40000000001165859, -62.64106563635154856 ) ) ;
#154628=EDGE_CURVE ( 'NONE', #121241, #158368, #21757, .T. ) ;
#154632=EDGE_CURVE ( 'NONE', #74222, #40972, #88349, .T. ) ;
#154673=EDGE_CURVE ( 'NONE', #156346, #30659, #168972, .T. ) ;
#154675=AXIS2_PLACEMENT_3D ( 'NONE', #179966, #236071, #1295 ) ;
#154686=CIRCLE ( 'NONE', #17131, 0.09999999999999939493 ) ;
#154716=LINE ( 'NONE', #37325, #63718 ) ;
#154720=EDGE_CURVE ( 'NONE', #9387, #17853, #188331, .T. ) ;
#154733=CARTESIAN_POINT ( 'NONE',  ( -20.54999999999999716, 85.50000000001179501, -79.41707660717668205 ) ) ;
#154748=DIRECTION ( 'NONE',  ( 1.000000000000000000, 0.000000000000000000, 0.000000000000000000 ) ) ;
#154774=ORIENTED_EDGE ( 'NONE', *, *, #186153, .T. ) ;
#154786=ORIENTED_EDGE ( 'NONE', *, *, #115285, .F. ) ;
#154814=DIRECTION ( 'NONE',  ( 0.000000000000000000, 7.116814260417668513E-15, -1.000000000000000000 ) ) ;
#154818=EDGE_LOOP ( 'NONE', ( #202144, #151373, #184972 ) ) ;
#154831=CARTESIAN_POINT ( 'NONE',  ( -18.59999999999999787, 64.25000000001170974, -69.52310748452438816 ) ) ;
#154877=CARTESIAN_POINT ( 'NONE',  ( 18.59999999999998366, 68.97833521811159585, -65.68954208262705663 ) ) ;
#154928=ORIENTED_EDGE ( 'NONE', *, *, #112760, .F. ) ;
#154956=CARTESIAN_POINT ( 'NONE',  ( -21.14999999999999858, 64.25000000001190870, -96.23924182154622997 ) ) ;
#154975=CARTESIAN_POINT ( 'NONE',  ( -21.05000000000000071, 75.90220970870321082, -109.2809220950004203 ) ) ;
#154980=EDGE_LOOP ( 'NONE', ( #165788, #158376, #241809, #209177 ) ) ;
#154993=ORIENTED_EDGE ( 'NONE', *, *, #131688, .T. ) ;
#154997=DIRECTION ( 'NONE',  ( -0.000000000000000000, -6.982962677686266711E-15, 1.000000000000000000 ) ) ;
#155012=CARTESIAN_POINT ( 'NONE',  ( 21.05000000000000071, 76.10000000001194564, -103.0231074845243171 ) ) ;
#155059=AXIS2_PLACEMENT_3D ( 'NONE', #83086, #81806, #80529 ) ;
#155101=LINE ( 'NONE', #82860, #123254 ) ;
#155119=AXIS2_PLACEMENT_3D ( 'NONE', #192397, #93284, #153306 ) ;
#155125=FACE_OUTER_BOUND ( 'NONE', #111383, .T. ) ;
#155186=DIRECTION ( 'NONE',  ( -1.000000000000000000, 2.952720810173289112E-16, 2.061873921506763405E-30 ) ) ;
#155190=ORIENTED_EDGE ( 'NONE', *, *, #187950, .T. ) ;
#155243=CARTESIAN_POINT ( 'NONE',  ( -18.50000000000000000, 76.00000000001170974, -69.52310748452431710 ) ) ;
#155271=DIRECTION ( 'NONE',  ( 1.000000000000000000, 0.000000000000000000, 0.000000000000000000 ) ) ;
#155291=DIRECTION ( 'NONE',  ( 2.827886303505249259E-16, 0.8660254037844377084, 0.5000000000000016653 ) ) ;
#155330=ORIENTED_EDGE ( 'NONE', *, *, #198067, .T. ) ;
#155355=AXIS2_PLACEMENT_3D ( 'NONE', #112541, #14743, #151691 ) ;
#155360=ORIENTED_EDGE ( 'NONE', *, *, #43026, .T. ) ;
#155391=AXIS2_PLACEMENT_3D ( 'NONE', #195614, #96460, #136893 ) ;
#155395=AXIS2_PLACEMENT_3D ( 'NONE', #63265, #179392, #80229 ) ;
#155423=ADVANCED_FACE ( 'NONE', ( #251703 ), #33987, .F. ) ;
#155429=DIRECTION ( 'NONE',  ( 1.000000000000000000, 0.000000000000000000, 0.000000000000000000 ) ) ;
#155441=CARTESIAN_POINT ( 'NONE',  ( 18.59999999999999787, 76.00000000001195133, -103.0231074845243171 ) ) ;
#155448=CYLINDRICAL_SURFACE ( 'NONE', #159836, 11.74999999999999645 ) ;
#155456=ORIENTED_EDGE ( 'NONE', *, *, #203929, .F. ) ;
#155461=DIRECTION ( 'NONE',  ( 0.000000000000000000, 0.000000000000000000, 1.000000000000000000 ) ) ;
#155473=CARTESIAN_POINT ( 'NONE',  ( 23.25000000000000000, 85.00000000001179501, -79.41707660717668205 ) ) ;
#155489=DIRECTION ( 'NONE',  ( -1.000000000000000000, 0.000000000000000000, 0.000000000000000000 ) ) ;
#155490=CARTESIAN_POINT ( 'NONE',  ( 22.43288208788031568, 75.99510014512664213, -114.6727593282433872 ) ) ;
#155492=ORIENTED_EDGE ( 'NONE', *, *, #38029, .F. ) ;
#155501=VECTOR ( 'NONE', #160697, 1000.000000000000000 ) ;
#155509=CARTESIAN_POINT ( 'NONE',  ( 21.05000000000000071, 76.00000000001195133, -103.0231074845243171 ) ) ;
#155548=ORIENTED_EDGE ( 'NONE', *, *, #24403, .T. ) ;
#155562=EDGE_CURVE ( 'NONE', #53558, #256577, #11839, .T. ) ;
#155571=DIRECTION ( 'NONE',  ( -1.000000000000000000, 3.265361837132813093E-16, 2.280189983783949500E-30 ) ) ;
#155577=TOROIDAL_SURFACE ( 'NONE', #72342, 0.2000000000000000111, 0.1000000000000000056 ) ;
#155578=DIRECTION ( 'NONE',  ( -0.000000000000000000, 1.000000000000000000, 6.982962677686266711E-15 ) ) ;
#155591=VERTEX_POINT ( 'NONE', #121221 ) ;
#155595=ORIENTED_EDGE ( 'NONE', *, *, #251627, .F. ) ;
#155597=VERTEX_POINT ( 'NONE', #117331 ) ;
#155608=CARTESIAN_POINT ( 'NONE',  ( 23.14999999999999858, 70.50000000001180922, -81.92837350343744163 ) ) ;
#155624=ADVANCED_FACE ( 'NONE', ( #177339 ), #119934, .F. ) ;
#155644=ADVANCED_FACE ( 'NONE', ( #159052 ), #178617, .F. ) ;
#155656=FACE_OUTER_BOUND ( 'NONE', #166557, .T. ) ;
#155663=CARTESIAN_POINT ( 'NONE',  ( -23.15000000000000213, 71.65000000001187175, -90.87310748452432563 ) ) ;
#155669=FACE_OUTER_BOUND ( 'NONE', #210929, .T. ) ;
#155684=CIRCLE ( 'NONE', #176513, 0.1000000000000014488 ) ;
#155711=DIRECTION ( 'NONE',  ( 1.000000000000000000, 0.000000000000000000, 0.000000000000000000 ) ) ;
#155727=DIRECTION ( 'NONE',  ( 0.000000000000000000, 5.880418562633242623E-15, -1.000000000000000000 ) ) ;
#155729=DIRECTION ( 'NONE',  ( -1.000000000000000000, 2.952720810173289112E-16, 2.061873921506763405E-30 ) ) ;
#155736=DIRECTION ( 'NONE',  ( -1.000000000000000000, 0.000000000000000000, -0.000000000000000000 ) ) ;
#155786=ORIENTED_EDGE ( 'NONE', *, *, #43192, .F. ) ;
#155791=ORIENTED_EDGE ( 'NONE', *, *, #216778, .T. ) ;
#155810=ORIENTED_EDGE ( 'NONE', *, *, #176937, .T. ) ;
#155811=CARTESIAN_POINT ( 'NONE',  ( 21.05000000000000071, 87.65000000001172964, -72.42310748452422331 ) ) ;
#155820=FACE_OUTER_BOUND ( 'NONE', #77227, .T. ) ;
#155866=ADVANCED_FACE ( 'NONE', ( #171898 ), #5124, .T. ) ;
#155916=VERTEX_POINT ( 'NONE', #213539 ) ;
#155954=VERTEX_POINT ( 'NONE', #240825 ) ;
#155971=DIRECTION ( 'NONE',  ( 0.000000000000000000, -7.272083257015735086E-15, 1.000000000000000000 ) ) ;
#155979=ORIENTED_EDGE ( 'NONE', *, *, #133816, .T. ) ;
#155980=AXIS2_PLACEMENT_3D ( 'NONE', #111891, #193998, #113159 ) ;
#155994=ORIENTED_EDGE ( 'NONE', *, *, #159691, .F. ) ;
#156029=VECTOR ( 'NONE', #93702, 1000.000000000000000 ) ;
#156101=EDGE_CURVE ( 'NONE', #192851, #164178, #88523, .T. ) ;
#156111=ORIENTED_EDGE ( 'NONE', *, *, #89306, .T. ) ;
#156116=CARTESIAN_POINT ( 'NONE',  ( 20.94999999999999929, 69.35000000001186038, -90.87310748452435405 ) ) ;
#156133=AXIS2_PLACEMENT_3D ( 'NONE', #180451, #160904, #1791 ) ;
#156170=VERTEX_POINT ( 'NONE', #82988 ) ;
#156193=ORIENTED_EDGE ( 'NONE', *, *, #13932, .F. ) ;
#156195=CARTESIAN_POINT ( 'NONE',  ( -21.05000000000000071, 70.10000000001177511, -79.74220724918072278 ) ) ;
#156207=AXIS2_PLACEMENT_3D ( 'NONE', #106556, #249945, #71328 ) ;
#156215=CARTESIAN_POINT ( 'NONE',  ( -21.05000000000000071, 77.16270174994990327, -95.02310748452430289 ) ) ;
#156230=DIRECTION ( 'NONE',  ( 0.000000000000000000, 0.000000000000000000, 1.000000000000000000 ) ) ;
#156232=EDGE_CURVE ( 'NONE', #5184, #82775, #30783, .T. ) ;
#156259=VECTOR ( 'NONE', #136266, 1000.000000000000000 ) ;
#156264=CARTESIAN_POINT ( 'NONE',  ( -23.15000000000000213, 76.00000000001170974, -69.52310748452431710 ) ) ;
#156266=DIRECTION ( 'NONE',  ( 1.000000000000000000, -7.304098846218134667E-16, -5.100424963727256530E-30 ) ) ;
#156271=LINE ( 'NONE', #113261, #156401 ) ;
#156297=ORIENTED_EDGE ( 'NONE', *, *, #84739, .F. ) ;
#156338=EDGE_CURVE ( 'NONE', #242014, #200486, #1873, .T. ) ;
#156346=VERTEX_POINT ( 'NONE', #58951 ) ;
#156354=CARTESIAN_POINT ( 'NONE',  ( 23.24999999999999645, 71.22429906543244726, -91.17433938047835795 ) ) ;
#156358=ORIENTED_EDGE ( 'NONE', *, *, #169580, .F. ) ;
#156366=DIRECTION ( 'NONE',  ( 0.000000000000000000, 0.8700118002898356018, -0.4930308989875170078 ) ) ;
#156401=VECTOR ( 'NONE', #256560, 1000.000000000000000 ) ;
#156406=ORIENTED_EDGE ( 'NONE', *, *, #188411, .T. ) ;
#156416=CARTESIAN_POINT ( 'NONE',  ( -20.64999999999999858, 85.50000000001179501, -79.41707660717668205 ) ) ;
#156428=ORIENTED_EDGE ( 'NONE', *, *, #256308, .F. ) ;
#156429=AXIS2_PLACEMENT_3D ( 'NONE', #46860, #164275, #85973 ) ;
#156450=CARTESIAN_POINT ( 'NONE',  ( -21.05000000000000071, 77.26178616857691850, -94.93660852097882241 ) ) ;
#156452=EDGE_LOOP ( 'NONE', ( #204483, #238238, #25778, #19373 ) ) ;
#156492=CYLINDRICAL_SURFACE ( 'NONE', #188510, 0.09999999999999520384 ) ;
#156505=TOROIDAL_SURFACE ( 'NONE', #44032, 0.2000000000000000111, 0.1000000000000000056 ) ;
#156529=AXIS2_PLACEMENT_3D ( 'NONE', #199851, #23794, #103271 ) ;
#156544=DIRECTION ( 'NONE',  ( 0.000000000000000000, 0.000000000000000000, -1.000000000000000000 ) ) ;
#156567=EDGE_CURVE ( 'NONE', #155954, #229799, #9281, .T. ) ;
#156612=DIRECTION ( 'NONE',  ( 0.000000000000000000, -6.982962677686266711E-15, 1.000000000000000000 ) ) ;
#156653=CARTESIAN_POINT ( 'NONE',  ( 21.78635804494511419, 75.90099493450432533, -110.0587689696774873 ) ) ;
#156663=EDGE_LOOP ( 'NONE', ( #217387, #46208, #88684 ) ) ;
#156675=CIRCLE ( 'NONE', #189959, 0.1000000000000028644 ) ;
#156705=DIRECTION ( 'NONE',  ( -1.000000000000000000, 0.000000000000000000, -0.000000000000000000 ) ) ;
#156708=DIRECTION ( 'NONE',  ( 0.000000000000000000, 6.982962677686266711E-15, -1.000000000000000000 ) ) ;
#156716=CARTESIAN_POINT ( 'NONE',  ( 18.59999999999998721, 56.14960075277838314, -100.7428044267230973 ) ) ;
#156745=CIRCLE ( 'NONE', #119299, 0.1000000000000028644 ) ;
#156763=CARTESIAN_POINT ( 'NONE',  ( 22.46250603428203618, 75.97885582387323211, -114.6729705818644049 ) ) ;
#156778=VERTEX_POINT ( 'NONE', #202044 ) ;
#156806=AXIS2_PLACEMENT_3D ( 'NONE', #247142, #170243, #213158 ) ;
#156825=CARTESIAN_POINT ( 'NONE',  ( 21.05000000000000071, 65.27628289530434813, -90.87310748452438247 ) ) ;
#156829=VERTEX_POINT ( 'NONE', #228026 ) ;
#156860=AXIS2_PLACEMENT_3D ( 'NONE', #154571, #176687, #94549 ) ;
#156869=DIRECTION ( 'NONE',  ( 1.000000000000000000, 7.304098846218134667E-16, 5.100424963727256530E-30 ) ) ;
#156889=ORIENTED_EDGE ( 'NONE', *, *, #87612, .F. ) ;
#156892=ADVANCED_FACE ( 'NONE', ( #27292 ), #67661, .F. ) ;
#156895=DIRECTION ( 'NONE',  ( 1.000000000000000000, 0.000000000000000000, 0.000000000000000000 ) ) ;
#156902=ADVANCED_FACE ( 'NONE', ( #15411 ), #97726, .F. ) ;
#156926=CARTESIAN_POINT ( 'NONE',  ( -18.50000000000000000, 85.48068669529064323, -62.58199231576639932 ) ) ;
#156948=EDGE_LOOP ( 'NONE', ( #139283, #190630, #142455 ) ) ;
#156969=DIRECTION ( 'NONE',  ( 0.000000000000000000, 7.026728003956683390E-15, -1.000000000000000000 ) ) ;
#156970=AXIS2_PLACEMENT_3D ( 'NONE', #21074, #78437, #56298 ) ;
#156976=FACE_OUTER_BOUND ( 'NONE', #152653, .T. ) ;
#156998=EDGE_CURVE ( 'NONE', #91045, #237782, #174528, .T. ) ;
#156999=CARTESIAN_POINT ( 'NONE',  ( 18.49999999999999645, 76.00000000001195133, -103.0231074845243171 ) ) ;
#157002=CARTESIAN_POINT ( 'NONE',  ( -18.50000000000000000, 77.73625713160926409, -91.45445515550680682 ) ) ;
#157041=DIRECTION ( 'NONE',  ( 7.304098846218134667E-16, 1.000000000000000000, 6.982962677686267499E-15 ) ) ;
#157067=VERTEX_POINT ( 'NONE', #252703 ) ;
#157082=ADVANCED_FACE ( 'NONE', ( #213583 ), #2236, .F. ) ;
#157083=DIRECTION ( 'NONE',  ( 1.301042606982683734E-14, 0.8660254037844367092, -0.5000000000000037748 ) ) ;
#157084=ORIENTED_EDGE ( 'NONE', *, *, #160448, .T. ) ;
#157089=ORIENTED_EDGE ( 'NONE', *, *, #233851, .F. ) ;
#157130=CARTESIAN_POINT ( 'NONE',  ( -20.85000000000000142, 77.73670573947921980, -58.00568489690056850 ) ) ;
#157184=ADVANCED_FACE ( 'NONE', ( #146862 ), #166483, .T. ) ;
#157219=CARTESIAN_POINT ( 'NONE',  ( 21.05000000000000071, 76.00000000001168132, -65.42310748452432279 ) ) ;
#157231=B_SPLINE_CURVE_WITH_KNOTS ( 'NONE', 3,
 ( #118146, #39923, #97253, #176856, #54305, #93432, #135119, #19041, #178143, #257591 ),
 .UNSPECIFIED., .F., .F.,
 ( 4, 3, 3, 4 ),
 ( 0.000000000000000000, 3.394313611809514494E-05, 6.779740500699831776E-05, 0.0001049857339142602552 ),
 .UNSPECIFIED. ) ;
#157306=ORIENTED_EDGE ( 'NONE', *, *, #96733, .T. ) ;
#157360=ORIENTED_EDGE ( 'NONE', *, *, #35803, .T. ) ;
#157365=EDGE_CURVE ( 'NONE', #66860, #190582, #231244, .T. ) ;
#157378=ORIENTED_EDGE ( 'NONE', *, *, #199663, .F. ) ;
#157422=EDGE_CURVE ( 'NONE', #20758, #77073, #39706, .T. ) ;
#157425=CIRCLE ( 'NONE', #240779, 0.2000000000000057288 ) ;
#157438=CARTESIAN_POINT ( 'NONE',  ( 22.50000000000000000, 75.90000000001199965, -110.8138870828976934 ) ) ;
#157448=DIRECTION ( 'NONE',  ( 0.000000000000000000, 0.1298341882519953583, 0.9915357197604862671 ) ) ;
#157464=ORIENTED_EDGE ( 'NONE', *, *, #200097, .F. ) ;
#157475=CARTESIAN_POINT ( 'NONE',  ( 21.05000000000000071, 77.16270174994990327, -94.92310748452430857 ) ) ;
#157485=DIRECTION ( 'NONE',  ( -0.000000000000000000, -6.982962677686266711E-15, 1.000000000000000000 ) ) ;
#157507=EDGE_CURVE ( 'NONE', #64319, #200486, #164382, .T. ) ;
#157530=( BOUNDED_SURFACE ( )  B_SPLINE_SURFACE ( 3, 2, ( 
 ( #45133, #43857, #187234 ),
 ( #86807, #243320, #8579 ),
 ( #46399, #167671, #144213 ),
 ( #108945, #68555, #247170 ) ),
 .UNSPECIFIED., .F., .F., .F. ) 
 B_SPLINE_SURFACE_WITH_KNOTS ( ( 4, 4 ),
 ( 3, 3 ),
 ( 0.0006461284895274055275, 0.0007503702773986016886 ),
 ( 0.000000000000000000, 1.000000000000000000 ),
 .UNSPECIFIED. ) 
 GEOMETRIC_REPRESENTATION_ITEM ( )  RATIONAL_B_SPLINE_SURFACE ( (
 ( 1.000000000000000000, 0.7071067811865471286, 1.000000000000000000),
 ( 1.000000000000000000, 0.7076476444648464037, 1.000000000000000000),
 ( 1.000000000000000000, 0.7075727925192379919, 1.000000000000000000),
 ( 1.000000000000000000, 0.7071067811865229258, 1.000000000000000000) ) ) 
 REPRESENTATION_ITEM ( '' )  SURFACE ( )  );
#157542=CARTESIAN_POINT ( 'NONE',  ( 21.05000000000000071, 69.45934304831071415, -102.9231074845243512 ) ) ;
#157544=ORIENTED_EDGE ( 'NONE', *, *, #90341, .T. ) ;
#157559=CARTESIAN_POINT ( 'NONE',  ( 23.25000000000000000, 64.25000000001179501, -81.67310748452439384 ) ) ;
#157577=EDGE_LOOP ( 'NONE', ( #177209, #154480, #194987, #126369 ) ) ;
#157583=CIRCLE ( 'NONE', #165939, 0.09999999999999938105 ) ;
#157610=VERTEX_POINT ( 'NONE', #97137 ) ;
#157645=DIRECTION ( 'NONE',  ( -2.952720810173289112E-16, -1.000000000000000000, -6.982962677686266711E-15 ) ) ;
#157656=EDGE_CURVE ( 'NONE', #147363, #235864, #8371, .T. ) ;
#157658=LINE ( 'NONE', #237156, #13526 ) ;
#157683=DIRECTION ( 'NONE',  ( 0.000000000000000000, -6.982962677686266711E-15, 1.000000000000000000 ) ) ;
#157714=CARTESIAN_POINT ( 'NONE',  ( -23.15000000000000213, 64.35000000001180354, -81.67310748452439384 ) ) ;
#157718=CIRCLE ( 'NONE', #253512, 0.09999999999999939493 ) ;
#157789=FACE_OUTER_BOUND ( 'NONE', #26723, .T. ) ;
#157805=FACE_OUTER_BOUND ( 'NONE', #4522, .T. ) ;
#157856=FACE_OUTER_BOUND ( 'NONE', #136814, .T. ) ;
#157870=DIRECTION ( 'NONE',  ( 1.000000000000000000, 0.000000000000000000, 0.000000000000000000 ) ) ;
#157897=DIRECTION ( 'NONE',  ( 0.000000000000000000, -1.000000000000000000, 0.000000000000000000 ) ) ;
#157902=LINE ( 'NONE', #177447, #103953 ) ;
#157906=CARTESIAN_POINT ( 'NONE',  ( 18.59999999999999076, 64.35000000001170406, -69.52310748452438816 ) ) ;
#157910=DIRECTION ( 'NONE',  ( 1.000000000000000000, -0.000000000000000000, 0.000000000000000000 ) ) ;
#157914=TOROIDAL_SURFACE ( 'NONE', #70409, 0.6000000000000015321, 0.1000000000000000056 ) ;
#157919=CARTESIAN_POINT ( 'NONE',  ( 23.24999999999999645, 76.00000000001170974, -69.52310748452431710 ) ) ;
#157948=DIRECTION ( 'NONE',  ( 0.000000000000000000, -0.8660254037844468122, -0.4999999999999859557 ) ) ;
#157954=CARTESIAN_POINT ( 'NONE',  ( -23.15000000000000213, 76.00000000001173817, -73.52310748452431710 ) ) ;
#157973=CARTESIAN_POINT ( 'NONE',  ( 18.52130828395273099, 85.48139550263771014, -95.99860076064064174 ) ) ;
#157975=VERTEX_POINT ( 'NONE', #165730 ) ;
#157979=ORIENTED_EDGE ( 'NONE', *, *, #200952, .T. ) ;
#158010=CYLINDRICAL_SURFACE ( 'NONE', #114796, 0.09999999999999867328 ) ;
#158015=EDGE_CURVE ( 'NONE', #82517, #237924, #77064, .T. ) ;
#158021=CIRCLE ( 'NONE', #37188, 0.09999999999999967248 ) ;
#158054=DIRECTION ( 'NONE',  ( 0.000000000000000000, 0.000000000000000000, -1.000000000000000000 ) ) ;
#158062=DIRECTION ( 'NONE',  ( 1.000000000000000000, 0.000000000000000000, 0.000000000000000000 ) ) ;
#158071=VECTOR ( 'NONE', #120286, 1000.000000000000000 ) ;
#158110=ORIENTED_EDGE ( 'NONE', *, *, #241800, .F. ) ;
#158157=CARTESIAN_POINT ( 'NONE',  ( -22.50485643085238863, 76.07878633908924826, -114.7729024236967206 ) ) ;
#158160=DIRECTION ( 'NONE',  ( 1.000000000000000000, -0.000000000000000000, 0.000000000000000000 ) ) ;
#158175=DIRECTION ( 'NONE',  ( 1.000000000000000000, 0.000000000000000000, 0.000000000000000000 ) ) ;
#158182=DIRECTION ( 'NONE',  ( 1.000000000000000000, 0.000000000000000000, 0.000000000000000000 ) ) ;
#158183=ORIENTED_EDGE ( 'NONE', *, *, #70126, .F. ) ;
#158209=EDGE_CURVE ( 'NONE', #226147, #1991, #231388, .T. ) ;
#158238=CIRCLE ( 'NONE', #41700, 0.09999999999999939493 ) ;
#158239=ORIENTED_EDGE ( 'NONE', *, *, #126456, .F. ) ;
#158244=VECTOR ( 'NONE', #202619, 1000.000000000000000 ) ;
#158249=DIRECTION ( 'NONE',  ( 0.000000000000000000, 0.000000000000000000, 1.000000000000000000 ) ) ;
#158283=ORIENTED_EDGE ( 'NONE', *, *, #112913, .F. ) ;
#158294=VECTOR ( 'NONE', #33841, 1000.000000000000000 ) ;
#158307=CIRCLE ( 'NONE', #133336, 0.1000000000000028644 ) ;
#158332=CARTESIAN_POINT ( 'NONE',  ( 23.14999999999999503, 69.45000000001181206, -81.77310748452434552 ) ) ;
#158347=DIRECTION ( 'NONE',  ( 1.000000000000000000, 0.000000000000000000, 0.000000000000000000 ) ) ;
#158368=VERTEX_POINT ( 'NONE', #86037 ) ;
#158376=ORIENTED_EDGE ( 'NONE', *, *, #249436, .F. ) ;
#158426=FACE_OUTER_BOUND ( 'NONE', #226767, .T. ) ;
#158433=CARTESIAN_POINT ( 'NONE',  ( -23.15000000000000213, 64.25000000001175238, -76.36470817442145176 ) ) ;
#158440=DIRECTION ( 'NONE',  ( 0.000000000000000000, -1.000000000000000000, -6.982962677686265922E-15 ) ) ;
#158445=CARTESIAN_POINT ( 'NONE',  ( -21.98333005346336932, 76.00000000001200817, -110.3971828135809972 ) ) ;
#158453=CARTESIAN_POINT ( 'NONE',  ( 20.85000000000000142, 77.36242903720497566, -61.63422623660309796 ) ) ;
#158461=EDGE_CURVE ( 'NONE', #96396, #201799, #52290, .T. ) ;
#158477=ORIENTED_EDGE ( 'NONE', *, *, #166920, .T. ) ;
#158482=TOROIDAL_SURFACE ( 'NONE', #116754, 0.2000000000000000111, 0.1000000000000000056 ) ;
#158484=EDGE_CURVE ( 'NONE', #140050, #129734, #77242, .T. ) ;
#158527=PLANE ( 'NONE',  #84582 ) ;
#158557=ORIENTED_EDGE ( 'NONE', *, *, #224924, .F. ) ;
#158565=CARTESIAN_POINT ( 'NONE',  ( -21.29999999999995808, 76.00000000001195133, -103.0231074845243171 ) ) ;
#158577=FACE_OUTER_BOUND ( 'NONE', #42135, .T. ) ;
#158581=DIRECTION ( 'NONE',  ( 1.000000000000000000, 0.000000000000000000, 0.000000000000000000 ) ) ;
#158604=CIRCLE ( 'NONE', #104392, 11.70000000000000284 ) ;
#158615=VERTEX_POINT ( 'NONE', #216276 ) ;
#158733=ORIENTED_EDGE ( 'NONE', *, *, #43565, .F. ) ;
#158742=CARTESIAN_POINT ( 'NONE',  ( -21.65000000000000213, 68.29142135624910281, -81.87310748452436826 ) ) ;
#158756=ORIENTED_EDGE ( 'NONE', *, *, #127131, .T. ) ;
#158766=CARTESIAN_POINT ( 'NONE',  ( -18.50000000000000000, 74.13328508995456900, -91.27043223824230722 ) ) ;
#158767=EDGE_CURVE ( 'NONE', #68348, #127173, #48389, .T. ) ;
#158768=CYLINDRICAL_SURFACE ( 'NONE', #1765, 0.09999999999999939493 ) ;
#158769=DIRECTION ( 'NONE',  ( 1.000000000000000000, 0.000000000000000000, 0.000000000000000000 ) ) ;
#158780=CARTESIAN_POINT ( 'NONE',  ( -20.64999999999999858, 85.00000000001188027, -93.12913836187181005 ) ) ;
#158794=ORIENTED_EDGE ( 'NONE', *, *, #111778, .F. ) ;
#158814=CARTESIAN_POINT ( 'NONE',  ( -23.15000000000000213, 74.00000000001186606, -90.29848556176222019 ) ) ;
#158833=VERTEX_POINT ( 'NONE', #110455 ) ;
#158847=CARTESIAN_POINT ( 'NONE',  ( 23.14999999999999858, 73.90000000001170122, -69.52310748452431710 ) ) ;
#158857=DIRECTION ( 'NONE',  ( 0.000000000000000000, 0.000000000000000000, 1.000000000000000000 ) ) ;
#158859=VERTEX_POINT ( 'NONE', #127458 ) ;
#158868=FACE_OUTER_BOUND ( 'NONE', #112488, .T. ) ;
#158869=AXIS2_PLACEMENT_3D ( 'NONE', #189329, #51053, #109771 ) ;
#158885=DIRECTION ( 'NONE',  ( 0.000000000000000000, 0.8660254037844377084, 0.5000000000000016653 ) ) ;
#158891=CARTESIAN_POINT ( 'NONE',  ( 18.59999999999999787, 77.83534155023627932, -91.46795619196132066 ) ) ;
#158900=EDGE_CURVE ( 'NONE', #10704, #118654, #97269, .T. ) ;
#158905=CARTESIAN_POINT ( 'NONE',  ( 20.95595012432476523, 65.39582078693575795, -95.42733815430624134 ) ) ;
#158924=DIRECTION ( 'NONE',  ( 0.000000000000000000, 0.000000000000000000, -1.000000000000000000 ) ) ;
#158972=ORIENTED_EDGE ( 'NONE', *, *, #201553, .T. ) ;
#159011=EDGE_LOOP ( 'NONE', ( #58699, #114342, #1328, #25099 ) ) ;
#159034=CARTESIAN_POINT ( 'NONE',  ( 18.49999999999999289, 64.25000000001176659, -78.17310748452439384 ) ) ;
#159045=CARTESIAN_POINT ( 'NONE',  ( 18.39999999999999858, 85.68240343348806221, -62.86626410711144786 ) ) ;
#159052=FACE_OUTER_BOUND ( 'NONE', #186421, .T. ) ;
#159053=( BOUNDED_SURFACE ( )  B_SPLINE_SURFACE ( 3, 2, ( 
 ( #201058, #224463, #142361 ),
 ( #1560, #141096, #221878 ),
 ( #122826, #163230, #202343 ),
 ( #43276, #45835, #83638 ) ),
 .UNSPECIFIED., .F., .F., .F. ) 
 B_SPLINE_SURFACE_WITH_KNOTS ( ( 4, 4 ),
 ( 3, 3 ),
 ( -3.469446951953614189E-18, 0.001979672783031532438 ),
 ( 0.000000000000000000, 1.000000000000000000 ),
 .UNSPECIFIED. ) 
 GEOMETRIC_REPRESENTATION_ITEM ( )  RATIONAL_B_SPLINE_SURFACE ( (
 ( 1.000000000000000000, 0.7103081912008384347, 1.000000000000000000),
 ( 1.000000000000000000, 0.7104998333558171231, 1.000000000000000000),
 ( 1.000000000000000000, 0.7107238315755857183, 1.000000000000000000),
 ( 1.000000000000000000, 0.7110073749538864396, 1.000000000000000000) ) ) 
 REPRESENTATION_ITEM ( '' )  SURFACE ( )  );
#159067=CARTESIAN_POINT ( 'NONE',  ( -22.39999999999999858, 76.00000000001203659, -114.6726782920691079 ) ) ;
#159125=ORIENTED_EDGE ( 'NONE', *, *, #189455, .F. ) ;
#159138=AXIS2_PLACEMENT_3D ( 'NONE', #80683, #175046, #234975 ) ;
#159144=ORIENTED_EDGE ( 'NONE', *, *, #107179, .T. ) ;
#159175=CARTESIAN_POINT ( 'NONE',  ( -20.54999999999999716, 76.00000000001185185, -90.04810748452430857 ) ) ;
#159179=CARTESIAN_POINT ( 'NONE',  ( -21.14999999999999858, 76.10000000001203091, -114.6726782920691221 ) ) ;
#159187=AXIS2_PLACEMENT_3D ( 'NONE', #33940, #13065, #55988 ) ;
#159215=EDGE_LOOP ( 'NONE', ( #196750, #66147, #174138, #198390 ) ) ;
#159228=VERTEX_POINT ( 'NONE', #252219 ) ;
#159264=ORIENTED_EDGE ( 'NONE', *, *, #118928, .F. ) ;
#159280=ADVANCED_FACE ( 'NONE', ( #197384 ), #18752, .F. ) ;
#159287=DIRECTION ( 'NONE',  ( 0.000000000000000000, -1.000000000000000000, -6.982962677686265922E-15 ) ) ;
#159325=DIRECTION ( 'NONE',  ( -1.000000000000000000, 0.000000000000000000, 0.000000000000000000 ) ) ;
#159341=CARTESIAN_POINT ( 'NONE',  ( 21.05000000000000071, 67.22371710471946926, -103.0231074845243739 ) ) ;
#159354=CARTESIAN_POINT ( 'NONE',  ( 21.97500000000000497, 66.25000000001179501, -81.87310748452438247 ) ) ;
#159392=LINE ( 'NONE', #238920, #155501 ) ;
#159404=CARTESIAN_POINT ( 'NONE',  ( -18.50000000000000000, 66.75000000001179501, -81.77310748452437394 ) ) ;
#159420=DIRECTION ( 'NONE',  ( 0.000000000000000000, -0.1350103645451807555, -0.9908441862701610203 ) ) ;
#159443=DIRECTION ( 'NONE',  ( 0.000000000000000000, 0.000000000000000000, 1.000000000000000000 ) ) ;
#159444=ORIENTED_EDGE ( 'NONE', *, *, #212283, .T. ) ;
#159466=ORIENTED_EDGE ( 'NONE', *, *, #122767, .T. ) ;
#159509=ORIENTED_EDGE ( 'NONE', *, *, #149297, .F. ) ;
#159551=ORIENTED_EDGE ( 'NONE', *, *, #175412, .T. ) ;
#159588=AXIS2_PLACEMENT_3D ( 'NONE', #139022, #20420, #239457 ) ;
#159653=VERTEX_POINT ( 'NONE', #139341 ) ;
#159656=DIRECTION ( 'NONE',  ( 1.000000000000000000, -0.000000000000000000, 0.000000000000000000 ) ) ;
#159666=DIRECTION ( 'NONE',  ( 0.000000000000000000, -6.982962677686266711E-15, 1.000000000000000000 ) ) ;
#159683=ORIENTED_EDGE ( 'NONE', *, *, #27657, .T. ) ;
#159685=CARTESIAN_POINT ( 'NONE',  ( 18.49999999999999289, 69.35000000001180354, -81.67310748452436542 ) ) ;
#159691=EDGE_CURVE ( 'NONE', #155954, #208580, #207184, .T. ) ;
#159697=AXIS2_PLACEMENT_3D ( 'NONE', #176871, #175578, #214678 ) ;
#159725=ORIENTED_EDGE ( 'NONE', *, *, #6296, .F. ) ;
#159731=AXIS2_PLACEMENT_3D ( 'NONE', #213016, #193474, #110061 ) ;
#159753=DIRECTION ( 'NONE',  ( -1.000000000000000000, -0.000000000000000000, -0.000000000000000000 ) ) ;
#159778=CARTESIAN_POINT ( 'NONE',  ( -22.48970261584617703, 64.35000000001195986, -103.0784769727418109 ) ) ;
#159786=AXIS2_PLACEMENT_3D ( 'NONE', #243421, #79201, #43941 ) ;
#159794=EDGE_CURVE ( 'NONE', #71706, #108747, #130055, .T. ) ;
#159799=LINE ( 'NONE', #254964, #138577 ) ;
#159810=EDGE_CURVE ( 'NONE', #47226, #35900, #232137, .T. ) ;
#159836=AXIS2_PLACEMENT_3D ( 'NONE', #194562, #15928, #56288 ) ;
#159871=DIRECTION ( 'NONE',  ( 1.000000000000000000, 0.000000000000000000, 0.000000000000000000 ) ) ;
#159874=CARTESIAN_POINT ( 'NONE',  ( 18.45068634130097962, 85.48650607335470397, -95.95432905335616169 ) ) ;
#159882=FACE_OUTER_BOUND ( 'NONE', #108209, .T. ) ;
#159908=ORIENTED_EDGE ( 'NONE', *, *, #227, .F. ) ;
#159925=DIRECTION ( 'NONE',  ( 1.000000000000000000, 0.000000000000000000, 0.000000000000000000 ) ) ;
#159954=DIRECTION ( 'NONE',  ( 0.000000000000000000, -1.000000000000000000, -6.352154140967427193E-15 ) ) ;
#159965=CARTESIAN_POINT ( 'NONE',  ( 21.13498764882293557, 69.50438185653807466, -103.0247638792556870 ) ) ;
#159978=AXIS2_PLACEMENT_3D ( 'NONE', #210462, #231319, #110059 ) ;
#159979=DIRECTION ( 'NONE',  ( 6.938893903907030216E-14, 0.000000000000000000, -1.000000000000000000 ) ) ;
#159981=ORIENTED_EDGE ( 'NONE', *, *, #177151, .F. ) ;
#159990=ORIENTED_EDGE ( 'NONE', *, *, #58745, .T. ) ;
#159994=CYLINDRICAL_SURFACE ( 'NONE', #67187, 0.09999999999999939493 ) ;
#160001=CARTESIAN_POINT ( 'NONE',  ( -23.15000000000000213, 76.00000000001170974, -69.52310748452431710 ) ) ;
#160030=AXIS2_PLACEMENT_3D ( 'NONE', #1256, #181217, #104209 ) ;
#160035=DIRECTION ( 'NONE',  ( 0.000000000000000000, -1.000000000000000000, -6.352154140967427193E-15 ) ) ;
#160040=ADVANCED_FACE ( 'NONE', ( #145458 ), #211443, .F. ) ;
#160044=CARTESIAN_POINT ( 'NONE',  ( 18.50596464788227280, 65.69367753730634263, -64.01892380663478832 ) ) ;
#160047=DIRECTION ( 'NONE',  ( 0.000000000000000000, 0.000000000000000000, 1.000000000000000000 ) ) ;
#160062=DIRECTION ( 'NONE',  ( 0.000000000000000000, -7.116814260417668513E-15, 1.000000000000000000 ) ) ;
#160099=CONICAL_SURFACE ( 'NONE', #226698, 6.250000000000005329, 0.7853981633974431720 ) ;
#160108=EDGE_LOOP ( 'NONE', ( #59476, #237161, #117561, #130276 ) ) ;
#160112=AXIS2_PLACEMENT_3D ( 'NONE', #144298, #118365, #21825 ) ;
#160117=CARTESIAN_POINT ( 'NONE',  ( 21.14999999999999858, 75.90220970870321082, -109.2809220950004345 ) ) ;
#160124=ORIENTED_EDGE ( 'NONE', *, *, #183465, .T. ) ;
#160133=ORIENTED_EDGE ( 'NONE', *, *, #246271, .F. ) ;
#160148=EDGE_CURVE ( 'NONE', #50342, #98958, #245859, .T. ) ;
#160155=DIRECTION ( 'NONE',  ( 1.000000000000000000, 0.000000000000000000, 0.000000000000000000 ) ) ;
#160179=CARTESIAN_POINT ( 'NONE',  ( 21.05000000000000071, 85.00000000001179501, -78.91707660717668205 ) ) ;
#160184=DIRECTION ( 'NONE',  ( 0.000000000000000000, 0.000000000000000000, -1.000000000000000000 ) ) ;
#160189=VERTEX_POINT ( 'NONE', #33265 ) ;
#160204=VERTEX_POINT ( 'NONE', #12404 ) ;
#160221=ORIENTED_EDGE ( 'NONE', *, *, #106530, .F. ) ;
#160232=DIRECTION ( 'NONE',  ( 0.000000000000000000, -6.982962677686266711E-15, 1.000000000000000000 ) ) ;
#160288=CYLINDRICAL_SURFACE ( 'NONE', #47638, 0.1000000000000028644 ) ;
#160311=AXIS2_PLACEMENT_3D ( 'NONE', #41004, #176652, #59205 ) ;
#160324=ADVANCED_FACE ( 'NONE', ( #177889 ), #19934, .F. ) ;
#160336=CARTESIAN_POINT ( 'NONE',  ( -21.05000000000000071, 61.95000000001191154, -97.50941241376341395 ) ) ;
#160338=CARTESIAN_POINT ( 'NONE',  ( 20.85000000000000142, 77.14957036958736580, -61.70719500002233815 ) ) ;
#160356=EDGE_CURVE ( 'NONE', #92109, #242050, #253121, .T. ) ;
#160384=CIRCLE ( 'NONE', #143598, 0.1000000000000028644 ) ;
#160388=DIRECTION ( 'NONE',  ( -1.000000000000000000, 2.952720810173289112E-16, 2.061873921506763405E-30 ) ) ;
#160406=EDGE_CURVE ( 'NONE', #71369, #94746, #20094, .T. ) ;
#160415=FACE_OUTER_BOUND ( 'NONE', #107643, .T. ) ;
#160420=EDGE_CURVE ( 'NONE', #174146, #170518, #32419, .T. ) ;
#160429=ORIENTED_EDGE ( 'NONE', *, *, #182856, .F. ) ;
#160434=EDGE_LOOP ( 'NONE', ( #157464, #183905, #88308, #10418 ) ) ;
#160440=CARTESIAN_POINT ( 'NONE',  ( 20.94999999999999574, 87.75000000001190870, -100.1231074845242262 ) ) ;
#160448=EDGE_CURVE ( 'NONE', #255325, #88867, #161590, .T. ) ;
#160471=ORIENTED_EDGE ( 'NONE', *, *, #102467, .F. ) ;
#160498=ORIENTED_EDGE ( 'NONE', *, *, #66572, .F. ) ;
#160512=ORIENTED_EDGE ( 'NONE', *, *, #32269, .T. ) ;
#160552=DIRECTION ( 'NONE',  ( 1.000000000000000000, -3.265361837132813093E-16, -2.280189983783949500E-30 ) ) ;
#160567=VECTOR ( 'NONE', #11310, 1000.000000000000000 ) ;
#160633=ADVANCED_FACE ( 'NONE', ( #34245 ), #38084, .T. ) ;
#160670=DIRECTION ( 'NONE',  ( 0.000000000000000000, -1.000000000000000000, 0.000000000000000000 ) ) ;
#160683=CARTESIAN_POINT ( 'NONE',  ( 20.94999999999999929, 69.35000000001187459, -93.00608031408432907 ) ) ;
#160697=DIRECTION ( 'NONE',  ( -0.000000000000000000, -6.982962677686266711E-15, 1.000000000000000000 ) ) ;
#160701=ORIENTED_EDGE ( 'NONE', *, *, #100838, .F. ) ;
#160714=VECTOR ( 'NONE', #68137, 1000.000000000000000 ) ;
#160721=EDGE_LOOP ( 'NONE', ( #175068, #27391, #108136, #115750 ) ) ;
#160733=VERTEX_POINT ( 'NONE', #197126 ) ;
#160785=CARTESIAN_POINT ( 'NONE',  ( -23.15000000000000213, 85.00000000001179501, -79.41707660717668205 ) ) ;
#160805=DIRECTION ( 'NONE',  ( -1.000000000000000000, -0.000000000000000000, -0.000000000000000000 ) ) ;
#160826=FACE_OUTER_BOUND ( 'NONE', #250449, .T. ) ;
#160851=LINE ( 'NONE', #25195, #226679 ) ;
#160875=ORIENTED_EDGE ( 'NONE', *, *, #142467, .F. ) ;
#160887=CARTESIAN_POINT ( 'NONE',  ( 20.85000000000000142, 77.75000000001162448, -57.90415744590205094 ) ) ;
#160888=CARTESIAN_POINT ( 'NONE',  ( -20.94999999999999929, 70.15000000001178648, -79.65560470880228650 ) ) ;
#160890=AXIS2_PLACEMENT_3D ( 'NONE', #249952, #15205, #209539 ) ;
#160904=DIRECTION ( 'NONE',  ( 0.000000000000000000, -0.4999999999999943379, -0.8660254037844420383 ) ) ;
#160921=EDGE_CURVE ( 'NONE', #107353, #214060, #124513, .T. ) ;
#161008=FACE_BOUND ( 'NONE', #99503, .T. ) ;
#161025=EDGE_CURVE ( 'NONE', #254110, #206570, #224273, .T. ) ;
#161029=DIRECTION ( 'NONE',  ( -1.000000000000000000, 7.304098846218135653E-16, 4.639676173203994055E-30 ) ) ;
#161034=VECTOR ( 'NONE', #172676, 1000.000000000000000 ) ;
#161035=ADVANCED_FACE ( 'NONE', ( #71774 ), #134271, .T. ) ;
#161049=DIRECTION ( 'NONE',  ( 0.000000000000000000, 0.000000000000000000, 1.000000000000000000 ) ) ;
#161064=AXIS2_PLACEMENT_3D ( 'NONE', #1890, #179296, #24074 ) ;
#161089=DIRECTION ( 'NONE',  ( 1.000000000000000000, -3.265361837132813093E-16, -2.280189983783949500E-30 ) ) ;
#161104=PLANE ( 'NONE',  #165945 ) ;
#161117=CARTESIAN_POINT ( 'NONE',  ( -21.05000000000068638, 75.94867256767054187, -109.3232908207938294 ) ) ;
#161133=EDGE_CURVE ( 'NONE', #5347, #111551, #86810, .T. ) ;
#161134=CARTESIAN_POINT ( 'NONE',  ( 23.15000000000000213, 87.75000000001186606, -90.87310748452424036 ) ) ;
#161203=ORIENTED_EDGE ( 'NONE', *, *, #76319, .F. ) ;
#161218=ORIENTED_EDGE ( 'NONE', *, *, #119723, .T. ) ;
#161236=CARTESIAN_POINT ( 'NONE',  ( 21.07928932188134397, 69.67148334361864670, -103.1220026301787414 ) ) ;
#161244=DIRECTION ( 'NONE',  ( -0.000000000000000000, -1.000000000000000000, -6.982962677686266711E-15 ) ) ;
#161277=LINE ( 'NONE', #219948, #168354 ) ;
#161285=AXIS2_PLACEMENT_3D ( 'NONE', #18721, #57825, #56531 ) ;
#161296=CIRCLE ( 'NONE', #7335, 0.1000000000000028644 ) ;
#161330=ADVANCED_FACE ( 'NONE', ( #29466 ), #216255, .T. ) ;
#161350=AXIS2_PLACEMENT_3D ( 'NONE', #157219, #236706, #141474 ) ;
#161374=CYLINDRICAL_SURFACE ( 'NONE', #29960, 0.1000000000000064587 ) ;
#161387=AXIS2_PLACEMENT_3D ( 'NONE', #177241, #15602, #100209 ) ;
#161395=DIRECTION ( 'NONE',  ( -0.000000000000000000, 6.982962677686266711E-15, -1.000000000000000000 ) ) ;
#161410=CARTESIAN_POINT ( 'NONE',  ( -21.14999999893415250, 64.25000000001189449, -96.17861214099801259 ) ) ;
#161446=DIRECTION ( 'NONE',  ( 0.000000000000000000, -0.5000000000000209832, 0.8660254037844264952 ) ) ;
#161464=ADVANCED_FACE ( 'NONE', ( #15015 ), #87067, .T. ) ;
#161478=LINE ( 'NONE', #218843, #163555 ) ;
#161481=VERTEX_POINT ( 'NONE', #80059 ) ;
#161493=CARTESIAN_POINT ( 'NONE',  ( -18.59999999999999787, 66.65000000001180069, -81.67310748452437963 ) ) ;
#161497=VERTEX_POINT ( 'NONE', #39724 ) ;
#161499=ORIENTED_EDGE ( 'NONE', *, *, #185169, .T. ) ;
#161519=AXIS2_PLACEMENT_3D ( 'NONE', #50579, #31079, #96127 ) ;
#161538=CARTESIAN_POINT ( 'NONE',  ( -18.52328366898032996, 85.64232108905291341, -62.80828814695419027 ) ) ;
#161540=ORIENTED_EDGE ( 'NONE', *, *, #90412, .T. ) ;
#161543=VERTEX_POINT ( 'NONE', #100900 ) ;
#161590=CIRCLE ( 'NONE', #3506, 11.80000000000000426 ) ;
#161595=AXIS2_PLACEMENT_3D ( 'NONE', #29086, #107288, #108580 ) ;
#161601=LINE ( 'NONE', #96440, #81136 ) ;
#161616=DIRECTION ( 'NONE',  ( -1.000000000000000000, -0.000000000000000000, 0.000000000000000000 ) ) ;
#161628=CARTESIAN_POINT ( 'NONE',  ( -20.85000000000000142, 87.65000000001171543, -69.52310748452423184 ) ) ;
#161637=FACE_OUTER_BOUND ( 'NONE', #248155, .T. ) ;
#161643=CARTESIAN_POINT ( 'NONE',  ( 20.95017935633852346, 65.52451072038657287, -95.44566768713390559 ) ) ;
#161646=SPHERICAL_SURFACE ( 'NONE', #181298, 0.1000000000000000056 ) ;
#161649=ORIENTED_EDGE ( 'NONE', *, *, #216630, .T. ) ;
#161670=CARTESIAN_POINT ( 'NONE',  ( -20.85000000000000142, 68.97833521811159585, -65.68954208262705663 ) ) ;
#161692=DIRECTION ( 'NONE',  ( 1.000000000000000000, -0.000000000000000000, 0.000000000000000000 ) ) ;
#161737=EDGE_LOOP ( 'NONE', ( #200591, #22800, #181552, #11342 ) ) ;
#161749=ORIENTED_EDGE ( 'NONE', *, *, #125621, .F. ) ;
#161841=CARTESIAN_POINT ( 'NONE',  ( 21.05000000000000426, 75.96513199699892027, -109.2931933482134355 ) ) ;
#161857=ORIENTED_EDGE ( 'NONE', *, *, #21957, .F. ) ;
#161882=CYLINDRICAL_SURFACE ( 'NONE', #193509, 11.80000000000000426 ) ;
#161902=AXIS2_PLACEMENT_3D ( 'NONE', #116648, #197460, #95782 ) ;
#161904=DIRECTION ( 'NONE',  ( -1.000000000000000000, 0.000000000000000000, -0.000000000000000000 ) ) ;
#161916=DIRECTION ( 'NONE',  ( 0.000000000000000000, -6.652207440891569552E-15, 1.000000000000000000 ) ) ;
#161926=CARTESIAN_POINT ( 'NONE',  ( -21.65000000000000213, 68.29142135624910281, -81.77310748452435973 ) ) ;
#161949=CIRCLE ( 'NONE', #49502, 0.3999999999999975797 ) ;
#161953=ORIENTED_EDGE ( 'NONE', *, *, #160406, .T. ) ;
#161991=FACE_OUTER_BOUND ( 'NONE', #190942, .T. ) ;
#162008=AXIS2_PLACEMENT_3D ( 'NONE', #141683, #120879, #180830 ) ;
#162014=DIRECTION ( 'NONE',  ( 0.000000000000000000, 0.000000000000000000, 1.000000000000000000 ) ) ;
#162043=EDGE_CURVE ( 'NONE', #89644, #102088, #217404, .T. ) ;
#162072=DIRECTION ( 'NONE',  ( -6.938893903907224433E-15, -1.000000000000000000, -6.982962677686266711E-15 ) ) ;
#162087=EDGE_CURVE ( 'NONE', #208239, #22313, #190975, .T. ) ;
#162117=VERTEX_POINT ( 'NONE', #7356 ) ;
#162179=ORIENTED_EDGE ( 'NONE', *, *, #31543, .T. ) ;
#162182=DIRECTION ( 'NONE',  ( 0.000000000000000000, 7.162729191130023213E-15, -1.000000000000000000 ) ) ;
#162241=DIRECTION ( 'NONE',  ( 4.504528286903032433E-15, 0.1298341882520054891, 0.9915357197604850459 ) ) ;
#162244=CARTESIAN_POINT ( 'NONE',  ( 21.13461538461538680, 67.11458296203741725, -90.77310748452435973 ) ) ;
#162254=AXIS2_PLACEMENT_3D ( 'NONE', #11836, #246550, #245290 ) ;
#162277=ORIENTED_EDGE ( 'NONE', *, *, #226144, .T. ) ;
#162350=DIRECTION ( 'NONE',  ( 2.952720810173289112E-16, 1.000000000000000000, -6.088138035986627436E-46 ) ) ;
#162374=ORIENTED_EDGE ( 'NONE', *, *, #179472, .F. ) ;
#162452=B_SPLINE_CURVE_WITH_KNOTS ( 'NONE', 3,
 ( #93932, #114786, #213882, #230904, #95219, #14431, #13128 ),
 .UNSPECIFIED., .F., .F.,
 ( 4, 3, 4 ),
 ( 0.000000000000000000, 0.0009834301579440022593, 0.001767853679402679300 ),
 .UNSPECIFIED. ) ;
#162456=CARTESIAN_POINT ( 'NONE',  ( -20.99142135623731065, 64.40000000001175806, -76.45131071479988805 ) ) ;
#162479=CARTESIAN_POINT ( 'NONE',  ( 21.14999999999999858, 67.21339244341174890, -90.77310748452437394 ) ) ;
#162511=VECTOR ( 'NONE', #66942, 1000.000000000000114 ) ;
#162527=CARTESIAN_POINT ( 'NONE',  ( 21.05000000000000071, 87.65000000001194280, -103.0231074845242318 ) ) ;
#162538=EDGE_CURVE ( 'NONE', #249207, #174346, #191149, .T. ) ;
#162555=CARTESIAN_POINT ( 'NONE',  ( -18.50000000000000000, 77.16412189325286874, -61.60825939895269698 ) ) ;
#162587=ORIENTED_EDGE ( 'NONE', *, *, #112561, .F. ) ;
#162590=DIRECTION ( 'NONE',  ( 1.000000000000000000, 0.000000000000000000, 0.000000000000000000 ) ) ;
#162619=AXIS2_PLACEMENT_3D ( 'NONE', #170950, #65370, #210039 ) ;
#162621=DIRECTION ( 'NONE',  ( -1.000000000000000000, -0.000000000000000000, -0.000000000000000000 ) ) ;
#162637=CARTESIAN_POINT ( 'NONE',  ( 20.94999999999999929, 76.00000000001173817, -73.62310748452429721 ) ) ;
#162640=CARTESIAN_POINT ( 'NONE',  ( 21.00000000000000000, 66.25000000001179501, -81.77310748452437394 ) ) ;
#162641=DIRECTION ( 'NONE',  ( 0.000000000000000000, -7.056502275159894776E-15, 1.000000000000000000 ) ) ;
#162653=ADVANCED_FACE ( 'NONE', ( #255560 ), #257705, .T. ) ;
#162669=DIRECTION ( 'NONE',  ( 1.000000000000000000, -3.265361837132813093E-16, -2.280189983783949500E-30 ) ) ;
#162675=DIRECTION ( 'NONE',  ( 0.000000000000000000, -1.000000000000000000, -6.982962677686265922E-15 ) ) ;
#162683=CARTESIAN_POINT ( 'NONE',  ( -20.94999999999999929, 64.25000000001189449, -96.18150679462726771 ) ) ;
#162697=ORIENTED_EDGE ( 'NONE', *, *, #118850, .F. ) ;
#162738=AXIS2_PLACEMENT_3D ( 'NONE', #242339, #59829, #23329 ) ;
#162753=DIRECTION ( 'NONE',  ( 1.000000000000000000, 0.000000000000000000, 0.000000000000000000 ) ) ;
#162759=DIRECTION ( 'NONE',  ( -0.000000000000000000, 1.000000000000000000, 6.982962677686266711E-15 ) ) ;
#162763=CARTESIAN_POINT ( 'NONE',  ( -21.05315837410545043, 64.25000000001175238, -76.36475148275638958 ) ) ;
#162770=ORIENTED_EDGE ( 'NONE', *, *, #242838, .F. ) ;
#162781=DIRECTION ( 'NONE',  ( 0.000000000000000000, 0.5907332058517377193, -0.8068669527896954463 ) ) ;
#162806=EDGE_LOOP ( 'NONE', ( #6352, #164206, #213018, #50466 ) ) ;
#162816=DIRECTION ( 'NONE',  ( 1.000000000000000000, 0.000000000000000000, 0.000000000000000000 ) ) ;
#162876=CIRCLE ( 'NONE', #96367, 0.1000000000000028644 ) ;
#162879=AXIS2_PLACEMENT_3D ( 'NONE', #112218, #195612, #235982 ) ;
#162927=DIRECTION ( 'NONE',  ( 1.000000000000000000, 0.000000000000000000, 0.000000000000000000 ) ) ;
#162954=EDGE_CURVE ( 'NONE', #129819, #145746, #70284, .T. ) ;
#162962=AXIS2_PLACEMENT_3D ( 'NONE', #129951, #206948, #28347 ) ;
#162981=CARTESIAN_POINT ( 'NONE',  ( 21.14999999999999858, 76.00000000001195133, -103.0231074845243171 ) ) ;
#163017=DIRECTION ( 'NONE',  ( 1.000000000000000000, 0.000000000000000000, 0.000000000000000000 ) ) ;
#163022=EDGE_CURVE ( 'NONE', #85729, #231733, #170515, .T. ) ;
#163032=DIRECTION ( 'NONE',  ( 0.000000000000000000, 6.982962677686266711E-15, -1.000000000000000000 ) ) ;
#163048=EDGE_CURVE ( 'NONE', #154309, #116247, #174799, .T. ) ;
#163084=ORIENTED_EDGE ( 'NONE', *, *, #29780, .T. ) ;
#163169=AXIS2_PLACEMENT_3D ( 'NONE', #38440, #59238, #252338 ) ;
#163194=DIRECTION ( 'NONE',  ( 0.000000000000000000, 0.000000000000000000, -1.000000000000000000 ) ) ;
#163211=AXIS2_PLACEMENT_3D ( 'NONE', #254497, #56310, #139372 ) ;
#163230=CARTESIAN_POINT ( 'NONE',  ( 21.53699400384887852, 75.99999999997994848, -109.8108192777622634 ) ) ;
#163237=LINE ( 'NONE', #64127, #101167 ) ;
#163248=AXIS2_PLACEMENT_3D ( 'NONE', #214275, #156895, #215545 ) ;
#163251=VERTEX_POINT ( 'NONE', #205579 ) ;
#163253=VECTOR ( 'NONE', #59288, 1000.000000000000114 ) ;
#163263=DIRECTION ( 'NONE',  ( -0.000000000000000000, 6.982962677686266711E-15, -1.000000000000000000 ) ) ;
#163275=DIRECTION ( 'NONE',  ( 0.000000000000000000, -0.4930308989875575865, -0.8700118002898125091 ) ) ;
#163290=EDGE_LOOP ( 'NONE', ( #7487, #142515, #204144, #244840 ) ) ;
#163299=CIRCLE ( 'NONE', #171510, 0.1000000000000028644 ) ;
#163308=CARTESIAN_POINT ( 'NONE',  ( -20.64999999999999858, 85.40000000001178648, -79.41707660717668205 ) ) ;
#163311=DIRECTION ( 'NONE',  ( 0.000000000000000000, 1.000000000000000000, -2.775557561562888827E-14 ) ) ;
#163329=CARTESIAN_POINT ( 'NONE',  ( -18.54260524012588007, 85.62421939008548577, -62.78233443875351583 ) ) ;
#163338=EDGE_LOOP ( 'NONE', ( #7019, #219668, #104244, #109308 ) ) ;
#163345=CARTESIAN_POINT ( 'NONE',  ( -21.44999999999999929, 68.65000000001187175, -90.77310748452435973 ) ) ;
#163355=EDGE_CURVE ( 'NONE', #161543, #157067, #11254, .T. ) ;
#163362=ORIENTED_EDGE ( 'NONE', *, *, #104740, .T. ) ;
#163385=AXIS2_PLACEMENT_3D ( 'NONE', #160336, #19527, #181171 ) ;
#163395=DIRECTION ( 'NONE',  ( 0.000000000000000000, -7.172728831056617961E-15, 1.000000000000000000 ) ) ;
#163404=AXIS2_PLACEMENT_3D ( 'NONE', #196224, #253617, #213211 ) ;
#163409=CARTESIAN_POINT ( 'NONE',  ( -20.54999999999999716, 85.00000000001188027, -93.12913836187181005 ) ) ;
#163436=CARTESIAN_POINT ( 'NONE',  ( 20.85000000000000142, 87.75000000001172396, -72.42310748452422331 ) ) ;
#163464=CARTESIAN_POINT ( 'NONE',  ( 20.77526135991773515, 67.06799098339033094, -94.55453894179980523 ) ) ;
#163493=VECTOR ( 'NONE', #35784, 1000.000000000000000 ) ;
#163511=CARTESIAN_POINT ( 'NONE',  ( -18.59999999999999787, 64.35000000001180354, -81.67310748452439384 ) ) ;
#163527=DIRECTION ( 'NONE',  ( 1.040834085586054469E-13, -1.000000000000000000, 0.000000000000000000 ) ) ;
#163539=CIRCLE ( 'NONE', #51066, 0.09999999999999939493 ) ;
#163549=AXIS2_PLACEMENT_3D ( 'NONE', #50262, #129810, #209347 ) ;
#163555=VECTOR ( 'NONE', #217556, 1000.000000000000000 ) ;
#163567=CARTESIAN_POINT ( 'NONE',  ( 20.94999999999999574, 77.83534155023627932, -91.46795619196130644 ) ) ;
#163595=LINE ( 'NONE', #138843, #29983 ) ;
#163618=DIRECTION ( 'NONE',  ( 1.000000000000000000, -2.952720810173289112E-16, -2.061873921506763405E-30 ) ) ;
#163622=CARTESIAN_POINT ( 'NONE',  ( 23.14999999999999858, 71.00000000001180922, -81.92837350343744163 ) ) ;
#163649=EDGE_LOOP ( 'NONE', ( #107931, #138966, #148626, #210406 ) ) ;
#163652=ORIENTED_EDGE ( 'NONE', *, *, #182856, .T. ) ;
#163655=DIRECTION ( 'NONE',  ( 0.000000000000000000, -7.429790795770644761E-15, 1.000000000000000000 ) ) ;
#163663=EDGE_CURVE ( 'NONE', #112510, #173885, #190905, .T. ) ;
#163725=AXIS2_PLACEMENT_3D ( 'NONE', #20035, #79952, #38304 ) ;
#163772=ORIENTED_EDGE ( 'NONE', *, *, #34867, .T. ) ;
#163797=EDGE_CURVE ( 'NONE', #3957, #242308, #79227, .T. ) ;
#163820=DIRECTION ( 'NONE',  ( 0.000000000000000000, -6.982962677686266711E-15, 1.000000000000000000 ) ) ;
#163840=CARTESIAN_POINT ( 'NONE',  ( -20.94999999999999929, 77.83534155023627932, -91.46795619196132066 ) ) ;
#163870=ADVANCED_FACE ( 'NONE', ( #235138 ), #34393, .F. ) ;
#163874=DIRECTION ( 'NONE',  ( 2.952720810173289112E-16, 1.000000000000000000, 6.938893903907229955E-15 ) ) ;
#163882=CIRCLE ( 'NONE', #180627, 0.09999999999999971412 ) ;
#163892=CARTESIAN_POINT ( 'NONE',  ( 23.14999999999999503, 64.35000000001178933, -81.67310748452439384 ) ) ;
#163903=EDGE_CURVE ( 'NONE', #77606, #156170, #129322, .T. ) ;
#163904=AXIS2_PLACEMENT_3D ( 'NONE', #220660, #204924, #100668 ) ;
#163918=FACE_OUTER_BOUND ( 'NONE', #174954, .T. ) ;
#163923=ORIENTED_EDGE ( 'NONE', *, *, #122018, .F. ) ;
#163964=DIRECTION ( 'NONE',  ( 0.000000000000000000, -1.000000000000000000, -6.982962677686265922E-15 ) ) ;
#163976=VECTOR ( 'NONE', #57855, 1000.000000000000000 ) ;
#163979=DIRECTION ( 'NONE',  ( 0.000000000000000000, 1.000000000000000000, 0.000000000000000000 ) ) ;
#163995=CIRCLE ( 'NONE', #109999, 0.5000000000000004441 ) ;
#164025=DIRECTION ( 'NONE',  ( 1.000000000000000000, 0.000000000000000000, 0.000000000000000000 ) ) ;
#164038=EDGE_LOOP ( 'NONE', ( #78384, #206317, #70104, #69106 ) ) ;
#164045=AXIS2_PLACEMENT_3D ( 'NONE', #117410, #237361, #75728 ) ;
#164057=CARTESIAN_POINT ( 'NONE',  ( 21.00000000000000000, 66.25000000001186606, -90.67310748452437963 ) ) ;
#164085=ADVANCED_FACE ( 'NONE', ( #112007 ), #126741, .F. ) ;
#164086=ADVANCED_FACE ( 'NONE', ( #12922 ), #234495, .F. ) ;
#164094=ORIENTED_EDGE ( 'NONE', *, *, #218440, .F. ) ;
#164132=DIRECTION ( 'NONE',  ( 2.940209281316621016E-16, 1.000000000000000000, 7.056502275159890832E-15 ) ) ;
#164136=CARTESIAN_POINT ( 'NONE',  ( -18.59999999999999787, 77.83585931145526615, -58.01866831572577610 ) ) ;
#164140=LINE ( 'NONE', #3769, #141681 ) ;
#164144=CARTESIAN_POINT ( 'NONE',  ( -18.52139480978223318, 85.48135884507880178, -95.99855091740519697 ) ) ;
#164161=DIRECTION ( 'NONE',  ( -1.836970198721029934E-16, -1.000000000000000000, -6.982962677686266711E-15 ) ) ;
#164172=EDGE_CURVE ( 'NONE', #120661, #256898, #121172, .T. ) ;
#164178=VERTEX_POINT ( 'NONE', #257863 ) ;
#164188=DIRECTION ( 'NONE',  ( 0.000000000000000000, 0.000000000000000000, 1.000000000000000000 ) ) ;
#164204=EDGE_LOOP ( 'NONE', ( #96945, #26016, #178950, #68565 ) ) ;
#164206=ORIENTED_EDGE ( 'NONE', *, *, #47757, .F. ) ;
#164244=CYLINDRICAL_SURFACE ( 'NONE', #220345, 0.1000000000000028644 ) ;
#164246=AXIS2_PLACEMENT_3D ( 'NONE', #28553, #7664, #246270 ) ;
#164258=AXIS2_PLACEMENT_3D ( 'NONE', #173004, #34761, #73893 ) ;
#164259=ORIENTED_EDGE ( 'NONE', *, *, #126082, .F. ) ;
#164263=DIRECTION ( 'NONE',  ( 1.000000000000000000, -7.304098846218134667E-16, -5.100424963727256530E-30 ) ) ;
#164265=ORIENTED_EDGE ( 'NONE', *, *, #73763, .F. ) ;
#164275=DIRECTION ( 'NONE',  ( 1.000000000000000000, 0.000000000000000000, 0.000000000000000000 ) ) ;
#164289=VERTEX_POINT ( 'NONE', #127394 ) ;
#164291=ADVANCED_FACE ( 'NONE', ( #6141 ), #223902, .T. ) ;
#164317=ORIENTED_EDGE ( 'NONE', *, *, #53518, .F. ) ;
#164318=EDGE_CURVE ( 'NONE', #71479, #173939, #206930, .T. ) ;
#164367=ORIENTED_EDGE ( 'NONE', *, *, #105025, .F. ) ;
#164382=CIRCLE ( 'NONE', #243474, 0.09999999999999799327 ) ;
#164392=ORIENTED_EDGE ( 'NONE', *, *, #17896, .T. ) ;
#164432=ORIENTED_EDGE ( 'NONE', *, *, #22227, .F. ) ;
#164441=DIRECTION ( 'NONE',  ( 0.000000000000000000, 1.000000000000000000, 0.000000000000000000 ) ) ;
#164442=AXIS2_PLACEMENT_3D ( 'NONE', #3564, #139205, #63538 ) ;
#164459=VECTOR ( 'NONE', #241852, 1000.000000000000000 ) ;
#164503=DIRECTION ( 'NONE',  ( 0.7071359030027593029, -0.7070776581709197206, 0.000000000000000000 ) ) ;
#164594=CARTESIAN_POINT ( 'NONE',  ( -23.15000000000000213, 74.00000000001186606, -89.79848556176222019 ) ) ;
#164597=SPHERICAL_SURFACE ( 'NONE', #8082, 0.1000000000000000056 ) ;
#164634=LINE ( 'NONE', #205009, #148450 ) ;
#164735=DIRECTION ( 'NONE',  ( -1.000000000000000000, 0.000000000000000000, -0.000000000000000000 ) ) ;
#164760=ORIENTED_EDGE ( 'NONE', *, *, #83538, .F. ) ;
#164764=DIRECTION ( 'NONE',  ( 0.000000000000000000, -0.4930308989875170078, -0.8700118002898356018 ) ) ;
#164805=VERTEX_POINT ( 'NONE', #64101 ) ;
#164843=EDGE_CURVE ( 'NONE', #11451, #193738, #9067, .T. ) ;
#164860=ORIENTED_EDGE ( 'NONE', *, *, #79647, .T. ) ;
#164862=PLANE ( 'NONE',  #55431 ) ;
#164889=LINE ( 'NONE', #108762, #121308 ) ;
#164893=CARTESIAN_POINT ( 'NONE',  ( -21.55000000000000071, 68.75000000001185185, -90.67310748452436542 ) ) ;
#164901=EDGE_LOOP ( 'NONE', ( #106996, #252673, #242781, #84047 ) ) ;
#164904=CARTESIAN_POINT ( 'NONE',  ( 21.08489834409762054, 65.37767610527633622, -90.67310748452440805 ) ) ;
#164938=ORIENTED_EDGE ( 'NONE', *, *, #250642, .F. ) ;
#164973=ORIENTED_EDGE ( 'NONE', *, *, #39666, .T. ) ;
#165033=CARTESIAN_POINT ( 'NONE',  ( 23.14999999999999858, 79.90000000001171543, -69.52310748452428868 ) ) ;
#165035=CYLINDRICAL_SURFACE ( 'NONE', #228968, 0.1000000000000026007 ) ;
#165072=DIRECTION ( 'NONE',  ( 0.000000000000000000, 0.000000000000000000, -1.000000000000000000 ) ) ;
#165075=CARTESIAN_POINT ( 'NONE',  ( 21.08035267497491105, 69.66829316022892726, -103.1057961093004849 ) ) ;
#165085=CIRCLE ( 'NONE', #85946, 0.09999999999999939493 ) ;
#165088=ORIENTED_EDGE ( 'NONE', *, *, #156998, .T. ) ;
#165096=CARTESIAN_POINT ( 'NONE',  ( 18.50000000000000355, 85.41907808086121179, -62.69318213431594700 ) ) ;
#165121=ORIENTED_EDGE ( 'NONE', *, *, #49755, .F. ) ;
#165145=DIRECTION ( 'NONE',  ( 1.000000000000000000, 0.000000000000000000, 0.000000000000000000 ) ) ;
#165177=ORIENTED_EDGE ( 'NONE', *, *, #195117, .T. ) ;
#165179=AXIS2_PLACEMENT_3D ( 'NONE', #151611, #130728, #48620 ) ;
#165205=ORIENTED_EDGE ( 'NONE', *, *, #200492, .T. ) ;
#165242=CARTESIAN_POINT ( 'NONE',  ( -21.03922262424652345, 64.37609936600713922, -96.16389944163073267 ) ) ;
#165247=VERTEX_POINT ( 'NONE', #173686 ) ;
#165267=CARTESIAN_POINT ( 'NONE',  ( -23.15000000000000213, 71.65000000001180069, -81.87310748452433984 ) ) ;
#165291=CIRCLE ( 'NONE', #107022, 0.09999999999999939493 ) ;
#165308=CARTESIAN_POINT ( 'NONE',  ( 21.05000000000000071, 77.25000000001189449, -95.12310748452429721 ) ) ;
#165321=AXIS2_PLACEMENT_3D ( 'NONE', #159179, #97857, #17094 ) ;
#165322=AXIS2_PLACEMENT_3D ( 'NONE', #255755, #17209, #100540 ) ;
#165351=CIRCLE ( 'NONE', #40489, 0.1000000000000028644 ) ;
#165378=CARTESIAN_POINT ( 'NONE',  ( -18.50000000000000000, 65.70729864260985664, -64.06574559737244101 ) ) ;
#165406=CARTESIAN_POINT ( 'NONE',  ( 23.14999999999998437, 87.75000000001193712, -103.0231074845242318 ) ) ;
#165425=ADVANCED_FACE ( 'NONE', ( #118800 ), #182629, .T. ) ;
#165434=EDGE_CURVE ( 'NONE', #23607, #148851, #192782, .T. ) ;
#165445=DIRECTION ( 'NONE',  ( 0.000000000000000000, -0.1568667991644355497, -0.9876197685951332295 ) ) ;
#165472=CARTESIAN_POINT ( 'NONE',  ( -22.59999970745345976, 76.00935637733951467, -114.7736206921935320 ) ) ;
#165477=LINE ( 'NONE', #186319, #244299 ) ;
#165478=DIRECTION ( 'NONE',  ( -1.000000000000000000, -0.000000000000000000, -0.000000000000000000 ) ) ;
#165493=CARTESIAN_POINT ( 'NONE',  ( -21.05000000000000426, 69.72991413632281876, -103.0579754875374476 ) ) ;
#165515=ORIENTED_EDGE ( 'NONE', *, *, #226275, .F. ) ;
#165573=CARTESIAN_POINT ( 'NONE',  ( 21.70464131381650219, 68.90464198104409377, -103.0231074845243739 ) ) ;
#165593=VERTEX_POINT ( 'NONE', #251563 ) ;
#165594=CARTESIAN_POINT ( 'NONE',  ( 19.86930884467576419, 64.31308993304064359, -78.28388484558554694 ) ) ;
#165601=ADVANCED_FACE ( 'NONE', ( #54639 ), #149926, .T. ) ;
#165603=DIRECTION ( 'NONE',  ( -0.000000000000000000, 1.000000000000000000, 6.982962677686266711E-15 ) ) ;
#165625=CIRCLE ( 'NONE', #149062, 0.1000000000000028644 ) ;
#165633=AXIS2_PLACEMENT_3D ( 'NONE', #76896, #14394, #113459 ) ;
#165648=EDGE_CURVE ( 'NONE', #221652, #120417, #161478, .T. ) ;
#165655=ADVANCED_FACE ( 'NONE', ( #21960 ), #88510, .F. ) ;
#165674=ORIENTED_EDGE ( 'NONE', *, *, #175412, .F. ) ;
#165680=AXIS2_PLACEMENT_3D ( 'NONE', #14965, #73667, #94471 ) ;
#165687=DIRECTION ( 'NONE',  ( 0.000000000000000000, -6.853228547068871147E-15, 1.000000000000000000 ) ) ;
#165730=CARTESIAN_POINT ( 'NONE',  ( -20.94999999999999929, 64.35000000001176090, -76.30697314750248950 ) ) ;
#165753=AXIS2_PLACEMENT_3D ( 'NONE', #161134, #24201, #5883 ) ;
#165763=EDGE_CURVE ( 'NONE', #29920, #227881, #101428, .T. ) ;
#165788=ORIENTED_EDGE ( 'NONE', *, *, #203704, .T. ) ;
#165790=DIRECTION ( 'NONE',  ( -1.000000000000000000, 2.952720810173289112E-16, 2.061873921506763405E-30 ) ) ;
#165793=DIRECTION ( 'NONE',  ( 0.000000000000000000, -0.1350103645451807555, -0.9908441862701609093 ) ) ;
#165827=ORIENTED_EDGE ( 'NONE', *, *, #110011, .F. ) ;
#165849=CARTESIAN_POINT ( 'NONE',  ( 18.49999999999999289, 65.74999999739273449, -78.33593553489180294 ) ) ;
#165850=CARTESIAN_POINT ( 'NONE',  ( 21.05000000000000071, 76.00000000001170974, -69.52310748452431710 ) ) ;
#165869=ADVANCED_FACE ( 'NONE', ( #248373 ), #83158, .T. ) ;
#165871=APPLICATION_CONTEXT ( 'automotive_design' ) ;
#165898=AXIS2_PLACEMENT_3D ( 'NONE', #142830, #24219, #103706 ) ;
#165939=AXIS2_PLACEMENT_3D ( 'NONE', #219605, #82640, #60531 ) ;
#165945=AXIS2_PLACEMENT_3D ( 'NONE', #120708, #82795, #222312 ) ;
#165950=EDGE_CURVE ( 'NONE', #237061, #148456, #47190, .T. ) ;
#165962=CIRCLE ( 'NONE', #107666, 11.74999999999999645 ) ;
#165970=EDGE_CURVE ( 'NONE', #85340, #71686, #172166, .T. ) ;
#165978=ORIENTED_EDGE ( 'NONE', *, *, #69228, .T. ) ;
#165984=EDGE_CURVE ( 'NONE', #65772, #190642, #192976, .T. ) ;
#165998=LINE ( 'NONE', #72016, #54407 ) ;
#166037=CARTESIAN_POINT ( 'NONE',  ( 18.42595409746844837, 85.49999981257613513, -96.02374513277639778 ) ) ;
#166059=ADVANCED_FACE ( 'NONE', ( #237802 ), #59121, .T. ) ;
#166114=CARTESIAN_POINT ( 'NONE',  ( 21.04105312098505109, 67.12466737696824737, -90.69460073731197269 ) ) ;
#166131=CARTESIAN_POINT ( 'NONE',  ( -23.25000000000000000, 76.00000000001195133, -103.0231074845243171 ) ) ;
#166132=DIRECTION ( 'NONE',  ( 1.000000000000000000, -3.469446951953718318E-14, 2.003086131649645455E-14 ) ) ;
#166134=CARTESIAN_POINT ( 'NONE',  ( -21.45000000000000284, 68.29142135624915966, -90.67310748452436542 ) ) ;
#166237=CONICAL_SURFACE ( 'NONE', #203625, 4.049999999999998046, 0.7853981633974604915 ) ;
#166265=ADVANCED_FACE ( 'NONE', ( #9451 ), #246544, .T. ) ;
#166291=ADVANCED_FACE ( 'NONE', ( #214077 ), #101314, .F. ) ;
#166306=EDGE_CURVE ( 'NONE', #41677, #4874, #191974, .T. ) ;
#166318=DIRECTION ( 'NONE',  ( 1.000000000000000000, 0.000000000000000000, 0.000000000000000000 ) ) ;
#166322=DIRECTION ( 'NONE',  ( -3.440080580676165868E-14, 0.1298341882520054891, 0.9915357197604850459 ) ) ;
#166326=DIRECTION ( 'NONE',  ( 1.000000000000000000, 0.000000000000000000, 0.000000000000000000 ) ) ;
#166347=DIRECTION ( 'NONE',  ( 0.000000000000000000, 0.000000000000000000, -1.000000000000000000 ) ) ;
#166349=CYLINDRICAL_SURFACE ( 'NONE', #188958, 0.8750000000000007772 ) ;
#166418=EDGE_CURVE ( 'NONE', #97655, #170518, #50957, .T. ) ;
#166428=DIRECTION ( 'NONE',  ( 1.000000000000000000, 0.000000000000000000, 0.000000000000000000 ) ) ;
#166462=ORIENTED_EDGE ( 'NONE', *, *, #5726, .F. ) ;
#166463=CARTESIAN_POINT ( 'NONE',  ( 18.49999999999999645, 77.29973367124280514, -112.9949779616549108 ) ) ;
#166483=SPHERICAL_SURFACE ( 'NONE', #110404, 0.1000000000000000056 ) ;
#166484=LINE ( 'NONE', #132462, #166792 ) ;
#166522=CARTESIAN_POINT ( 'NONE',  ( 20.95512820512820440, 67.12384868372375024, -90.82293462539561801 ) ) ;
#166531=AXIS2_PLACEMENT_3D ( 'NONE', #220675, #23789, #44609 ) ;
#166554=AXIS2_PLACEMENT_3D ( 'NONE', #27373, #126422, #108153 ) ;
#166557=EDGE_LOOP ( 'NONE', ( #57948, #203861, #7913, #54092, #215159 ) ) ;
#166574=SPHERICAL_SURFACE ( 'NONE', #223245, 0.1000000000000000056 ) ;
#166576=CARTESIAN_POINT ( 'NONE',  ( 18.59999999999999076, 74.16465844978745281, -91.36795619196134055 ) ) ;
#166579=CARTESIAN_POINT ( 'NONE',  ( -21.05000000000000071, 64.35000000001190301, -96.23924182154622997 ) ) ;
#166584=DIRECTION ( 'NONE',  ( 0.000000000000000000, 0.000000000000000000, 1.000000000000000000 ) ) ;
#166590=CIRCLE ( 'NONE', #145696, 0.1000000000000052097 ) ;
#166626=CIRCLE ( 'NONE', #224838, 0.1000000000000028644 ) ;
#166694=DIRECTION ( 'NONE',  ( 0.7071067811865474617, -0.7071067811865474617, -4.937700262164531476E-15 ) ) ;
#166713=LINE ( 'NONE', #246221, #109047 ) ;
#166724=DIRECTION ( 'NONE',  ( 0.000000000000000000, 0.000000000000000000, 1.000000000000000000 ) ) ;
#166727=CARTESIAN_POINT ( 'NONE',  ( -21.14999999999999858, 76.10085836911075319, -114.7726746080137019 ) ) ;
#166731=CIRCLE ( 'NONE', #166531, 11.74999999999999645 ) ;
#166753=DIRECTION ( 'NONE',  ( 1.000000000000000000, 0.000000000000000000, 0.000000000000000000 ) ) ;
#166784=CARTESIAN_POINT ( 'NONE',  ( -23.15000000000000213, 76.00000000001195133, -103.0231074845243171 ) ) ;
#166792=VECTOR ( 'NONE', #33399, 1000.000000000000000 ) ;
#166797=DIRECTION ( 'NONE',  ( -3.265361837132813093E-16, -1.000000000000000000, -6.938893903907222067E-15 ) ) ;
#166801=AXIS2_PLACEMENT_3D ( 'NONE', #232473, #113778, #214174 ) ;
#166803=CARTESIAN_POINT ( 'NONE',  ( 20.94999999999999929, 70.50000000001180922, -81.92837350343744163 ) ) ;
#166823=CARTESIAN_POINT ( 'NONE',  ( -22.50000000000000000, 75.90000000001194280, -103.0231074845243171 ) ) ;
#166828=CIRCLE ( 'NONE', #75232, 0.1000000000000028644 ) ;
#166837=CARTESIAN_POINT ( 'NONE',  ( -18.59999999999999787, 64.25000000001179501, -81.77310748452438816 ) ) ;
#166846=ADVANCED_FACE ( 'NONE', ( #115970 ), #73018, .T. ) ;
#166869=DIRECTION ( 'NONE',  ( 1.000000000000000000, 0.000000000000000000, 0.000000000000000000 ) ) ;
#166900=DIRECTION ( 'NONE',  ( 0.000000000000000000, 0.000000000000000000, 1.000000000000000000 ) ) ;
#166920=EDGE_CURVE ( 'NONE', #20048, #156829, #163539, .T. ) ;
#166927=CIRCLE ( 'NONE', #162619, 0.9750000000000036415 ) ;
#166936=CARTESIAN_POINT ( 'NONE',  ( 21.05000000000000071, 69.52293297888719792, -102.9231074845243654 ) ) ;
#166937=DIRECTION ( 'NONE',  ( 0.000000000000000000, -6.982962677686266711E-15, 1.000000000000000000 ) ) ;
#166947=CIRCLE ( 'NONE', #71063, 0.1000000000000028644 ) ;
#166973=CARTESIAN_POINT ( 'NONE',  ( -18.59999999999999787, 66.75000000001185185, -90.67310748452436542 ) ) ;
#166986=AXIS2_PLACEMENT_3D ( 'NONE', #33989, #95202, #75661 ) ;
#166989=DIRECTION ( 'NONE',  ( 0.000000000000000000, -0.8700118002898354908, 0.4930308989875170078 ) ) ;
#167066=ORIENTED_EDGE ( 'NONE', *, *, #179878, .T. ) ;
#167073=CARTESIAN_POINT ( 'NONE',  ( -20.86777300164945004, 65.66799936921512426, -63.92993998886009877 ) ) ;
#167083=ORIENTED_EDGE ( 'NONE', *, *, #82052, .F. ) ;
#167084=EDGE_LOOP ( 'NONE', ( #192156, #248604, #142116, #255753 ) ) ;
#167119=DIRECTION ( 'NONE',  ( 0.000000000000000000, -0.4999999999999689138, -0.8660254037844565822 ) ) ;
#167135=CARTESIAN_POINT ( 'NONE',  ( 23.15000000000000213, 87.48912529308779540, -72.62310748452422615 ) ) ;
#167144=DIRECTION ( 'NONE',  ( 0.9880948137434723000, -0.1538461538461484146, -1.074301950413233906E-15 ) ) ;
#167147=DIRECTION ( 'NONE',  ( 0.000000000000000000, -0.8700118002898357128, 0.4930308989875171188 ) ) ;
#167170=EDGE_CURVE ( 'NONE', #68348, #75696, #189144, .T. ) ;
#167171=CARTESIAN_POINT ( 'NONE',  ( 20.96077737575347300, 64.37609936600699712, -76.38231552741797259 ) ) ;
#167202=DIRECTION ( 'NONE',  ( 0.000000000000000000, -0.9999631594459057471, 0.008583690987121077309 ) ) ;
#167208=DIRECTION ( 'NONE',  ( 1.000000000000000000, 0.000000000000000000, 0.000000000000000000 ) ) ;
#167237=ORIENTED_EDGE ( 'NONE', *, *, #242805, .T. ) ;
#167256=VERTEX_POINT ( 'NONE', #799 ) ;
#167285=CARTESIAN_POINT ( 'NONE',  ( 23.14999999999999147, 76.00000000001195133, -103.0231074845243171 ) ) ;
#167287=AXIS2_PLACEMENT_3D ( 'NONE', #91050, #233155, #54480 ) ;
#167312=CARTESIAN_POINT ( 'NONE',  ( -23.15000000000000213, 87.75000000001173817, -72.62310748452422615 ) ) ;
#167332=CIRCLE ( 'NONE', #200628, 0.1000000000000028644 ) ;
#167337=AXIS2_PLACEMENT_3D ( 'NONE', #36013, #155971, #38566 ) ;
#167338=ORIENTED_EDGE ( 'NONE', *, *, #249521, .T. ) ;
#167350=FACE_OUTER_BOUND ( 'NONE', #22256, .T. ) ;
#167375=EDGE_CURVE ( 'NONE', #5545, #118409, #250900, .T. ) ;
#167390=FACE_BOUND ( 'NONE', #25784, .T. ) ;
#167394=VERTEX_POINT ( 'NONE', #176933 ) ;
#167397=FACE_OUTER_BOUND ( 'NONE', #53278, .T. ) ;
#167422=CARTESIAN_POINT ( 'NONE',  ( -20.94999999999999929, 76.00000000001170974, -69.52310748452431710 ) ) ;
#167423=EDGE_CURVE ( 'NONE', #148456, #255325, #46893, .T. ) ;
#167428=EDGE_CURVE ( 'NONE', #110088, #194795, #80188, .T. ) ;
#167501=DIRECTION ( 'NONE',  ( 0.000000000000000000, -1.000000000000000000, 0.000000000000000000 ) ) ;
#167503=CIRCLE ( 'NONE', #159138, 0.09999999999999939493 ) ;
#167537=AXIS2_PLACEMENT_3D ( 'NONE', #6308, #227939, #49295 ) ;
#167592=DIRECTION ( 'NONE',  ( -1.000000000000000000, -0.000000000000000000, -0.000000000000000000 ) ) ;
#167611=AXIS2_PLACEMENT_3D ( 'NONE', #233240, #170729, #194110 ) ;
#167634=ORIENTED_EDGE ( 'NONE', *, *, #53518, .T. ) ;
#167657=DIRECTION ( 'NONE',  ( 0.000000000000000000, 0.1298341882519953583, 0.9915357197604862671 ) ) ;
#167664=ORIENTED_EDGE ( 'NONE', *, *, #168008, .F. ) ;
#167665=CARTESIAN_POINT ( 'NONE',  ( -18.59999999999999787, 74.83729825007388570, -94.92310748452432279 ) ) ;
#167671=CARTESIAN_POINT ( 'NONE',  ( 22.49544290803778424, 64.25012976215489857, -103.0884194437818167 ) ) ;
#167674=TOROIDAL_SURFACE ( 'NONE', #176057, 0.6000000000000009770, 0.1000000000000000056 ) ;
#167682=VERTEX_POINT ( 'NONE', #121472 ) ;
#167694=AXIS2_PLACEMENT_3D ( 'NONE', #207146, #28551, #87169 ) ;
#167706=DIRECTION ( 'NONE',  ( 1.000000000000000000, 0.000000000000000000, 0.000000000000000000 ) ) ;
#167765=EDGE_CURVE ( 'NONE', #126928, #64660, #105306, .T. ) ;
#167822=ORIENTED_EDGE ( 'NONE', *, *, #184120, .T. ) ;
#167823=CARTESIAN_POINT ( 'NONE',  ( -20.54999999999999716, 68.75000000001179501, -81.77310748452435973 ) ) ;
#167826=CARTESIAN_POINT ( 'NONE',  ( 20.85000000000000142, 64.35000000001170406, -69.52310748452438816 ) ) ;
#167830=DIRECTION ( 'NONE',  ( -1.000000000000000000, 0.000000000000000000, 0.000000000000000000 ) ) ;
#167838=AXIS2_PLACEMENT_3D ( 'NONE', #155473, #150306, #211558 ) ;
#167851=CARTESIAN_POINT ( 'NONE',  ( 20.12500000000000000, 66.25000000001189449, -94.91133620241009794 ) ) ;
#167871=AXIS2_PLACEMENT_3D ( 'NONE', #200041, #82614, #83891 ) ;
#167872=EDGE_CURVE ( 'NONE', #162117, #189189, #204725, .T. ) ;
#167874=AXIS2_PLACEMENT_3D ( 'NONE', #221012, #101025, #21556 ) ;
#167940=CARTESIAN_POINT ( 'NONE',  ( -21.05000000000000071, 69.70076908991968878, -103.1215449845246468 ) ) ;
#167954=VERTEX_POINT ( 'NONE', #153898 ) ;
#167962=ORIENTED_EDGE ( 'NONE', *, *, #7479, .T. ) ;
#167973=B_SPLINE_CURVE_WITH_KNOTS ( 'NONE', 3,
 ( #199884, #1644, #42099, #39543, #121636, #81176, #56479, #100721 ),
 .UNSPECIFIED., .F., .F.,
 ( 4, 2, 2, 4 ),
 ( 0.000000000000000000, 0.0001306511400391193183, 0.0001959767100587024775, 0.0002613022800782856367 ),
 .UNSPECIFIED. ) ;
#167981=DIRECTION ( 'NONE',  ( 0.000000000000000000, -6.853228547068871147E-15, 1.000000000000000000 ) ) ;
#167982=CARTESIAN_POINT ( 'NONE',  ( 19.75857864376268935, 64.25000000001176659, -78.17310748452439384 ) ) ;
#168002=DIRECTION ( 'NONE',  ( 0.000000000000000000, 0.6728971962617172897, -0.7397360091702445128 ) ) ;
#168008=EDGE_CURVE ( 'NONE', #214060, #125402, #91310, .T. ) ;
#168011=DIRECTION ( 'NONE',  ( 0.000000000000000000, 0.000000000000000000, 1.000000000000000000 ) ) ;
#168031=LINE ( 'NONE', #186280, #170405 ) ;
#168034=DIRECTION ( 'NONE',  ( -0.000000000000000000, 0.1350103645451807555, 0.9908441862701610203 ) ) ;
#168072=ORIENTED_EDGE ( 'NONE', *, *, #92631, .F. ) ;
#168081=CARTESIAN_POINT ( 'NONE',  ( 20.95512820512820440, 65.37615131630001031, -95.35819391543677170 ) ) ;
#168101=CARTESIAN_POINT ( 'NONE',  ( -23.15000000000000213, 64.25000000001173817, -72.62310748452439668 ) ) ;
#168105=DIRECTION ( 'NONE',  ( 1.000000000000000000, -0.000000000000000000, 0.000000000000000000 ) ) ;
#168117=ADVANCED_FACE ( 'NONE', ( #119879 ), #109235, .F. ) ;
#168129=DIRECTION ( 'NONE',  ( 1.000000000000000000, 0.000000000000000000, 0.000000000000000000 ) ) ;
#168181=ORIENTED_EDGE ( 'NONE', *, *, #39920, .T. ) ;
#168199=VERTEX_POINT ( 'NONE', #165406 ) ;
#168207=ORIENTED_EDGE ( 'NONE', *, *, #77039, .F. ) ;
#168274=EDGE_CURVE ( 'NONE', #55246, #237061, #166713, .T. ) ;
#168289=CARTESIAN_POINT ( 'NONE',  ( 20.94999999999999574, 76.00000000001195133, -103.0231074845243171 ) ) ;
#168299=EDGE_LOOP ( 'NONE', ( #20315, #86616, #248399, #54965 ) ) ;
#168309=EDGE_CURVE ( 'NONE', #121066, #216063, #180007, .T. ) ;
#168318=ADVANCED_FACE ( 'NONE', ( #247501 ), #148409, .T. ) ;
#168354=VECTOR ( 'NONE', #157448, 999.9999999999998863 ) ;
#168355=DIRECTION ( 'NONE',  ( 1.000000000000000000, -2.952720810173289112E-16, -2.061873921506763405E-30 ) ) ;
#168362=DIRECTION ( 'NONE',  ( -4.391705002472927119E-16, -1.000000000000000000, -7.026728003956683390E-15 ) ) ;
#168365=DIRECTION ( 'NONE',  ( 0.000000000000000000, 0.4930308989875575865, 0.8700118002898125091 ) ) ;
#168371=AXIS2_PLACEMENT_3D ( 'NONE', #80152, #138841, #625 ) ;
#168375=FACE_OUTER_BOUND ( 'NONE', #185170, .T. ) ;
#168384=LINE ( 'NONE', #133066, #28565 ) ;
#168414=CARTESIAN_POINT ( 'NONE',  ( -21.07954640115405809, 69.67071230398704529, -103.0891151916641775 ) ) ;
#168424=EDGE_CURVE ( 'NONE', #200329, #87867, #25878, .T. ) ;
#168444=ORIENTED_EDGE ( 'NONE', *, *, #34428, .F. ) ;
#168450=CIRCLE ( 'NONE', #34562, 0.1000000000000028644 ) ;
#168491=FACE_OUTER_BOUND ( 'NONE', #250979, .T. ) ;
#168535=DIRECTION ( 'NONE',  ( 0.000000000000000000, -6.982962677686266711E-15, 1.000000000000000000 ) ) ;
#168550=CARTESIAN_POINT ( 'NONE',  ( -20.54999999999999716, 85.40000000001178648, -79.41707660717668205 ) ) ;
#168580=VERTEX_POINT ( 'NONE', #98649 ) ;
#168600=EDGE_CURVE ( 'NONE', #254886, #237868, #142728, .T. ) ;
#168607=ORIENTED_EDGE ( 'NONE', *, *, #247839, .F. ) ;
#168630=DIRECTION ( 'NONE',  ( 0.000000000000000000, -1.000000000000000000, -6.352154140967427193E-15 ) ) ;
#168631=DIRECTION ( 'NONE',  ( 0.000000000000000000, -6.467318590049456648E-15, 1.000000000000000000 ) ) ;
#168635=DIRECTION ( 'NONE',  ( -1.000000000000000000, -7.304098846218163263E-16, 4.217023435051627211E-16 ) ) ;
#168663=DIRECTION ( 'NONE',  ( 0.000000000000000000, 0.000000000000000000, 1.000000000000000000 ) ) ;
#168675=CARTESIAN_POINT ( 'NONE',  ( 18.49999999999999289, 65.79142135624906018, -78.25595019699899524 ) ) ;
#168730=ORIENTED_EDGE ( 'NONE', *, *, #2562, .T. ) ;
#168794=EDGE_LOOP ( 'NONE', ( #52049, #96416, #134348, #49949 ) ) ;
#168804=ORIENTED_EDGE ( 'NONE', *, *, #46038, .F. ) ;
#168840=AXIS2_PLACEMENT_3D ( 'NONE', #252691, #135309, #212320 ) ;
#168871=CARTESIAN_POINT ( 'NONE',  ( -18.50000000000000000, 65.70729864260985664, -64.06574559737244101 ) ) ;
#168899=VERTEX_POINT ( 'NONE', #200060 ) ;
#168902=EDGE_CURVE ( 'NONE', #231733, #85086, #257394, .T. ) ;
#168908=EDGE_LOOP ( 'NONE', ( #135796, #167664, #116593, #49546 ) ) ;
#168915=EDGE_CURVE ( 'NONE', #36183, #239427, #74243, .T. ) ;
#168929=CARTESIAN_POINT ( 'NONE',  ( -1.739115166359751801E-14, 64.35000000001178933, -78.17310748452437963 ) ) ;
#168932=FACE_OUTER_BOUND ( 'NONE', #251714, .T. ) ;
#168937=DIRECTION ( 'NONE',  ( 1.000000000000000000, 0.000000000000000000, 0.000000000000000000 ) ) ;
#168972=LINE ( 'NONE', #69848, #125967 ) ;
#168978=AXIS2_PLACEMENT_3D ( 'NONE', #48969, #9847, #165072 ) ;
#169001=DIRECTION ( 'NONE',  ( -1.000000000000000000, 0.000000000000000000, -0.000000000000000000 ) ) ;
#169006=CYLINDRICAL_SURFACE ( 'NONE', #257605, 11.79999999999999716 ) ;
#169017=AXIS2_PLACEMENT_3D ( 'NONE', #152903, #168635, #171194 ) ;
#169028=CARTESIAN_POINT ( 'NONE',  ( -20.85000000000000142, 65.66751761918648356, -63.92826094061123143 ) ) ;
#169030=DIRECTION ( 'NONE',  ( -1.000000000000000000, 0.000000000000000000, -0.000000000000000000 ) ) ;
#169044=CARTESIAN_POINT ( 'NONE',  ( 18.36493879433277243, 85.50000080620219478, -62.60095882417268598 ) ) ;
#169063=EDGE_CURVE ( 'NONE', #155591, #5814, #117187, .T. ) ;
#169088=CARTESIAN_POINT ( 'NONE',  ( 20.94999999999999929, 77.83534155023627932, -91.46795619196130644 ) ) ;
#169105=CARTESIAN_POINT ( 'NONE',  ( -20.94999999999999929, 74.26374286841446803, -91.45445515550682103 ) ) ;
#169109=ORIENTED_EDGE ( 'NONE', *, *, #17896, .F. ) ;
#169116=DIRECTION ( 'NONE',  ( 0.000000000000000000, -6.853228547068871147E-15, 1.000000000000000000 ) ) ;
#169130=EDGE_LOOP ( 'NONE', ( #35395, #61040, #190416, #119929 ) ) ;
#169158=TOROIDAL_SURFACE ( 'NONE', #214913, 6.258578643762700899, 0.1000000000000000056 ) ;
#169166=DIRECTION ( 'NONE',  ( 0.000000000000000000, -1.000000000000000000, 0.000000000000000000 ) ) ;
#169198=ORIENTED_EDGE ( 'NONE', *, *, #243010, .F. ) ;
#169212=ORIENTED_EDGE ( 'NONE', *, *, #107179, .F. ) ;
#169216=EDGE_LOOP ( 'NONE', ( #143743, #170212, #254508, #237708 ) ) ;
#169222=EDGE_LOOP ( 'NONE', ( #123839, #133054, #184242, #107859 ) ) ;
#169232=DIRECTION ( 'NONE',  ( -0.000000000000000000, 0.9908441862701591329, 0.1350103645451946055 ) ) ;
#169246=ORIENTED_EDGE ( 'NONE', *, *, #44656, .T. ) ;
#169280=CIRCLE ( 'NONE', #244223, 0.09999999999999520384 ) ;
#169289=VECTOR ( 'NONE', #33286, 1000.000000000000114 ) ;
#169296=CARTESIAN_POINT ( 'NONE',  ( 20.94999999999999929, 76.00000000001170974, -69.52310748452431710 ) ) ;
#169300=CIRCLE ( 'NONE', #244078, 0.1000000000000028644 ) ;
#169313=ORIENTED_EDGE ( 'NONE', *, *, #160420, .T. ) ;
#169322=EDGE_CURVE ( 'NONE', #77493, #71577, #34801, .T. ) ;
#169328=AXIS2_PLACEMENT_3D ( 'NONE', #185568, #242963, #6928 ) ;
#169339=CIRCLE ( 'NONE', #6797, 0.3999999999999975797 ) ;
#169412=AXIS2_PLACEMENT_3D ( 'NONE', #8509, #160232, #248398 ) ;
#169425=ORIENTED_EDGE ( 'NONE', *, *, #58546, .T. ) ;
#169428=VECTOR ( 'NONE', #73933, 1000.000000000000000 ) ;
#169440=DIRECTION ( 'NONE',  ( 0.000000000000000000, 0.000000000000000000, 1.000000000000000000 ) ) ;
#169446=CARTESIAN_POINT ( 'NONE',  ( -18.59999999999999787, 70.10000000001193143, -92.80400771986793984 ) ) ;
#169452=CARTESIAN_POINT ( 'NONE',  ( 22.39999999999999503, 68.20922040163857503, -103.0231074845243739 ) ) ;
#169508=DIRECTION ( 'NONE',  ( 0.000000000000000000, -1.000000000000000000, -6.982962677686266711E-15 ) ) ;
#169518=ORIENTED_EDGE ( 'NONE', *, *, #28964, .F. ) ;
#169552=EDGE_CURVE ( 'NONE', #79511, #55514, #151335, .T. ) ;
#169580=EDGE_CURVE ( 'NONE', #237061, #10791, #204740, .T. ) ;
#169593=EDGE_CURVE ( 'NONE', #237924, #123705, #213853, .T. ) ;
#169608=CARTESIAN_POINT ( 'NONE',  ( 19.97071067811864609, 64.27928932189311695, -78.37310748452439668 ) ) ;
#169610=CARTESIAN_POINT ( 'NONE',  ( 21.05000000000000071, 87.65000000001194280, -103.0231074845242318 ) ) ;
#169613=AXIS2_PLACEMENT_3D ( 'NONE', #213212, #132416, #230223 ) ;
#169617=DIRECTION ( 'NONE',  ( 1.000000000000000000, 0.000000000000000000, 0.000000000000000000 ) ) ;
#169624=DIRECTION ( 'NONE',  ( 0.000000000000000000, 0.000000000000000000, 1.000000000000000000 ) ) ;
#169631=AXIS2_PLACEMENT_3D ( 'NONE', #18112, #216305, #238446 ) ;
#169635=EDGE_CURVE ( 'NONE', #24156, #250150, #138979, .T. ) ;
#169639=DIRECTION ( 'NONE',  ( 0.000000000000000000, -0.5000000000000209832, -0.8660254037844264952 ) ) ;
#169645=DIRECTION ( 'NONE',  ( 1.000000000000000000, -3.265361837132813093E-16, -2.280189983783949500E-30 ) ) ;
#169656=CARTESIAN_POINT ( 'NONE',  ( -18.43599941264914222, 85.51932742860660142, -96.05013069500279244 ) ) ;
#169664=EDGE_LOOP ( 'NONE', ( #225163, #50677, #116147, #23152 ) ) ;
#169703=FACE_OUTER_BOUND ( 'NONE', #20115, .T. ) ;
#169709=AXIS2_PLACEMENT_3D ( 'NONE', #38797, #115758, #118339 ) ;
#169741=CARTESIAN_POINT ( 'NONE',  ( 21.04999999999999716, 64.25000000001175238, -76.36470817442145176 ) ) ;
#169753=EDGE_LOOP ( 'NONE', ( #130183, #236485, #255768, #210369 ) ) ;
#169776=DIRECTION ( 'NONE',  ( 0.000000000000000000, -1.000000000000000000, 0.000000000000000000 ) ) ;
#169786=CARTESIAN_POINT ( 'NONE',  ( 23.24999999999999645, 76.00000000001195133, -103.0231074845243171 ) ) ;
#169820=VERTEX_POINT ( 'NONE', #12359 ) ;
#169842=ADVANCED_FACE ( 'NONE', ( #132274 ), #47427, .F. ) ;
#169850=CYLINDRICAL_SURFACE ( 'NONE', #21736, 0.1000000000000052097 ) ;
#169909=DIRECTION ( 'NONE',  ( 1.000000000000000000, 0.000000000000000000, 0.000000000000000000 ) ) ;
#169913=DIRECTION ( 'NONE',  ( 0.000000000000000000, 0.1350103645451835865, 0.9908441862701605762 ) ) ;
#169922=LINE ( 'NONE', #51175, #95665 ) ;
#169924=VECTOR ( 'NONE', #19196, 1000.000000000000000 ) ;
#169934=DIRECTION ( 'NONE',  ( -0.7071067811865475727, 0.7071067811865475727, 4.937700262164531476E-15 ) ) ;
#169945=CARTESIAN_POINT ( 'NONE',  ( -22.57320508075687115, 64.35000000001195986, -103.0231074845243739 ) ) ;
#169971=ORIENTED_EDGE ( 'NONE', *, *, #47016, .T. ) ;
#170012=AXIS2_PLACEMENT_3D ( 'NONE', #20710, #100194, #179781 ) ;
#170015=DIRECTION ( 'NONE',  ( -1.000000000000000000, 0.000000000000000000, 0.000000000000000000 ) ) ;
#170042=ORIENTED_EDGE ( 'NONE', *, *, #101414, .F. ) ;
#170055=EDGE_CURVE ( 'NONE', #170631, #208027, #256021, .T. ) ;
#170106=EDGE_CURVE ( 'NONE', #69997, #91291, #160851, .T. ) ;
#170117=ORIENTED_EDGE ( 'NONE', *, *, #247839, .T. ) ;
#170156=CARTESIAN_POINT ( 'NONE',  ( -20.54999999999999716, 74.00000000001186606, -89.79848556176222019 ) ) ;
#170168=ADVANCED_FACE ( 'NONE', ( #225906 ), #43535, .T. ) ;
#170181=CARTESIAN_POINT ( 'NONE',  ( -21.05000000000000071, 69.70000000001193996, -102.9231074845243512 ) ) ;
#170205=DIRECTION ( 'NONE',  ( 1.000000000000000000, 0.000000000000000000, 0.000000000000000000 ) ) ;
#170212=ORIENTED_EDGE ( 'NONE', *, *, #131915, .T. ) ;
#170243=DIRECTION ( 'NONE',  ( -0.000000000000000000, 1.000000000000000000, 6.982962677686266711E-15 ) ) ;
#170247=AXIS2_PLACEMENT_3D ( 'NONE', #153130, #255980, #13587 ) ;
#170339=CARTESIAN_POINT ( 'NONE',  ( 18.37172112093826115, 85.57096165225489415, -62.70637303104068394 ) ) ;
#170340=CYLINDRICAL_SURFACE ( 'NONE', #35146, 0.1000000000000064587 ) ;
#170353=DIRECTION ( 'NONE',  ( -1.000000000000000000, -0.000000000000000000, -0.000000000000000000 ) ) ;
#170363=CARTESIAN_POINT ( 'NONE',  ( -22.50000000000000000, 76.00000000001199396, -109.2731074845243171 ) ) ;
#170366=EDGE_CURVE ( 'NONE', #101254, #88561, #214231, .T. ) ;
#170374=DIRECTION ( 'NONE',  ( 0.000000000000000000, 1.000000000000000000, 6.982962677686266711E-15 ) ) ;
#170389=ORIENTED_EDGE ( 'NONE', *, *, #174078, .F. ) ;
#170391=CARTESIAN_POINT ( 'NONE',  ( 23.15000000000000213, 87.75000000001179501, -81.67310748452422331 ) ) ;
#170393=DIRECTION ( 'NONE',  ( 0.7071067811865474617, -0.7071067811865474617, -4.937700262164531476E-15 ) ) ;
#170405=VECTOR ( 'NONE', #7638, 1000.000000000000000 ) ;
#170412=ORIENTED_EDGE ( 'NONE', *, *, #183154, .T. ) ;
#170414=ORIENTED_EDGE ( 'NONE', *, *, #147266, .T. ) ;
#170431=ORIENTED_EDGE ( 'NONE', *, *, #247710, .F. ) ;
#170434=ORIENTED_EDGE ( 'NONE', *, *, #50853, .F. ) ;
#170456=ORIENTED_EDGE ( 'NONE', *, *, #104010, .F. ) ;
#170471=EDGE_CURVE ( 'NONE', #17853, #163251, #139365, .T. ) ;
#170500=EDGE_LOOP ( 'NONE', ( #64263, #42447, #149825, #9247 ) ) ;
#170509=EDGE_CURVE ( 'NONE', #17499, #54475, #26944, .T. ) ;
#170512=DIRECTION ( 'NONE',  ( 0.000000000000000000, -7.086529944415894657E-15, 1.000000000000000000 ) ) ;
#170514=B_SPLINE_CURVE_WITH_KNOTS ( 'NONE', 3,
 ( #191775, #7978, #247860, #48370 ),
 .UNSPECIFIED., .F., .F.,
 ( 4, 4 ),
 ( 0.000000000000000000, 0.0002118541922231814993 ),
 .UNSPECIFIED. ) ;
#170515=CIRCLE ( 'NONE', #199716, 0.09999999999999939493 ) ;
#170518=VERTEX_POINT ( 'NONE', #46979 ) ;
#170543=DIRECTION ( 'NONE',  ( 0.000000000000000000, -7.116814260417668513E-15, 1.000000000000000000 ) ) ;
#170566=COLOUR_RGB ( '', 0.66274510, 0.83137255, 0.94901961) ;
#170579=EDGE_LOOP ( 'NONE', ( #85400, #242549, #204939, #144239 ) ) ;
#170631=VERTEX_POINT ( 'NONE', #252564 ) ;
#170656=CARTESIAN_POINT ( 'NONE',  ( 21.00000000000000000, 66.25000000001179501, -81.87310748452438247 ) ) ;
#170671=DIRECTION ( 'NONE',  ( 0.000000000000000000, 7.056502275159890043E-15, -1.000000000000000000 ) ) ;
#170693=DIRECTION ( 'NONE',  ( -1.000000000000000000, 2.952720810173289112E-16, 2.061873921506763405E-30 ) ) ;
#170712=CYLINDRICAL_SURFACE ( 'NONE', #64216, 0.09999999999999939493 ) ;
#170727=CIRCLE ( 'NONE', #133254, 7.791421356237310469 ) ;
#170729=DIRECTION ( 'NONE',  ( 1.000000000000000000, 0.000000000000000000, 0.000000000000000000 ) ) ;
#170796=VERTEX_POINT ( 'NONE', #226255 ) ;
#170827=VERTEX_POINT ( 'NONE', #122057 ) ;
#170850=VECTOR ( 'NONE', #200355, 1000.000000000000000 ) ;
#170856=VERTEX_POINT ( 'NONE', #162479 ) ;
#170874=ADVANCED_FACE ( 'NONE', ( #84146 ), #251991, .T. ) ;
#170907=FACE_OUTER_BOUND ( 'NONE', #201187, .T. ) ;
#170913=DIRECTION ( 'NONE',  ( 0.000000000000000000, 1.000000000000000000, 6.982962677686266711E-15 ) ) ;
#170920=EDGE_CURVE ( 'NONE', #72979, #206286, #214566, .T. ) ;
#170922=VECTOR ( 'NONE', #41728, 1000.000000000000000 ) ;
#170936=ORIENTED_EDGE ( 'NONE', *, *, #200952, .F. ) ;
#170945=CARTESIAN_POINT ( 'NONE',  ( -20.94999999999999929, 65.70729864260985664, -64.06574559737245522 ) ) ;
#170950=CARTESIAN_POINT ( 'NONE',  ( 21.00000000000000000, 66.25000000001179501, -81.77310748452437394 ) ) ;
#170953=ADVANCED_FACE ( 'NONE', ( #191037 ), #51467, .T. ) ;
#170959=CARTESIAN_POINT ( 'NONE',  ( -22.01447462590973103, 68.73619979878202457, -103.1221444845838846 ) ) ;
#170979=CARTESIAN_POINT ( 'NONE',  ( -21.05000000000000071, 69.52192177891696190, -102.9231075492185568 ) ) ;
#170994=FACE_OUTER_BOUND ( 'NONE', #148570, .T. ) ;
#171014=ORIENTED_EDGE ( 'NONE', *, *, #41956, .T. ) ;
#171018=CARTESIAN_POINT ( 'NONE',  ( 18.49999999999999289, 65.79142135392861235, -78.32060061889450253 ) ) ;
#171023=EDGE_CURVE ( 'NONE', #82199, #161543, #172777, .T. ) ;
#171044=CIRCLE ( 'NONE', #29374, 4.000000000000003553 ) ;
#171051=VERTEX_POINT ( 'NONE', #37098 ) ;
#171067=AXIS2_PLACEMENT_3D ( 'NONE', #55387, #134931, #231513 ) ;
#171117=CARTESIAN_POINT ( 'NONE',  ( 21.04999999999963478, 65.45624872451622878, -95.46671967585933771 ) ) ;
#171153=DIRECTION ( 'NONE',  ( 0.000000000000000000, -6.417474130781252121E-15, 1.000000000000000000 ) ) ;
#171182=CARTESIAN_POINT ( 'NONE',  ( -20.54999999999999716, 85.50000000001188027, -93.12913836187179584 ) ) ;
#171187=EDGE_LOOP ( 'NONE', ( #48857, #167066, #252732, #105616 ) ) ;
#171194=DIRECTION ( 'NONE',  ( 0.000000000000000000, 1.000000000000000000, 0.000000000000000000 ) ) ;
#171196=CARTESIAN_POINT ( 'NONE',  ( 18.46082813847993975, 85.48074965091940669, -95.93873738180860755 ) ) ;
#171199=DIRECTION ( 'NONE',  ( 0.000000000000000000, 0.1495327102803078179, 0.9887567792719429427 ) ) ;
#171244=DIRECTION ( 'NONE',  ( 0.000000000000000000, -6.352154140967427193E-15, 1.000000000000000000 ) ) ;
#171247=AXIS2_PLACEMENT_3D ( 'NONE', #7006, #63114, #68277 ) ;
#171272=AXIS2_PLACEMENT_3D ( 'NONE', #192463, #145315, #81464 ) ;
#171290=CARTESIAN_POINT ( 'NONE',  ( -18.50000000000000000, 77.16270174994990327, -94.92310748452430857 ) ) ;
#171294=ORIENTED_EDGE ( 'NONE', *, *, #156101, .T. ) ;
#171345=ORIENTED_EDGE ( 'NONE', *, *, #116598, .T. ) ;
#171347=ADVANCED_FACE ( 'NONE', ( #228565 ), #207723, .T. ) ;
#171372=CARTESIAN_POINT ( 'NONE',  ( -23.25000000000000000, 76.00000000001170974, -69.52310748452431710 ) ) ;
#171401=EDGE_CURVE ( 'NONE', #196796, #145911, #235596, .T. ) ;
#171431=DIRECTION ( 'NONE',  ( 0.000000000000000000, -6.530723674265620862E-15, 1.000000000000000000 ) ) ;
#171473=CARTESIAN_POINT ( 'NONE',  ( 23.24999999999999289, 69.35000000001180354, -81.87310748452435405 ) ) ;
#171487=CARTESIAN_POINT ( 'NONE',  ( -20.85000000000000142, 76.00000000001170974, -69.52310748452431710 ) ) ;
#171489=CARTESIAN_POINT ( 'NONE',  ( 20.46382478191414833, 65.40137955871450970, -95.34529301517892463 ) ) ;
#171494=CARTESIAN_POINT ( 'NONE',  ( -21.05000000000000071, 77.16270174994990327, -95.02310748452430289 ) ) ;
#171510=AXIS2_PLACEMENT_3D ( 'NONE', #119917, #144565, #221523 ) ;
#171557=FACE_OUTER_BOUND ( 'NONE', #173250, .T. ) ;
#171568=DIRECTION ( 'NONE',  ( -1.000000000000000000, 0.000000000000000000, -0.000000000000000000 ) ) ;
#171576=EDGE_CURVE ( 'NONE', #173596, #229669, #177580, .T. ) ;
#171594=AXIS2_PLACEMENT_3D ( 'NONE', #3003, #58152, #145085 ) ;
#171607=EDGE_CURVE ( 'NONE', #11996, #92498, #44274, .T. ) ;
#171610=DIRECTION ( 'NONE',  ( 0.000000000000000000, -0.9915357197604804940, 0.1298341882520397950 ) ) ;
#171667=DIRECTION ( 'NONE',  ( 0.000000000000000000, 0.000000000000000000, 1.000000000000000000 ) ) ;
#171678=PLANE ( 'NONE',  #171924 ) ;
#171734=CIRCLE ( 'NONE', #204995, 11.70000000000000284 ) ;
#171740=DIRECTION ( 'NONE',  ( -1.000000000000000000, 7.304098846218134667E-16, 5.100424963727256530E-30 ) ) ;
#171759=VERTEX_POINT ( 'NONE', #126586 ) ;
#171787=ORIENTED_EDGE ( 'NONE', *, *, #231444, .T. ) ;
#171791=EDGE_LOOP ( 'NONE', ( #111794, #192548, #14721, #241233 ) ) ;
#171806=DIRECTION ( 'NONE',  ( 0.000000000000000000, -7.304098846218139203E-15, 1.000000000000000000 ) ) ;
#171807=DIRECTION ( 'NONE',  ( 0.000000000000000000, -1.000000000000000000, -6.982962677686265922E-15 ) ) ;
#171810=EDGE_LOOP ( 'NONE', ( #51089, #77628, #51028, #81530 ) ) ;
#171823=ORIENTED_EDGE ( 'NONE', *, *, #101472, .T. ) ;
#171832=ORIENTED_EDGE ( 'NONE', *, *, #43026, .F. ) ;
#171863=ORIENTED_EDGE ( 'NONE', *, *, #53047, .F. ) ;
#171898=FACE_OUTER_BOUND ( 'NONE', #187304, .T. ) ;
#171909=CARTESIAN_POINT ( 'NONE',  ( -20.54999999999999716, 84.66355140188105111, -93.49900636645693908 ) ) ;
#171921=DIRECTION ( 'NONE',  ( 0.000000000000000000, 0.000000000000000000, 1.000000000000000000 ) ) ;
#171924=AXIS2_PLACEMENT_3D ( 'NONE', #167823, #206921, #69998 ) ;
#171936=VERTEX_POINT ( 'NONE', #136847 ) ;
#171947=VERTEX_POINT ( 'NONE', #36500 ) ;
#171948=DIRECTION ( 'NONE',  ( 1.000000000000000000, 0.000000000000000000, 0.000000000000000000 ) ) ;
#171958=CIRCLE ( 'NONE', #205218, 12.97499999999999964 ) ;
#171995=VERTEX_POINT ( 'NONE', #95160 ) ;
#172054=DIRECTION ( 'NONE',  ( 0.000000000000000000, -0.8660254037844387076, 0.4999999999999998335 ) ) ;
#172061=CARTESIAN_POINT ( 'NONE',  ( 23.14999999999999503, 61.95000000001175522, -75.03680255528533394 ) ) ;
#172083=CARTESIAN_POINT ( 'NONE',  ( -18.50000000000000000, 77.36242903720497566, -61.63422623660309796 ) ) ;
#172135=DIRECTION ( 'NONE',  ( 0.000000000000000000, -0.8660254037844377084, -0.5000000000000016653 ) ) ;
#172137=CARTESIAN_POINT ( 'NONE',  ( -20.64999999999999858, 68.75000000001185185, -90.67310748452436542 ) ) ;
#172139=CARTESIAN_POINT ( 'NONE',  ( -20.64999999999999858, 76.00000000001170974, -69.52310748452431710 ) ) ;
#172148=EDGE_CURVE ( 'NONE', #239427, #11679, #252527, .T. ) ;
#172166=CIRCLE ( 'NONE', #80484, 11.80000000000000426 ) ;
#172191=FACE_BOUND ( 'NONE', #62740, .T. ) ;
#172194=CYLINDRICAL_SURFACE ( 'NONE', #256583, 0.1000000000000028644 ) ;
#172206=CARTESIAN_POINT ( 'NONE',  ( -22.48660254037843487, 64.25000000001193712, -103.0731074845243711 ) ) ;
#172269=DIRECTION ( 'NONE',  ( 0.000000000000000000, 0.000000000000000000, -1.000000000000000000 ) ) ;
#172282=EDGE_CURVE ( 'NONE', #245381, #190040, #77930, .T. ) ;
#172284=AXIS2_PLACEMENT_3D ( 'NONE', #137269, #138532, #36937 ) ;
#172303=ADVANCED_FACE ( 'NONE', ( #109263 ), #10193, .T. ) ;
#172311=CARTESIAN_POINT ( 'NONE',  ( -22.39999999999999858, 68.20922040163854660, -103.1231074845243540 ) ) ;
#172314=LINE ( 'NONE', #147563, #27026 ) ;
#172333=DIRECTION ( 'NONE',  ( 1.387778780781405791E-13, 0.9999176327611370985, 0.01283462868040226822 ) ) ;
#172338=CARTESIAN_POINT ( 'NONE',  ( 20.94999999999999929, 65.70729864260985664, -64.06574559737245522 ) ) ;
#172357=CARTESIAN_POINT ( 'NONE',  ( 21.04999999999999716, 67.10527618163416719, -94.53602316137545358 ) ) ;
#172400=ORIENTED_EDGE ( 'NONE', *, *, #35913, .F. ) ;
#172439=DIRECTION ( 'NONE',  ( 0.000000000000000000, 6.982962677686266711E-15, -1.000000000000000000 ) ) ;
#172467=CARTESIAN_POINT ( 'NONE',  ( -20.05000000000000426, 66.75000000001185185, -90.67310748452436542 ) ) ;
#172484=CARTESIAN_POINT ( 'NONE',  ( 18.40000000000000568, 85.50000000001192291, -96.02374538734412113 ) ) ;
#172517=CARTESIAN_POINT ( 'NONE',  ( 21.05000000000000071, 76.08559286337390404, -109.4367702193939351 ) ) ;
#172557=CARTESIAN_POINT ( 'NONE',  ( 21.14999999999999858, 65.28660755661196902, -90.77310748452438816 ) ) ;
#172586=ORIENTED_EDGE ( 'NONE', *, *, #202590, .F. ) ;
#172601=CARTESIAN_POINT ( 'NONE',  ( 21.04999999999908411, 67.22371710472118878, -90.86519848187187165 ) ) ;
#172642=AXIS2_PLACEMENT_3D ( 'NONE', #22450, #60259, #104500 ) ;
#172648=ORIENTED_EDGE ( 'NONE', *, *, #168424, .T. ) ;
#172658=CARTESIAN_POINT ( 'NONE',  ( -22.49917693094574389, 75.91477003579036875, -114.6729032690549701 ) ) ;
#172676=DIRECTION ( 'NONE',  ( -1.000000000000000000, 0.000000000000000000, -0.000000000000000000 ) ) ;
#172695=CARTESIAN_POINT ( 'NONE',  ( 20.94999027547553894, 65.70673848566956110, -64.06382523348288771 ) ) ;
#172726=EDGE_LOOP ( 'NONE', ( #106927, #15207, #121817, #81525 ) ) ;
#172738=CARTESIAN_POINT ( 'NONE',  ( -21.05000000000000071, 76.00000000001170974, -69.52310748452431710 ) ) ;
#172740=DIRECTION ( 'NONE',  ( 1.000000000000000000, 0.000000000000000000, 0.000000000000000000 ) ) ;
#172749=DIRECTION ( 'NONE',  ( 0.000000000000000000, -6.240597636138643358E-14, -1.000000000000000000 ) ) ;
#172777=LINE ( 'NONE', #208026, #102119 ) ;
#172782=DIRECTION ( 'NONE',  ( 0.000000000000000000, 0.000000000000000000, -1.000000000000000000 ) ) ;
#172804=CARTESIAN_POINT ( 'NONE',  ( 20.85000000000000142, 87.65000000001170122, -69.52310748452423184 ) ) ;
#172881=ORIENTED_EDGE ( 'NONE', *, *, #38029, .T. ) ;
#172884=DIRECTION ( 'NONE',  ( 0.000000000000000000, -1.000000000000000000, -7.272083257015735086E-15 ) ) ;
#172895=CIRCLE ( 'NONE', #139522, 0.1000000000000028644 ) ;
#172902=AXIS2_PLACEMENT_3D ( 'NONE', #117368, #255534, #236022 ) ;
#172905=CARTESIAN_POINT ( 'NONE',  ( -20.54999999999999716, 87.75000000001180922, -81.87310748452422615 ) ) ;
#172921=ORIENTED_EDGE ( 'NONE', *, *, #58101, .F. ) ;
#172929=EDGE_CURVE ( 'NONE', #59708, #222143, #211226, .T. ) ;
#172934=DIRECTION ( 'NONE',  ( 1.000000000000000000, 0.000000000000000000, 0.000000000000000000 ) ) ;
#172945=DIRECTION ( 'NONE',  ( 1.000000000000000000, 0.000000000000000000, 0.000000000000000000 ) ) ;
#172949=DIRECTION ( 'NONE',  ( 2.952720810173289112E-16, 1.000000000000000000, 6.982962677686266711E-15 ) ) ;
#172952=ORIENTED_EDGE ( 'NONE', *, *, #241800, .T. ) ;
#172988=FACE_OUTER_BOUND ( 'NONE', #36235, .T. ) ;
#173004=CARTESIAN_POINT ( 'NONE',  ( -21.14999999999999858, 76.00000000001195133, -103.0231074845243171 ) ) ;
#173023=EDGE_CURVE ( 'NONE', #16177, #111684, #178678, .T. ) ;
#173078=ORIENTED_EDGE ( 'NONE', *, *, #134286, .F. ) ;
#173093=VERTEX_POINT ( 'NONE', #165378 ) ;
#173101=CARTESIAN_POINT ( 'NONE',  ( 18.59999999999999787, 77.73670573947921980, -58.00568489690056850 ) ) ;
#173139=LINE ( 'NONE', #252609, #12592 ) ;
#173150=CIRCLE ( 'NONE', #155980, 12.87499999999999822 ) ;
#173159=ORIENTED_EDGE ( 'NONE', *, *, #84131, .T. ) ;
#173175=EDGE_CURVE ( 'NONE', #140050, #185475, #110521, .T. ) ;
#173180=CARTESIAN_POINT ( 'NONE',  ( 21.05000000000000071, 77.84908441863888129, -91.36709696307717365 ) ) ;
#173190=CARTESIAN_POINT ( 'NONE',  ( 20.94999999999999574, 74.16465844978745281, -91.46795619196133487 ) ) ;
#173200=CYLINDRICAL_SURFACE ( 'NONE', #99605, 0.1000000000000028644 ) ;
#173213=CARTESIAN_POINT ( 'NONE',  ( -21.05000000000000071, 76.00000000001195133, -103.0231074845243171 ) ) ;
#173231=CARTESIAN_POINT ( 'NONE',  ( -20.94999999999999929, 68.97833521811159585, -65.68954208262705663 ) ) ;
#173243=ORIENTED_EDGE ( 'NONE', *, *, #9337, .F. ) ;
#173247=CIRCLE ( 'NONE', #6780, 0.5000000000000004441 ) ;
#173250=EDGE_LOOP ( 'NONE', ( #189255, #100307, #81758, #8950 ) ) ;
#173275=EDGE_LOOP ( 'NONE', ( #224323, #75654, #129303, #169212, #151245 ) ) ;
#173282=CARTESIAN_POINT ( 'NONE',  ( -18.59999999999999787, 64.35000000001190301, -96.10830171387040366 ) ) ;
#173294=DIRECTION ( 'NONE',  ( 0.000000000000000000, -1.000000000000000000, -6.982962677686265922E-15 ) ) ;
#173333=CARTESIAN_POINT ( 'NONE',  ( -20.64999999999999858, 68.85000000001186038, -90.67310748452435121 ) ) ;
#173374=CARTESIAN_POINT ( 'NONE',  ( 21.14999999999999858, 69.45934304831071415, -103.0231074845243597 ) ) ;
#173421=EDGE_CURVE ( 'NONE', #156346, #57105, #211028, .T. ) ;
#173426=VERTEX_POINT ( 'NONE', #206750 ) ;
#173484=ADVANCED_FACE ( 'NONE', ( #9831 ), #93211, .T. ) ;
#173502=B_SPLINE_CURVE_WITH_KNOTS ( 'NONE', 3,
 ( #81590, #45070, #182020, #142857, #22971, #145442, #101138, #106303, #124615, #204128, #4638, #43792, #239430, #202852, #104995, #221124, #103727, #25522, #243255 ),
 .UNSPECIFIED., .F., .F.,
 ( 4, 3, 3, 3, 3, 3, 4 ),
 ( 0.000000000000000000, 1.655171619026205498E-05, 2.773500582849481967E-05, 5.941817267378896972E-05, 0.0001114174635873639254, 0.0001914169455916358881, 0.0002627181070750633351 ),
 .UNSPECIFIED. ) ;
#173561=EDGE_CURVE ( 'NONE', #5814, #31606, #91930, .T. ) ;
#173578=DIRECTION ( 'NONE',  ( 1.000000000000000000, 0.000000000000000000, 0.000000000000000000 ) ) ;
#173596=VERTEX_POINT ( 'NONE', #1500 ) ;
#173639=AXIS2_PLACEMENT_3D ( 'NONE', #109962, #166132, #228658 ) ;
#173668=ORIENTED_EDGE ( 'NONE', *, *, #210428, .T. ) ;
#173676=FACE_OUTER_BOUND ( 'NONE', #90392, .T. ) ;
#173685=AXIS2_PLACEMENT_3D ( 'NONE', #251131, #116774, #174228 ) ;
#173686=CARTESIAN_POINT ( 'NONE',  ( -20.94999999999999929, 87.29603075034701476, -72.57100664418810254 ) ) ;
#173699=ORIENTED_EDGE ( 'NONE', *, *, #154628, .T. ) ;
#173702=DIRECTION ( 'NONE',  ( -3.890533409366484652E-14, 0.1298341882520054891, 0.9915357197604850459 ) ) ;
#173713=VECTOR ( 'NONE', #221563, 1000.000000000000000 ) ;
#173737=CYLINDRICAL_SURFACE ( 'NONE', #82615, 0.09999999999999939493 ) ;
#173764=AXIS2_PLACEMENT_3D ( 'NONE', #120165, #41898, #82244 ) ;
#173771=EDGE_LOOP ( 'NONE', ( #60142, #69612, #103, #122380 ) ) ;
#173796=VECTOR ( 'NONE', #134157, 1000.000000000000000 ) ;
#173802=AXIS2_PLACEMENT_3D ( 'NONE', #188786, #124977, #167981 ) ;
#173804=DIRECTION ( 'NONE',  ( -0.000000000000000000, 1.000000000000000000, 6.982962677686267499E-15 ) ) ;
#173840=CARTESIAN_POINT ( 'NONE',  ( 21.04999999999999716, 65.37127968600751160, -90.87310748452436826 ) ) ;
#173872=EDGE_CURVE ( 'NONE', #253910, #113736, #119636, .T. ) ;
#173885=VERTEX_POINT ( 'NONE', #133031 ) ;
#173898=DIRECTION ( 'NONE',  ( 1.000000000000000000, -0.000000000000000000, 0.000000000000000000 ) ) ;
#173904=VECTOR ( 'NONE', #247447, 1000.000000000000000 ) ;
#173939=VERTEX_POINT ( 'NONE', #11817 ) ;
#173942=CIRCLE ( 'NONE', #182272, 0.5000000000000004441 ) ;
#173951=DIRECTION ( 'NONE',  ( -2.602085213965226419E-14, 6.982962677686266711E-15, -1.000000000000000000 ) ) ;
#173958=EDGE_CURVE ( 'NONE', #30387, #182622, #207124, .T. ) ;
#173970=ORIENTED_EDGE ( 'NONE', *, *, #15605, .T. ) ;
#173973=AXIS2_PLACEMENT_3D ( 'NONE', #156116, #120839, #179518 ) ;
#173981=CARTESIAN_POINT ( 'NONE',  ( 20.89878130938411616, 65.67252876774509218, -63.94570419949945261 ) ) ;
#174010=DIRECTION ( 'NONE',  ( -1.000000000000000000, 0.000000000000000000, 0.000000000000000000 ) ) ;
#174019=DIRECTION ( 'NONE',  ( 1.000000000000000000, 0.000000000000000000, -0.000000000000000000 ) ) ;
#174065=CARTESIAN_POINT ( 'NONE',  ( 20.12500000000000355, 65.75804927292921320, -95.16290375743827212 ) ) ;
#174078=EDGE_CURVE ( 'NONE', #146439, #199102, #82172, .T. ) ;
#174085=CARTESIAN_POINT ( 'NONE',  ( 18.59999999999999076, 69.45000000001188312, -93.00608031408432907 ) ) ;
#174126=DIRECTION ( 'NONE',  ( 0.000000000000000000, -0.008583690987162452199, 0.9999631594459053030 ) ) ;
#174138=ORIENTED_EDGE ( 'NONE', *, *, #129670, .T. ) ;
#174139=CARTESIAN_POINT ( 'NONE',  ( 18.60000000000000142, 85.40000000001184333, -95.72584772486095517 ) ) ;
#174142=DIRECTION ( 'NONE',  ( 0.000000000000000000, -0.6728971962617172897, 0.7397360091702445128 ) ) ;
#174146=VERTEX_POINT ( 'NONE', #226659 ) ;
#174159=CARTESIAN_POINT ( 'NONE',  ( 20.94999999999999574, 70.10000000001193143, -92.80400771986793984 ) ) ;
#174163=ORIENTED_EDGE ( 'NONE', *, *, #105184, .F. ) ;
#174188=CARTESIAN_POINT ( 'NONE',  ( 18.48197441911473504, 85.51795479471654460, -62.63289584231627316 ) ) ;
#174193=EDGE_CURVE ( 'NONE', #106895, #4548, #207309, .T. ) ;
#174196=CIRCLE ( 'NONE', #120577, 0.09999999999999739653 ) ;
#174197=TOROIDAL_SURFACE ( 'NONE', #7754, 7.791421356237335338, 0.1000000000000000056 ) ;
#174227=CARTESIAN_POINT ( 'NONE',  ( 20.85000000000000142, 75.83895117929300511, -69.80729732888453043 ) ) ;
#174228=DIRECTION ( 'NONE',  ( 0.000000000000000000, -7.304098846218139203E-15, 1.000000000000000000 ) ) ;
#174243=CARTESIAN_POINT ( 'NONE',  ( -22.50000000000000000, 64.35042919246716053, -103.1231074845243825 ) ) ;
#174250=EDGE_LOOP ( 'NONE', ( #38074, #160429, #83398, #121427 ) ) ;
#174271=CIRCLE ( 'NONE', #178731, 0.09999999999999520384 ) ;
#174274=FACE_OUTER_BOUND ( 'NONE', #146266, .T. ) ;
#174285=ORIENTED_EDGE ( 'NONE', *, *, #184144, .F. ) ;
#174292=CARTESIAN_POINT ( 'NONE',  ( 20.94999999999999929, 76.00000000001172396, -71.42310748452430857 ) ) ;
#174310=CARTESIAN_POINT ( 'NONE',  ( -23.15000000000000213, 76.00000000001179501, -81.32310748452431426 ) ) ;
#174346=VERTEX_POINT ( 'NONE', #58281 ) ;
#174356=ORIENTED_EDGE ( 'NONE', *, *, #100838, .T. ) ;
#174365=CARTESIAN_POINT ( 'NONE',  ( 18.59999999999999787, 70.10000000001193143, -92.80400771986793984 ) ) ;
#174374=ORIENTED_EDGE ( 'NONE', *, *, #170471, .F. ) ;
#174393=CARTESIAN_POINT ( 'NONE',  ( 21.05000000000000071, 70.50000000001180922, -81.92837350343744163 ) ) ;
#174397=CARTESIAN_POINT ( 'NONE',  ( -23.15000000000000213, 71.65000000001187175, -90.77310748452434552 ) ) ;
#174419=CARTESIAN_POINT ( 'NONE',  ( 21.05000000000000071, 76.00000000001195133, -103.0231074845243171 ) ) ;
#174427=ORIENTED_EDGE ( 'NONE', *, *, #178311, .F. ) ;
#174489=CIRCLE ( 'NONE', #191198, 0.1000000000000028644 ) ;
#174507=DIRECTION ( 'NONE',  ( 2.840903330521631775E-16, 0.8700118002898354908, -0.4930308989875170078 ) ) ;
#174515=DIRECTION ( 'NONE',  ( 1.000000000000000000, 0.000000000000000000, 0.000000000000000000 ) ) ;
#174519=AXIS2_PLACEMENT_3D ( 'NONE', #243409, #239574, #64771 ) ;
#174528=LINE ( 'NONE', #156215, #193619 ) ;
#174553=CARTESIAN_POINT ( 'NONE',  ( 21.04999999999879279, 69.50331341424386267, -103.0084513660114993 ) ) ;
#174556=DIRECTION ( 'NONE',  ( 2.715809747126117987E-16, 1.000000000000000000, 5.431619494252235382E-15 ) ) ;
#174572=AXIS2_PLACEMENT_3D ( 'NONE', #173231, #114489, #190193 ) ;
#174592=CARTESIAN_POINT ( 'NONE',  ( -20.64999999999999858, 68.85000000001186038, -90.67310748452435121 ) ) ;
#174625=CARTESIAN_POINT ( 'NONE',  ( 18.59999999999999432, 77.83585931145526615, -58.01866831572577610 ) ) ;
#174646=AXIS2_PLACEMENT_3D ( 'NONE', #196572, #77903, #160047 ) ;
#174658=ORIENTED_EDGE ( 'NONE', *, *, #174791, .F. ) ;
#174687=DIRECTION ( 'NONE',  ( 1.000000000000000000, -2.952720810173289112E-16, -2.061873921506763405E-30 ) ) ;
#174716=CARTESIAN_POINT ( 'NONE',  ( 21.13507111622890022, 65.28231661301347799, -90.77393889816359263 ) ) ;
#174768=DIRECTION ( 'NONE',  ( 0.000000000000000000, -1.000000000000000000, -6.982962677686265922E-15 ) ) ;
#174771=ORIENTED_EDGE ( 'NONE', *, *, #57925, .F. ) ;
#174791=EDGE_CURVE ( 'NONE', #84480, #23304, #95808, .T. ) ;
#174799=CIRCLE ( 'NONE', #241399, 0.09999999999999939493 ) ;
#174800=ADVANCED_FACE ( 'NONE', ( #196212 ), #18857, .F. ) ;
#174804=VERTEX_POINT ( 'NONE', #254844 ) ;
#174825=EDGE_CURVE ( 'NONE', #85729, #229669, #245070, .T. ) ;
#174839=AXIS2_PLACEMENT_3D ( 'NONE', #174419, #175663, #199065 ) ;
#174847=LINE ( 'NONE', #134361, #43299 ) ;
#174877=AXIS2_PLACEMENT_3D ( 'NONE', #227764, #146929, #49127 ) ;
#174880=CIRCLE ( 'NONE', #4124, 0.09999999999999939493 ) ;
#174886=EDGE_CURVE ( 'NONE', #159228, #183385, #124279, .T. ) ;
#174895=ADVANCED_FACE ( 'NONE', ( #63107 ), #174197, .F. ) ;
#174938=EDGE_LOOP ( 'NONE', ( #125423, #40944 ) ) ;
#174954=EDGE_LOOP ( 'NONE', ( #164973, #85835, #93209, #47648, #232947, #29385, #103164 ) ) ;
#174962=ORIENTED_EDGE ( 'NONE', *, *, #198600, .T. ) ;
#174980=ORIENTED_EDGE ( 'NONE', *, *, #220058, .F. ) ;
#174983=CARTESIAN_POINT ( 'NONE',  ( -18.59999999999999787, 77.83585931145526615, -58.01866831572577610 ) ) ;
#174990=DIRECTION ( 'NONE',  ( -1.000000000000000000, -0.000000000000000000, -0.000000000000000000 ) ) ;
#175003=CARTESIAN_POINT ( 'NONE',  ( -23.15000000000000213, 64.25000000001186606, -90.77310748452440237 ) ) ;
#175025=CIRCLE ( 'NONE', #45969, 0.1000000000000028644 ) ;
#175027=AXIS2_PLACEMENT_3D ( 'NONE', #9204, #169617, #50872 ) ;
#175046=DIRECTION ( 'NONE',  ( -0.000000000000000000, 6.982962677686266711E-15, -1.000000000000000000 ) ) ;
#175064=DIRECTION ( 'NONE',  ( 1.000000000000000000, 0.000000000000000000, 0.000000000000000000 ) ) ;
#175068=ORIENTED_EDGE ( 'NONE', *, *, #69932, .T. ) ;
#175080=EDGE_CURVE ( 'NONE', #4874, #132890, #216009, .T. ) ;
#175096=ORIENTED_EDGE ( 'NONE', *, *, #204205, .T. ) ;
#175121=CARTESIAN_POINT ( 'NONE',  ( 21.05000012384952868, 65.37127970113623121, -90.84513015448881390 ) ) ;
#175128=CIRCLE ( 'NONE', #54252, 0.1000000000000028644 ) ;
#175131=CARTESIAN_POINT ( 'NONE',  ( -21.05000000000000071, 74.73821383144687047, -94.93660852097883662 ) ) ;
#175154=PLANE ( 'NONE',  #114201 ) ;
#175175=ORIENTED_EDGE ( 'NONE', *, *, #104635, .T. ) ;
#175203=CIRCLE ( 'NONE', #75219, 0.1000000000000028644 ) ;
#175221=ADVANCED_FACE ( 'NONE', ( #241462 ), #182783, .F. ) ;
#175227=EDGE_CURVE ( 'NONE', #213743, #45676, #236867, .T. ) ;
#175236=CIRCLE ( 'NONE', #137754, 12.97499999999999964 ) ;
#175256=EDGE_LOOP ( 'NONE', ( #35108, #192539, #38979, #95214 ) ) ;
#175280=ORIENTED_EDGE ( 'NONE', *, *, #104654, .F. ) ;
#175281=EDGE_LOOP ( 'NONE', ( #51786, #117796, #5248, #217068, #124071 ) ) ;
#175363=EDGE_CURVE ( 'NONE', #221901, #80949, #231867, .T. ) ;
#175367=EDGE_CURVE ( 'NONE', #248733, #79511, #213554, .T. ) ;
#175403=CARTESIAN_POINT ( 'NONE',  ( -23.25000000000000000, 73.40000000001185754, -89.79848556176223440 ) ) ;
#175412=EDGE_CURVE ( 'NONE', #131827, #127173, #21794, .T. ) ;
#175435=CYLINDRICAL_SURFACE ( 'NONE', #100750, 4.000000000000003553 ) ;
#175451=ORIENTED_EDGE ( 'NONE', *, *, #237595, .F. ) ;
#175496=CARTESIAN_POINT ( 'NONE',  ( 23.14999999999998437, 76.00000000001195133, -103.0231074845243171 ) ) ;
#175497=ORIENTED_EDGE ( 'NONE', *, *, #240741, .F. ) ;
#175530=ORIENTED_EDGE ( 'NONE', *, *, #88795, .F. ) ;
#175578=DIRECTION ( 'NONE',  ( 1.000000000000000000, -7.304098846218134667E-16, -5.100424963727255829E-30 ) ) ;
#175583=CARTESIAN_POINT ( 'NONE',  ( 20.12500000000000000, 66.25000000001189449, -94.91133620241009794 ) ) ;
#175587=DIRECTION ( 'NONE',  ( 0.000000000000000000, -1.000000000000000000, -6.982962677686265922E-15 ) ) ;
#175663=DIRECTION ( 'NONE',  ( 1.000000000000000000, 0.000000000000000000, 0.000000000000000000 ) ) ;
#175690=ORIENTED_EDGE ( 'NONE', *, *, #129473, .T. ) ;
#175694=CARTESIAN_POINT ( 'NONE',  ( 21.05000000000000071, 67.17357026049469937, -94.60905277158067861 ) ) ;
#175707=AXIS2_PLACEMENT_3D ( 'NONE', #195096, #97201, #55516 ) ;
#175726=EDGE_CURVE ( 'NONE', #11088, #227300, #137280, .T. ) ;
#175750=ORIENTED_EDGE ( 'NONE', *, *, #186996, .F. ) ;
#175829=CARTESIAN_POINT ( 'NONE',  ( -20.54999999999999716, 76.00000000001179501, -82.39810748452430289 ) ) ;
#175899=VERTEX_POINT ( 'NONE', #123149 ) ;
#175935=DIRECTION ( 'NONE',  ( 1.000000000000000000, 0.000000000000000000, 0.000000000000000000 ) ) ;
#175973=CYLINDRICAL_SURFACE ( 'NONE', #203650, 0.1000000000000028644 ) ;
#176019=DIRECTION ( 'NONE',  ( 1.000000000000000000, 0.000000000000000000, 0.000000000000000000 ) ) ;
#176024=EDGE_CURVE ( 'NONE', #111063, #17499, #220505, .T. ) ;
#176057=AXIS2_PLACEMENT_3D ( 'NONE', #16785, #216229, #15505 ) ;
#176059=AXIS2_PLACEMENT_3D ( 'NONE', #199310, #117198, #237145 ) ;
#176100=DIRECTION ( 'NONE',  ( -1.000000000000000000, 0.000000000000000000, -0.000000000000000000 ) ) ;
#176108=CARTESIAN_POINT ( 'NONE',  ( 21.14999999999999858, 69.45000000001186891, -90.67310748452435121 ) ) ;
#176157=ORIENTED_EDGE ( 'NONE', *, *, #16280, .T. ) ;
#176191=CIRCLE ( 'NONE', #59607, 0.5000000000000004441 ) ;
#176238=EDGE_LOOP ( 'NONE', ( #54550, #62975, #83988, #247580, #191839 ) ) ;
#176288=DIRECTION ( 'NONE',  ( 1.000000000000000000, 0.000000000000000000, 0.000000000000000000 ) ) ;
#176301=EDGE_CURVE ( 'NONE', #16177, #233882, #81600, .T. ) ;
#176319=DIRECTION ( 'NONE',  ( 0.000000000000000000, -0.7397360091702802620, 0.6728971962616779878 ) ) ;
#176321=CARTESIAN_POINT ( 'NONE',  ( 22.49999999999999645, 75.91119002362509605, -114.6728704025562422 ) ) ;
#176377=CARTESIAN_POINT ( 'NONE',  ( 20.85000000000000142, 64.25000000001175238, -76.30697314750248950 ) ) ;
#176378=DIRECTION ( 'NONE',  ( 1.000000000000000000, 0.000000000000000000, 0.000000000000000000 ) ) ;
#176388=ADVANCED_FACE ( 'NONE', ( #145449 ), #62474, .F. ) ;
#176424=CARTESIAN_POINT ( 'NONE',  ( 21.08832698747859169, 67.22463560659464576, -90.79439001806022702 ) ) ;
#176434=CIRCLE ( 'NONE', #80710, 0.09999999999999939493 ) ;
#176461=DIRECTION ( 'NONE',  ( 6.484947573744954877E-15, -0.9274965247785555977, 0.3738317757009190223 ) ) ;
#176483=CARTESIAN_POINT ( 'NONE',  ( 21.53699400380198981, 69.21228820681629657, -103.0231074845243455 ) ) ;
#176503=CARTESIAN_POINT ( 'NONE',  ( -20.94999999999999929, 76.00000000001189449, -95.12310748452431142 ) ) ;
#176513=AXIS2_PLACEMENT_3D ( 'NONE', #150174, #233560, #189291 ) ;
#176546=CARTESIAN_POINT ( 'NONE',  ( -23.25000000000000000, 76.00000000001170974, -69.52310748452431710 ) ) ;
#176550=AXIS2_PLACEMENT_3D ( 'NONE', #130283, #204679, #49476 ) ;
#176551=AXIS2_PLACEMENT_3D ( 'NONE', #43335, #143700, #64177 ) ;
#176558=DIRECTION ( 'NONE',  ( 1.000000000000000000, -0.000000000000000000, 0.000000000000000000 ) ) ;
#176561=CARTESIAN_POINT ( 'NONE',  ( -20.94999999999999929, 74.16465844978745281, -91.46795619196133487 ) ) ;
#176566=AXIS2_PLACEMENT_3D ( 'NONE', #628, #220978, #181872 ) ;
#176575=DIRECTION ( 'NONE',  ( 0.000000000000000000, 0.000000000000000000, -1.000000000000000000 ) ) ;
#176582=CYLINDRICAL_SURFACE ( 'NONE', #240162, 0.09999999999999939493 ) ;
#176588=AXIS2_PLACEMENT_3D ( 'NONE', #77904, #55747, #195328 ) ;
#176620=ORIENTED_EDGE ( 'NONE', *, *, #72883, .F. ) ;
#176629=SPHERICAL_SURFACE ( 'NONE', #73600, 0.1000000000000000056 ) ;
#176634=EDGE_CURVE ( 'NONE', #237868, #154400, #60157, .T. ) ;
#176652=DIRECTION ( 'NONE',  ( -1.000000000000000000, 2.952720810173289112E-16, 2.061873921506763405E-30 ) ) ;
#176663=CARTESIAN_POINT ( 'NONE',  ( 21.05000000000000071, 70.60000000001178933, -79.41707660717679573 ) ) ;
#176668=ORIENTED_EDGE ( 'NONE', *, *, #227153, .T. ) ;
#176671=DIRECTION ( 'NONE',  ( 1.000000000000000000, -0.000000000000000000, 0.000000000000000000 ) ) ;
#176683=FACE_OUTER_BOUND ( 'NONE', #212485, .T. ) ;
#176687=DIRECTION ( 'NONE',  ( 1.000000000000000000, 0.000000000000000000, 0.000000000000000000 ) ) ;
#176719=ORIENTED_EDGE ( 'NONE', *, *, #227022, .T. ) ;
#176740=CARTESIAN_POINT ( 'NONE',  ( -18.59999999999999787, 66.65000000001187175, -90.77310748452437394 ) ) ;
#176766=CARTESIAN_POINT ( 'NONE',  ( -18.47690164073607377, 85.46484453802391101, -62.82172654468813278 ) ) ;
#176791=CIRCLE ( 'NONE', #22861, 0.1000000000000052097 ) ;
#176797=DIRECTION ( 'NONE',  ( 2.694716079187273439E-16, 1.000000000000000000, 6.467318590049456648E-15 ) ) ;
#176828=DIRECTION ( 'NONE',  ( 1.000000000000000000, 0.000000000000000000, 0.000000000000000000 ) ) ;
#176856=CARTESIAN_POINT ( 'NONE',  ( 20.95224633520496127, 67.09947783345465666, -94.52983103660311315 ) ) ;
#176865=ADVANCED_FACE ( 'NONE', ( #114706 ), #96407, .F. ) ;
#176871=CARTESIAN_POINT ( 'NONE',  ( 21.14999999999999858, 64.35000000001186038, -90.87310748452438247 ) ) ;
#176873=DIRECTION ( 'NONE',  ( 0.000000000000000000, -0.6728971962616412394, -0.7397360091703134577 ) ) ;
#176886=CIRCLE ( 'NONE', #64448, 12.87499999999999822 ) ;
#176892=CARTESIAN_POINT ( 'NONE',  ( -18.59999999999999787, 69.06610602788535402, -65.73746165015079157 ) ) ;
#176895=CIRCLE ( 'NONE', #239418, 0.1000000000000028644 ) ;
#176909=DIRECTION ( 'NONE',  ( -1.000000000000000000, 0.000000000000000000, 0.000000000000000000 ) ) ;
#176910=ORIENTED_EDGE ( 'NONE', *, *, #99719, .T. ) ;
#176915=ORIENTED_EDGE ( 'NONE', *, *, #226144, .F. ) ;
#176933=CARTESIAN_POINT ( 'NONE',  ( 21.05000000000000071, 74.16465844978745281, -91.46795619196133487 ) ) ;
#176937=EDGE_CURVE ( 'NONE', #110864, #193738, #234157, .T. ) ;
#176939=FACE_OUTER_BOUND ( 'NONE', #254420, .T. ) ;
#176957=AXIS2_PLACEMENT_3D ( 'NONE', #55203, #115213, #70984 ) ;
#176971=PLANE ( 'NONE',  #15676 ) ;
#176992=DIRECTION ( 'NONE',  ( 1.000000000000000000, 0.000000000000000000, 0.000000000000000000 ) ) ;
#177023=FACE_OUTER_BOUND ( 'NONE', #143133, .T. ) ;
#177115=EDGE_LOOP ( 'NONE', ( #118703, #203491, #162587, #99519 ) ) ;
#177121=DIRECTION ( 'NONE',  ( 1.000000000000000000, -3.265361837132813093E-16, -2.280189983783949500E-30 ) ) ;
#177128=DIRECTION ( 'NONE',  ( 1.000000000000000000, 0.000000000000000000, 0.000000000000000000 ) ) ;
#177151=EDGE_CURVE ( 'NONE', #39117, #32631, #144520, .T. ) ;
#177180=DIRECTION ( 'NONE',  ( 0.000000000000000000, -6.982962677686266711E-15, 1.000000000000000000 ) ) ;
#177194=CARTESIAN_POINT ( 'NONE',  ( 18.49999999999998934, 56.14960075277838314, -100.7428044267230973 ) ) ;
#177209=ORIENTED_EDGE ( 'NONE', *, *, #35244, .T. ) ;
#177215=ORIENTED_EDGE ( 'NONE', *, *, #238624, .F. ) ;
#177219=EDGE_LOOP ( 'NONE', ( #64620, #216516, #218997, #9396, #13243 ) ) ;
#177233=ORIENTED_EDGE ( 'NONE', *, *, #108050, .T. ) ;
#177237=DIRECTION ( 'NONE',  ( 1.000000000000000000, 0.000000000000000000, 0.000000000000000000 ) ) ;
#177239=AXIS2_PLACEMENT_3D ( 'NONE', #207965, #244492, #29347 ) ;
#177241=CARTESIAN_POINT ( 'NONE',  ( 20.94999999999999574, 74.83729825007388570, -94.92310748452432279 ) ) ;
#177249=EDGE_LOOP ( 'NONE', ( #231098, #233979, #205020, #159725 ) ) ;
#177339=FACE_OUTER_BOUND ( 'NONE', #171791, .T. ) ;
#177344=CIRCLE ( 'NONE', #64862, 0.1000000000000028644 ) ;
#177349=CARTESIAN_POINT ( 'NONE',  ( -18.47079683080346513, 85.47166410525677804, -95.91424694353177927 ) ) ;
#177371=ADVANCED_FACE ( 'NONE', ( #17850 ), #176971, .F. ) ;
#177396=DIRECTION ( 'NONE',  ( 1.000000000000000000, 0.000000000000000000, 0.000000000000000000 ) ) ;
#177409=ORIENTED_EDGE ( 'NONE', *, *, #197116, .T. ) ;
#177414=CARTESIAN_POINT ( 'NONE',  ( -23.15000000000000213, 85.00000000001179501, -78.81707660717668773 ) ) ;
#177447=CARTESIAN_POINT ( 'NONE',  ( -23.25000000000000000, 87.75000000001192291, -99.92310748452422331 ) ) ;
#177479=DIRECTION ( 'NONE',  ( 0.000000000000000000, 0.000000000000000000, -1.000000000000000000 ) ) ;
#177493=EDGE_CURVE ( 'NONE', #23304, #200329, #182236, .T. ) ;
#177502=ORIENTED_EDGE ( 'NONE', *, *, #185848, .T. ) ;
#177523=DIRECTION ( 'NONE',  ( 1.000000000000000000, 0.000000000000000000, 0.000000000000000000 ) ) ;
#177538=ORIENTED_EDGE ( 'NONE', *, *, #124477, .F. ) ;
#177542=ORIENTED_EDGE ( 'NONE', *, *, #173421, .F. ) ;
#177557=AXIS2_PLACEMENT_3D ( 'NONE', #34868, #253866, #154814 ) ;
#177580=CIRCLE ( 'NONE', #252348, 0.1999999999999987899 ) ;
#177597=ORIENTED_EDGE ( 'NONE', *, *, #244473, .T. ) ;
#177615=DIRECTION ( 'NONE',  ( 0.000000000000000000, -0.1495327102803078179, 0.9887567792719429427 ) ) ;
#177648=ORIENTED_EDGE ( 'NONE', *, *, #62336, .F. ) ;
#177671=CARTESIAN_POINT ( 'NONE',  ( 21.13461538461538325, 65.38541703798631488, -90.77310748452440237 ) ) ;
#177694=AXIS2_PLACEMENT_3D ( 'NONE', #26512, #85145, #65614 ) ;
#177698=ORIENTED_EDGE ( 'NONE', *, *, #53569, .F. ) ;
#177731=ORIENTED_EDGE ( 'NONE', *, *, #102143, .F. ) ;
#177739=VECTOR ( 'NONE', #106184, 1000.000000000000000 ) ;
#177756=DIRECTION ( 'NONE',  ( 0.000000000000000000, 7.086529944415894657E-15, -1.000000000000000000 ) ) ;
#177765=ORIENTED_EDGE ( 'NONE', *, *, #254957, .T. ) ;
#177771=CARTESIAN_POINT ( 'NONE',  ( -18.46919391072063021, 85.67072438828941472, -62.84930395272471060 ) ) ;
#177783=EDGE_CURVE ( 'NONE', #239427, #82199, #40801, .T. ) ;
#177786=ORIENTED_EDGE ( 'NONE', *, *, #191581, .T. ) ;
#177819=CIRCLE ( 'NONE', #165322, 0.09999999999999939493 ) ;
#177836=DIRECTION ( 'NONE',  ( 0.000000000000000000, 0.000000000000000000, 1.000000000000000000 ) ) ;
#177875=CIRCLE ( 'NONE', #77892, 0.1000000000000055705 ) ;
#177889=FACE_OUTER_BOUND ( 'NONE', #142862, .T. ) ;
#177940=CARTESIAN_POINT ( 'NONE',  ( -18.50000000000000355, 77.26327546522891510, -61.62124281777789037 ) ) ;
#177943=CARTESIAN_POINT ( 'NONE',  ( -21.65000000000000213, 68.25000000001185185, -90.67310748452436542 ) ) ;
#177968=DIRECTION ( 'NONE',  ( 1.000000000000000000, 0.000000000000000000, 0.000000000000000000 ) ) ;
#177997=LINE ( 'NONE', #41066, #127885 ) ;
#177999=TOROIDAL_SURFACE ( 'NONE', #65550, 0.9750000000000019762, 0.1000000000000000056 ) ;
#178001=VERTEX_POINT ( 'NONE', #94207 ) ;
#178035=AXIS2_PLACEMENT_3D ( 'NONE', #46615, #8800, #199644 ) ;
#178054=EDGE_CURVE ( 'NONE', #3957, #50671, #69439, .T. ) ;
#178063=EDGE_CURVE ( 'NONE', #142820, #215945, #211609, .T. ) ;
#178078=AXIS2_PLACEMENT_3D ( 'NONE', #192095, #255850, #112550 ) ;
#178143=CARTESIAN_POINT ( 'NONE',  ( 20.95483826173900255, 67.12383379524190730, -94.47683193162485793 ) ) ;
#178229=AXIS2_PLACEMENT_3D ( 'NONE', #178266, #62146, #142933 ) ;
#178248=CARTESIAN_POINT ( 'NONE',  ( 21.76363531954645936, 68.98706345214023372, -103.1221093588238062 ) ) ;
#178266=CARTESIAN_POINT ( 'NONE',  ( 21.05000000000000071, 69.55000000001187743, -93.00608031408432907 ) ) ;
#178288=DIRECTION ( 'NONE',  ( 0.000000000000000000, -1.000000000000000000, -6.982962677686265922E-15 ) ) ;
#178311=EDGE_CURVE ( 'NONE', #25605, #249684, #253931, .T. ) ;
#178326=CARTESIAN_POINT ( 'NONE',  ( 18.50000324121758055, 65.70692517833191459, -64.06446533783041275 ) ) ;
#178383=TOROIDAL_SURFACE ( 'NONE', #65923, 6.258578643762712446, 0.1000000000000000056 ) ;
#178399=DIRECTION ( 'NONE',  ( 1.000000000000000000, 0.000000000000000000, 0.000000000000000000 ) ) ;
#178407=FACE_OUTER_BOUND ( 'NONE', #89684, .T. ) ;
#178413=CIRCLE ( 'NONE', #61871, 0.1000000000000028644 ) ;
#178419=ORIENTED_EDGE ( 'NONE', *, *, #248022, .T. ) ;
#178424=TOROIDAL_SURFACE ( 'NONE', #132606, 11.90000000000000391, 0.1000000000000000056 ) ;
#178511=CARTESIAN_POINT ( 'NONE',  ( 21.14999999999999503, 87.75000000001202238, -114.7731074845242318 ) ) ;
#178517=DIRECTION ( 'NONE',  ( 0.000000000000000000, -1.000000000000000000, -7.272083257015735086E-15 ) ) ;
#178528=AXIS2_PLACEMENT_3D ( 'NONE', #170656, #247569, #89766 ) ;
#178537=SHAPE_REPRESENTATION ( 'Injection Molded Chain Links 14', ( #2425 ), #185415 ) ;
#178548=ORIENTED_EDGE ( 'NONE', *, *, #189856, .F. ) ;
#178561=VERTEX_POINT ( 'NONE', #62173 ) ;
#178566=VERTEX_POINT ( 'NONE', #123426 ) ;
#178567=ORIENTED_EDGE ( 'NONE', *, *, #151533, .T. ) ;
#178599=CARTESIAN_POINT ( 'NONE',  ( -20.94999999999999929, 74.16465844978745281, -91.46795619196133487 ) ) ;
#178617=CYLINDRICAL_SURFACE ( 'NONE', #30126, 2.000000000000001776 ) ;
#178620=ADVANCED_FACE ( 'NONE', ( #127276 ), #204234, .T. ) ;
#178633=EDGE_CURVE ( 'NONE', #170631, #44131, #23839, .T. ) ;
#178641=ADVANCED_FACE ( 'NONE', ( #243361 ), #89419, .F. ) ;
#178656=B_SPLINE_CURVE_WITH_KNOTS ( 'NONE', 3,
 ( #200375, #165096, #128536, #226323, #127254, #106380, #247186, #67275, #206790, #26899 ),
 .UNSPECIFIED., .F., .F.,
 ( 4, 2, 2, 2, 4 ),
 ( 0.000000000000000000, 0.0001660831991682119001, 0.0002491247987523189885, 0.0002906455985443902866, 0.0003321663983364616930 ),
 .UNSPECIFIED. ) ;
#178663=AXIS2_PLACEMENT_3D ( 'NONE', #112214, #169645, #168362 ) ;
#178678=B_SPLINE_CURVE_WITH_KNOTS ( 'NONE', 3,
 ( #221463, #101497, #181100, #161538, #78116, #218907, #237214, #16892 ),
 .UNSPECIFIED., .F., .F.,
 ( 4, 2, 2, 4 ),
 ( 0.000000000000000000, 0.0001094981963948503753, 0.0002189963927897007505, 0.0004379927855793972185 ),
 .UNSPECIFIED. ) ;
#178731=AXIS2_PLACEMENT_3D ( 'NONE', #63799, #22125, #41684 ) ;
#178742=EDGE_CURVE ( 'NONE', #129819, #2197, #119682, .T. ) ;
#178748=MECHANICAL_DESIGN_GEOMETRIC_PRESENTATION_REPRESENTATION('',(#253690),#207942);
#178769=VERTEX_POINT ( 'NONE', #210661 ) ;
#178780=EDGE_CURVE ( 'NONE', #18436, #168199, #37180, .T. ) ;
#178832=DIRECTION ( 'NONE',  ( 0.000000000000000000, 6.982962677686266711E-15, -1.000000000000000000 ) ) ;
#178873=SPHERICAL_SURFACE ( 'NONE', #56958, 0.1000000000000000056 ) ;
#178874=DIRECTION ( 'NONE',  ( -1.000000000000000000, 0.000000000000000000, 0.000000000000000000 ) ) ;
#178879=( LENGTH_UNIT ( ) NAMED_UNIT ( * ) SI_UNIT ( .MILLI., .METRE. ) );
#178881=DIRECTION ( 'NONE',  ( -0.000000000000000000, -6.982962677686266711E-15, 1.000000000000000000 ) ) ;
#178905=CYLINDRICAL_SURFACE ( 'NONE', #205906, 0.09999999999999939493 ) ;
#178913=EDGE_CURVE ( 'NONE', #233299, #48831, #149095, .T. ) ;
#178948=ORIENTED_EDGE ( 'NONE', *, *, #56616, .T. ) ;
#178950=ORIENTED_EDGE ( 'NONE', *, *, #207793, .F. ) ;
#178963=FACE_OUTER_BOUND ( 'NONE', #108020, .T. ) ;
#178978=LINE ( 'NONE', #81100, #158071 ) ;
#178991=ORIENTED_EDGE ( 'NONE', *, *, #18236, .T. ) ;
#178996=DIRECTION ( 'NONE',  ( 0.000000000000000000, -6.982962677686266711E-15, 1.000000000000000000 ) ) ;
#179032=CARTESIAN_POINT ( 'NONE',  ( -20.94999999999999929, 74.83729825007388570, -94.92310748452432279 ) ) ;
#179046=ORIENTED_EDGE ( 'NONE', *, *, #87635, .T. ) ;
#179047=DIRECTION ( 'NONE',  ( 0.000000000000000000, -8.905812670947865054E-15, 1.000000000000000000 ) ) ;
#179048=DIRECTION ( 'NONE',  ( 1.000000000000000000, 0.000000000000000000, 0.000000000000000000 ) ) ;
#179049=CARTESIAN_POINT ( 'NONE',  ( -18.59999999999999787, 76.00000000001170974, -69.52310748452431710 ) ) ;
#179060=EDGE_CURVE ( 'NONE', #21468, #224619, #66995, .T. ) ;
#179066=DIRECTION ( 'NONE',  ( 1.000000000000000000, 0.000000000000000000, 0.000000000000000000 ) ) ;
#179072=ORIENTED_EDGE ( 'NONE', *, *, #86583, .T. ) ;
#179144=AXIS2_PLACEMENT_3D ( 'NONE', #167422, #170015, #46159 ) ;
#179155=CARTESIAN_POINT ( 'NONE',  ( -18.59999999999999787, 66.65000000001180069, -81.87310748452438247 ) ) ;
#179160=ORIENTED_EDGE ( 'NONE', *, *, #56156, .T. ) ;
#179192=CARTESIAN_POINT ( 'NONE',  ( 20.04142135623730070, 64.35000000001180354, -81.67310748452439384 ) ) ;
#179216=LINE ( 'NONE', #535, #65085 ) ;
#179225=EDGE_LOOP ( 'NONE', ( #86156, #71697, #187085, #122725 ) ) ;
#179229=CARTESIAN_POINT ( 'NONE',  ( 20.85000000000000142, 76.00000000001170974, -69.52310748452431710 ) ) ;
#179267=CIRCLE ( 'NONE', #66812, 0.1000000000000052097 ) ;
#179276=DIRECTION ( 'NONE',  ( -1.000000000000000000, 0.000000000000000000, 0.000000000000000000 ) ) ;
#179296=DIRECTION ( 'NONE',  ( -1.000000000000000000, -0.000000000000000000, -0.000000000000000000 ) ) ;
#179311=AXIS2_PLACEMENT_3D ( 'NONE', #143135, #240979, #160184 ) ;
#179364=ORIENTED_EDGE ( 'NONE', *, *, #239345, .T. ) ;
#179392=DIRECTION ( 'NONE',  ( 0.7070776581708965169, 4.937903618720407826E-15, -0.7071359030027827286 ) ) ;
#179403=DIRECTION ( 'NONE',  ( 0.000000000000000000, 0.1350103645451807555, 0.9908441862701609093 ) ) ;
#179406=ORIENTED_EDGE ( 'NONE', *, *, #167872, .T. ) ;
#179415=DIRECTION ( 'NONE',  ( 0.000000000000000000, 1.000000000000000000, 0.000000000000000000 ) ) ;
#179431=CIRCLE ( 'NONE', #166986, 0.1000000000000026007 ) ;
#179436=DIRECTION ( 'NONE',  ( 1.000000000000000000, -0.000000000000000000, 0.000000000000000000 ) ) ;
#179440=CARTESIAN_POINT ( 'NONE',  ( 23.15000000000000213, 85.60000000001177511, -79.41707660717668205 ) ) ;
#179462=ORIENTED_EDGE ( 'NONE', *, *, #165434, .T. ) ;
#179472=EDGE_CURVE ( 'NONE', #34831, #192857, #128595, .T. ) ;
#179506=VERTEX_POINT ( 'NONE', #224470 ) ;
#179515=DIRECTION ( 'NONE',  ( -0.000000000000000000, 7.272083257015735086E-15, -1.000000000000000000 ) ) ;
#179518=DIRECTION ( 'NONE',  ( 1.000000000000000000, 0.000000000000000000, 0.000000000000000000 ) ) ;
#179535=VECTOR ( 'NONE', #162072, 1000.000000000000000 ) ;
#179559=EDGE_CURVE ( 'NONE', #192753, #82161, #130506, .T. ) ;
#179584=ORIENTED_EDGE ( 'NONE', *, *, #71412, .F. ) ;
#179586=ADVANCED_FACE ( 'NONE', ( #229624 ), #135408, .T. ) ;
#179588=CARTESIAN_POINT ( 'NONE',  ( -18.39999999999999858, 85.50000000001189449, -96.02382180668539036 ) ) ;
#179601=CARTESIAN_POINT ( 'NONE',  ( 18.49999999999998934, 65.70711192142341872, -64.06510546851222898 ) ) ;
#179622=DIRECTION ( 'NONE',  ( 0.000000000000000000, 0.9908441862701605762, 0.1350103645451835310 ) ) ;
#179634=FACE_OUTER_BOUND ( 'NONE', #39005, .T. ) ;
#179640=DIRECTION ( 'NONE',  ( 1.000000000000000000, 0.000000000000000000, 0.000000000000000000 ) ) ;
#179653=ORIENTED_EDGE ( 'NONE', *, *, #250360, .F. ) ;
#179679=CYLINDRICAL_SURFACE ( 'NONE', #88363, 12.87499999999999822 ) ;
#179715=DIRECTION ( 'NONE',  ( 1.000000000000000000, 0.000000000000000000, 0.000000000000000000 ) ) ;
#179718=ADVANCED_FACE ( 'NONE', ( #145760 ), #187493, .F. ) ;
#179735=VECTOR ( 'NONE', #250127, 1000.000000000000000 ) ;
#179739=CARTESIAN_POINT ( 'NONE',  ( 21.05000000000000071, 65.57661458509899433, -95.53105556065429482 ) ) ;
#179746=EDGE_CURVE ( 'NONE', #253445, #187280, #224267, .T. ) ;
#179781=DIRECTION ( 'NONE',  ( 0.000000000000000000, -6.938893903907222067E-15, 1.000000000000000000 ) ) ;
#179796=DIRECTION ( 'NONE',  ( -1.000000000000000000, 0.000000000000000000, 0.000000000000000000 ) ) ;
#179838=CARTESIAN_POINT ( 'NONE',  ( 20.94999999999999574, 87.41227409416161720, -100.0231074845242318 ) ) ;
#179868=ORIENTED_EDGE ( 'NONE', *, *, #100280, .F. ) ;
#179872=ORIENTED_EDGE ( 'NONE', *, *, #26493, .F. ) ;
#179878=EDGE_CURVE ( 'NONE', #239900, #242842, #253656, .T. ) ;
#179884=EDGE_LOOP ( 'NONE', ( #147087, #154786, #182956, #76912, #25920 ) ) ;
#179961=DIRECTION ( 'NONE',  ( -3.265361837132813093E-16, -1.000000000000000000, -6.982962677686266711E-15 ) ) ;
#179966=CARTESIAN_POINT ( 'NONE',  ( -20.85000000000000142, 76.00000000001170974, -69.52310748452431710 ) ) ;
#179969=FACE_OUTER_BOUND ( 'NONE', #125119, .T. ) ;
#179977=EDGE_LOOP ( 'NONE', ( #200775, #45423, #113329 ) ) ;
#180007=CIRCLE ( 'NONE', #96574, 0.1000000000000067224 ) ;
#180011=ORIENTED_EDGE ( 'NONE', *, *, #16963, .T. ) ;
#180013=ADVANCED_FACE ( 'NONE', ( #132300 ), #87055, .F. ) ;
#180026=EDGE_CURVE ( 'NONE', #221652, #147354, #120443, .T. ) ;
#180029=CARTESIAN_POINT ( 'NONE',  ( 22.40000000000010516, 76.00000000001297451, -114.6726782920694205 ) ) ;
#180050=CARTESIAN_POINT ( 'NONE',  ( 18.59999999999999076, 77.83585931145526615, -58.01866831572577610 ) ) ;
#180091=AXIS2_PLACEMENT_3D ( 'NONE', #122252, #124823, #201772 ) ;
#180145=AXIS2_PLACEMENT_3D ( 'NONE', #160440, #18327, #239957 ) ;
#180166=DIRECTION ( 'NONE',  ( 0.000000000000000000, 0.000000000000000000, 1.000000000000000000 ) ) ;
#180179=DIRECTION ( 'NONE',  ( 0.000000000000000000, 0.000000000000000000, -1.000000000000000000 ) ) ;
#180266=CIRCLE ( 'NONE', #167611, 0.1000000000000028644 ) ;
#180294=CIRCLE ( 'NONE', #246920, 0.2000000000000057288 ) ;
#180298=CIRCLE ( 'NONE', #26365, 11.74999999999999645 ) ;
#180337=DIRECTION ( 'NONE',  ( 0.000000000000000000, -7.272083257015735086E-15, 1.000000000000000000 ) ) ;
#180358=EDGE_LOOP ( 'NONE', ( #90951, #201723, #167083, #2947 ) ) ;
#180375=DIRECTION ( 'NONE',  ( 1.000000000000000000, -3.265361837132813093E-16, -2.280189983783949500E-30 ) ) ;
#180379=EDGE_CURVE ( 'NONE', #218126, #214994, #12087, .T. ) ;
#180401=DIRECTION ( 'NONE',  ( -1.000000000000000000, 0.000000000000000000, -0.000000000000000000 ) ) ;
#180436=ORIENTED_EDGE ( 'NONE', *, *, #27090, .T. ) ;
#180451=CARTESIAN_POINT ( 'NONE',  ( 20.94999999999999929, 61.95000000001175522, -75.03680255528533394 ) ) ;
#180459=EDGE_CURVE ( 'NONE', #49802, #14341, #137148, .T. ) ;
#180477=FACE_OUTER_BOUND ( 'NONE', #14850, .T. ) ;
#180481=DIRECTION ( 'NONE',  ( -1.000000000000000000, 7.304098846218163263E-16, -4.217023435051627211E-16 ) ) ;
#180498=CARTESIAN_POINT ( 'NONE',  ( -21.07928932188134041, 75.90110485435759813, -109.3516241409176075 ) ) ;
#180504=DIRECTION ( 'NONE',  ( 0.000000000000000000, 0.000000000000000000, -1.000000000000000000 ) ) ;
#180509=ADVANCED_FACE ( 'NONE', ( #83559 ), #86125, .F. ) ;
#180510=FACE_OUTER_BOUND ( 'NONE', #126784, .T. ) ;
#180529=DIRECTION ( 'NONE',  ( 0.000000000000000000, -0.4999999999999689138, 0.8660254037844565822 ) ) ;
#180545=ORIENTED_EDGE ( 'NONE', *, *, #243441, .F. ) ;
#180586=CARTESIAN_POINT ( 'NONE',  ( -21.52071067811865746, 68.22071067813045886, -81.87310748452436826 ) ) ;
#180627=AXIS2_PLACEMENT_3D ( 'NONE', #14811, #252098, #26977 ) ;
#180629=AXIS2_PLACEMENT_3D ( 'NONE', #243711, #105445, #164188 ) ;
#180633=EDGE_CURVE ( 'NONE', #233882, #129578, #66613, .T. ) ;
#180638=FACE_OUTER_BOUND ( 'NONE', #253198, .T. ) ;
#180674=CARTESIAN_POINT ( 'NONE',  ( 20.94999999999999574, 74.16465844978745281, -91.36795619196134055 ) ) ;
#180685=ORIENTED_EDGE ( 'NONE', *, *, #64005, .F. ) ;
#180712=DIRECTION ( 'NONE',  ( -1.000000000000000000, -0.000000000000000000, -0.000000000000000000 ) ) ;
#180772=VERTEX_POINT ( 'NONE', #195559 ) ;
#180796=CARTESIAN_POINT ( 'NONE',  ( 21.14999999999999858, 69.35000000001186038, -90.87310748452435405 ) ) ;
#180807=VECTOR ( 'NONE', #43016, 1000.000000000000000 ) ;
#180830=DIRECTION ( 'NONE',  ( 0.000000000000000000, -7.086529944415894657E-15, 1.000000000000000000 ) ) ;
#180834=CARTESIAN_POINT ( 'NONE',  ( -21.05000000000000071, 76.00000000001195133, -103.0231074845243171 ) ) ;
#180839=ORIENTED_EDGE ( 'NONE', *, *, #6371, .T. ) ;
#180855=DIRECTION ( 'NONE',  ( 0.000000000000000000, 0.000000000000000000, -1.000000000000000000 ) ) ;
#180884=DIRECTION ( 'NONE',  ( 1.000000000000000000, 0.000000000000000000, 0.000000000000000000 ) ) ;
#180892=ORIENTED_EDGE ( 'NONE', *, *, #58639, .F. ) ;
#180903=CARTESIAN_POINT ( 'NONE',  ( 21.05000000000000071, 69.35000000001187459, -93.00608031408432907 ) ) ;
#180918=ORIENTED_EDGE ( 'NONE', *, *, #96816, .F. ) ;
#180937=ORIENTED_EDGE ( 'NONE', *, *, #243049, .T. ) ;
#180943=DIRECTION ( 'NONE',  ( 0.000000000000000000, -6.982962677686266711E-15, 1.000000000000000000 ) ) ;
#180953=DIRECTION ( 'NONE',  ( -1.000000000000000000, 0.000000000000000000, 0.000000000000000000 ) ) ;
#180955=CARTESIAN_POINT ( 'NONE',  ( -20.54999999999999716, 76.00000000001195133, -103.0231074845243171 ) ) ;
#180973=ORIENTED_EDGE ( 'NONE', *, *, #141925, .F. ) ;
#180991=EDGE_LOOP ( 'NONE', ( #44762, #214603, #82140 ) ) ;
#180999=FACE_OUTER_BOUND ( 'NONE', #10349, .T. ) ;
#181027=AXIS2_PLACEMENT_3D ( 'NONE', #121342, #157910, #142141 ) ;
#181068=DIRECTION ( 'NONE',  ( 0.000000000000000000, 6.982962677686267499E-15, -1.000000000000000000 ) ) ;
#181100=CARTESIAN_POINT ( 'NONE',  ( -18.47140463609788341, 85.67147468523253906, -62.85034702625018355 ) ) ;
#181119=ORIENTED_EDGE ( 'NONE', *, *, #76319, .T. ) ;
#181138=CARTESIAN_POINT ( 'NONE',  ( -21.05000000000000071, 76.00000000001173817, -73.62310748452429721 ) ) ;
#181144=AXIS2_PLACEMENT_3D ( 'NONE', #148276, #89571, #187415 ) ;
#181153=DIRECTION ( 'NONE',  ( -0.000000000000000000, -0.8700118002898356018, 0.4930308989875170078 ) ) ;
#181162=CIRCLE ( 'NONE', #101997, 0.1000000000000028644 ) ;
#181171=DIRECTION ( 'NONE',  ( 0.000000000000000000, -0.8660254037844377084, -0.5000000000000016653 ) ) ;
#181178=CIRCLE ( 'NONE', #76914, 0.1000000000000028644 ) ;
#181181=CIRCLE ( 'NONE', #218539, 7.791421356237338003 ) ;
#181182=FACE_OUTER_BOUND ( 'NONE', #240727, .T. ) ;
#181212=EDGE_CURVE ( 'NONE', #138100, #167256, #100878, .T. ) ;
#181217=DIRECTION ( 'NONE',  ( 1.000000000000000000, 0.000000000000000000, 0.000000000000000000 ) ) ;
#181253=CARTESIAN_POINT ( 'NONE',  ( -18.50000000000000000, 66.65000000001180069, -81.87310748452438247 ) ) ;
#181260=AXIS2_PLACEMENT_3D ( 'NONE', #76945, #114799, #136924 ) ;
#181298=AXIS2_PLACEMENT_3D ( 'NONE', #102902, #182486, #162927 ) ;
#181318=CARTESIAN_POINT ( 'NONE',  ( 22.45380639572251624, 75.99999985734478969, -114.7735403756311996 ) ) ;
#181324=AXIS2_PLACEMENT_3D ( 'NONE', #238742, #199641, #33203 ) ;
#181345=ADVANCED_FACE ( 'NONE', ( #167350 ), #98821, .T. ) ;
#181358=EDGE_LOOP ( 'NONE', ( #227940, #100401, #41834, #14791 ) ) ;
#181360=EDGE_CURVE ( 'NONE', #178769, #164289, #117040, .T. ) ;
#181362=CIRCLE ( 'NONE', #231416, 0.1000000000000028644 ) ;
#181395=CARTESIAN_POINT ( 'NONE',  ( -18.44362607810621313, 85.49049615809671820, -95.96515361767714580 ) ) ;
#181399=EDGE_CURVE ( 'NONE', #10704, #74828, #200241, .T. ) ;
#181402=CARTESIAN_POINT ( 'NONE',  ( 21.05000000000000071, 76.10000000001198828, -109.5001538663141787 ) ) ;
#181437=CIRCLE ( 'NONE', #73121, 0.09999999999999739653 ) ;
#181447=FACE_OUTER_BOUND ( 'NONE', #94996, .T. ) ;
#181464=AXIS2_PLACEMENT_3D ( 'NONE', #229834, #51164, #151612 ) ;
#181469=CARTESIAN_POINT ( 'NONE',  ( -21.07016717457011978, 76.00000000001202238, -109.3440483226251985 ) ) ;
#181471=ADVANCED_FACE ( 'NONE', ( #198436 ), #108660, .F. ) ;
#181495=ADVANCED_FACE ( 'NONE', ( #194622 ), #77198, .F. ) ;
#181521=ORIENTED_EDGE ( 'NONE', *, *, #82959, .T. ) ;
#181533=AXIS2_PLACEMENT_3D ( 'NONE', #195127, #131270, #16484 ) ;
#181536=DIRECTION ( 'NONE',  ( 0.000000000000000000, 6.982962677686266711E-15, -1.000000000000000000 ) ) ;
#181539=AXIS2_PLACEMENT_3D ( 'NONE', #104531, #167144, #86258 ) ;
#181552=ORIENTED_EDGE ( 'NONE', *, *, #152722, .F. ) ;
#181562=CARTESIAN_POINT ( 'NONE',  ( 23.14999999999999858, 76.00000000001186606, -90.14810748452431710 ) ) ;
#181580=ADVANCED_FACE ( 'NONE', ( #224413 ), #84870, .F. ) ;
#181599=EDGE_LOOP ( 'NONE', ( #81277, #236837, #58124 ) ) ;
#181602=DIRECTION ( 'NONE',  ( 1.000000000000000000, 0.000000000000000000, 0.000000000000000000 ) ) ;
#181636=LINE ( 'NONE', #79911, #256716 ) ;
#181647=EDGE_CURVE ( 'NONE', #10791, #40828, #25470, .T. ) ;
#181659=ADVANCED_FACE ( 'NONE', ( #49636 ), #212732, .F. ) ;
#181681=ORIENTED_EDGE ( 'NONE', *, *, #128039, .T. ) ;
#181690=CARTESIAN_POINT ( 'NONE',  ( 21.14999999999999858, 64.35000000001195986, -102.9231074845243938 ) ) ;
#181713=VECTOR ( 'NONE', #60733, 1000.000000000000000 ) ;
#181715=DIRECTION ( 'NONE',  ( 0.000000000000000000, -1.000000000000000000, -7.272083257015735086E-15 ) ) ;
#181728=CARTESIAN_POINT ( 'NONE',  ( -23.25000000000000000, 71.75000000001180922, -81.87310748452433984 ) ) ;
#181730=DIRECTION ( 'NONE',  ( 1.000000000000000000, 7.304098846218163263E-16, -4.217023435051627211E-16 ) ) ;
#181749=TOROIDAL_SURFACE ( 'NONE', #202411, 0.2000000000000000111, 0.1000000000000000056 ) ;
#181772=DIRECTION ( 'NONE',  ( -1.000000000000000000, 1.836970198721029934E-16, 1.282749433769087757E-30 ) ) ;
#181786=CARTESIAN_POINT ( 'NONE',  ( 18.59999999999999787, 77.36242903720497566, -61.63422623660309796 ) ) ;
#181789=CARTESIAN_POINT ( 'NONE',  ( 21.09787244211741708, 67.22462929267454967, -90.78385410020683821 ) ) ;
#181805=VERTEX_POINT ( 'NONE', #95188 ) ;
#181813=AXIS2_PLACEMENT_3D ( 'NONE', #124683, #187239, #110237 ) ;
#181817=ORIENTED_EDGE ( 'NONE', *, *, #123236, .T. ) ;
#181863=AXIS2_PLACEMENT_3D ( 'NONE', #151881, #13627, #231400 ) ;
#181872=DIRECTION ( 'NONE',  ( 0.000000000000000000, -0.4999999999999689138, 0.8660254037844565822 ) ) ;
#181912=ORIENTED_EDGE ( 'NONE', *, *, #158484, .T. ) ;
#181929=AXIS2_PLACEMENT_3D ( 'NONE', #218479, #99806, #256274 ) ;
#181937=EDGE_LOOP ( 'NONE', ( #202264, #3640, #239688, #125904 ) ) ;
#181945=VECTOR ( 'NONE', #23957, 1000.000000000000000 ) ;
#181953=FACE_OUTER_BOUND ( 'NONE', #86063, .T. ) ;
#181980=EDGE_CURVE ( 'NONE', #80064, #174146, #117226, .T. ) ;
#181991=ORIENTED_EDGE ( 'NONE', *, *, #43593, .T. ) ;
#182005=CIRCLE ( 'NONE', #190405, 0.09999999999999939493 ) ;
#182011=ORIENTED_EDGE ( 'NONE', *, *, #52338, .T. ) ;
#182020=CARTESIAN_POINT ( 'NONE',  ( -21.07971444708686093, 75.91217656369416034, -109.3528995661508674 ) ) ;
#182025=DIRECTION ( 'NONE',  ( -1.000000000000000000, 0.000000000000000000, -0.000000000000000000 ) ) ;
#182026=ORIENTED_EDGE ( 'NONE', *, *, #128742, .T. ) ;
#182067=VECTOR ( 'NONE', #228569, 1000.000000000000000 ) ;
#182080=CARTESIAN_POINT ( 'NONE',  ( 21.08134388332232234, 69.66531941949399709, -103.0989264020313669 ) ) ;
#182106=DIRECTION ( 'NONE',  ( 1.000000000000000000, -0.000000000000000000, 0.000000000000000000 ) ) ;
#182124=CARTESIAN_POINT ( 'NONE',  ( -18.59999999999999787, 77.16412189325286874, -61.70825939895269840 ) ) ;
#182128=FACE_OUTER_BOUND ( 'NONE', #240700, .T. ) ;
#182144=AXIS2_PLACEMENT_3D ( 'NONE', #240847, #73785, #232850 ) ;
#182147=AXIS2_PLACEMENT_3D ( 'NONE', #50031, #129579, #209104 ) ;
#182168=CIRCLE ( 'NONE', #69749, 11.65000000000000746 ) ;
#182173=EDGE_LOOP ( 'NONE', ( #191330, #229035, #219495, #67737, #33125 ) ) ;
#182178=CARTESIAN_POINT ( 'NONE',  ( -18.59999999999999787, 77.68707439010360360, -115.8376804510659497 ) ) ;
#182185=VECTOR ( 'NONE', #147577, 1000.000000000000000 ) ;
#182191=CIRCLE ( 'NONE', #223852, 0.1000000000000052097 ) ;
#182210=EDGE_LOOP ( 'NONE', ( #196259, #145589, #41359, #87969 ) ) ;
#182236=CIRCLE ( 'NONE', #257007, 0.1000000000000028644 ) ;
#182272=AXIS2_PLACEMENT_3D ( 'NONE', #101490, #162816, #227567 ) ;
#182275=CIRCLE ( 'NONE', #69861, 0.09999999999999739653 ) ;
#182280=DIRECTION ( 'NONE',  ( 1.000000000000000000, 0.000000000000000000, 0.000000000000000000 ) ) ;
#182364=ORIENTED_EDGE ( 'NONE', *, *, #162538, .T. ) ;
#182368=DIRECTION ( 'NONE',  ( -1.000000000000000000, 2.952720810173289112E-16, 2.061873921506763405E-30 ) ) ;
#182384=VERTEX_POINT ( 'NONE', #243366 ) ;
#182411=ADVANCED_FACE ( 'NONE', ( #182128 ), #240815, .F. ) ;
#182428=CIRCLE ( 'NONE', #16021, 1.899999999999999023 ) ;
#182482=CARTESIAN_POINT ( 'NONE',  ( 20.95052659398289308, 65.52017563223198238, -95.44786872865877569 ) ) ;
#182486=DIRECTION ( 'NONE',  ( 0.000000000000000000, -1.000000000000000000, -6.982962677686265922E-15 ) ) ;
#182518=DIRECTION ( 'NONE',  ( 0.000000000000000000, -0.9915357197604892647, 0.1298341882519715440 ) ) ;
#182557=CARTESIAN_POINT ( 'NONE',  ( -20.64999999999999858, 85.00000000001188027, -93.12913836187181005 ) ) ;
#182559=CARTESIAN_POINT ( 'NONE',  ( -22.39999999999999503, 68.20922040163854660, -103.0231074845243597 ) ) ;
#182571=CARTESIAN_POINT ( 'NONE',  ( -20.94999999999999929, 77.83534155023627932, -91.46795619196130644 ) ) ;
#182583=DIRECTION ( 'NONE',  ( 0.000000000000000000, -6.982962677686266711E-15, 1.000000000000000000 ) ) ;
#182591=CARTESIAN_POINT ( 'NONE',  ( 19.94784844284961167, 64.28691006698288390, -78.32090876722591588 ) ) ;
#182597=FACE_OUTER_BOUND ( 'NONE', #29208, .T. ) ;
#182622=VERTEX_POINT ( 'NONE', #174159 ) ;
#182629=CYLINDRICAL_SURFACE ( 'NONE', #196863, 0.09999999999999939493 ) ;
#182630=AXIS2_PLACEMENT_3D ( 'NONE', #5383, #87501, #126648 ) ;
#182639=ORIENTED_EDGE ( 'NONE', *, *, #154555, .T. ) ;
#182641=EDGE_CURVE ( 'NONE', #72979, #5184, #166947, .T. ) ;
#182643=ORIENTED_EDGE ( 'NONE', *, *, #201297, .T. ) ;
#182645=CARTESIAN_POINT ( 'NONE',  ( -21.55000000000000071, 68.85000000001180354, -81.77310748452435973 ) ) ;
#182756=DIRECTION ( 'NONE',  ( -1.000000000000000000, -0.000000000000000000, -0.000000000000000000 ) ) ;
#182783=SPHERICAL_SURFACE ( 'NONE', #203567, 0.1000000000000000056 ) ;
#182812=DIRECTION ( 'NONE',  ( 0.000000000000000000, 8.770518838402102073E-15, -1.000000000000000000 ) ) ;
#182840=FACE_OUTER_BOUND ( 'NONE', #241711, .T. ) ;
#182856=EDGE_CURVE ( 'NONE', #116798, #82199, #133578, .T. ) ;
#182860=ORIENTED_EDGE ( 'NONE', *, *, #92532, .F. ) ;
#182898=CARTESIAN_POINT ( 'NONE',  ( -18.48408745364670480, 85.66432225867477257, -62.84002895119587606 ) ) ;
#182912=AXIS2_PLACEMENT_3D ( 'NONE', #155509, #182756, #161916 ) ;
#182956=ORIENTED_EDGE ( 'NONE', *, *, #77556, .F. ) ;
#182982=DIRECTION ( 'NONE',  ( 0.000000000000000000, 0.000000000000000000, -1.000000000000000000 ) ) ;
#182988=EDGE_LOOP ( 'NONE', ( #235248, #120143, #191139 ) ) ;
#182995=ORIENTED_EDGE ( 'NONE', *, *, #35846, .F. ) ;
#183014=LINE ( 'NONE', #160887, #99498 ) ;
#183019=ORIENTED_EDGE ( 'NONE', *, *, #178311, .T. ) ;
#183043=AXIS2_PLACEMENT_3D ( 'NONE', #152328, #147157, #10235 ) ;
#183053=CARTESIAN_POINT ( 'NONE',  ( 21.05000000000000071, 75.90220970870321082, -109.2809220950004345 ) ) ;
#183063=EDGE_LOOP ( 'NONE', ( #209545, #60716, #88029, #126672 ) ) ;
#183082=CARTESIAN_POINT ( 'NONE',  ( 21.11345278033283890, 67.11787792664061669, -90.77708531376950418 ) ) ;
#183098=CARTESIAN_POINT ( 'NONE',  ( -18.50000000000000000, 64.25000000001195133, -102.9231074845243938 ) ) ;
#183103=LINE ( 'NONE', #123125, #25773 ) ;
#183154=EDGE_CURVE ( 'NONE', #213696, #94420, #221235, .T. ) ;
#183194=DIRECTION ( 'NONE',  ( 0.000000000000000000, 6.982962677686267499E-15, -1.000000000000000000 ) ) ;
#183201=ORIENTED_EDGE ( 'NONE', *, *, #111284, .T. ) ;
#183243=CARTESIAN_POINT ( 'NONE',  ( -21.05000000000000426, 75.98514436511810288, -109.3674665265678385 ) ) ;
#183247=EDGE_CURVE ( 'NONE', #108747, #4968, #148482, .T. ) ;
#183261=CARTESIAN_POINT ( 'NONE',  ( -18.59999999999999787, 77.83585931145526615, -58.01866831572577610 ) ) ;
#183272=AXIS2_PLACEMENT_3D ( 'NONE', #162555, #182106, #46423 ) ;
#183275=CIRCLE ( 'NONE', #216595, 0.1000000000000028644 ) ;
#183297=CARTESIAN_POINT ( 'NONE',  ( -21.14999999999999858, 87.75000000001193712, -103.0231074845242318 ) ) ;
#183325=TOROIDAL_SURFACE ( 'NONE', #229114, 0.4000000000000012990, 0.1000000000000000056 ) ;
#183364=DIRECTION ( 'NONE',  ( 1.000000000000000000, -0.000000000000000000, -0.000000000000000000 ) ) ;
#183367=CARTESIAN_POINT ( 'NONE',  ( 21.08884785362045378, 69.64280663258671211, -103.0728905795912027 ) ) ;
#183373=ORIENTED_EDGE ( 'NONE', *, *, #229993, .F. ) ;
#183375=DIRECTION ( 'NONE',  ( -0.000000000000000000, 6.982962677686266711E-15, -1.000000000000000000 ) ) ;
#183385=VERTEX_POINT ( 'NONE', #183297 ) ;
#183394=AXIS2_PLACEMENT_3D ( 'NONE', #206648, #227480, #243192 ) ;
#183410=CARTESIAN_POINT ( 'NONE',  ( -21.05000000000000071, 77.83534155023627932, -91.46795619196132066 ) ) ;
#183416=VERTEX_POINT ( 'NONE', #45064 ) ;
#183454=CYLINDRICAL_SURFACE ( 'NONE', #33039, 0.5000000000000004441 ) ;
#183456=ORIENTED_EDGE ( 'NONE', *, *, #106259, .T. ) ;
#183464=CARTESIAN_POINT ( 'NONE',  ( -21.05000000000000071, 69.60000000001187459, -93.09268285446279378 ) ) ;
#183465=EDGE_CURVE ( 'NONE', #145746, #114547, #112386, .T. ) ;
#183466=ORIENTED_EDGE ( 'NONE', *, *, #126646, .T. ) ;
#183504=VERTEX_POINT ( 'NONE', #151529 ) ;
#183524=CARTESIAN_POINT ( 'NONE',  ( -21.29999999999995808, 76.00000000001192291, -98.97310748452431994 ) ) ;
#183547=CIRCLE ( 'NONE', #125292, 0.1000000000000014488 ) ;
#183548=ORIENTED_EDGE ( 'NONE', *, *, #92950, .F. ) ;
#183580=EDGE_LOOP ( 'NONE', ( #80556, #110887, #5634, #245503 ) ) ;
#183590=AXIS2_PLACEMENT_3D ( 'NONE', #212209, #233062, #75277 ) ;
#183606=CIRCLE ( 'NONE', #75309, 0.5000000000000004441 ) ;
#183709=ADVANCED_FACE ( 'NONE', ( #19707 ), #56229, .F. ) ;
#183762=CARTESIAN_POINT ( 'NONE',  ( -21.05000000000000426, 69.66772772607630770, -102.9855714212386744 ) ) ;
#183804=LINE ( 'NONE', #101663, #218925 ) ;
#183819=CARTESIAN_POINT ( 'NONE',  ( -21.46681500593007996, 69.14248884062476463, -103.0231074845243597 ) ) ;
#183826=EDGE_CURVE ( 'NONE', #17324, #136972, #30112, .T. ) ;
#183853=ORIENTED_EDGE ( 'NONE', *, *, #216567, .F. ) ;
#183862=EDGE_CURVE ( 'NONE', #66328, #83116, #225684, .T. ) ;
#183875=CIRCLE ( 'NONE', #196332, 0.5000000000000004441 ) ;
#183905=ORIENTED_EDGE ( 'NONE', *, *, #248794, .F. ) ;
#183913=B_SPLINE_CURVE_WITH_KNOTS ( 'NONE', 3,
 ( #36466, #96386, #254180, #114688, #153871, #35195, #95125, #232090, #115987, #73035, #233384, #16890, #136808, #174716, #195538, #13049 ),
 .UNSPECIFIED., .F., .F.,
 ( 4, 3, 3, 3, 3, 4 ),
 ( 0.000000000000000000, 3.357088238233600668E-05, 6.714213034886770139E-05, 0.0001007408646120938085, 0.0001343627955914254344, 0.0001573956632896058639 ),
 .UNSPECIFIED. ) ;
#184044=DIRECTION ( 'NONE',  ( 0.000000000000000000, -1.000000000000000000, -6.982962677686265922E-15 ) ) ;
#184061=EDGE_CURVE ( 'NONE', #252315, #66860, #115927, .T. ) ;
#184103=DIRECTION ( 'NONE',  ( -1.000000000000000000, -0.000000000000000000, -0.000000000000000000 ) ) ;
#184109=DIRECTION ( 'NONE',  ( 0.000000000000000000, -1.000000000000000000, -8.609265936414504429E-15 ) ) ;
#184113=VERTEX_POINT ( 'NONE', #19393 ) ;
#184119=CARTESIAN_POINT ( 'NONE',  ( -1.739115166359751801E-14, 64.35000000001187459, -90.77310748452438816 ) ) ;
#184120=EDGE_CURVE ( 'NONE', #125280, #27505, #153763, .T. ) ;
#184125=CARTESIAN_POINT ( 'NONE',  ( 20.12500000000000000, 66.25000000001179501, -81.77310748452437394 ) ) ;
#184144=EDGE_CURVE ( 'NONE', #208027, #143163, #157658, .T. ) ;
#184149=VECTOR ( 'NONE', #143443, 1000.000000000000000 ) ;
#184156=DIRECTION ( 'NONE',  ( 0.000000000000000000, 6.982962677686266711E-15, -1.000000000000000000 ) ) ;
#184234=VECTOR ( 'NONE', #191126, 1000.000000000000000 ) ;
#184242=ORIENTED_EDGE ( 'NONE', *, *, #152780, .F. ) ;
#184245=CARTESIAN_POINT ( 'NONE',  ( -20.85000000000000142, 68.97833521811159585, -65.68954208262705663 ) ) ;
#184265=ORIENTED_EDGE ( 'NONE', *, *, #252667, .F. ) ;
#184275=EDGE_CURVE ( 'NONE', #235864, #86355, #113472, .T. ) ;
#184342=CARTESIAN_POINT ( 'NONE',  ( 21.05000000000000071, 67.22371710471938400, -90.87310748452436826 ) ) ;
#184374=CARTESIAN_POINT ( 'NONE',  ( -20.54999999999999716, 73.50000000001186606, -89.79848556176223440 ) ) ;
#184409=EDGE_CURVE ( 'NONE', #89644, #223762, #151076, .T. ) ;
#184422=FACE_OUTER_BOUND ( 'NONE', #52161, .T. ) ;
#184431=ADVANCED_FACE ( 'NONE', ( #141268 ), #38329, .F. ) ;
#184480=EDGE_CURVE ( 'NONE', #195387, #107897, #199971, .T. ) ;
#184520=AXIS2_PLACEMENT_3D ( 'NONE', #237620, #137224, #198481 ) ;
#184557=CARTESIAN_POINT ( 'NONE',  ( 18.59999999999999432, 85.48068669529062902, -62.58199231576638510 ) ) ;
#184558=CIRCLE ( 'NONE', #126311, 0.1000000000000028644 ) ;
#184567=PRODUCT_DEFINITION_SHAPE ( 'NONE', 'NONE',  #32578 ) ;
#184571=ORIENTED_EDGE ( 'NONE', *, *, #189300, .T. ) ;
#184577=EDGE_CURVE ( 'NONE', #110088, #61112, #180298, .T. ) ;
#184580=ORIENTED_EDGE ( 'NONE', *, *, #181980, .T. ) ;
#184584=DIRECTION ( 'NONE',  ( 0.000000000000000000, 0.000000000000000000, 1.000000000000000000 ) ) ;
#184645=CARTESIAN_POINT ( 'NONE',  ( -23.15000000000000213, 71.65000000001187175, -90.67310748452433700 ) ) ;
#184656=AXIS2_PLACEMENT_3D ( 'NONE', #126760, #184156, #167208 ) ;
#184695=EDGE_CURVE ( 'NONE', #178001, #53093, #109546, .T. ) ;
#184732=CARTESIAN_POINT ( 'NONE',  ( -21.05000000000000071, 76.10000000001198828, -109.5637644362255543 ) ) ;
#184736=EDGE_CURVE ( 'NONE', #127766, #117549, #171958, .T. ) ;
#184758=EDGE_LOOP ( 'NONE', ( #20671, #116226, #26567, #156297 ) ) ;
#184780=AXIS2_PLACEMENT_3D ( 'NONE', #63302, #43753, #87983 ) ;
#184790=CARTESIAN_POINT ( 'NONE',  ( 23.25000000000000000, 85.60000000001204512, -114.7731074845242460 ) ) ;
#184797=CARTESIAN_POINT ( 'NONE',  ( -21.00219873199078435, 64.39461131213531075, -96.11046005622981170 ) ) ;
#184859=ADVANCED_FACE ( 'NONE', ( #255730 ), #155577, .F. ) ;
#184874=AXIS2_PLACEMENT_3D ( 'NONE', #41533, #218844, #140598 ) ;
#184876=ORIENTED_EDGE ( 'NONE', *, *, #29642, .T. ) ;
#184882=EDGE_LOOP ( 'NONE', ( #126862, #228690, #1702, #228552 ) ) ;
#184907=CYLINDRICAL_SURFACE ( 'NONE', #99557, 0.09999999999999939493 ) ;
#184955=CIRCLE ( 'NONE', #176588, 0.09999999999999939493 ) ;
#184972=ORIENTED_EDGE ( 'NONE', *, *, #24403, .F. ) ;
#184978=CARTESIAN_POINT ( 'NONE',  ( -18.58671080940900211, 85.40693285883851615, -95.89895301961956875 ) ) ;
#184982=( BOUNDED_CURVE ( )  B_SPLINE_CURVE ( 3, ( #252551, #115624, #32263, #92198 ),
 .UNSPECIFIED., .F., .F. ) 
 B_SPLINE_CURVE_WITH_KNOTS ( ( 4, 4 ),
 ( 0.000000000000000000, 1.570796326794908992 ),
 .UNSPECIFIED. ) 
 CURVE ( )  GEOMETRIC_REPRESENTATION_ITEM ( )  RATIONAL_B_SPLINE_CURVE ( ( 1.000000000000000000, 0.8047378541243619399, 0.8047378541243619399, 1.000000000000000000 ) ) 
 REPRESENTATION_ITEM ( '' )  );
#184983=AXIS2_PLACEMENT_3D ( 'NONE', #234579, #216293, #156366 ) ;
#185034=VERTEX_POINT ( 'NONE', #84805 ) ;
#185043=DIRECTION ( 'NONE',  ( -0.000000000000000000, -1.000000000000000000, -8.609265936414532828E-15 ) ) ;
#185050=CIRCLE ( 'NONE', #68537, 12.87499999999999822 ) ;
#185069=CARTESIAN_POINT ( 'NONE',  ( -22.59999999999999787, 64.25043287652255231, -103.1239658536231047 ) ) ;
#185103=ORIENTED_EDGE ( 'NONE', *, *, #186549, .T. ) ;
#185117=AXIS2_PLACEMENT_3D ( 'NONE', #141180, #142452, #61640 ) ;
#185141=CARTESIAN_POINT ( 'NONE',  ( 19.81427058490526605, 64.33143601963001856, -78.27310748452438816 ) ) ;
#185149=DIRECTION ( 'NONE',  ( 1.000000000000000000, 0.000000000000000000, 0.000000000000000000 ) ) ;
#185161=AXIS2_PLACEMENT_3D ( 'NONE', #42025, #26303, #40763 ) ;
#185169=EDGE_CURVE ( 'NONE', #153341, #70373, #222135, .T. ) ;
#185170=EDGE_LOOP ( 'NONE', ( #57696, #68476, #164432, #160133 ) ) ;
#185231=EDGE_LOOP ( 'NONE', ( #147684, #22371, #144179, #93661 ) ) ;
#185237=DIRECTION ( 'NONE',  ( 1.000000000000000000, 0.000000000000000000, 0.000000000000000000 ) ) ;
#185241=DIRECTION ( 'NONE',  ( -1.000000000000000000, 1.836970198721029934E-16, 1.282749433769087757E-30 ) ) ;
#185273=VECTOR ( 'NONE', #152034, 1000.000000000000000 ) ;
#185314=CARTESIAN_POINT ( 'NONE',  ( 18.59999999999999076, 68.87972903831409610, -65.86354444268503983 ) ) ;
#185335=DIRECTION ( 'NONE',  ( 0.000000000000000000, -1.000000000000000000, -6.982962677686266711E-15 ) ) ;
#185342=CARTESIAN_POINT ( 'NONE',  ( 21.05000000000000071, 77.83534155023627932, -91.46795619196130644 ) ) ;
#185359=ORIENTED_EDGE ( 'NONE', *, *, #101734, .T. ) ;
#185367=CARTESIAN_POINT ( 'NONE',  ( 18.59999999999999076, 77.85161776048053639, -57.91991776492063337 ) ) ;
#185371=ORIENTED_EDGE ( 'NONE', *, *, #184736, .T. ) ;
#185394=CARTESIAN_POINT ( 'NONE',  ( 18.49999999999999289, 65.71984138295462685, -78.29853541332350630 ) ) ;
#185404=CIRCLE ( 'NONE', #135494, 0.2000000000000057288 ) ;
#185407=CARTESIAN_POINT ( 'NONE',  ( -20.64999999999999858, 73.50000000001180922, -82.74772940728642823 ) ) ;
#185415=( GEOMETRIC_REPRESENTATION_CONTEXT ( 3 ) GLOBAL_UNCERTAINTY_ASSIGNED_CONTEXT ( ( #209444 ) ) GLOBAL_UNIT_ASSIGNED_CONTEXT ( ( #178879, #225318, #139689 ) ) REPRESENTATION_CONTEXT ( 'NONE', 'WORKASPACE' ) );
#185417=CARTESIAN_POINT ( 'NONE',  ( 20.96428641294179585, 64.25000000001175238, -76.34821430658304564 ) ) ;
#185422=ADVANCED_FACE ( 'NONE', ( #226597 ), #143233, .T. ) ;
#185430=AXIS2_PLACEMENT_3D ( 'NONE', #115454, #170353, #153355 ) ;
#185436=DIRECTION ( 'NONE',  ( 1.000000000000000000, 0.000000000000000000, 0.000000000000000000 ) ) ;
#185475=VERTEX_POINT ( 'NONE', #174397 ) ;
#185488=VECTOR ( 'NONE', #207308, 1000.000000000000000 ) ;
#185531=CARTESIAN_POINT ( 'NONE',  ( 23.14999999999999503, 64.35000000001178933, -81.77310748452438816 ) ) ;
#185568=CARTESIAN_POINT ( 'NONE',  ( 22.60000000000000142, 76.00000000001195133, -103.0231074845243171 ) ) ;
#185571=CARTESIAN_POINT ( 'NONE',  ( 18.41789779300679086, 85.50000000001189449, -95.99103781816336323 ) ) ;
#185580=( LENGTH_UNIT ( ) NAMED_UNIT ( * ) SI_UNIT ( .MILLI., .METRE. ) );
#185582=CARTESIAN_POINT ( 'NONE',  ( -20.64999999999999858, 76.00000000001172396, -71.52310748452431710 ) ) ;
#185628=LINE ( 'NONE', #205167, #158244 ) ;
#185712=EDGE_LOOP ( 'NONE', ( #124274, #67389, #160701, #195056 ) ) ;
#185737=DIRECTION ( 'NONE',  ( 1.000000000000000000, 0.000000000000000000, 0.000000000000000000 ) ) ;
#185751=EDGE_LOOP ( 'NONE', ( #97302, #188165, #237542, #152717 ) ) ;
#185752=DIRECTION ( 'NONE',  ( 0.7071067811865127117, 0.7071067811865821007, 0.000000000000000000 ) ) ;
#185758=DIRECTION ( 'NONE',  ( -2.940209281316621016E-16, -1.000000000000000000, -4.704334850106593625E-15 ) ) ;
#185776=CARTESIAN_POINT ( 'NONE',  ( 20.85000000000000142, 77.83585931145526615, -58.01866831572577610 ) ) ;
#185813=EDGE_LOOP ( 'NONE', ( #40644, #213527, #87011 ) ) ;
#185819=DIRECTION ( 'NONE',  ( 1.000000000000000000, 0.000000000000000000, 0.000000000000000000 ) ) ;
#185831=CYLINDRICAL_SURFACE ( 'NONE', #203383, 0.1000000000000028644 ) ;
#185848=EDGE_CURVE ( 'NONE', #9918, #76960, #124645, .T. ) ;
#185849=CIRCLE ( 'NONE', #256726, 0.1999999999999987899 ) ;
#185855=DIRECTION ( 'NONE',  ( 0.000000000000000000, -7.272083257015735086E-15, 1.000000000000000000 ) ) ;
#185903=ORIENTED_EDGE ( 'NONE', *, *, #138964, .T. ) ;
#185905=ORIENTED_EDGE ( 'NONE', *, *, #134772, .F. ) ;
#185912=FACE_OUTER_BOUND ( 'NONE', #159215, .T. ) ;
#185922=ORIENTED_EDGE ( 'NONE', *, *, #234516, .T. ) ;
#185948=CIRCLE ( 'NONE', #44313, 4.299999999999956302 ) ;
#186002=DIRECTION ( 'NONE',  ( 1.000000000000000000, 0.000000000000000000, 0.000000000000000000 ) ) ;
#186003=DIRECTION ( 'NONE',  ( 1.000000000000000000, 0.000000000000000000, 0.000000000000000000 ) ) ;
#186026=CARTESIAN_POINT ( 'NONE',  ( 21.05000000000000071, 70.10000000001177511, -79.74220724918072278 ) ) ;
#186040=UNCERTAINTY_MEASURE_WITH_UNIT (LENGTH_MEASURE( 1.000000000000000082E-05 ), #58860, 'distance_accuracy_value', 'NONE');
#186051=EDGE_LOOP ( 'NONE', ( #149143, #146500, #30151, #149442 ) ) ;
#186056=ORIENTED_EDGE ( 'NONE', *, *, #140940, .T. ) ;
#186083=ORIENTED_EDGE ( 'NONE', *, *, #236007, .T. ) ;
#186094=CARTESIAN_POINT ( 'NONE',  ( -21.05000000000000071, 64.36312671090743720, -96.20134827119950671 ) ) ;
#186106=FACE_OUTER_BOUND ( 'NONE', #151642, .T. ) ;
#186141=ADVANCED_FACE ( 'NONE', ( #39373 ), #161882, .F. ) ;
#186150=CARTESIAN_POINT ( 'NONE',  ( 18.49999999999998934, 65.75000000001176659, -78.37310748452438247 ) ) ;
#186153=EDGE_CURVE ( 'NONE', #97301, #8175, #226816, .T. ) ;
#186162=DIRECTION ( 'NONE',  ( 1.000000000000000000, 0.000000000000000000, 0.000000000000000000 ) ) ;
#186186=CARTESIAN_POINT ( 'NONE',  ( 21.05000000000000071, 84.73084112150709757, -79.12118220350858167 ) ) ;
#186195=CARTESIAN_POINT ( 'NONE',  ( -21.07928932188134041, 69.67148334361326079, -103.1220026301789972 ) ) ;
#186260=ORIENTED_EDGE ( 'NONE', *, *, #112633, .F. ) ;
#186280=CARTESIAN_POINT ( 'NONE',  ( -18.50000000000000000, 70.65875701002036635, -112.8297576910123752 ) ) ;
#186299=ORIENTED_EDGE ( 'NONE', *, *, #230612, .T. ) ;
#186303=CARTESIAN_POINT ( 'NONE',  ( 20.94999999999999929, 87.29603075034701476, -72.57100664418810254 ) ) ;
#186319=CARTESIAN_POINT ( 'NONE',  ( 21.05000000000000071, 69.35000000001187459, -93.17928539484123007 ) ) ;
#186323=CARTESIAN_POINT ( 'NONE',  ( 20.95575313997065336, 65.38544669673706267, -95.40181678257957287 ) ) ;
#186325=LINE ( 'NONE', #106763, #49523 ) ;
#186331=AXIS2_PLACEMENT_3D ( 'NONE', #49108, #46530, #7410 ) ;
#186393=AXIS2_PLACEMENT_3D ( 'NONE', #118862, #74625, #18460 ) ;
#186396=EDGE_LOOP ( 'NONE', ( #100557, #60225, #106825 ) ) ;
#186399=AXIS2_PLACEMENT_3D ( 'NONE', #240488, #98358, #138775 ) ;
#186405=CARTESIAN_POINT ( 'NONE',  ( -21.53752568617673191, 69.21319212550804423, -103.1220819457949318 ) ) ;
#186411=PLANE ( 'NONE',  #132723 ) ;
#186421=EDGE_LOOP ( 'NONE', ( #13804, #82696, #92256, #182643, #37283 ) ) ;
#186463=CIRCLE ( 'NONE', #82374, 11.65000000000000036 ) ;
#186482=VERTEX_POINT ( 'NONE', #113438 ) ;
#186549=EDGE_CURVE ( 'NONE', #120661, #50342, #118596, .T. ) ;
#186551=CARTESIAN_POINT ( 'NONE',  ( -23.25000000000000000, 77.73670573947921980, -58.00568489690056850 ) ) ;
#186572=EDGE_CURVE ( 'NONE', #214994, #44904, #218946, .T. ) ;
#186597=FACE_OUTER_BOUND ( 'NONE', #31640, .T. ) ;
#186613=DIRECTION ( 'NONE',  ( -0.000000000000000000, 1.000000000000000000, 6.982962677686266711E-15 ) ) ;
#186618=CARTESIAN_POINT ( 'NONE',  ( -20.89192007715127986, 65.67101464000481315, -63.94043916224794089 ) ) ;
#186648=DIRECTION ( 'NONE',  ( 0.000000000000000000, 6.982962677686266711E-15, -1.000000000000000000 ) ) ;
#186659=ORIENTED_EDGE ( 'NONE', *, *, #150844, .F. ) ;
#186681=VECTOR ( 'NONE', #244912, 1000.000000000000000 ) ;
#186711=AXIS2_PLACEMENT_3D ( 'NONE', #257116, #135919, #99354 ) ;
#186737=EDGE_LOOP ( 'NONE', ( #242057, #178567, #209007, #182011, #136414, #180436, #209942 ) ) ;
#186767=DIRECTION ( 'NONE',  ( 1.000000000000000000, 0.000000000000000000, 0.000000000000000000 ) ) ;
#186798=CARTESIAN_POINT ( 'NONE',  ( -23.25000000000000000, 76.10000000001203091, -114.6726782920691079 ) ) ;
#186807=ORIENTED_EDGE ( 'NONE', *, *, #178054, .T. ) ;
#186816=DIRECTION ( 'NONE',  ( -1.000000000000000000, 0.000000000000000000, -0.000000000000000000 ) ) ;
#186837=CIRCLE ( 'NONE', #149432, 7.900000000000003908 ) ;
#186889=DIRECTION ( 'NONE',  ( 0.000000000000000000, 1.000000000000000000, 0.000000000000000000 ) ) ;
#186902=CARTESIAN_POINT ( 'NONE',  ( 20.97250901189795513, 65.37543196631001763, -95.35856176755739000 ) ) ;
#186919=CIRCLE ( 'NONE', #78720, 11.80000000000000426 ) ;
#186924=CARTESIAN_POINT ( 'NONE',  ( -23.15000000000000213, 64.35000000001187459, -90.77310748452440237 ) ) ;
#186932=ORIENTED_EDGE ( 'NONE', *, *, #31641, .F. ) ;
#186940=AXIS2_PLACEMENT_3D ( 'NONE', #241157, #82030, #25955 ) ;
#186987=DIRECTION ( 'NONE',  ( 1.000000000000000000, 4.758098676964952635E-14, 0.000000000000000000 ) ) ;
#186996=EDGE_CURVE ( 'NONE', #94420, #168199, #165291, .T. ) ;
#187012=ORIENTED_EDGE ( 'NONE', *, *, #55574, .F. ) ;
#187013=DIRECTION ( 'NONE',  ( -0.000000000000000000, 1.000000000000000000, 6.982962677686266711E-15 ) ) ;
#187039=VECTOR ( 'NONE', #168630, 1000.000000000000000 ) ;
#187055=CARTESIAN_POINT ( 'NONE',  ( -22.48479450179659977, 75.95300841882514931, -114.6731059307759324 ) ) ;
#187085=ORIENTED_EDGE ( 'NONE', *, *, #507, .F. ) ;
#187087=FACE_OUTER_BOUND ( 'NONE', #7712, .T. ) ;
#187104=DIRECTION ( 'NONE',  ( 1.000000000000000000, 0.000000000000000000, 0.000000000000000000 ) ) ;
#187175=EDGE_CURVE ( 'NONE', #61112, #128191, #139631, .T. ) ;
#187181=CARTESIAN_POINT ( 'NONE',  ( -18.59999999999999787, 68.97833521811159585, -65.88954208262707368 ) ) ;
#187204=FACE_OUTER_BOUND ( 'NONE', #45760, .T. ) ;
#187234=CARTESIAN_POINT ( 'NONE',  ( 22.49999999999999645, 64.35042919246716053, -103.1231074845243825 ) ) ;
#187239=DIRECTION ( 'NONE',  ( 1.875376730785737719E-16, 1.000000000000000000, 6.982962677686266711E-15 ) ) ;
#187243=FACE_OUTER_BOUND ( 'NONE', #209462, .T. ) ;
#187261=CARTESIAN_POINT ( 'NONE',  ( 22.60000000000000142, 75.89914163091332000, -114.7726746080137019 ) ) ;
#187266=VECTOR ( 'NONE', #18198, 1000.000000000000114 ) ;
#187280=VERTEX_POINT ( 'NONE', #168550 ) ;
#187304=EDGE_LOOP ( 'NONE', ( #222037, #122556, #250105, #70431 ) ) ;
#187337=DIRECTION ( 'NONE',  ( -0.000000000000000000, 6.982962677686266711E-15, -1.000000000000000000 ) ) ;
#187341=CARTESIAN_POINT ( 'NONE',  ( -21.05000000000000071, 76.00000000001197975, -107.3231074845242716 ) ) ;
#187348=CIRCLE ( 'NONE', #12384, 12.77499999999999503 ) ;
#187356=CARTESIAN_POINT ( 'NONE',  ( 21.08489247129321242, 67.12232480914178723, -90.67310748452436542 ) ) ;
#187365=AXIS2_PLACEMENT_3D ( 'NONE', #171487, #11099, #51469 ) ;
#187386=ORIENTED_EDGE ( 'NONE', *, *, #248022, .F. ) ;
#187414=CARTESIAN_POINT ( 'NONE',  ( 20.94999999999999929, 68.97833521811159585, -65.68954208262705663 ) ) ;
#187415=DIRECTION ( 'NONE',  ( 0.000000000000000000, -6.938893903907222067E-15, 1.000000000000000000 ) ) ;
#187430=VECTOR ( 'NONE', #19266, 1000.000000000000000 ) ;
#187445=CARTESIAN_POINT ( 'NONE',  ( -21.05000000000000071, 76.00000000001168132, -65.52310748452430289 ) ) ;
#187469=ORIENTED_EDGE ( 'NONE', *, *, #233427, .F. ) ;
#187484=ORIENTED_EDGE ( 'NONE', *, *, #155562, .T. ) ;
#187493=CYLINDRICAL_SURFACE ( 'NONE', #37044, 0.1000000000000038219 ) ;
#187513=CARTESIAN_POINT ( 'NONE',  ( 23.14999999999999858, 76.00000000001170974, -69.52310748452431710 ) ) ;
#187531=LINE ( 'NONE', #64984, #148980 ) ;
#187552=DIRECTION ( 'NONE',  ( 0.000000000000000000, -0.7397360091702647189, -0.6728971962616949742 ) ) ;
#187579=ORIENTED_EDGE ( 'NONE', *, *, #11089, .T. ) ;
#187586=FACE_OUTER_BOUND ( 'NONE', #70532, .T. ) ;
#187588=CARTESIAN_POINT ( 'NONE',  ( -23.15000000000000213, 76.00000000001195133, -103.0231074845243171 ) ) ;
#187597=DIRECTION ( 'NONE',  ( 1.000000000000000000, 0.000000000000000000, 0.000000000000000000 ) ) ;
#187601=DIRECTION ( 'NONE',  ( -1.000000000000000000, 0.000000000000000000, 0.000000000000000000 ) ) ;
#187632=DIRECTION ( 'NONE',  ( -1.000000000000000000, -0.000000000000000000, -0.000000000000000000 ) ) ;
#187638=ORIENTED_EDGE ( 'NONE', *, *, #75751, .F. ) ;
#187649=VECTOR ( 'NONE', #243659, 1000.000000000000000 ) ;
#187709=CARTESIAN_POINT ( 'NONE',  ( 21.33487959338958717, 69.27444184810076422, -103.0231074845243597 ) ) ;
#187711=ORIENTED_EDGE ( 'NONE', *, *, #109033, .F. ) ;
#187717=DIRECTION ( 'NONE',  ( -4.391705002472927119E-16, -1.000000000000000000, -7.026728003956683390E-15 ) ) ;
#187759=ADVANCED_FACE ( 'NONE', ( #84920 ), #214844, .T. ) ;
#187763=CARTESIAN_POINT ( 'NONE',  ( 21.05000000000000071, 69.45934304831071415, -102.9231074845243512 ) ) ;
#187804=AXIS2_PLACEMENT_3D ( 'NONE', #121903, #3201, #22814 ) ;
#187814=TOROIDAL_SURFACE ( 'NONE', #75396, 0.2000000000000000111, 0.1000000000000000056 ) ;
#187822=CYLINDRICAL_SURFACE ( 'NONE', #31442, 0.1000000000000028644 ) ;
#187823=CARTESIAN_POINT ( 'NONE',  ( 20.85000000000000142, 77.83585931145526615, -58.01866831572577610 ) ) ;
#187824=AXIS2_PLACEMENT_3D ( 'NONE', #63509, #179640, #81765 ) ;
#187898=CARTESIAN_POINT ( 'NONE',  ( -20.94999027547553894, 65.70673848566956110, -64.06382523348288771 ) ) ;
#187906=VERTEX_POINT ( 'NONE', #194027 ) ;
#187935=ORIENTED_EDGE ( 'NONE', *, *, #221241, .T. ) ;
#187950=EDGE_CURVE ( 'NONE', #12008, #20238, #23092, .T. ) ;
#187965=ORIENTED_EDGE ( 'NONE', *, *, #210127, .T. ) ;
#188034=VECTOR ( 'NONE', #85389, 1000.000000000000000 ) ;
#188062=CARTESIAN_POINT ( 'NONE',  ( -23.25000000000000000, 87.65000000001195701, -103.0231074845242318 ) ) ;
#188096=EDGE_CURVE ( 'NONE', #146711, #190547, #208144, .T. ) ;
#188101=FACE_OUTER_BOUND ( 'NONE', #184882, .T. ) ;
#188117=EDGE_LOOP ( 'NONE', ( #101819, #11115, #75458, #237676 ) ) ;
#188140=LINE ( 'NONE', #130725, #187039 ) ;
#188147=CARTESIAN_POINT ( 'NONE',  ( 18.50000000000000000, 85.40000000001188596, -95.72584772486098359 ) ) ;
#188152=LINE ( 'NONE', #43505, #181945 ) ;
#188165=ORIENTED_EDGE ( 'NONE', *, *, #188096, .F. ) ;
#188173=ORIENTED_EDGE ( 'NONE', *, *, #16400, .F. ) ;
#188177=ORIENTED_EDGE ( 'NONE', *, *, #89826, .F. ) ;
#188178=CARTESIAN_POINT ( 'NONE',  ( 21.07928932188134397, 75.90110485435735654, -109.3516241409230219 ) ) ;
#188192=CARTESIAN_POINT ( 'NONE',  ( 18.49999999999999289, 65.50857864377445594, -78.17310748452437963 ) ) ;
#188213=CARTESIAN_POINT ( 'NONE',  ( -20.54999999999999716, 85.00000000001179501, -79.41707660717668205 ) ) ;
#188262=DIRECTION ( 'NONE',  ( 0.000000000000000000, -1.000000000000000000, -6.860497997771531562E-15 ) ) ;
#188268=ORIENTED_EDGE ( 'NONE', *, *, #244189, .T. ) ;
#188269=CARTESIAN_POINT ( 'NONE',  ( -23.15000000000000213, 87.39257802171739797, -72.59705706435616435 ) ) ;
#188331=CIRCLE ( 'NONE', #204510, 0.2000000000000057288 ) ;
#188357=AXIS2_PLACEMENT_3D ( 'NONE', #59849, #62455, #141972 ) ;
#188368=CARTESIAN_POINT ( 'NONE',  ( -21.05000000000000071, 76.00000000001179501, -81.32310748452431426 ) ) ;
#188400=CARTESIAN_POINT ( 'NONE',  ( -20.54999999999999716, 71.65000000001187175, -90.67310748452433700 ) ) ;
#188411=EDGE_CURVE ( 'NONE', #151730, #127649, #6921, .T. ) ;
#188431=ORIENTED_EDGE ( 'NONE', *, *, #228316, .F. ) ;
#188436=VERTEX_POINT ( 'NONE', #220945 ) ;
#188459=DIRECTION ( 'NONE',  ( 0.000000000000000000, -7.026728003956683390E-15, 1.000000000000000000 ) ) ;
#188471=DIRECTION ( 'NONE',  ( 1.000000000000000000, 0.000000000000000000, 0.000000000000000000 ) ) ;
#188490=DIRECTION ( 'NONE',  ( 1.000000000000000000, -3.265361837132813093E-16, -2.280189983783949500E-30 ) ) ;
#188494=AXIS2_PLACEMENT_3D ( 'NONE', #147331, #69099, #123936 ) ;
#188503=CARTESIAN_POINT ( 'NONE',  ( -23.25000000000000000, 77.83585931145526615, -57.91866831572577468 ) ) ;
#188510=AXIS2_PLACEMENT_3D ( 'NONE', #75656, #200720, #1204 ) ;
#188528=DIRECTION ( 'NONE',  ( 0.000000000000000000, 6.982962677686266711E-15, -1.000000000000000000 ) ) ;
#188540=AXIS2_PLACEMENT_3D ( 'NONE', #80378, #240780, #159979 ) ;
#188541=ORIENTED_EDGE ( 'NONE', *, *, #253503, .F. ) ;
#188552=LINE ( 'NONE', #89444, #173713 ) ;
#188558=DIRECTION ( 'NONE',  ( 1.000000000000000000, 0.000000000000000000, 0.000000000000000000 ) ) ;
#188575=LINE ( 'NONE', #86888, #37789 ) ;
#188601=DIRECTION ( 'NONE',  ( -1.000000000000000000, 0.000000000000000000, 0.000000000000000000 ) ) ;
#188603=PLANE ( 'NONE',  #87356 ) ;
#188610=ORIENTED_EDGE ( 'NONE', *, *, #69963, .F. ) ;
#188614=EDGE_CURVE ( 'NONE', #71577, #6826, #231412, .T. ) ;
#188632=EDGE_CURVE ( 'NONE', #24156, #170856, #60405, .T. ) ;
#188635=EDGE_CURVE ( 'NONE', #80949, #86681, #235099, .T. ) ;
#188636=DIRECTION ( 'NONE',  ( 1.000000000000000000, 0.000000000000000000, 0.000000000000000000 ) ) ;
#188656=CARTESIAN_POINT ( 'NONE',  ( 21.14999999999999858, 69.35000000001186038, -90.87310748452435405 ) ) ;
#188677=ORIENTED_EDGE ( 'NONE', *, *, #145944, .T. ) ;
#188689=ADVANCED_FACE ( 'NONE', ( #241511 ), #139825, .F. ) ;
#188719=VERTEX_POINT ( 'NONE', #4172 ) ;
#188762=ORIENTED_EDGE ( 'NONE', *, *, #232087, .F. ) ;
#188780=ORIENTED_EDGE ( 'NONE', *, *, #109799, .T. ) ;
#188786=CARTESIAN_POINT ( 'NONE',  ( -23.15000000000000213, 76.00000000001195133, -103.0231074845243171 ) ) ;
#188802=AXIS2_PLACEMENT_3D ( 'NONE', #241624, #85080, #202499 ) ;
#188851=DIRECTION ( 'NONE',  ( 0.000000000000000000, -6.938893903907222067E-15, 1.000000000000000000 ) ) ;
#188858=ORIENTED_EDGE ( 'NONE', *, *, #255019, .F. ) ;
#188875=LINE ( 'NONE', #57029, #234990 ) ;
#188882=DIRECTION ( 'NONE',  ( 0.000000000000000000, -6.853228547068871147E-15, 1.000000000000000000 ) ) ;
#188884=CARTESIAN_POINT ( 'NONE',  ( 20.95520789717937404, 65.42306940062692888, -95.44287451064953132 ) ) ;
#188896=CARTESIAN_POINT ( 'NONE',  ( -23.25000000000000000, 77.14957036958736580, -61.70719500002233815 ) ) ;
#188900=DIRECTION ( 'NONE',  ( -1.000000000000000000, 0.000000000000000000, 0.000000000000000000 ) ) ;
#188901=DIRECTION ( 'NONE',  ( 1.000000000000000000, 0.000000000000000000, 0.000000000000000000 ) ) ;
#188907=ORIENTED_EDGE ( 'NONE', *, *, #142213, .F. ) ;
#188927=EDGE_CURVE ( 'NONE', #74197, #170856, #56577, .T. ) ;
#188941=EDGE_CURVE ( 'NONE', #27505, #51895, #69107, .T. ) ;
#188958=AXIS2_PLACEMENT_3D ( 'NONE', #103739, #47624, #250654 ) ;
#189015=DIRECTION ( 'NONE',  ( -0.000000000000000000, 6.982962677686266711E-15, -1.000000000000000000 ) ) ;
#189057=ORIENTED_EDGE ( 'NONE', *, *, #156232, .T. ) ;
#189066=CARTESIAN_POINT ( 'NONE',  ( 23.24999999999999645, 76.00000000001170974, -69.52310748452431710 ) ) ;
#189070=ORIENTED_EDGE ( 'NONE', *, *, #128426, .T. ) ;
#189085=CARTESIAN_POINT ( 'NONE',  ( -20.85000000000000142, 77.13501884592184865, -61.80613060109197932 ) ) ;
#189128=CARTESIAN_POINT ( 'NONE',  ( 23.14999999999999858, 71.00000000001186606, -90.61784146561124942 ) ) ;
#189144=CIRCLE ( 'NONE', #14387, 0.09999999999999976963 ) ;
#189147=FACE_OUTER_BOUND ( 'NONE', #60571, .T. ) ;
#189154=AXIS2_PLACEMENT_3D ( 'NONE', #160001, #238219, #217360 ) ;
#189176=CARTESIAN_POINT ( 'NONE',  ( -20.85882249326303040, 65.66751761918648356, -63.92826094061123143 ) ) ;
#189182=DIRECTION ( 'NONE',  ( 1.000000000000000000, 0.000000000000000000, 0.000000000000000000 ) ) ;
#189189=VERTEX_POINT ( 'NONE', #219054 ) ;
#189215=CARTESIAN_POINT ( 'NONE',  ( -21.05000000000001492, 69.45934304831069994, -103.0231074845243597 ) ) ;
#189241=AXIS2_PLACEMENT_3D ( 'NONE', #193596, #78758, #76195 ) ;
#189243=ORIENTED_EDGE ( 'NONE', *, *, #171607, .F. ) ;
#189250=ORIENTED_EDGE ( 'NONE', *, *, #213288, .F. ) ;
#189253=CARTESIAN_POINT ( 'NONE',  ( 18.49999999999999289, 65.75000000001175238, -78.37310748452439668 ) ) ;
#189255=ORIENTED_EDGE ( 'NONE', *, *, #116300, .T. ) ;
#189260=EDGE_CURVE ( 'NONE', #2690, #138100, #244048, .T. ) ;
#189281=CARTESIAN_POINT ( 'NONE',  ( 19.58285714285715073, 66.98499851036331165, -94.60245466844267526 ) ) ;
#189291=DIRECTION ( 'NONE',  ( 0.000000000000000000, -0.1575844902526579161, -0.9875055080513779338 ) ) ;
#189300=EDGE_CURVE ( 'NONE', #57574, #201690, #203364, .T. ) ;
#189329=CARTESIAN_POINT ( 'NONE',  ( -21.14999999999999858, 76.10000000001198828, -109.2731074845243029 ) ) ;
#189411=CARTESIAN_POINT ( 'NONE',  ( 18.59999999999999076, 77.83585931145526615, -57.91866831572577468 ) ) ;
#189416=TOROIDAL_SURFACE ( 'NONE', #68612, 0.2000000000000000111, 0.1000000000000000056 ) ;
#189437=CARTESIAN_POINT ( 'NONE',  ( 18.47073956224743085, 85.47172941248386735, -95.91442173170634078 ) ) ;
#189453=ORIENTED_EDGE ( 'NONE', *, *, #151575, .F. ) ;
#189455=EDGE_CURVE ( 'NONE', #108089, #56290, #16725, .T. ) ;
#189456=CARTESIAN_POINT ( 'NONE',  ( 20.21494484322215968, 66.69682926214304075, -94.68284229275414532 ) ) ;
#189462=CARTESIAN_POINT ( 'NONE',  ( 21.11825140030105175, 75.99279637937921450, -109.4685150499444575 ) ) ;
#189482=EDGE_LOOP ( 'NONE', ( #11992, #44301, #123240, #247212, #87787 ) ) ;
#189496=ORIENTED_EDGE ( 'NONE', *, *, #13535, .F. ) ;
#189503=DIRECTION ( 'NONE',  ( 0.000000000000000000, 0.000000000000000000, 1.000000000000000000 ) ) ;
#189545=( BOUNDED_SURFACE ( )  B_SPLINE_SURFACE ( 3, 2, ( 
 ( #222329, #224913, #43726 ),
 ( #221064, #161117, #60699 ),
 ( #45010, #183243, #2009 ),
 ( #124559, #123263, #121982 ),
 ( #125820, #202795, #4580 ),
 ( #713, #42437, #81532 ) ),
 .UNSPECIFIED., .F., .F., .F. ) 
 B_SPLINE_SURFACE_WITH_KNOTS ( ( 4, 2, 4 ),
 ( 3, 3 ),
 ( 0.0001792624049599507918, 0.0003686986002124736754, 0.0005581347954649965590 ),
 ( 0.000000000000000000, 1.000000000000000000 ),
 .UNSPECIFIED. ) 
 GEOMETRIC_REPRESENTATION_ITEM ( )  RATIONAL_B_SPLINE_SURFACE ( (
 ( 1.000000000000000000, 0.9238795325112831858, 1.000000000000000000),
 ( 1.000000000000000000, 0.9229318695239602244, 1.000000000000000000),
 ( 1.000000000000000000, 0.8926288119229300877, 1.000000000000000000),
 ( 1.000000000000000000, 0.8123777807272952733, 1.000000000000000000),
 ( 1.000000000000000000, 0.7629087100930300736, 1.000000000000000000),
 ( 1.000000000000000000, 0.7071067811865475727, 1.000000000000000000) ) ) 
 REPRESENTATION_ITEM ( '' )  SURFACE ( )  );
#189618=DIRECTION ( 'NONE',  ( 1.000000000000000000, 0.000000000000000000, 0.000000000000000000 ) ) ;
#189620=DIRECTION ( 'NONE',  ( 1.000000000000000000, 0.000000000000000000, 0.000000000000000000 ) ) ;
#189629=VECTOR ( 'NONE', #211714, 1000.000000000000000 ) ;
#189633=ORIENTED_EDGE ( 'NONE', *, *, #3460, .T. ) ;
#189650=CARTESIAN_POINT ( 'NONE',  ( 20.94999999999999574, 77.26178616857691850, -94.93660852097882241 ) ) ;
#189667=DIRECTION ( 'NONE',  ( 0.000000000000000000, -6.467318590049456648E-15, 1.000000000000000000 ) ) ;
#189683=AXIS2_PLACEMENT_3D ( 'NONE', #110765, #252837, #212455 ) ;
#189736=DIRECTION ( 'NONE',  ( 0.000000000000000000, 0.000000000000000000, 1.000000000000000000 ) ) ;
#189758=ORIENTED_EDGE ( 'NONE', *, *, #109462, .T. ) ;
#189780=AXIS2_PLACEMENT_3D ( 'NONE', #81646, #183364, #123385 ) ;
#189785=EDGE_CURVE ( 'NONE', #11679, #116798, #15501, .T. ) ;
#189822=CARTESIAN_POINT ( 'NONE',  ( -23.25000000000000000, 87.75000000001193712, -103.0231074845242318 ) ) ;
#189852=CARTESIAN_POINT ( 'NONE',  ( 18.43630871534871574, 85.67980087481460316, -62.86247541654014981 ) ) ;
#189853=CARTESIAN_POINT ( 'NONE',  ( -20.94999999999999929, 74.16465844978745281, -91.36795619196134055 ) ) ;
#189856=EDGE_CURVE ( 'NONE', #66860, #34745, #11380, .T. ) ;
#189878=VERTEX_POINT ( 'NONE', #83714 ) ;
#189898=CARTESIAN_POINT ( 'NONE',  ( 20.94999999999999929, 65.27628289530433392, -90.87310748452438247 ) ) ;
#189901=ORIENTED_EDGE ( 'NONE', *, *, #233427, .T. ) ;
#189912=CARTESIAN_POINT ( 'NONE',  ( 20.94999999999999929, 69.55000000001187743, -93.00608031408432907 ) ) ;
#189927=DIRECTION ( 'NONE',  ( -3.469446951953515108E-14, 0.000000000000000000, -1.000000000000000000 ) ) ;
#189950=CARTESIAN_POINT ( 'NONE',  ( -23.25000000000000000, 64.25000000001179501, -81.67310748452440805 ) ) ;
#189959=AXIS2_PLACEMENT_3D ( 'NONE', #211883, #110184, #189736 ) ;
#189974=CIRCLE ( 'NONE', #135791, 0.5000000000000004441 ) ;
#189981=ORIENTED_EDGE ( 'NONE', *, *, #206134, .F. ) ;
#189996=ORIENTED_EDGE ( 'NONE', *, *, #118891, .F. ) ;
#190013=AXIS2_PLACEMENT_3D ( 'NONE', #5757, #85291, #63176 ) ;
#190040=VERTEX_POINT ( 'NONE', #70649 ) ;
#190045=PLANE ( 'NONE',  #95489 ) ;
#190048=VERTEX_POINT ( 'NONE', #88868 ) ;
#190052=AXIS2_PLACEMENT_3D ( 'NONE', #137528, #241778, #21474 ) ;
#190061=EDGE_LOOP ( 'NONE', ( #162697, #139828, #18353, #98988 ) ) ;
#190113=EDGE_CURVE ( 'NONE', #97301, #98180, #140540, .T. ) ;
#190115=LINE ( 'NONE', #115705, #94581 ) ;
#190193=DIRECTION ( 'NONE',  ( 0.000000000000000000, 0.000000000000000000, -1.000000000000000000 ) ) ;
#190227=DIRECTION ( 'NONE',  ( -0.000000000000000000, -6.982962677686266711E-15, 1.000000000000000000 ) ) ;
#190239=ORIENTED_EDGE ( 'NONE', *, *, #128009, .F. ) ;
#190290=VERTEX_POINT ( 'NONE', #53 ) ;
#190346=CIRCLE ( 'NONE', #169709, 11.65000000000000746 ) ;
#190351=DIRECTION ( 'NONE',  ( 0.000000000000000000, 0.000000000000000000, -1.000000000000000000 ) ) ;
#190372=DIRECTION ( 'NONE',  ( 0.000000000000000000, 6.938893903907030216E-14, -1.000000000000000000 ) ) ;
#190385=CYLINDRICAL_SURFACE ( 'NONE', #42586, 0.1000000000000028644 ) ;
#190403=ORIENTED_EDGE ( 'NONE', *, *, #200069, .F. ) ;
#190405=AXIS2_PLACEMENT_3D ( 'NONE', #189898, #11266, #204307 ) ;
#190416=ORIENTED_EDGE ( 'NONE', *, *, #39696, .T. ) ;
#190422=ORIENTED_EDGE ( 'NONE', *, *, #81405, .T. ) ;
#190425=EDGE_CURVE ( 'NONE', #215026, #8175, #72423, .T. ) ;
#190435=CARTESIAN_POINT ( 'NONE',  ( 18.59999999999998721, 69.06610602788535402, -65.73746165015079157 ) ) ;
#190485=CARTESIAN_POINT ( 'NONE',  ( -18.45037301276651576, 85.49020044755381775, -96.01043334810995589 ) ) ;
#190489=AXIS2_PLACEMENT_3D ( 'NONE', #56279, #197078, #195836 ) ;
#190505=ORIENTED_EDGE ( 'NONE', *, *, #105477, .T. ) ;
#190507=CARTESIAN_POINT ( 'NONE',  ( 21.05000000000000071, 64.35000000001195986, -102.9231074845243938 ) ) ;
#190547=VERTEX_POINT ( 'NONE', #151143 ) ;
#190582=VERTEX_POINT ( 'NONE', #252780 ) ;
#190601=CIRCLE ( 'NONE', #91191, 0.09999999999999939493 ) ;
#190606=ORIENTED_EDGE ( 'NONE', *, *, #225496, .F. ) ;
#190614=VERTEX_POINT ( 'NONE', #153755 ) ;
#190620=ADVANCED_FACE ( 'NONE', ( #152444 ), #12933, .F. ) ;
#190630=ORIENTED_EDGE ( 'NONE', *, *, #212081, .F. ) ;
#190642=VERTEX_POINT ( 'NONE', #114573 ) ;
#190668=CIRCLE ( 'NONE', #223938, 0.1000000000000016431 ) ;
#190678=DIRECTION ( 'NONE',  ( 0.000000000000000000, -0.9908441862701605762, 0.1350103645451835310 ) ) ;
#190685=VECTOR ( 'NONE', #61139, 1000.000000000000000 ) ;
#190697=DIRECTION ( 'NONE',  ( -1.000000000000000000, 2.952720810173289112E-16, 2.061873921506763405E-30 ) ) ;
#190741=CARTESIAN_POINT ( 'NONE',  ( -20.94999999999999929, 77.83534155023627932, -91.46795619196130644 ) ) ;
#190764=CARTESIAN_POINT ( 'NONE',  ( 20.72390388899075475, 65.41003688158664886, -95.51175918877980564 ) ) ;
#190769=AXIS2_PLACEMENT_3D ( 'NONE', #81810, #217491, #235783 ) ;
#190776=CIRCLE ( 'NONE', #28277, 12.77499999999999503 ) ;
#190782=DIRECTION ( 'NONE',  ( 0.000000000000000000, 0.1568667991644355497, -0.9876197685951332295 ) ) ;
#190792=PLANE ( 'NONE',  #116682 ) ;
#190805=ORIENTED_EDGE ( 'NONE', *, *, #184695, .T. ) ;
#190812=FACE_BOUND ( 'NONE', #28651, .T. ) ;
#190842=ORIENTED_EDGE ( 'NONE', *, *, #252701, .T. ) ;
#190893=VECTOR ( 'NONE', #245919, 1000.000000000000000 ) ;
#190905=LINE ( 'NONE', #248278, #45930 ) ;
#190916=CARTESIAN_POINT ( 'NONE',  ( -22.41119224318417125, 76.00000000001203659, -114.6726782920691221 ) ) ;
#190921=CARTESIAN_POINT ( 'NONE',  ( -18.50000000000000000, 85.40000000001167280, -62.64106563635157698 ) ) ;
#190924=EDGE_CURVE ( 'NONE', #225321, #40998, #20129, .T. ) ;
#190926=DIRECTION ( 'NONE',  ( 0.000000000000000000, -6.982962677686266711E-15, 1.000000000000000000 ) ) ;
#190929=ORIENTED_EDGE ( 'NONE', *, *, #141565, .T. ) ;
#190934=EDGE_LOOP ( 'NONE', ( #234809, #159990, #219857 ) ) ;
#190942=EDGE_LOOP ( 'NONE', ( #188762, #144110, #202857, #118253, #26981 ) ) ;
#190944=AXIS2_PLACEMENT_3D ( 'NONE', #220364, #199527, #23470 ) ;
#190974=EDGE_LOOP ( 'NONE', ( #189901, #178991, #14524, #45501, #98397, #92170, #113616, #254994, #85822, #79559, #253592, #199646, #183019, #253754, #200807, #188907, #239725, #225543, #179072, #151734, #138523, #80578, #93545 ) ) ;
#190975=CIRCLE ( 'NONE', #49485, 11.65000000000000036 ) ;
#191037=FACE_OUTER_BOUND ( 'NONE', #86773, .T. ) ;
#191117=CIRCLE ( 'NONE', #20230, 0.09999999999999938105 ) ;
#191126=DIRECTION ( 'NONE',  ( 0.000000000000000000, -0.8660254037844377084, -0.5000000000000016653 ) ) ;
#191138=CIRCLE ( 'NONE', #128573, 0.09999999999999938105 ) ;
#191139=ORIENTED_EDGE ( 'NONE', *, *, #229229, .F. ) ;
#191148=AXIS2_PLACEMENT_3D ( 'NONE', #256652, #140604, #79336 ) ;
#191149=CIRCLE ( 'NONE', #20462, 2.000000000000001776 ) ;
#191160=CARTESIAN_POINT ( 'NONE',  ( 18.33996824403518744, 85.56963985944304341, -62.70404184700760908 ) ) ;
#191163=CARTESIAN_POINT ( 'NONE',  ( -18.50000000000000000, 64.35000000001187459, -90.77310748452440237 ) ) ;
#191166=CARTESIAN_POINT ( 'NONE',  ( -23.15000000000000213, 64.35000000001195986, -103.0231074845244024 ) ) ;
#191198=AXIS2_PLACEMENT_3D ( 'NONE', #208952, #227225, #72024 ) ;
#191209=FACE_OUTER_BOUND ( 'NONE', #28853, .T. ) ;
#191223=ADVANCED_FACE ( 'NONE', ( #143514 ), #141121, .T. ) ;
#191263=DIRECTION ( 'NONE',  ( 1.000000000000000000, 0.000000000000000000, 0.000000000000000000 ) ) ;
#191287=ORIENTED_EDGE ( 'NONE', *, *, #69222, .F. ) ;
#191294=TOROIDAL_SURFACE ( 'NONE', #249550, 0.2000000000000000111, 0.1000000000000000056 ) ;
#191330=ORIENTED_EDGE ( 'NONE', *, *, #189856, .T. ) ;
#191351=ORIENTED_EDGE ( 'NONE', *, *, #137705, .T. ) ;
#191353=ORIENTED_EDGE ( 'NONE', *, *, #75751, .T. ) ;
#191358=ADVANCED_FACE ( 'NONE', ( #49560 ), #157914, .T. ) ;
#191381=ORIENTED_EDGE ( 'NONE', *, *, #235639, .T. ) ;
#191431=LINE ( 'NONE', #12781, #100299 ) ;
#191458=ORIENTED_EDGE ( 'NONE', *, *, #9337, .T. ) ;
#191484=CIRCLE ( 'NONE', #124813, 12.87499999999999822 ) ;
#191487=DIRECTION ( 'NONE',  ( 0.000000000000000000, 0.000000000000000000, -1.000000000000000000 ) ) ;
#191493=DIRECTION ( 'NONE',  ( 1.000000000000000000, -3.265361837132813093E-16, -2.280189983783949500E-30 ) ) ;
#191497=CARTESIAN_POINT ( 'NONE',  ( -23.15000000000000213, 64.35000000001187459, -90.87310748452438247 ) ) ;
#191518=DIRECTION ( 'NONE',  ( -1.000000000000000000, 3.265361837132813093E-16, 2.280189983783949500E-30 ) ) ;
#191546=DIRECTION ( 'NONE',  ( -1.000000000000000000, -0.000000000000000000, -0.000000000000000000 ) ) ;
#191553=CARTESIAN_POINT ( 'NONE',  ( -21.07094088545304444, 69.67983277809545939, -103.1220011870765774 ) ) ;
#191564=VERTEX_POINT ( 'NONE', #96363 ) ;
#191581=EDGE_CURVE ( 'NONE', #252315, #146049, #120472, .T. ) ;
#191613=ORIENTED_EDGE ( 'NONE', *, *, #60540, .T. ) ;
#191619=VERTEX_POINT ( 'NONE', #241043 ) ;
#191632=AXIS2_PLACEMENT_3D ( 'NONE', #97989, #254491, #74645 ) ;
#191664=DIRECTION ( 'NONE',  ( 0.000000000000000000, -6.982962677686266711E-15, 1.000000000000000000 ) ) ;
#191673=ADVANCED_FACE ( 'NONE', ( #62398 ), #184907, .T. ) ;
#191717=ADVANCED_FACE ( 'NONE', ( #148348 ), #190045, .F. ) ;
#191722=DIRECTION ( 'NONE',  ( 0.000000000000000000, 1.000000000000000000, 6.352154140967427193E-15 ) ) ;
#191751=CARTESIAN_POINT ( 'NONE',  ( 20.85000000000000142, 76.00000000001170974, -69.52310748452431710 ) ) ;
#191775=CARTESIAN_POINT ( 'NONE',  ( 21.05000000000000071, 67.22371710471941242, -94.46447848938342418 ) ) ;
#191787=VECTOR ( 'NONE', #171740, 1000.000000000000000 ) ;
#191839=ORIENTED_EDGE ( 'NONE', *, *, #232087, .T. ) ;
#191869=AXIS2_PLACEMENT_3D ( 'NONE', #214486, #115383, #194951 ) ;
#191876=ORIENTED_EDGE ( 'NONE', *, *, #192449, .T. ) ;
#191903=DIRECTION ( 'NONE',  ( 0.000000000000000000, 0.4999999999999689138, -0.8660254037844565822 ) ) ;
#191928=FACE_OUTER_BOUND ( 'NONE', #49271, .T. ) ;
#191936=ORIENTED_EDGE ( 'NONE', *, *, #51602, .F. ) ;
#191942=ORIENTED_EDGE ( 'NONE', *, *, #24372, .T. ) ;
#191961=DIRECTION ( 'NONE',  ( 0.000000000000000000, -0.9915357197604892647, 0.1298341882519715440 ) ) ;
#191974=LINE ( 'NONE', #151568, #222149 ) ;
#191975=ORIENTED_EDGE ( 'NONE', *, *, #167872, .F. ) ;
#192007=CIRCLE ( 'NONE', #46225, 7.900000000000003908 ) ;
#192031=CARTESIAN_POINT ( 'NONE',  ( 21.05000000000000071, 76.00000000001172396, -71.42310748452430857 ) ) ;
#192034=ORIENTED_EDGE ( 'NONE', *, *, #153644, .T. ) ;
#192069=DIRECTION ( 'NONE',  ( 0.000000000000000000, 1.000000000000000000, 6.982962677686267499E-15 ) ) ;
#192095=CARTESIAN_POINT ( 'NONE',  ( 20.94999999999999929, 76.00000000001170974, -69.52310748452431710 ) ) ;
#192097=DIRECTION ( 'NONE',  ( 1.000000000000000000, 0.000000000000000000, 0.000000000000000000 ) ) ;
#192113=TOROIDAL_SURFACE ( 'NONE', #71304, 0.2000000000000000111, 0.1000000000000000056 ) ;
#192120=CARTESIAN_POINT ( 'NONE',  ( 23.14999999999999503, 69.35000000001186038, -90.77310748452435973 ) ) ;
#192134=CARTESIAN_POINT ( 'NONE',  ( 21.05543885634738643, 67.22422895316432800, -90.83872301380968395 ) ) ;
#192156=ORIENTED_EDGE ( 'NONE', *, *, #165984, .T. ) ;
#192160=ORIENTED_EDGE ( 'NONE', *, *, #225261, .F. ) ;
#192169=AXIS2_PLACEMENT_3D ( 'NONE', #200126, #59277, #197540 ) ;
#192188=EDGE_CURVE ( 'NONE', #196796, #97301, #55313, .T. ) ;
#192213=AXIS2_PLACEMENT_3D ( 'NONE', #42622, #97429, #21793 ) ;
#192247=ORIENTED_EDGE ( 'NONE', *, *, #164172, .T. ) ;
#192252=ORIENTED_EDGE ( 'NONE', *, *, #195110, .F. ) ;
#192258=DIRECTION ( 'NONE',  ( 0.000000000000000000, 0.000000000000000000, 1.000000000000000000 ) ) ;
#192269=AXIS2_PLACEMENT_3D ( 'NONE', #221961, #102013, #181602 ) ;
#192288=CARTESIAN_POINT ( 'NONE',  ( -18.59999999999999787, 77.83585931145526615, -58.01866831572577610 ) ) ;
#192312=DIRECTION ( 'NONE',  ( 0.000000000000000000, -1.000000000000000000, -6.982962677686265922E-15 ) ) ;
#192372=DIRECTION ( 'NONE',  ( 0.000000000000000000, 6.982962677686266711E-15, -1.000000000000000000 ) ) ;
#192382=VERTEX_POINT ( 'NONE', #128173 ) ;
#192397=CARTESIAN_POINT ( 'NONE',  ( -20.54999999999999716, 74.00000000001180922, -82.74772940728641402 ) ) ;
#192449=EDGE_CURVE ( 'NONE', #223676, #208027, #20882, .T. ) ;
#192451=VECTOR ( 'NONE', #74085, 1000.000000000000000 ) ;
#192463=CARTESIAN_POINT ( 'NONE',  ( 21.05000000000000071, 85.00000000001179501, -79.41707660717668205 ) ) ;
#192512=ORIENTED_EDGE ( 'NONE', *, *, #201225, .T. ) ;
#192539=ORIENTED_EDGE ( 'NONE', *, *, #118914, .F. ) ;
#192547=CARTESIAN_POINT ( 'NONE',  ( 23.14999999999999503, 64.35000000001176090, -76.53791325517833855 ) ) ;
#192548=ORIENTED_EDGE ( 'NONE', *, *, #126539, .T. ) ;
#192566=CARTESIAN_POINT ( 'NONE',  ( 18.39999999999999858, 85.60000000001166143, -62.82291809330219223 ) ) ;
#192568=CARTESIAN_POINT ( 'NONE',  ( 20.95512820512820440, 67.12384868372377866, -94.46447848938342418 ) ) ;
#192596=VECTOR ( 'NONE', #161395, 1000.000000000000000 ) ;
#192604=DIRECTION ( 'NONE',  ( -0.000000000000000000, 0.8700118002898356018, -0.4930308989875170078 ) ) ;
#192607=DIRECTION ( 'NONE',  ( 1.000000000000000000, 0.000000000000000000, -0.000000000000000000 ) ) ;
#192611=ORIENTED_EDGE ( 'NONE', *, *, #125804, .F. ) ;
#192630=CARTESIAN_POINT ( 'NONE',  ( -21.05000000000000071, 77.85102823015273543, -91.36919421510179973 ) ) ;
#192649=EDGE_CURVE ( 'NONE', #85729, #116639, #221492, .T. ) ;
#192716=DIRECTION ( 'NONE',  ( 0.000000000000000000, -1.000000000000000000, 0.000000000000000000 ) ) ;
#192723=ADVANCED_FACE ( 'NONE', ( #111846 ), #74032, .T. ) ;
#192728=CARTESIAN_POINT ( 'NONE',  ( -23.15000000000000213, 64.25000000001203659, -114.7731074845243882 ) ) ;
#192743=CIRCLE ( 'NONE', #76028, 0.1999999999999987899 ) ;
#192753=VERTEX_POINT ( 'NONE', #53143 ) ;
#192782=CIRCLE ( 'NONE', #188494, 11.79999999999999716 ) ;
#192795=AXIS2_PLACEMENT_3D ( 'NONE', #6137, #85646, #227761 ) ;
#192851=VERTEX_POINT ( 'NONE', #841 ) ;
#192857=VERTEX_POINT ( 'NONE', #54424 ) ;
#192866=LINE ( 'NONE', #32535, #105548 ) ;
#192879=ADVANCED_FACE ( 'NONE', ( #216056 ), #37453, .T. ) ;
#192892=EDGE_LOOP ( 'NONE', ( #11067, #210794, #140647, #112519 ) ) ;
#192893=EDGE_LOOP ( 'NONE', ( #168072, #30670, #107900, #147316 ) ) ;
#192895=FACE_OUTER_BOUND ( 'NONE', #211717, .T. ) ;
#192926=AXIS2_PLACEMENT_3D ( 'NONE', #135642, #93955, #116106 ) ;
#192931=DIRECTION ( 'NONE',  ( 1.000000000000000000, 0.000000000000000000, 0.000000000000000000 ) ) ;
#192946=DIRECTION ( 'NONE',  ( 1.000000000000000000, 0.000000000000000000, 0.000000000000000000 ) ) ;
#192972=ORIENTED_EDGE ( 'NONE', *, *, #42049, .F. ) ;
#192976=CIRCLE ( 'NONE', #205400, 0.1000000000000028644 ) ;
#193012=DIRECTION ( 'NONE',  ( 0.000000000000000000, 0.000000000000000000, 1.000000000000000000 ) ) ;
#193036=ADVANCED_FACE ( 'NONE', ( #148090 ), #116512, .T. ) ;
#193050=ADVANCED_FACE ( 'NONE', ( #90664 ), #87266, .T. ) ;
#193077=CARTESIAN_POINT ( 'NONE',  ( -21.00857864376268935, 64.40000000001188596, -96.09490425424884563 ) ) ;
#193112=VECTOR ( 'NONE', #87504, 1000.000000000000000 ) ;
#193136=CIRCLE ( 'NONE', #101498, 11.74999999999999645 ) ;
#193240=ORIENTED_EDGE ( 'NONE', *, *, #435, .T. ) ;
#193294=ORIENTED_EDGE ( 'NONE', *, *, #192649, .F. ) ;
#193314=VECTOR ( 'NONE', #213933, 1000.000000000000000 ) ;
#193317=CARTESIAN_POINT ( 'NONE',  ( 21.05000000000000071, 76.09999993531907592, -109.5011857056189086 ) ) ;
#193343=AXIS2_PLACEMENT_3D ( 'NONE', #146238, #223207, #82393 ) ;
#193349=ADVANCED_FACE ( 'NONE', ( #547 ), #83903, .F. ) ;
#193390=ORIENTED_EDGE ( 'NONE', *, *, #254426, .T. ) ;
#193408=CARTESIAN_POINT ( 'NONE',  ( -21.14999999999999858, 64.35000000001195986, -102.9231074845243938 ) ) ;
#193415=DIRECTION ( 'NONE',  ( 0.000000000000000000, 0.000000000000000000, 1.000000000000000000 ) ) ;
#193423=ORIENTED_EDGE ( 'NONE', *, *, #8165, .F. ) ;
#193429=CARTESIAN_POINT ( 'NONE',  ( 21.05000000000000071, 77.73625713160926409, -91.45445515550680682 ) ) ;
#193434=EDGE_CURVE ( 'NONE', #227881, #123705, #158238, .T. ) ;
#193449=ORIENTED_EDGE ( 'NONE', *, *, #124166, .T. ) ;
#193453=ORIENTED_EDGE ( 'NONE', *, *, #248014, .F. ) ;
#193457=VERTEX_POINT ( 'NONE', #231191 ) ;
#193463=AXIS2_PLACEMENT_3D ( 'NONE', #168101, #224162, #106781 ) ;
#193474=DIRECTION ( 'NONE',  ( -4.408576920032447972E-17, -0.1350103645451946055, 0.9908441862701591329 ) ) ;
#193500=ORIENTED_EDGE ( 'NONE', *, *, #23451, .F. ) ;
#193509=AXIS2_PLACEMENT_3D ( 'NONE', #40670, #221800, #38077 ) ;
#193534=PLANE ( 'NONE',  #212599 ) ;
#193538=DIRECTION ( 'NONE',  ( 0.000000000000000000, -6.982962677686266711E-15, 1.000000000000000000 ) ) ;
#193549=DIRECTION ( 'NONE',  ( 0.000000000000000000, 1.000000000000000000, 6.938893903907222067E-15 ) ) ;
#193554=ADVANCED_FACE ( 'NONE', ( #111220 ), #190792, .F. ) ;
#193574=CIRCLE ( 'NONE', #18771, 0.1000000000000028644 ) ;
#193596=CARTESIAN_POINT ( 'NONE',  ( -18.59999999999999787, 76.00000000001170974, -69.52310748452431710 ) ) ;
#193614=ORIENTED_EDGE ( 'NONE', *, *, #212308, .T. ) ;
#193619=VECTOR ( 'NONE', #250158, 1000.000000000000000 ) ;
#193647=ADVANCED_FACE ( 'NONE', ( #254546 ), #154347, .F. ) ;
#193651=LINE ( 'NONE', #115379, #217689 ) ;
#193675=LINE ( 'NONE', #55403, #109468 ) ;
#193714=CARTESIAN_POINT ( 'NONE',  ( 18.33683296300430854, 85.51114997114436278, -62.61740007181408174 ) ) ;
#193734=EDGE_CURVE ( 'NONE', #232638, #111080, #200083, .T. ) ;
#193738=VERTEX_POINT ( 'NONE', #241447 ) ;
#193749=DIRECTION ( 'NONE',  ( 0.000000000000000000, 0.8700118002898357128, -0.4930308989875170633 ) ) ;
#193756=ORIENTED_EDGE ( 'NONE', *, *, #184409, .F. ) ;
#193763=CARTESIAN_POINT ( 'NONE',  ( -22.49806830649814415, 64.35011034517287953, -103.1005718008498917 ) ) ;
#193770=CARTESIAN_POINT ( 'NONE',  ( 18.49999999999999289, 65.70729864260985664, -64.06574559737245522 ) ) ;
#193777=ORIENTED_EDGE ( 'NONE', *, *, #25622, .F. ) ;
#193791=B_SPLINE_CURVE_WITH_KNOTS ( 'NONE', 3,
 ( #20448, #99934, #830, #140361, #240770, #82933, #178248, #41307, #3413, #80367 ),
 .UNSPECIFIED., .F., .F.,
 ( 4, 3, 3, 4 ),
 ( 0.000000000000000000, 0.0002000000000002908468, 0.001000000000045115191, 0.001967863649472098748 ),
 .UNSPECIFIED. ) ;
#193872=EDGE_CURVE ( 'NONE', #111080, #146711, #41887, .T. ) ;
#193888=EDGE_CURVE ( 'NONE', #158615, #25415, #45951, .T. ) ;
#193911=DIRECTION ( 'NONE',  ( -1.000000000000000000, -0.000000000000000000, -0.000000000000000000 ) ) ;
#193914=CARTESIAN_POINT ( 'NONE',  ( -18.59999999999999787, 74.83729825007388570, -94.92310748452432279 ) ) ;
#193919=CARTESIAN_POINT ( 'NONE',  ( 22.50000000000000000, 75.90000000001202807, -114.6726782920691221 ) ) ;
#193940=DIRECTION ( 'NONE',  ( 0.000000000000000000, 0.000000000000000000, 1.000000000000000000 ) ) ;
#193946=CARTESIAN_POINT ( 'NONE',  ( -23.25000000000000000, 71.85000000001178933, -81.87310748452433984 ) ) ;
#193967=VERTEX_POINT ( 'NONE', #109617 ) ;
#193998=DIRECTION ( 'NONE',  ( -1.000000000000000000, -0.000000000000000000, -0.000000000000000000 ) ) ;
#194020=EDGE_CURVE ( 'NONE', #51208, #129128, #196162, .T. ) ;
#194022=VERTEX_POINT ( 'NONE', #18237 ) ;
#194024=DIRECTION ( 'NONE',  ( -0.000000000000000000, 6.982962677686266711E-15, -1.000000000000000000 ) ) ;
#194027=CARTESIAN_POINT ( 'NONE',  ( -23.25000000000000000, 64.35000000001176090, -76.53791325517833855 ) ) ;
#194030=EDGE_CURVE ( 'NONE', #214994, #254425, #179431, .T. ) ;
#194036=CARTESIAN_POINT ( 'NONE',  ( 20.94999999999999574, 74.83729825007388570, -95.12310748452432563 ) ) ;
#194039=LINE ( 'NONE', #36250, #251582 ) ;
#194040=DIRECTION ( 'NONE',  ( -1.000000000000000000, 0.000000000000000000, -0.000000000000000000 ) ) ;
#194110=DIRECTION ( 'NONE',  ( 0.000000000000000000, 0.000000000000000000, 1.000000000000000000 ) ) ;
#194138=VERTEX_POINT ( 'NONE', #241150 ) ;
#194148=CARTESIAN_POINT ( 'NONE',  ( -21.05000000000000071, 76.00000000001197975, -107.3231074845242716 ) ) ;
#194165=AXIS2_PLACEMENT_3D ( 'NONE', #26613, #203940, #7021 ) ;
#194189=ORIENTED_EDGE ( 'NONE', *, *, #41768, .F. ) ;
#194190=ORIENTED_EDGE ( 'NONE', *, *, #248501, .T. ) ;
#194194=AXIS2_PLACEMENT_3D ( 'NONE', #199530, #239931, #43011 ) ;
#194203=ADVANCED_FACE ( 'NONE', ( #78190 ), #187814, .F. ) ;
#194206=CARTESIAN_POINT ( 'NONE',  ( -23.25000000000000000, 76.00000000001170974, -69.52310748452431710 ) ) ;
#194244=DIRECTION ( 'NONE',  ( 0.000000000000000000, 6.982962677686266711E-15, -1.000000000000000000 ) ) ;
#194273=ORIENTED_EDGE ( 'NONE', *, *, #67528, .T. ) ;
#194287=VECTOR ( 'NONE', #54027, 1000.000000000000000 ) ;
#194326=CYLINDRICAL_SURFACE ( 'NONE', #245453, 0.09999999999999939493 ) ;
#194429=AXIS2_PLACEMENT_3D ( 'NONE', #216019, #256380, #55638 ) ;
#194443=CARTESIAN_POINT ( 'NONE',  ( 20.04142135623730070, 64.25000000001176659, -78.37310748452439668 ) ) ;
#194451=TOROIDAL_SURFACE ( 'NONE', #140220, 0.2000000000000000111, 0.1000000000000000056 ) ;
#194466=FACE_OUTER_BOUND ( 'NONE', #164038, .T. ) ;
#194494=DIRECTION ( 'NONE',  ( 0.000000000000000000, 1.000000000000000000, 6.938893903907222067E-15 ) ) ;
#194496=CIRCLE ( 'NONE', #173685, 1.899999999999999023 ) ;
#194507=VERTEX_POINT ( 'NONE', #92826 ) ;
#194522=ORIENTED_EDGE ( 'NONE', *, *, #247646, .T. ) ;
#194562=CARTESIAN_POINT ( 'NONE',  ( -23.25000000000000000, 76.00000000001195133, -103.0231074845243171 ) ) ;
#194580=LINE ( 'NONE', #17215, #133340 ) ;
#194581=CARTESIAN_POINT ( 'NONE',  ( -22.59999999999999787, 64.25012875563544412, -103.0885370755380706 ) ) ;
#194606=CARTESIAN_POINT ( 'NONE',  ( 21.05000000000000071, 87.65000000001172964, -72.42310748452422331 ) ) ;
#194607=EDGE_CURVE ( 'NONE', #190048, #80064, #29966, .T. ) ;
#194609=ORIENTED_EDGE ( 'NONE', *, *, #126456, .T. ) ;
#194610=VECTOR ( 'NONE', #144424, 1000.000000000000000 ) ;
#194621=CIRCLE ( 'NONE', #148818, 0.1000000000000028644 ) ;
#194622=FACE_OUTER_BOUND ( 'NONE', #4484, .T. ) ;
#194667=SPHERICAL_SURFACE ( 'NONE', #106423, 0.1000000000000000056 ) ;
#194709=CARTESIAN_POINT ( 'NONE',  ( 21.05000000000000071, 67.22371710471938400, -90.87310748452436826 ) ) ;
#194750=DIRECTION ( 'NONE',  ( 8.673617379884087537E-15, 6.982962677686266711E-15, -1.000000000000000000 ) ) ;
#194782=ORIENTED_EDGE ( 'NONE', *, *, #42279, .F. ) ;
#194795=VERTEX_POINT ( 'NONE', #60869 ) ;
#194817=EDGE_LOOP ( 'NONE', ( #252754, #44468, #242671, #159125 ) ) ;
#194823=ORIENTED_EDGE ( 'NONE', *, *, #77629, .T. ) ;
#194832=CARTESIAN_POINT ( 'NONE',  ( -21.05000000000000071, 76.00000000001192291, -98.72310748452436258 ) ) ;
#194834=EDGE_CURVE ( 'NONE', #158368, #189878, #97402, .T. ) ;
#194837=DIRECTION ( 'NONE',  ( 0.000000000000000000, -0.01562499999999307672, 0.9998779222360100194 ) ) ;
#194894=CIRCLE ( 'NONE', #257348, 0.1000000000000028644 ) ;
#194951=DIRECTION ( 'NONE',  ( 0.000000000000000000, 0.9654727137038715545, -0.2605042016806676242 ) ) ;
#194987=ORIENTED_EDGE ( 'NONE', *, *, #236842, .F. ) ;
#195010=LINE ( 'NONE', #256174, #156259 ) ;
#195014=DIRECTION ( 'NONE',  ( 2.952720810173289112E-16, 1.000000000000000000, 6.982962677686266711E-15 ) ) ;
#195036=ORIENTED_EDGE ( 'NONE', *, *, #87118, .F. ) ;
#195056=ORIENTED_EDGE ( 'NONE', *, *, #101141, .T. ) ;
#195061=AXIS2_PLACEMENT_3D ( 'NONE', #122411, #84508, #204492 ) ;
#195094=CARTESIAN_POINT ( 'NONE',  ( -20.94999999999999929, 76.00000000001170974, -69.52310748452431710 ) ) ;
#195096=CARTESIAN_POINT ( 'NONE',  ( 21.14999999999999858, 64.35000000001201670, -114.7731074845243882 ) ) ;
#195099=DIRECTION ( 'NONE',  ( 0.000000000000000000, 0.000000000000000000, 1.000000000000000000 ) ) ;
#195103=DIRECTION ( 'NONE',  ( -0.000000000000000000, -0.9876197685951290106, 0.1568667991644625281 ) ) ;
#195107=AXIS2_PLACEMENT_3D ( 'NONE', #41998, #36877, #39442 ) ;
#195110=EDGE_CURVE ( 'NONE', #59708, #113902, #38504, .T. ) ;
#195117=EDGE_CURVE ( 'NONE', #129506, #134706, #30767, .T. ) ;
#195127=CARTESIAN_POINT ( 'NONE',  ( -21.44999999999999929, 68.65000000001180069, -81.77310748452435973 ) ) ;
#195193=CARTESIAN_POINT ( 'NONE',  ( -18.59999999999999787, 66.85000000001180354, -81.87310748452438247 ) ) ;
#195198=VERTEX_POINT ( 'NONE', #157130 ) ;
#195261=EDGE_LOOP ( 'NONE', ( #20592, #142004, #197339, #126719 ) ) ;
#195265=DIRECTION ( 'NONE',  ( 1.000000000000000000, 0.000000000000000000, 0.000000000000000000 ) ) ;
#195271=EDGE_CURVE ( 'NONE', #90102, #156170, #215775, .T. ) ;
#195284=DIRECTION ( 'NONE',  ( 0.000000000000000000, 0.000000000000000000, 1.000000000000000000 ) ) ;
#195302=DIRECTION ( 'NONE',  ( -1.000000000000000000, 2.952720810173289112E-16, 2.061873921506763405E-30 ) ) ;
#195327=CARTESIAN_POINT ( 'NONE',  ( 23.24999999999999289, 64.35000000001201670, -114.7731074845243882 ) ) ;
#195328=DIRECTION ( 'NONE',  ( -1.000000000000000000, 0.000000000000000000, 0.000000000000000000 ) ) ;
#195339=ADVANCED_FACE ( 'NONE', ( #158426 ), #46855, .F. ) ;
#195355=CARTESIAN_POINT ( 'NONE',  ( 20.85000000000000142, 68.97833521811159585, -65.68954208262705663 ) ) ;
#195370=CARTESIAN_POINT ( 'NONE',  ( 18.39999999999999858, 85.51932773110434027, -96.05013110796491560 ) ) ;
#195387=VERTEX_POINT ( 'NONE', #159685 ) ;
#195396=CARTESIAN_POINT ( 'NONE',  ( 20.94999999999999929, 87.65000000001170122, -69.52310748452424605 ) ) ;
#195426=ORIENTED_EDGE ( 'NONE', *, *, #82554, .T. ) ;
#195438=DIRECTION ( 'NONE',  ( -1.000000000000000000, 3.265361837132813093E-16, 2.280189983783949500E-30 ) ) ;
#195452=DIRECTION ( 'NONE',  ( -1.000000000000000000, 0.000000000000000000, 0.000000000000000000 ) ) ;
#195461=ORIENTED_EDGE ( 'NONE', *, *, #81322, .T. ) ;
#195497=VERTEX_POINT ( 'NONE', #171290 ) ;
#195499=CARTESIAN_POINT ( 'NONE',  ( -21.44999999999999929, 68.65000000001187175, -90.67310748452436542 ) ) ;
#195519=ORIENTED_EDGE ( 'NONE', *, *, #251995, .T. ) ;
#195526=DIRECTION ( 'NONE',  ( 0.000000000000000000, -1.000000000000000000, 0.000000000000000000 ) ) ;
#195538=CARTESIAN_POINT ( 'NONE',  ( 21.14261333020286315, 65.28430735075696134, -90.77310748452416078 ) ) ;
#195559=CARTESIAN_POINT ( 'NONE',  ( -18.59999999999999787, 64.40000000001188596, -96.09490425424884563 ) ) ;
#195575=CARTESIAN_POINT ( 'NONE',  ( -21.04999999999999716, 85.60000000001190301, -95.99103808782457747 ) ) ;
#195579=DIRECTION ( 'NONE',  ( -1.000000000000000000, 0.000000000000000000, 0.000000000000000000 ) ) ;
#195607=ORIENTED_EDGE ( 'NONE', *, *, #34925, .T. ) ;
#195612=DIRECTION ( 'NONE',  ( -1.000000000000000000, -0.000000000000000000, -0.000000000000000000 ) ) ;
#195614=CARTESIAN_POINT ( 'NONE',  ( 23.14999999999999858, 69.35000000001186038, -90.67310748452435121 ) ) ;
#195625=VECTOR ( 'NONE', #36801, 1000.000000000000000 ) ;
#195627=CARTESIAN_POINT ( 'NONE',  ( -22.50047199487955041, 75.95509394809238302, -114.7731549034439524 ) ) ;
#195631=DIRECTION ( 'NONE',  ( -1.000000000000000000, -0.000000000000000000, -0.000000000000000000 ) ) ;
#195673=FACE_OUTER_BOUND ( 'NONE', #150911, .T. ) ;
#195682=DIRECTION ( 'NONE',  ( 0.000000000000000000, 0.000000000000000000, 1.000000000000000000 ) ) ;
#195690=CYLINDRICAL_SURFACE ( 'NONE', #164045, 0.09999999999999939493 ) ;
#195730=DIRECTION ( 'NONE',  ( 0.000000000000000000, 0.01283462868040226822, 0.9999176327611370985 ) ) ;
#195745=EDGE_CURVE ( 'NONE', #190290, #23758, #142716, .T. ) ;
#195778=ORIENTED_EDGE ( 'NONE', *, *, #220416, .F. ) ;
#195793=EDGE_LOOP ( 'NONE', ( #74277, #169198, #196158, #217157 ) ) ;
#195812=EDGE_CURVE ( 'NONE', #215983, #90102, #163237, .T. ) ;
#195822=AXIS2_PLACEMENT_3D ( 'NONE', #114825, #24746, #26006 ) ;
#195836=DIRECTION ( 'NONE',  ( 0.000000000000000000, -6.982962677686266711E-15, 1.000000000000000000 ) ) ;
#195841=DIRECTION ( 'NONE',  ( 0.000000000000000000, -6.982962677686266711E-15, 1.000000000000000000 ) ) ;
#195843=ORIENTED_EDGE ( 'NONE', *, *, #122167, .T. ) ;
#195848=TOROIDAL_SURFACE ( 'NONE', #175027, 0.6000000000000009770, 0.1000000000000000056 ) ;
#195859=CARTESIAN_POINT ( 'NONE',  ( -23.15000000000000213, 74.00000000001180922, -82.74772940728641402 ) ) ;
#195882=CARTESIAN_POINT ( 'NONE',  ( -20.64999999999999858, 74.05981308412400210, -90.19398827347099257 ) ) ;
#195937=DIRECTION ( 'NONE',  ( 0.000000000000000000, 0.000000000000000000, 1.000000000000000000 ) ) ;
#195944=TOROIDAL_SURFACE ( 'NONE', #237625, 0.4000000000000012990, 0.1000000000000000056 ) ;
#195965=SPHERICAL_SURFACE ( 'NONE', #60066, 0.1000000000000000056 ) ;
#195966=PLANE ( 'NONE',  #247079 ) ;
#195969=AXIS2_PLACEMENT_3D ( 'NONE', #183410, #59564, #202961 ) ;
#196023=DIRECTION ( 'NONE',  ( 0.000000000000000000, 0.000000000000000000, 1.000000000000000000 ) ) ;
#196036=FACE_OUTER_BOUND ( 'NONE', #65142, .T. ) ;
#196037=ORIENTED_EDGE ( 'NONE', *, *, #139499, .F. ) ;
#196050=CARTESIAN_POINT ( 'NONE',  ( 18.49999999999999645, 74.26374286841446803, -91.45445515550682103 ) ) ;
#196074=CARTESIAN_POINT ( 'NONE',  ( 23.14999999999999858, 72.00000000001170974, -69.52310748452433131 ) ) ;
#196078=DIRECTION ( 'NONE',  ( 0.000000000000000000, -0.6728971962616412394, 0.7397360091703134577 ) ) ;
#196079=ORIENTED_EDGE ( 'NONE', *, *, #178054, .F. ) ;
#196101=VERTEX_POINT ( 'NONE', #41383 ) ;
#196158=ORIENTED_EDGE ( 'NONE', *, *, #124166, .F. ) ;
#196162=CIRCLE ( 'NONE', #162879, 4.099999999999992539 ) ;
#196167=VERTEX_POINT ( 'NONE', #202990 ) ;
#196181=CYLINDRICAL_SURFACE ( 'NONE', #57733, 0.09999999999999939493 ) ;
#196212=FACE_OUTER_BOUND ( 'NONE', #179977, .T. ) ;
#196224=CARTESIAN_POINT ( 'NONE',  ( -20.00857864376270001, 66.85000000001180354, -81.87310748452438247 ) ) ;
#196259=ORIENTED_EDGE ( 'NONE', *, *, #205928, .T. ) ;
#196264=CARTESIAN_POINT ( 'NONE',  ( 20.94999999999999574, 77.25000000001189449, -95.02310748452430289 ) ) ;
#196275=LINE ( 'NONE', #214549, #206195 ) ;
#196284=ORIENTED_EDGE ( 'NONE', *, *, #80591, .T. ) ;
#196298=CARTESIAN_POINT ( 'NONE',  ( -20.15000000000000568, 66.70857864377450142, -81.77310748452437394 ) ) ;
#196302=DIRECTION ( 'NONE',  ( 0.000000000000000000, -7.086529944415894657E-15, 1.000000000000000000 ) ) ;
#196321=AXIS2_PLACEMENT_3D ( 'NONE', #63033, #23946, #181715 ) ;
#196322=CYLINDRICAL_SURFACE ( 'NONE', #110431, 0.1000000000000052097 ) ;
#196323=EDGE_CURVE ( 'NONE', #37627, #10839, #153338, .T. ) ;
#196332=AXIS2_PLACEMENT_3D ( 'NONE', #199570, #20932, #121330 ) ;
#196336=CARTESIAN_POINT ( 'NONE',  ( 23.25000000000000000, 87.75000000001202238, -114.7731074845242318 ) ) ;
#196344=EDGE_LOOP ( 'NONE', ( #36925, #59906, #209537, #132034 ) ) ;
#196349=DIRECTION ( 'NONE',  ( -0.000000000000000000, 1.000000000000000000, 6.982962677686266711E-15 ) ) ;
#196356=AXIS2_PLACEMENT_3D ( 'NONE', #60911, #222543, #140446 ) ;
#196381=EDGE_CURVE ( 'NONE', #165593, #113902, #195010, .T. ) ;
#196454=DIRECTION ( 'NONE',  ( 1.000000000000000000, 0.000000000000000000, 0.000000000000000000 ) ) ;
#196457=CARTESIAN_POINT ( 'NONE',  ( 20.94999999999999929, 85.00000000001179501, -79.41707660717668205 ) ) ;
#196468=CIRCLE ( 'NONE', #108981, 0.2000000000000057288 ) ;
#196487=ORIENTED_EDGE ( 'NONE', *, *, #196381, .T. ) ;
#196496=CARTESIAN_POINT ( 'NONE',  ( 18.59999999999999787, 86.35479209693714608, -75.76656650145046967 ) ) ;
#196534=ORIENTED_EDGE ( 'NONE', *, *, #84274, .F. ) ;
#196572=CARTESIAN_POINT ( 'NONE',  ( -23.25000000000000000, 85.00000000001188027, -93.12913836187181005 ) ) ;
#196580=ADVANCED_FACE ( 'NONE', ( #223521, #161008 ), #164862, .F. ) ;
#196615=CARTESIAN_POINT ( 'NONE',  ( 21.07954763557401634, 69.67070900997461536, -103.0889834031428620 ) ) ;
#196645=DIRECTION ( 'NONE',  ( 0.000000000000000000, -7.056502275159890043E-15, 1.000000000000000000 ) ) ;
#196650=VECTOR ( 'NONE', #126686, 1000.000000000000000 ) ;
#196726=ORIENTED_EDGE ( 'NONE', *, *, #153064, .F. ) ;
#196750=ORIENTED_EDGE ( 'NONE', *, *, #13535, .T. ) ;
#196796=VERTEX_POINT ( 'NONE', #138537 ) ;
#196809=CARTESIAN_POINT ( 'NONE',  ( 23.15000000000000213, 87.65000000001172964, -72.62310748452422615 ) ) ;
#196835=SPHERICAL_SURFACE ( 'NONE', #228478, 0.1000000000000000056 ) ;
#196844=CARTESIAN_POINT ( 'NONE',  ( 18.54286124688534088, 85.62391757880946841, -62.78190515266153682 ) ) ;
#196863=AXIS2_PLACEMENT_3D ( 'NONE', #106913, #166937, #226866 ) ;
#196864=DIRECTION ( 'NONE',  ( 0.000000000000000000, -6.938893903907222067E-15, 1.000000000000000000 ) ) ;
#196865=EDGE_CURVE ( 'NONE', #2197, #243331, #83684, .T. ) ;
#196868=AXIS2_PLACEMENT_3D ( 'NONE', #125995, #243376, #146831 ) ;
#196904=ORIENTED_EDGE ( 'NONE', *, *, #115962, .F. ) ;
#196910=VECTOR ( 'NONE', #182583, 1000.000000000000000 ) ;
#196936=CARTESIAN_POINT ( 'NONE',  ( -20.94999999999999929, 87.39257802171739797, -72.59705706435616435 ) ) ;
#196987=DIRECTION ( 'NONE',  ( -0.000000000000000000, 0.8660254037844424824, 0.4999999999999934497 ) ) ;
#197008=DIRECTION ( 'NONE',  ( 0.000000000000000000, 0.4999999999999689138, -0.8660254037844565822 ) ) ;
#197051=AXIS2_PLACEMENT_3D ( 'NONE', #126610, #91352, #169639 ) ;
#197053=DIRECTION ( 'NONE',  ( 0.000000000000000000, 7.147358527629766941E-15, -1.000000000000000000 ) ) ;
#197078=DIRECTION ( 'NONE',  ( 1.000000000000000000, 0.000000000000000000, 0.000000000000000000 ) ) ;
#197094=EDGE_LOOP ( 'NONE', ( #79045, #113050, #40778, #83732 ) ) ;
#197100=DIRECTION ( 'NONE',  ( 0.000000000000000000, -6.982962677686266711E-15, 1.000000000000000000 ) ) ;
#197116=EDGE_CURVE ( 'NONE', #201392, #192382, #27647, .T. ) ;
#197121=ORIENTED_EDGE ( 'NONE', *, *, #112105, .T. ) ;
#197126=CARTESIAN_POINT ( 'NONE',  ( 20.85000000000000142, 77.26327546522891510, -61.62124281777789037 ) ) ;
#197131=CARTESIAN_POINT ( 'NONE',  ( 22.50000000000000000, 75.90000000001202807, -114.6726782920691221 ) ) ;
#197169=EDGE_CURVE ( 'NONE', #11088, #191619, #163995, .T. ) ;
#197192=CARTESIAN_POINT ( 'NONE',  ( 21.11344571971268635, 65.38212097649370946, -90.77708659212511577 ) ) ;
#197276=VECTOR ( 'NONE', #70689, 1000.000000000000114 ) ;
#197279=AXIS2_PLACEMENT_3D ( 'NONE', #18991, #239339, #163655 ) ;
#197298=CARTESIAN_POINT ( 'NONE',  ( -18.44204374631833687, 85.49103638961001650, -62.89690621430324313 ) ) ;
#197313=DIRECTION ( 'NONE',  ( 0.000000000000000000, 0.000000000000000000, 1.000000000000000000 ) ) ;
#197322=CARTESIAN_POINT ( 'NONE',  ( 20.94999999999999929, 71.00000000001180922, -81.92837350343744163 ) ) ;
#197328=CIRCLE ( 'NONE', #118233, 0.1000000000000028644 ) ;
#197339=ORIENTED_EDGE ( 'NONE', *, *, #196323, .T. ) ;
#197370=DIRECTION ( 'NONE',  ( 0.000000000000000000, -7.056502275159890832E-15, 1.000000000000000000 ) ) ;
#197384=FACE_OUTER_BOUND ( 'NONE', #197447, .T. ) ;
#197432=CIRCLE ( 'NONE', #84989, 0.1000000000000028644 ) ;
#197442=ADVANCED_FACE ( 'NONE', ( #11602 ), #170712, .T. ) ;
#197447=EDGE_LOOP ( 'NONE', ( #62445, #76037, #158756, #163923 ) ) ;
#197460=DIRECTION ( 'NONE',  ( -0.000000000000000000, -1.000000000000000000, -6.982962677686266711E-15 ) ) ;
#197470=EDGE_CURVE ( 'NONE', #221237, #202146, #7743, .T. ) ;
#197473=CARTESIAN_POINT ( 'NONE',  ( -21.30740335185486245, 75.90106547423613392, -109.5797654065523119 ) ) ;
#197477=LINE ( 'NONE', #177940, #128498 ) ;
#197485=DIRECTION ( 'NONE',  ( 1.000000000000000000, 0.000000000000000000, 0.000000000000000000 ) ) ;
#197488=CARTESIAN_POINT ( 'NONE',  ( 22.39999999999999503, 64.25000000001193712, -103.1231074845243825 ) ) ;
#197507=CARTESIAN_POINT ( 'NONE',  ( -18.59999999999999787, 74.83729825007388570, -95.02310748452431710 ) ) ;
#197521=VECTOR ( 'NONE', #108389, 1000.000000000000114 ) ;
#197540=DIRECTION ( 'NONE',  ( 0.000000000000000000, 0.000000000000000000, -1.000000000000000000 ) ) ;
#197542=CARTESIAN_POINT ( 'NONE',  ( -20.94999999999999929, 87.29603075034721371, -99.97520832486037534 ) ) ;
#197574=VERTEX_POINT ( 'NONE', #46215 ) ;
#197654=ORIENTED_EDGE ( 'NONE', *, *, #70378, .F. ) ;
#197691=CIRCLE ( 'NONE', #106105, 0.1000000000000028644 ) ;
#197702=ORIENTED_EDGE ( 'NONE', *, *, #124477, .T. ) ;
#197758=CIRCLE ( 'NONE', #68770, 0.1000000000000028644 ) ;
#197767=FACE_OUTER_BOUND ( 'NONE', #70825, .T. ) ;
#197794=CIRCLE ( 'NONE', #181260, 0.1000000000000028644 ) ;
#197802=ADVANCED_FACE ( 'NONE', ( #53932 ), #160099, .T. ) ;
#197808=ORIENTED_EDGE ( 'NONE', *, *, #208401, .F. ) ;
#197809=EDGE_CURVE ( 'NONE', #196796, #72101, #152917, .T. ) ;
#197849=DIRECTION ( 'NONE',  ( 1.000000000000000000, 0.000000000000000000, 0.000000000000000000 ) ) ;
#197859=LINE ( 'NONE', #19231, #18935 ) ;
#197893=DIRECTION ( 'NONE',  ( 1.000000000000000000, 0.000000000000000000, 0.000000000000000000 ) ) ;
#197924=LINE ( 'NONE', #231956, #156029 ) ;
#197959=CARTESIAN_POINT ( 'NONE',  ( -20.54999999999999716, 85.00000000001179501, -79.01707660717669057 ) ) ;
#198011=ORIENTED_EDGE ( 'NONE', *, *, #81845, .T. ) ;
#198036=DIRECTION ( 'NONE',  ( 1.000000000000000000, 0.000000000000000000, 0.000000000000000000 ) ) ;
#198050=ADVANCED_FACE ( 'NONE', ( #62920 ), #220283, .F. ) ;
#198065=FACE_OUTER_BOUND ( 'NONE', #5096, .T. ) ;
#198067=EDGE_CURVE ( 'NONE', #72101, #246385, #97866, .T. ) ;
#198107=CARTESIAN_POINT ( 'NONE',  ( -23.25000000000000000, 87.75000000001172396, -69.52310748452423184 ) ) ;
#198126=EDGE_CURVE ( 'NONE', #155597, #42984, #161601, .T. ) ;
#198162=DIRECTION ( 'NONE',  ( 1.000000000000000000, 0.000000000000000000, 0.000000000000000000 ) ) ;
#198172=DIRECTION ( 'NONE',  ( -1.000000000000000000, -0.000000000000000000, -0.000000000000000000 ) ) ;
#198218=TOROIDAL_SURFACE ( 'NONE', #210685, 7.800000000000000711, 0.1000000000000000056 ) ;
#198231=ORIENTED_EDGE ( 'NONE', *, *, #812, .F. ) ;
#198287=CARTESIAN_POINT ( 'NONE',  ( 22.49999999999999645, 75.89914163091330579, -114.7726746080137161 ) ) ;
#198311=VECTOR ( 'NONE', #128810, 1000.000000000000000 ) ;
#198315=CARTESIAN_POINT ( 'NONE',  ( 21.05000000000000071, 74.83729825007388570, -95.12310748452432563 ) ) ;
#198364=ORIENTED_EDGE ( 'NONE', *, *, #115588, .T. ) ;
#198390=ORIENTED_EDGE ( 'NONE', *, *, #138006, .T. ) ;
#198423=DIRECTION ( 'NONE',  ( 0.000000000000000000, -0.6728971962616412394, -0.7397360091703134577 ) ) ;
#198425=CARTESIAN_POINT ( 'NONE',  ( 22.39999999999999503, 76.00000000001203659, -114.6726782920691221 ) ) ;
#198436=FACE_OUTER_BOUND ( 'NONE', #169222, .T. ) ;
#198455=CIRCLE ( 'NONE', #252612, 0.1000000000000028644 ) ;
#198481=DIRECTION ( 'NONE',  ( 0.000000000000000000, -1.000000000000000000, 0.000000000000000000 ) ) ;
#198507=ORIENTED_EDGE ( 'NONE', *, *, #253126, .T. ) ;
#198519=AXIS2_PLACEMENT_3D ( 'NONE', #11857, #133071, #109635 ) ;
#198521=DIRECTION ( 'NONE',  ( 0.000000000000000000, 6.769652589177795712E-15, -1.000000000000000000 ) ) ;
#198563=CARTESIAN_POINT ( 'NONE',  ( 18.59999999999999076, 69.55000000001187743, -93.00608031408432907 ) ) ;
#198583=CARTESIAN_POINT ( 'NONE',  ( -18.40000000000000213, 85.50000000001168132, -62.60095763519382928 ) ) ;
#198585=CARTESIAN_POINT ( 'NONE',  ( 22.47071067811864609, 68.27992525551390202, -103.1221999392269595 ) ) ;
#198592=ORIENTED_EDGE ( 'NONE', *, *, #221033, .F. ) ;
#198600=EDGE_CURVE ( 'NONE', #28459, #215370, #173150, .T. ) ;
#198607=CARTESIAN_POINT ( 'NONE',  ( -21.05000000000000071, 87.41227409416161720, -100.0231074845242318 ) ) ;
#198639=DIRECTION ( 'NONE',  ( -1.000000000000000000, 0.000000000000000000, -0.000000000000000000 ) ) ;
#198642=CARTESIAN_POINT ( 'NONE',  ( -21.05000000000000071, 87.48912529308779540, -72.52310748452423184 ) ) ;
#198713=DIRECTION ( 'NONE',  ( 1.000000000000000000, -7.304098846218135653E-16, -5.100424963727256530E-30 ) ) ;
#198720=FACE_OUTER_BOUND ( 'NONE', #43711, .T. ) ;
#198742=AXIS2_PLACEMENT_3D ( 'NONE', #216411, #37805, #33976 ) ;
#198759=CARTESIAN_POINT ( 'NONE',  ( -22.42357213249529124, 75.90091303601045070, -110.6960398708842490 ) ) ;
#198801=AXIS2_PLACEMENT_3D ( 'NONE', #222859, #143322, #44242 ) ;
#198830=FACE_OUTER_BOUND ( 'NONE', #138164, .T. ) ;
#198831=LINE ( 'NONE', #237952, #96989 ) ;
#198880=DIRECTION ( 'NONE',  ( 1.000000000000000000, 0.000000000000000000, -0.000000000000000000 ) ) ;
#198908=ADVANCED_FACE ( 'NONE', ( #34305 ), #194667, .T. ) ;
#198910=ADVANCED_FACE ( 'NONE', ( #113809 ), #24233, .F. ) ;
#198932=DIRECTION ( 'NONE',  ( 0.000000000000000000, 0.8068669527896844551, 0.5907332058517525963 ) ) ;
#198957=CARTESIAN_POINT ( 'NONE',  ( -18.59999999999999787, 77.16270174994990327, -95.02310748452430289 ) ) ;
#198961=TOROIDAL_SURFACE ( 'NONE', #15669, 1.900000000000002576, 0.1000000000000000056 ) ;
#198976=FACE_OUTER_BOUND ( 'NONE', #135781, .T. ) ;
#198982=DIRECTION ( 'NONE',  ( 0.000000000000000000, 0.000000000000000000, 1.000000000000000000 ) ) ;
#198986=EDGE_CURVE ( 'NONE', #161497, #123658, #2830, .T. ) ;
#198995=EDGE_LOOP ( 'NONE', ( #175530, #235076, #175750, #147129 ) ) ;
#199047=VERTEX_POINT ( 'NONE', #141086 ) ;
#199065=DIRECTION ( 'NONE',  ( 0.000000000000000000, -6.454785026890406770E-15, 1.000000000000000000 ) ) ;
#199089=CARTESIAN_POINT ( 'NONE',  ( 18.49999999999999645, 76.00000000001170974, -69.52310748452431710 ) ) ;
#199102=VERTEX_POINT ( 'NONE', #246587 ) ;
#199147=CARTESIAN_POINT ( 'NONE',  ( 18.50016250449482413, 65.70233904877102304, -64.04874109119650427 ) ) ;
#199159=FACE_OUTER_BOUND ( 'NONE', #124607, .T. ) ;
#199230=AXIS2_PLACEMENT_3D ( 'NONE', #172137, #50834, #147395 ) ;
#199276=CARTESIAN_POINT ( 'NONE',  ( 20.94999999999999574, 62.00000000001190870, -97.59601495414186445 ) ) ;
#199281=CARTESIAN_POINT ( 'NONE',  ( -20.94999999999999929, 87.65000000001171543, -69.52310748452423184 ) ) ;
#199310=CARTESIAN_POINT ( 'NONE',  ( 21.00000000000000000, 66.25000000001179501, -81.87310748452438247 ) ) ;
#199332=VERTEX_POINT ( 'NONE', #112241 ) ;
#199361=AXIS2_PLACEMENT_3D ( 'NONE', #252688, #194040, #82693 ) ;
#199403=ORIENTED_EDGE ( 'NONE', *, *, #100280, .T. ) ;
#199442=ADVANCED_FACE ( 'NONE', ( #100333 ), #161646, .T. ) ;
#199461=CARTESIAN_POINT ( 'NONE',  ( 23.15000000000000213, 87.39257802171739797, -72.59705706435616435 ) ) ;
#199470=ORIENTED_EDGE ( 'NONE', *, *, #105086, .T. ) ;
#199505=ORIENTED_EDGE ( 'NONE', *, *, #51991, .F. ) ;
#199506=CARTESIAN_POINT ( 'NONE',  ( 23.14999999999999858, 76.00000000001170974, -69.52310748452431710 ) ) ;
#199515=CARTESIAN_POINT ( 'NONE',  ( -23.15000000000000213, 74.00000000001186606, -89.79848556176222019 ) ) ;
#199527=DIRECTION ( 'NONE',  ( 0.000000000000000000, 6.982962677686266711E-15, -1.000000000000000000 ) ) ;
#199530=CARTESIAN_POINT ( 'NONE',  ( 21.05000000000000071, 76.00000000001195133, -103.0231074845243171 ) ) ;
#199558=CARTESIAN_POINT ( 'NONE',  ( 18.59999999999999076, 69.35000000001180354, -81.77310748452435973 ) ) ;
#199570=CARTESIAN_POINT ( 'NONE',  ( -23.15000000000000213, 85.00000000001179501, -79.41707660717668205 ) ) ;
#199574=DIRECTION ( 'NONE',  ( -1.000000000000000000, 1.836970198721029934E-16, 1.601412966608202925E-30 ) ) ;
#199612=EDGE_CURVE ( 'NONE', #37627, #22332, #68862, .T. ) ;
#199641=DIRECTION ( 'NONE',  ( 0.000000000000000000, 6.982962677686266711E-15, -1.000000000000000000 ) ) ;
#199644=DIRECTION ( 'NONE',  ( 0.000000000000000000, 0.000000000000000000, 1.000000000000000000 ) ) ;
#199646=ORIENTED_EDGE ( 'NONE', *, *, #212999, .F. ) ;
#199663=EDGE_CURVE ( 'NONE', #64319, #72979, #39649, .T. ) ;
#199675=CARTESIAN_POINT ( 'NONE',  ( -18.45068461519106506, 85.48650652910100689, -95.95433031561951509 ) ) ;
#199687=LINE ( 'NONE', #21052, #45637 ) ;
#199701=ORIENTED_EDGE ( 'NONE', *, *, #78336, .T. ) ;
#199710=ORIENTED_EDGE ( 'NONE', *, *, #50853, .T. ) ;
#199716=AXIS2_PLACEMENT_3D ( 'NONE', #153699, #15430, #229339 ) ;
#199757=FACE_OUTER_BOUND ( 'NONE', #186051, .T. ) ;
#199823=FACE_OUTER_BOUND ( 'NONE', #168794, .T. ) ;
#199851=CARTESIAN_POINT ( 'NONE',  ( -23.15000000000000213, 87.65000000001195701, -103.0231074845242318 ) ) ;
#199860=CIRCLE ( 'NONE', #141742, 0.1000000000000028644 ) ;
#199864=EDGE_CURVE ( 'NONE', #82161, #85729, #197859, .T. ) ;
#199878=CARTESIAN_POINT ( 'NONE',  ( 23.15000000000000213, 87.75000000001173817, -72.62310748452422615 ) ) ;
#199880=ORIENTED_EDGE ( 'NONE', *, *, #204784, .T. ) ;
#199884=CARTESIAN_POINT ( 'NONE',  ( 21.14999999999999858, 76.00000000001200817, -109.5637644362255685 ) ) ;
#199896=CARTESIAN_POINT ( 'NONE',  ( -18.33981767444248945, 85.56957578981656809, -62.70394564079953881 ) ) ;
#199897=CARTESIAN_POINT ( 'NONE',  ( 21.00023020733438273, 69.60913075474422840, -103.0231074845243597 ) ) ;
#199905=CARTESIAN_POINT ( 'NONE',  ( -20.94999999999999929, 65.70729864260985664, -64.06574559737245522 ) ) ;
#199971=LINE ( 'NONE', #63004, #251182 ) ;
#200027=CARTESIAN_POINT ( 'NONE',  ( 20.58091095332318332, 66.98152984665945553, -94.60445730236581596 ) ) ;
#200031=ORIENTED_EDGE ( 'NONE', *, *, #181647, .T. ) ;
#200041=CARTESIAN_POINT ( 'NONE',  ( 20.85000000000000142, 76.00000000001170974, -69.52310748452431710 ) ) ;
#200045=FACE_OUTER_BOUND ( 'NONE', #153475, .T. ) ;
#200059=CARTESIAN_POINT ( 'NONE',  ( -22.14074124539699895, 75.90094710416794044, -110.4131853355680875 ) ) ;
#200060=CARTESIAN_POINT ( 'NONE',  ( 21.14999999999999503, 76.10085836911075319, -114.7726746080137019 ) ) ;
#200069=EDGE_CURVE ( 'NONE', #66389, #71706, #94597, .T. ) ;
#200073=VECTOR ( 'NONE', #122201, 1000.000000000000000 ) ;
#200083=CIRCLE ( 'NONE', #141800, 0.1000000000000028644 ) ;
#200097=EDGE_CURVE ( 'NONE', #225545, #47226, #219037, .T. ) ;
#200126=CARTESIAN_POINT ( 'NONE',  ( -18.50000000000000000, 68.97833521811159585, -65.68954208262705663 ) ) ;
#200172=ADVANCED_FACE ( 'NONE', ( #236673 ), #81434, .F. ) ;
#200173=LINE ( 'NONE', #21541, #66977 ) ;
#200235=ORIENTED_EDGE ( 'NONE', *, *, #163903, .T. ) ;
#200241=CIRCLE ( 'NONE', #241922, 0.1000000000000028644 ) ;
#200266=CARTESIAN_POINT ( 'NONE',  ( -23.25000000000000000, 74.00000000001180922, -82.74772940728641402 ) ) ;
#200306=DIRECTION ( 'NONE',  ( 1.000000000000000000, 0.000000000000000000, 0.000000000000000000 ) ) ;
#200307=AXIS2_PLACEMENT_3D ( 'NONE', #192547, #229104, #109136 ) ;
#200310=ADVANCED_FACE ( 'NONE', ( #1910 ), #61909, .T. ) ;
#200329=VERTEX_POINT ( 'NONE', #60604 ) ;
#200355=DIRECTION ( 'NONE',  ( -0.000000000000000000, -1.000000000000000000, -6.982962677686266711E-15 ) ) ;
#200366=AXIS2_PLACEMENT_3D ( 'NONE', #229084, #50411, #205643 ) ;
#200371=CARTESIAN_POINT ( 'NONE',  ( 22.39999999999999503, 68.20922040163857503, -103.0231074845243739 ) ) ;
#200375=CARTESIAN_POINT ( 'NONE',  ( 18.50000000000000000, 85.40000000001165859, -62.64106563635156277 ) ) ;
#200379=CARTESIAN_POINT ( 'NONE',  ( -21.64999999999999858, 68.75000000001179501, -81.87310748452436826 ) ) ;
#200382=CIRCLE ( 'NONE', #254515, 11.64999999999999325 ) ;
#200404=DIRECTION ( 'NONE',  ( 0.000000000000000000, -1.000000000000000000, -6.982962677686265922E-15 ) ) ;
#200419=EDGE_CURVE ( 'NONE', #174804, #43089, #35914, .T. ) ;
#200428=DIRECTION ( 'NONE',  ( 1.000000000000000000, 0.000000000000000000, 0.000000000000000000 ) ) ;
#200442=CARTESIAN_POINT ( 'NONE',  ( -21.05000000000000071, 77.83534155023627932, -91.46795619196132066 ) ) ;
#200454=FACE_OUTER_BOUND ( 'NONE', #205058, .T. ) ;
#200455=ORIENTED_EDGE ( 'NONE', *, *, #156232, .F. ) ;
#200486=VERTEX_POINT ( 'NONE', #212976 ) ;
#200492=EDGE_CURVE ( 'NONE', #76326, #110160, #52606, .T. ) ;
#200494=FACE_OUTER_BOUND ( 'NONE', #64717, .T. ) ;
#200591=ORIENTED_EDGE ( 'NONE', *, *, #150844, .T. ) ;
#200628=AXIS2_PLACEMENT_3D ( 'NONE', #189912, #210754, #8705 ) ;
#200664=CARTESIAN_POINT ( 'NONE',  ( -20.94999999999999929, 87.48912529308798014, -99.92310748452423752 ) ) ;
#200697=ADVANCED_FACE ( 'NONE', ( #33751 ), #235740, .F. ) ;
#200698=VECTOR ( 'NONE', #147481, 1000.000000000000000 ) ;
#200714=DIRECTION ( 'NONE',  ( 0.000000000000000000, 6.982962677686266711E-15, -1.000000000000000000 ) ) ;
#200716=CARTESIAN_POINT ( 'NONE',  ( -18.59999999999999787, 77.85102823015273543, -91.36919421510179973 ) ) ;
#200720=DIRECTION ( 'NONE',  ( 0.000000000000000000, 0.8660254037844419273, -0.4999999999999942824 ) ) ;
#200722=CARTESIAN_POINT ( 'NONE',  ( 20.94999999999999929, 76.00000000001170974, -69.52310748452431710 ) ) ;
#200748=ADVANCED_FACE ( 'NONE', ( #92380 ), #97286, .T. ) ;
#200766=VERTEX_POINT ( 'NONE', #77945 ) ;
#200775=ORIENTED_EDGE ( 'NONE', *, *, #61717, .F. ) ;
#200807=ORIENTED_EDGE ( 'NONE', *, *, #188096, .T. ) ;
#200817=AXIS2_PLACEMENT_3D ( 'NONE', #167665, #247163, #208073 ) ;
#200832=CARTESIAN_POINT ( 'NONE',  ( 18.59999999999996945, 68.97833521811159585, -65.68954208262705663 ) ) ;
#200861=CARTESIAN_POINT ( 'NONE',  ( 22.50046968638156386, 75.95483015287055650, -114.7731526389968479 ) ) ;
#200862=CARTESIAN_POINT ( 'NONE',  ( -20.54999999999999716, 66.65000000001180069, -81.77310748452437394 ) ) ;
#200881=VECTOR ( 'NONE', #225382, 1000.000000000000000 ) ;
#200905=VERTEX_POINT ( 'NONE', #29573 ) ;
#200938=DIRECTION ( 'NONE',  ( 0.000000000000000000, -7.272083257015735086E-15, 1.000000000000000000 ) ) ;
#200940=VERTEX_POINT ( 'NONE', #67382 ) ;
#200952=EDGE_CURVE ( 'NONE', #39176, #101974, #148705, .T. ) ;
#200959=AXIS2_PLACEMENT_3D ( 'NONE', #176561, #111433, #112721 ) ;
#200961=EDGE_CURVE ( 'NONE', #194022, #194138, #182005, .T. ) ;
#200968=FILL_AREA_STYLE_COLOUR ( '', #31327 ) ;
#200979=EDGE_CURVE ( 'NONE', #227104, #46226, #194496, .T. ) ;
#201000=AXIS2_PLACEMENT_3D ( 'NONE', #208660, #87395, #165687 ) ;
#201034=AXIS2_PLACEMENT_3D ( 'NONE', #196457, #62098, #256375 ) ;
#201041=CARTESIAN_POINT ( 'NONE',  ( -21.17356465864818560, 69.57719687377023376, -103.1220187255382399 ) ) ;
#201055=CARTESIAN_POINT ( 'NONE',  ( -21.05000000000000071, 76.10000000001198828, -109.5637644362255543 ) ) ;
#201058=CARTESIAN_POINT ( 'NONE',  ( 22.39999999999999503, 76.00000000001200817, -110.8138870828976934 ) ) ;
#201108=CONICAL_SURFACE ( 'NONE', #117882, 4.299999999999956302, 0.7853981633974466137 ) ;
#201137=EDGE_CURVE ( 'NONE', #71369, #221901, #219398, .T. ) ;
#201146=CARTESIAN_POINT ( 'NONE',  ( -21.14999999999999858, 87.65000000001192859, -100.1231074845242262 ) ) ;
#201187=EDGE_LOOP ( 'NONE', ( #133967, #219092, #235759, #105938 ) ) ;
#201196=EDGE_CURVE ( 'NONE', #147363, #129128, #15425, .T. ) ;
#201203=CARTESIAN_POINT ( 'NONE',  ( 18.59999999999999432, 77.16270174994990327, -94.92310748452430857 ) ) ;
#201208=DIRECTION ( 'NONE',  ( 0.000000000000000000, 6.608470384673558123E-15, -1.000000000000000000 ) ) ;
#201225=EDGE_CURVE ( 'NONE', #167394, #229799, #182191, .T. ) ;
#201227=ORIENTED_EDGE ( 'NONE', *, *, #237094, .F. ) ;
#201284=CARTESIAN_POINT ( 'NONE',  ( 18.60000000000000497, 76.00000000001195133, -103.0231074845243171 ) ) ;
#201297=EDGE_CURVE ( 'NONE', #110864, #192851, #203015, .T. ) ;
#201306=VERTEX_POINT ( 'NONE', #249584 ) ;
#201322=CARTESIAN_POINT ( 'NONE',  ( 18.59999999999999076, 69.55000000001179217, -81.87310748452435405 ) ) ;
#201343=ORIENTED_EDGE ( 'NONE', *, *, #120056, .T. ) ;
#201344=CIRCLE ( 'NONE', #26395, 0.09999999999999913125 ) ;
#201366=CARTESIAN_POINT ( 'NONE',  ( -20.54999999999999716, 76.00000000001195133, -103.0231074845243171 ) ) ;
#201368=DIRECTION ( 'NONE',  ( 0.000000000000000000, 0.000000000000000000, 1.000000000000000000 ) ) ;
#201392=VERTEX_POINT ( 'NONE', #113910 ) ;
#201475=DIRECTION ( 'NONE',  ( 1.000000000000000000, 0.000000000000000000, 0.000000000000000000 ) ) ;
#201518=LINE ( 'NONE', #244499, #188034 ) ;
#201533=CIRCLE ( 'NONE', #72771, 0.2000000000000057288 ) ;
#201553=EDGE_CURVE ( 'NONE', #8374, #70373, #86296, .T. ) ;
#201559=EDGE_CURVE ( 'NONE', #127088, #90102, #52993, .T. ) ;
#201595=ORIENTED_EDGE ( 'NONE', *, *, #115962, .T. ) ;
#201596=VECTOR ( 'NONE', #178881, 1000.000000000000000 ) ;
#201604=EDGE_CURVE ( 'NONE', #244131, #178769, #190776, .T. ) ;
#201608=ORIENTED_EDGE ( 'NONE', *, *, #151575, .T. ) ;
#201629=CARTESIAN_POINT ( 'NONE',  ( 21.08621493067296626, 69.65070570884027745, -103.0793023240004658 ) ) ;
#201639=CIRCLE ( 'NONE', #80812, 0.1000000000000028644 ) ;
#201645=VECTOR ( 'NONE', #256265, 1000.000000000000000 ) ;
#201671=DIRECTION ( 'NONE',  ( 0.000000000000000000, 7.026728003956683390E-15, -1.000000000000000000 ) ) ;
#201682=ORIENTED_EDGE ( 'NONE', *, *, #119188, .F. ) ;
#201690=VERTEX_POINT ( 'NONE', #9147 ) ;
#201695=CIRCLE ( 'NONE', #151839, 4.099999999999992539 ) ;
#201707=CARTESIAN_POINT ( 'NONE',  ( 18.55807992284871588, 65.67101464000481315, -63.94043916224794089 ) ) ;
#201723=ORIENTED_EDGE ( 'NONE', *, *, #45106, .F. ) ;
#201735=EDGE_CURVE ( 'NONE', #220516, #210647, #69955, .T. ) ;
#201772=DIRECTION ( 'NONE',  ( 0.000000000000000000, -7.086529944415894657E-15, 1.000000000000000000 ) ) ;
#201774=CARTESIAN_POINT ( 'NONE',  ( 18.59999999999999076, 77.16412189325286874, -61.60825939895269698 ) ) ;
#201788=CIRCLE ( 'NONE', #226736, 0.1000000000000028644 ) ;
#201797=DIRECTION ( 'NONE',  ( 0.000000000000000000, 0.000000000000000000, -1.000000000000000000 ) ) ;
#201799=VERTEX_POINT ( 'NONE', #232059 ) ;
#201810=CIRCLE ( 'NONE', #60804, 0.1000000000000045158 ) ;
#201840=ORIENTED_EDGE ( 'NONE', *, *, #117614, .T. ) ;
#201861=CIRCLE ( 'NONE', #185117, 0.1000000000000028644 ) ;
#201930=DIRECTION ( 'NONE',  ( 3.469446951953635015E-14, 6.982962677686266711E-15, -1.000000000000000000 ) ) ;
#201948=CARTESIAN_POINT ( 'NONE',  ( -18.59999999999999787, 64.25000000001203659, -114.7731074845243882 ) ) ;
#201972=DIRECTION ( 'NONE',  ( 1.000000000000000000, 0.000000000000000000, 0.000000000000000000 ) ) ;
#201996=AXIS2_PLACEMENT_3D ( 'NONE', #22239, #61346, #237419 ) ;
#202031=CARTESIAN_POINT ( 'NONE',  ( -23.25000000000000000, 64.25000000001170974, -69.52310748452438816 ) ) ;
#202042=CARTESIAN_POINT ( 'NONE',  ( -21.04999999999999361, 69.69257478044653453, -103.0062876161386640 ) ) ;
#202044=CARTESIAN_POINT ( 'NONE',  ( 18.59999999999999076, 69.60000000001187459, -93.09268285446279378 ) ) ;
#202068=TOROIDAL_SURFACE ( 'NONE', #35509, 0.2000000000000000111, 0.1000000000000000056 ) ;
#202104=ORIENTED_EDGE ( 'NONE', *, *, #200069, .T. ) ;
#202119=CARTESIAN_POINT ( 'NONE',  ( 20.85000000000000142, 77.83585931145526615, -58.01866831572577610 ) ) ;
#202144=ORIENTED_EDGE ( 'NONE', *, *, #89929, .F. ) ;
#202146=VERTEX_POINT ( 'NONE', #247432 ) ;
#202205=CARTESIAN_POINT ( 'NONE',  ( -18.39999999999999858, 85.50000000001189449, -95.99103808782457747 ) ) ;
#202215=EDGE_CURVE ( 'NONE', #40998, #68348, #113066, .T. ) ;
#202229=CARTESIAN_POINT ( 'NONE',  ( 21.05000000000000426, 75.93429838968991419, -109.2814235418563555 ) ) ;
#202250=DIRECTION ( 'NONE',  ( 0.000000000000000000, -6.982962677686266711E-15, 1.000000000000000000 ) ) ;
#202264=ORIENTED_EDGE ( 'NONE', *, *, #76755, .T. ) ;
#202300=FACE_OUTER_BOUND ( 'NONE', #72389, .T. ) ;
#202343=CARTESIAN_POINT ( 'NONE',  ( 21.53752568622137886, 75.90102553874137925, -109.8099153590728605 ) ) ;
#202360=ORIENTED_EDGE ( 'NONE', *, *, #142453, .T. ) ;
#202390=DIRECTION ( 'NONE',  ( 0.000000000000000000, 1.000000000000000000, 6.982962677686266711E-15 ) ) ;
#202398=ORIENTED_EDGE ( 'NONE', *, *, #207472, .T. ) ;
#202411=AXIS2_PLACEMENT_3D ( 'NONE', #90846, #149573, #68734 ) ;
#202426=( BOUNDED_CURVE ( )  B_SPLINE_CURVE ( 3, ( #169608, #90009, #146134, #9196 ),
 .UNSPECIFIED., .F., .F. ) 
 B_SPLINE_CURVE_WITH_KNOTS ( ( 4, 4 ),
 ( 4.937700262165045813E-15, 1.570796326794912323 ),
 .UNSPECIFIED. ) 
 CURVE ( )  GEOMETRIC_REPRESENTATION_ITEM ( )  RATIONAL_B_SPLINE_CURVE ( ( 1.000000000000000000, 0.8047378541243623840, 0.8047378541243623840, 1.000000000000000000 ) ) 
 REPRESENTATION_ITEM ( '' )  );
#202441=ADVANCED_FACE ( 'NONE', ( #2078 ), #93180, .F. ) ;
#202457=EDGE_CURVE ( 'NONE', #223762, #32631, #191138, .T. ) ;
#202468=CARTESIAN_POINT ( 'NONE',  ( -21.64999999999999858, 68.75000000001179501, -81.77310748452435973 ) ) ;
#202487=CARTESIAN_POINT ( 'NONE',  ( 23.14999999999998437, 76.00000000001195133, -103.0231074845243171 ) ) ;
#202488=DIRECTION ( 'NONE',  ( 1.000000000000000000, 0.000000000000000000, 0.000000000000000000 ) ) ;
#202499=DIRECTION ( 'NONE',  ( 0.000000000000000000, 0.000000000000000000, 1.000000000000000000 ) ) ;
#202504=EDGE_LOOP ( 'NONE', ( #39391, #176668, #77932, #102786, #57805, #138021, #52270 ) ) ;
#202516=VERTEX_POINT ( 'NONE', #248414 ) ;
#202550=CARTESIAN_POINT ( 'NONE',  ( -21.55000000000000426, 68.29142135624910281, -81.87310748452436826 ) ) ;
#202570=ORIENTED_EDGE ( 'NONE', *, *, #167375, .T. ) ;
#202590=EDGE_CURVE ( 'NONE', #142060, #121241, #236538, .T. ) ;
#202600=CIRCLE ( 'NONE', #2675, 0.2000000000000057288 ) ;
#202619=DIRECTION ( 'NONE',  ( 0.000000000000000000, 6.982962677686266711E-15, -1.000000000000000000 ) ) ;
#202620=FACE_OUTER_BOUND ( 'NONE', #55937, .T. ) ;
#202627=CARTESIAN_POINT ( 'NONE',  ( 20.95512820512820440, 67.12384868372375024, -90.87310748452436826 ) ) ;
#202696=ADVANCED_FACE ( 'NONE', ( #145136 ), #64340, .T. ) ;
#202697=CIRCLE ( 'NONE', #90249, 0.1000000000000028644 ) ;
#202708=ORIENTED_EDGE ( 'NONE', *, *, #92950, .T. ) ;
#202714=EDGE_CURVE ( 'NONE', #160733, #206540, #183014, .T. ) ;
#202736=CARTESIAN_POINT ( 'NONE',  ( 21.03670563405601612, 65.37517631068362789, -90.69756059831524908 ) ) ;
#202747=DIRECTION ( 'NONE',  ( 0.000000000000000000, 0.000000000000000000, 1.000000000000000000 ) ) ;
#202791=CARTESIAN_POINT ( 'NONE',  ( 23.25000000000000000, 85.60000000001177511, -79.41707660717668205 ) ) ;
#202795=CARTESIAN_POINT ( 'NONE',  ( -21.05000000000000071, 76.01465611852468385, -109.5197940702921642 ) ) ;
#202811=EDGE_CURVE ( 'NONE', #158833, #128191, #188140, .T. ) ;
#202812=SPHERICAL_SURFACE ( 'NONE', #114132, 0.1000000000000000056 ) ;
#202814=DIRECTION ( 'NONE',  ( -0.000000000000000000, 1.000000000000000000, 6.982962677686267499E-15 ) ) ;
#202828=DIRECTION ( 'NONE',  ( -1.000000000000000000, -0.000000000000000000, -0.000000000000000000 ) ) ;
#202852=CARTESIAN_POINT ( 'NONE',  ( -21.11101077989000174, 75.98471473109772489, -109.4467922192504403 ) ) ;
#202856=DIRECTION ( 'NONE',  ( 0.000000000000000000, 0.000000000000000000, -1.000000000000000000 ) ) ;
#202857=ORIENTED_EDGE ( 'NONE', *, *, #173872, .F. ) ;
#202961=DIRECTION ( 'NONE',  ( 0.000000000000000000, 0.000000000000000000, 1.000000000000000000 ) ) ;
#202964=CIRCLE ( 'NONE', #94620, 0.1000000000000028644 ) ;
#202974=LINE ( 'NONE', #179588, #67740 ) ;
#202990=CARTESIAN_POINT ( 'NONE',  ( -23.25000000000000000, 76.00000000001173817, -73.42310748452430857 ) ) ;
#203015=CIRCLE ( 'NONE', #65650, 2.000000000000001776 ) ;
#203028=CARTESIAN_POINT ( 'NONE',  ( 21.00000000000000000, 66.25000000001179501, -81.77310748452437394 ) ) ;
#203072=EDGE_CURVE ( 'NONE', #229726, #14256, #220548, .T. ) ;
#203074=FACE_OUTER_BOUND ( 'NONE', #92401, .T. ) ;
#203077=CARTESIAN_POINT ( 'NONE',  ( -20.94999999999999929, 64.25000000001189449, -96.00830171387038092 ) ) ;
#203157=ORIENTED_EDGE ( 'NONE', *, *, #77677, .T. ) ;
#203167=DIRECTION ( 'NONE',  ( 1.000000000000000000, -0.000000000000000000, 0.000000000000000000 ) ) ;
#203191=ORIENTED_EDGE ( 'NONE', *, *, #105184, .T. ) ;
#203197=ORIENTED_EDGE ( 'NONE', *, *, #14933, .F. ) ;
#203206=AXIS2_PLACEMENT_3D ( 'NONE', #229950, #50026, #68316 ) ;
#203230=DIRECTION ( 'NONE',  ( 0.000000000000000000, -1.000000000000000000, -8.717686153663073805E-15 ) ) ;
#203263=DIRECTION ( 'NONE',  ( -0.000000000000000000, -1.000000000000000000, -6.982962677686266711E-15 ) ) ;
#203270=EDGE_CURVE ( 'NONE', #18900, #155597, #202426, .T. ) ;
#203306=ADVANCED_FACE ( 'NONE', ( #130424 ), #209981, .F. ) ;
#203316=CARTESIAN_POINT ( 'NONE',  ( 20.95132126680579887, 65.51005012986510678, -95.45278294608985448 ) ) ;
#203321=DIRECTION ( 'NONE',  ( 2.978066053179069723E-16, 1.000000000000000000, 7.147358527629766941E-15 ) ) ;
#203331=LINE ( 'NONE', #166803, #241577 ) ;
#203360=EDGE_LOOP ( 'NONE', ( #51834, #148243, #235494, #184876, #518, #75050, #127599, #88373, #231459, #32168 ) ) ;
#203364=LINE ( 'NONE', #166837, #148388 ) ;
#203382=ORIENTED_EDGE ( 'NONE', *, *, #81043, .F. ) ;
#203383=AXIS2_PLACEMENT_3D ( 'NONE', #107571, #71048, #227520 ) ;
#203393=CARTESIAN_POINT ( 'NONE',  ( -22.00411653962179415, 68.74655713164197834, -103.1221455903250330 ) ) ;
#203422=ADVANCED_FACE ( 'NONE', ( #131715 ), #32663, .F. ) ;
#203427=CARTESIAN_POINT ( 'NONE',  ( 19.75857864376269291, 64.25000000001176659, -78.17310748452437963 ) ) ;
#203429=CIRCLE ( 'NONE', #120255, 0.09999999999999939493 ) ;
#203458=ORIENTED_EDGE ( 'NONE', *, *, #165434, .F. ) ;
#203464=CARTESIAN_POINT ( 'NONE',  ( -20.64999999999999858, 74.05981308412395947, -82.35222669557765585 ) ) ;
#203467=AXIS2_PLACEMENT_3D ( 'NONE', #213885, #247876, #249173 ) ;
#203491=ORIENTED_EDGE ( 'NONE', *, *, #222865, .F. ) ;
#203504=ORIENTED_EDGE ( 'NONE', *, *, #19014, .T. ) ;
#203543=LINE ( 'NONE', #40660, #201596 ) ;
#203567=AXIS2_PLACEMENT_3D ( 'NONE', #221863, #184044, #43262 ) ;
#203604=DIRECTION ( 'NONE',  ( 0.000000000000000000, 0.1350103645451945777, -0.9908441862701589109 ) ) ;
#203610=CYLINDRICAL_SURFACE ( 'NONE', #94278, 0.1000000000000052097 ) ;
#203625=AXIS2_PLACEMENT_3D ( 'NONE', #14784, #52583, #50023 ) ;
#203636=EDGE_LOOP ( 'NONE', ( #171787, #27858, #105202, #13623 ) ) ;
#203650=AXIS2_PLACEMENT_3D ( 'NONE', #75591, #37745, #216347 ) ;
#203654=AXIS2_PLACEMENT_3D ( 'NONE', #253505, #155736, #78710 ) ;
#203682=EDGE_LOOP ( 'NONE', ( #193614, #158972, #16350, #180918, #187386, #123753 ) ) ;
#203689=LINE ( 'NONE', #185407, #239386 ) ;
#203690=CIRCLE ( 'NONE', #128681, 2.000000000000001776 ) ;
#203704=EDGE_CURVE ( 'NONE', #173885, #81780, #95235, .T. ) ;
#203725=EDGE_LOOP ( 'NONE', ( #94945, #131020, #448, #49786 ) ) ;
#203741=VECTOR ( 'NONE', #77890, 1000.000000000000000 ) ;
#203744=EDGE_LOOP ( 'NONE', ( #27794, #93561, #56809, #107808 ) ) ;
#203745=AXIS2_PLACEMENT_3D ( 'NONE', #6659, #84879, #220588 ) ;
#203770=ORIENTED_EDGE ( 'NONE', *, *, #203072, .F. ) ;
#203790=DIRECTION ( 'NONE',  ( 0.000000000000000000, 7.026728003956683390E-15, -1.000000000000000000 ) ) ;
#203798=CARTESIAN_POINT ( 'NONE',  ( -21.14999999999999858, 64.25000000001195133, -102.9231074845243938 ) ) ;
#203856=CARTESIAN_POINT ( 'NONE',  ( 21.97500000000000497, 66.25000000001179501, -81.77310748452437394 ) ) ;
#203861=ORIENTED_EDGE ( 'NONE', *, *, #50896, .T. ) ;
#203914=DIRECTION ( 'NONE',  ( 1.000000000000000000, 0.000000000000000000, 0.000000000000000000 ) ) ;
#203922=VERTEX_POINT ( 'NONE', #186924 ) ;
#203923=CIRCLE ( 'NONE', #162254, 0.09999999999999939493 ) ;
#203929=EDGE_CURVE ( 'NONE', #167394, #30387, #191117, .T. ) ;
#203940=DIRECTION ( 'NONE',  ( 0.000000000000000000, -1.000000000000000000, -6.982962677686265922E-15 ) ) ;
#203985=DIRECTION ( 'NONE',  ( 0.000000000000000000, -0.8660254037844377084, -0.5000000000000016653 ) ) ;
#204012=DIRECTION ( 'NONE',  ( 1.000000000000000000, 0.000000000000000000, 0.000000000000000000 ) ) ;
#204024=CARTESIAN_POINT ( 'NONE',  ( -22.39999999999999858, 64.35000000001195986, -102.9231074845243938 ) ) ;
#204044=VERTEX_POINT ( 'NONE', #239 ) ;
#204051=DIRECTION ( 'NONE',  ( 0.000000000000000000, 6.982962677686266711E-15, -1.000000000000000000 ) ) ;
#204084=CARTESIAN_POINT ( 'NONE',  ( -18.59999999999999787, 65.66751761918648356, -63.92826094061123143 ) ) ;
#204098=CARTESIAN_POINT ( 'NONE',  ( 18.39999999999999858, 85.50000000001189449, -95.99103808782457747 ) ) ;
#204101=DIRECTION ( 'NONE',  ( 1.000000000000000000, 0.000000000000000000, 0.000000000000000000 ) ) ;
#204114=EDGE_LOOP ( 'NONE', ( #78369, #47534, #142278, #8006 ) ) ;
#204117=ORIENTED_EDGE ( 'NONE', *, *, #225726, .T. ) ;
#204125=ORIENTED_EDGE ( 'NONE', *, *, #116697, .T. ) ;
#204128=CARTESIAN_POINT ( 'NONE',  ( -21.08884785362073089, 75.95021690494527888, -109.3803008519499258 ) ) ;
#204144=ORIENTED_EDGE ( 'NONE', *, *, #52025, .F. ) ;
#204153=ORIENTED_EDGE ( 'NONE', *, *, #173561, .F. ) ;
#204189=EDGE_CURVE ( 'NONE', #54475, #416, #16324, .T. ) ;
#204205=EDGE_CURVE ( 'NONE', #117549, #127088, #237065, .T. ) ;
#204215=DIRECTION ( 'NONE',  ( -1.000000000000000000, 0.000000000000000000, 0.000000000000000000 ) ) ;
#204234=CYLINDRICAL_SURFACE ( 'NONE', #28110, 0.09999999999999939493 ) ;
#204259=DIRECTION ( 'NONE',  ( 0.000000000000000000, 6.982962677686267499E-15, -1.000000000000000000 ) ) ;
#204267=EDGE_CURVE ( 'NONE', #6405, #49802, #78818, .T. ) ;
#204274=CARTESIAN_POINT ( 'NONE',  ( 20.94999999999999929, 85.00000000001188027, -93.12913836187181005 ) ) ;
#204307=DIRECTION ( 'NONE',  ( 1.000000000000000000, 0.000000000000000000, 0.000000000000000000 ) ) ;
#204310=ORIENTED_EDGE ( 'NONE', *, *, #194607, .T. ) ;
#204316=ORIENTED_EDGE ( 'NONE', *, *, #89826, .T. ) ;
#204317=EDGE_CURVE ( 'NONE', #84480, #131827, #28840, .T. ) ;
#204326=EDGE_CURVE ( 'NONE', #111418, #44904, #203923, .T. ) ;
#204333=DIRECTION ( 'NONE',  ( 1.836970198721029934E-16, 1.000000000000000000, 6.982962677686266711E-15 ) ) ;
#204336=FACE_OUTER_BOUND ( 'NONE', #107502, .T. ) ;
#204339=CARTESIAN_POINT ( 'NONE',  ( 21.14999999999999858, 69.45000000001186891, -90.87310748452435405 ) ) ;
#204354=CARTESIAN_POINT ( 'NONE',  ( -20.95613430942401223, 64.25000000001188027, -96.16594483630493073 ) ) ;
#204358=EDGE_LOOP ( 'NONE', ( #256952, #58817, #238316, #192611 ) ) ;
#204363=AXIS2_PLACEMENT_3D ( 'NONE', #89688, #28493, #8889 ) ;
#204364=AXIS2_PLACEMENT_3D ( 'NONE', #181138, #24648, #205816 ) ;
#204369=DIRECTION ( 'NONE',  ( 1.000000000000000000, 0.000000000000000000, 0.000000000000000000 ) ) ;
#204405=AXIS2_PLACEMENT_3D ( 'NONE', #78407, #160552, #99247 ) ;
#204416=VECTOR ( 'NONE', #27174, 1000.000000000000000 ) ;
#204421=ORIENTED_EDGE ( 'NONE', *, *, #111459, .T. ) ;
#204422=CARTESIAN_POINT ( 'NONE',  ( -20.94999999999999929, 64.35000000001176090, -76.30697314750248950 ) ) ;
#204441=DIRECTION ( 'NONE',  ( 0.000000000000000000, 0.9999631594459055250, 0.008583690987131395445 ) ) ;
#204483=ORIENTED_EDGE ( 'NONE', *, *, #170920, .F. ) ;
#204492=DIRECTION ( 'NONE',  ( 0.000000000000000000, -1.000000000000000000, 1.387778780781406043E-13 ) ) ;
#204499=ADVANCED_FACE ( 'NONE', ( #35259 ), #194326, .T. ) ;
#204510=AXIS2_PLACEMENT_3D ( 'NONE', #217019, #93229, #114073 ) ;
#204514=AXIS2_PLACEMENT_3D ( 'NONE', #95481, #18525, #180179 ) ;
#204517=CARTESIAN_POINT ( 'NONE',  ( 20.94999999999999929, 71.00000000001186606, -90.61784146561124942 ) ) ;
#204526=CARTESIAN_POINT ( 'NONE',  ( 18.49999999999999645, 74.83729825007388570, -94.92310748452432279 ) ) ;
#204553=FACE_OUTER_BOUND ( 'NONE', #86670, .T. ) ;
#204570=VERTEX_POINT ( 'NONE', #121218 ) ;
#204572=FACE_OUTER_BOUND ( 'NONE', #172726, .T. ) ;
#204576=DIRECTION ( 'NONE',  ( 1.000000000000000000, 0.000000000000000000, 0.000000000000000000 ) ) ;
#204583=DIRECTION ( 'NONE',  ( 6.938893903907224433E-15, 1.000000000000000000, 7.272083257015735086E-15 ) ) ;
#204635=EDGE_CURVE ( 'NONE', #19541, #200766, #133035, .T. ) ;
#204645=ORIENTED_EDGE ( 'NONE', *, *, #133816, .F. ) ;
#204655=ORIENTED_EDGE ( 'NONE', *, *, #186572, .T. ) ;
#204668=ORIENTED_EDGE ( 'NONE', *, *, #27279, .T. ) ;
#204671=FACE_OUTER_BOUND ( 'NONE', #71365, .T. ) ;
#204679=DIRECTION ( 'NONE',  ( -0.000000000000000000, -6.982962677686266711E-15, 1.000000000000000000 ) ) ;
#204713=ORIENTED_EDGE ( 'NONE', *, *, #232144, .F. ) ;
#204725=CIRCLE ( 'NONE', #134005, 11.74999999999999645 ) ;
#204740=B_SPLINE_CURVE_WITH_KNOTS ( 'NONE', 3,
 ( #116873, #97264, #77723, #38624, #118157, #159874, #65884, #46306, #3319, #204098 ),
 .UNSPECIFIED., .F., .F.,
 ( 4, 2, 2, 2, 4 ),
 ( 0.000000000000000000, 0.0001584437871625089497, 0.0002376656807437646035, 0.0002772766275343924169, 0.0003168875743250202845 ),
 .UNSPECIFIED. ) ;
#204753=CARTESIAN_POINT ( 'NONE',  ( -18.59999999999999787, 77.26327546522891510, -61.62124281777789037 ) ) ;
#204756=ADVANCED_FACE ( 'NONE', ( #91039 ), #74963, .F. ) ;
#204784=EDGE_CURVE ( 'NONE', #222143, #165593, #129106, .T. ) ;
#204792=ORIENTED_EDGE ( 'NONE', *, *, #97641, .T. ) ;
#204844=VERTEX_POINT ( 'NONE', #135277 ) ;
#204845=CYLINDRICAL_SURFACE ( 'NONE', #197051, 0.09999999999999867328 ) ;
#204875=CARTESIAN_POINT ( 'NONE',  ( 23.24999999999999645, 76.00000000001170974, -69.52310748452431710 ) ) ;
#204895=CARTESIAN_POINT ( 'NONE',  ( -23.15000000000000213, 64.25000000001179501, -81.67310748452439384 ) ) ;
#204909=ADVANCED_FACE ( 'NONE', ( #214824 ), #216580, .T. ) ;
#204917=CARTESIAN_POINT ( 'NONE',  ( -23.25000000000000000, 74.00000000001180922, -82.14772940728641970 ) ) ;
#204924=DIRECTION ( 'NONE',  ( 0.000000000000000000, -1.000000000000000000, -6.352154140967427193E-15 ) ) ;
#204939=ORIENTED_EDGE ( 'NONE', *, *, #144468, .F. ) ;
#204955=CARTESIAN_POINT ( 'NONE',  ( 20.94999999999999929, 64.35000000001176090, -76.30697314750248950 ) ) ;
#204972=CARTESIAN_POINT ( 'NONE',  ( 23.14999999999999503, 64.35000000001186038, -90.87310748452438247 ) ) ;
#204981=CIRCLE ( 'NONE', #948, 2.000000000000001776 ) ;
#204995=AXIS2_PLACEMENT_3D ( 'NONE', #61560, #82366, #101933 ) ;
#205000=ORIENTED_EDGE ( 'NONE', *, *, #222237, .F. ) ;
#205004=ORIENTED_EDGE ( 'NONE', *, *, #86583, .F. ) ;
#205009=CARTESIAN_POINT ( 'NONE',  ( 20.94999999999999929, 76.00000000001186606, -90.14810748452431710 ) ) ;
#205016=ADVANCED_FACE ( 'NONE', ( #177023 ), #62479, .F. ) ;
#205020=ORIENTED_EDGE ( 'NONE', *, *, #84046, .T. ) ;
#205042=ORIENTED_EDGE ( 'NONE', *, *, #153309, .F. ) ;
#205043=CIRCLE ( 'NONE', #146786, 0.09999999999999939493 ) ;
#205047=VERTEX_POINT ( 'NONE', #101249 ) ;
#205050=ORIENTED_EDGE ( 'NONE', *, *, #229156, .F. ) ;
#205053=EDGE_CURVE ( 'NONE', #252623, #118654, #199860, .T. ) ;
#205058=EDGE_LOOP ( 'NONE', ( #92897, #118390, #37613, #94016 ) ) ;
#205104=AXIS2_PLACEMENT_3D ( 'NONE', #160683, #240202, #5394 ) ;
#205108=ORIENTED_EDGE ( 'NONE', *, *, #153268, .F. ) ;
#205122=PLANE ( 'NONE',  #156133 ) ;
#205136=ORIENTED_EDGE ( 'NONE', *, *, #200419, .F. ) ;
#205141=EDGE_CURVE ( 'NONE', #70872, #116247, #175128, .T. ) ;
#205158=ADVANCED_FACE ( 'NONE', ( #30453 ), #195944, .F. ) ;
#205167=CARTESIAN_POINT ( 'NONE',  ( -21.05000000000000071, 64.35000000001195986, -102.9231074845243938 ) ) ;
#205189=DIRECTION ( 'NONE',  ( 1.000000000000000000, 0.000000000000000000, 0.000000000000000000 ) ) ;
#205198=EDGE_CURVE ( 'NONE', #132890, #195387, #125194, .T. ) ;
#205218=AXIS2_PLACEMENT_3D ( 'NONE', #15913, #91568, #171153 ) ;
#205247=DIRECTION ( 'NONE',  ( -1.000000000000000000, -0.000000000000000000, -0.000000000000000000 ) ) ;
#205255=ORIENTED_EDGE ( 'NONE', *, *, #94430, .T. ) ;
#205258=CARTESIAN_POINT ( 'NONE',  ( 20.94999999999999929, 76.00000000001168132, -65.52310748452430289 ) ) ;
#205260=AXIS2_PLACEMENT_3D ( 'NONE', #257103, #232484, #252016 ) ;
#205269=AXIS2_PLACEMENT_3D ( 'NONE', #169088, #127355, #107785 ) ;
#205274=ORIENTED_EDGE ( 'NONE', *, *, #107701, .F. ) ;
#205345=CARTESIAN_POINT ( 'NONE',  ( -18.59999999999999787, 74.83729825007388570, -94.92310748452432279 ) ) ;
#205350=CARTESIAN_POINT ( 'NONE',  ( -20.85000000000000497, 64.25000000001176659, -76.44225473048308572 ) ) ;
#205373=ADVANCED_FACE ( 'NONE', ( #176683 ), #21170, .T. ) ;
#205382=CARTESIAN_POINT ( 'NONE',  ( 23.24999999999999645, 71.22429906543236200, -81.37187558857031888 ) ) ;
#205389=CIRCLE ( 'NONE', #142838, 12.87499999999999822 ) ;
#205400=AXIS2_PLACEMENT_3D ( 'NONE', #113985, #174019, #233942 ) ;
#205410=AXIS2_PLACEMENT_3D ( 'NONE', #155663, #138594, #116508 ) ;
#205429=CARTESIAN_POINT ( 'NONE',  ( -21.37071067811865532, 67.92928932189313684, -81.87310748452436826 ) ) ;
#205472=DIRECTION ( 'NONE',  ( 0.000000000000000000, 0.000000000000000000, -1.000000000000000000 ) ) ;
#205488=CARTESIAN_POINT ( 'NONE',  ( -23.15000000000000213, 64.35000000001187459, -90.87310748452438247 ) ) ;
#205521=CARTESIAN_POINT ( 'NONE',  ( 21.14999999999999858, 76.00000000001186606, -90.87310748452429721 ) ) ;
#205530=CARTESIAN_POINT ( 'NONE',  ( -23.15000000000000213, 73.50000000001180922, -82.74772940728641402 ) ) ;
#205554=CARTESIAN_POINT ( 'NONE',  ( 18.39999999999999858, 85.50000000001166711, -62.92291809330220786 ) ) ;
#205571=ORIENTED_EDGE ( 'NONE', *, *, #8307, .F. ) ;
#205574=EDGE_CURVE ( 'NONE', #243017, #17324, #142650, .T. ) ;
#205579=CARTESIAN_POINT ( 'NONE',  ( 18.59999999999999076, 77.14957036958736580, -61.70719500002233815 ) ) ;
#205631=CARTESIAN_POINT ( 'NONE',  ( -18.59999999999999787, 64.35000000001190301, -96.00830171387039513 ) ) ;
#205643=DIRECTION ( 'NONE',  ( 2.952720810173289112E-16, 1.000000000000000000, 6.308085367188367561E-15 ) ) ;
#205665=DIRECTION ( 'NONE',  ( 0.000000000000000000, 0.000000000000000000, 1.000000000000000000 ) ) ;
#205673=ORIENTED_EDGE ( 'NONE', *, *, #35846, .T. ) ;
#205707=ORIENTED_EDGE ( 'NONE', *, *, #157507, .T. ) ;
#205712=ORIENTED_EDGE ( 'NONE', *, *, #83148, .F. ) ;
#205742=AXIS2_PLACEMENT_3D ( 'NONE', #172311, #251792, #230973 ) ;
#205799=CIRCLE ( 'NONE', #1768, 3.900000000000000799 ) ;
#205812=CARTESIAN_POINT ( 'NONE',  ( 21.05000000000000071, 87.65000000001172964, -72.52310748452423184 ) ) ;
#205816=DIRECTION ( 'NONE',  ( 0.000000000000000000, 0.000000000000000000, 1.000000000000000000 ) ) ;
#205819=EDGE_CURVE ( 'NONE', #183504, #158368, #135932, .T. ) ;
#205906=AXIS2_PLACEMENT_3D ( 'NONE', #79739, #75917, #159325 ) ;
#205928=EDGE_CURVE ( 'NONE', #136482, #56290, #96944, .T. ) ;
#205988=CARTESIAN_POINT ( 'NONE',  ( 19.83283456528359423, 64.25000000001176659, -78.17310748510507779 ) ) ;
#205990=ADVANCED_FACE ( 'NONE', ( #146209 ), #159053, .F. ) ;
#205993=EDGE_CURVE ( 'NONE', #109375, #145911, #118625, .T. ) ;
#206014=LINE ( 'NONE', #106894, #124944 ) ;
#206045=DIRECTION ( 'NONE',  ( -1.000000000000000000, 0.000000000000000000, 0.000000000000000000 ) ) ;
#206093=EDGE_LOOP ( 'NONE', ( #105311, #60094, #11804, #16602, #250648, #74861, #50785 ) ) ;
#206098=AXIS2_PLACEMENT_3D ( 'NONE', #149797, #109337, #188900 ) ;
#206103=ORIENTED_EDGE ( 'NONE', *, *, #208734, .T. ) ;
#206114=AXIS2_PLACEMENT_3D ( 'NONE', #20322, #98505, #64555 ) ;
#206117=ORIENTED_EDGE ( 'NONE', *, *, #43489, .F. ) ;
#206134=EDGE_CURVE ( 'NONE', #12289, #43410, #63656, .T. ) ;
#206141=EDGE_CURVE ( 'NONE', #89984, #188719, #234347, .T. ) ;
#206155=AXIS2_PLACEMENT_3D ( 'NONE', #237545, #43200, #158054 ) ;
#206168=CARTESIAN_POINT ( 'NONE',  ( -20.93302460841142931, 65.68434038414338261, -63.98668807260656166 ) ) ;
#206195=VECTOR ( 'NONE', #16379, 1000.000000000000000 ) ;
#206198=CARTESIAN_POINT ( 'NONE',  ( 22.60000000000000142, 64.25043287652255231, -103.1239658536231047 ) ) ;
#206212=DIRECTION ( 'NONE',  ( -0.000000000000000000, 1.000000000000000000, 6.982962677686266711E-15 ) ) ;
#206227=CARTESIAN_POINT ( 'NONE',  ( 22.39999999999999503, 64.25000000001195133, -103.0231074845244024 ) ) ;
#206286=VERTEX_POINT ( 'NONE', #242435 ) ;
#206301=EDGE_CURVE ( 'NONE', #155916, #11015, #90899, .T. ) ;
#206317=ORIENTED_EDGE ( 'NONE', *, *, #135607, .F. ) ;
#206411=DIRECTION ( 'NONE',  ( 0.000000000000000000, 1.000000000000000000, 2.775557561562888827E-14 ) ) ;
#206437=VERTEX_POINT ( 'NONE', #54174 ) ;
#206440=CARTESIAN_POINT ( 'NONE',  ( 20.12518398540832010, 66.02491127934419524, -95.02643923205445731 ) ) ;
#206449=ORIENTED_EDGE ( 'NONE', *, *, #103107, .F. ) ;
#206469=DIRECTION ( 'NONE',  ( -0.000000000000000000, -6.982962677686266711E-15, 1.000000000000000000 ) ) ;
#206487=DIRECTION ( 'NONE',  ( 1.000000000000000000, 0.000000000000000000, 0.000000000000000000 ) ) ;
#206514=AXIS2_PLACEMENT_3D ( 'NONE', #233372, #194244, #115977 ) ;
#206535=CARTESIAN_POINT ( 'NONE',  ( -22.39999999999999858, 64.25000000001195133, -103.1231074845243825 ) ) ;
#206540=VERTEX_POINT ( 'NONE', #81423 ) ;
#206556=CARTESIAN_POINT ( 'NONE',  ( 19.99999999999998934, 64.25000000001176659, -78.17310748452439384 ) ) ;
#206570=VERTEX_POINT ( 'NONE', #42335 ) ;
#206571=EDGE_CURVE ( 'NONE', #206286, #200486, #46378, .T. ) ;
#206573=AXIS2_PLACEMENT_3D ( 'NONE', #105702, #41933, #60175 ) ;
#206581=ORIENTED_EDGE ( 'NONE', *, *, #241631, .F. ) ;
#206586=CARTESIAN_POINT ( 'NONE',  ( -18.50000000000000000, 66.85000000001186038, -90.67310748452436542 ) ) ;
#206599=ADVANCED_FACE ( 'NONE', ( #198830 ), #240534, .T. ) ;
#206644=FACE_OUTER_BOUND ( 'NONE', #161737, .T. ) ;
#206648=CARTESIAN_POINT ( 'NONE',  ( 23.24999999999999289, 64.25000000001202238, -114.7731074845243882 ) ) ;
#206744=EDGE_CURVE ( 'NONE', #72101, #109375, #21647, .T. ) ;
#206750=CARTESIAN_POINT ( 'NONE',  ( -21.05000000000000071, 87.75000000001173817, -72.62310748452422615 ) ) ;
#206754=EDGE_LOOP ( 'NONE', ( #12911, #15580, #31549, #136560, #114923, #152289, #10141, #173970, #100377, #30985, #87967, #153558 ) ) ;
#206770=ORIENTED_EDGE ( 'NONE', *, *, #121612, .T. ) ;
#206790=CARTESIAN_POINT ( 'NONE',  ( 18.41416235934318379, 85.50000000001169553, -62.92291809330222208 ) ) ;
#206808=FACE_OUTER_BOUND ( 'NONE', #181358, .T. ) ;
#206891=AXIS2_PLACEMENT_3D ( 'NONE', #194036, #153662, #171921 ) ;
#206894=DIRECTION ( 'NONE',  ( 0.000000000000000000, -7.116814260417668513E-15, 1.000000000000000000 ) ) ;
#206908=DIRECTION ( 'NONE',  ( -1.000000000000000000, 0.000000000000000000, -0.000000000000000000 ) ) ;
#206918=VERTEX_POINT ( 'NONE', #181562 ) ;
#206921=DIRECTION ( 'NONE',  ( 0.000000000000000000, 6.982962677686266711E-15, -1.000000000000000000 ) ) ;
#206927=DIRECTION ( 'NONE',  ( -1.000000000000000000, 0.000000000000000000, -0.000000000000000000 ) ) ;
#206930=LINE ( 'NONE', #184790, #242101 ) ;
#206938=AXIS2_PLACEMENT_3D ( 'NONE', #26587, #89101, #248188 ) ;
#206948=DIRECTION ( 'NONE',  ( 0.000000000000000000, 6.982962677686266711E-15, -1.000000000000000000 ) ) ;
#206976=ADVANCED_FACE ( 'NONE', ( #42050 ), #143690, .F. ) ;
#206978=DIRECTION ( 'NONE',  ( -0.000000000000000000, 1.000000000000000000, 6.352154140967427193E-15 ) ) ;
#207007=CARTESIAN_POINT ( 'NONE',  ( -21.04999999999999716, 64.25000000001175238, -76.36470817442145176 ) ) ;
#207008=CARTESIAN_POINT ( 'NONE',  ( -20.64999999999999858, 74.07476635515199348, -82.25335101765045920 ) ) ;
#207060=DIRECTION ( 'NONE',  ( 1.000000000000000000, 0.000000000000000000, 0.000000000000000000 ) ) ;
#207062=CARTESIAN_POINT ( 'NONE',  ( -20.54999999999999716, 68.75000000001179501, -81.87310748452436826 ) ) ;
#207072=ORIENTED_EDGE ( 'NONE', *, *, #178633, .F. ) ;
#207109=FACE_OUTER_BOUND ( 'NONE', #101504, .T. ) ;
#207124=CIRCLE ( 'NONE', #144727, 11.80000000000000426 ) ;
#207128=ORIENTED_EDGE ( 'NONE', *, *, #239136, .F. ) ;
#207146=CARTESIAN_POINT ( 'NONE',  ( -21.05000000000000071, 74.83729825007388570, -94.92310748452432279 ) ) ;
#207148=LINE ( 'NONE', #108044, #118453 ) ;
#207180=DIRECTION ( 'NONE',  ( -0.000000000000000000, -1.000000000000000000, -6.982962677686266711E-15 ) ) ;
#207184=CIRCLE ( 'NONE', #161387, 0.1000000000000028644 ) ;
#207261=FACE_OUTER_BOUND ( 'NONE', #93977, .T. ) ;
#207275=TOROIDAL_SURFACE ( 'NONE', #248962, 4.149999999999999467, 0.1000000000000000056 ) ;
#207291=FACE_OUTER_BOUND ( 'NONE', #226109, .T. ) ;
#207308=DIRECTION ( 'NONE',  ( -1.000000000000000000, -0.000000000000000000, -0.000000000000000000 ) ) ;
#207309=CIRCLE ( 'NONE', #161519, 11.64999999999999325 ) ;
#207325=CARTESIAN_POINT ( 'NONE',  ( -20.64999999999999858, 71.65000000001187175, -90.67310748452433700 ) ) ;
#207328=AXIS2_PLACEMENT_3D ( 'NONE', #189066, #174687, #32600 ) ;
#207334=EDGE_LOOP ( 'NONE', ( #146698, #241073, #85510, #114095 ) ) ;
#207368=AXIS2_PLACEMENT_3D ( 'NONE', #124327, #164735, #241699 ) ;
#207372=DIRECTION ( 'NONE',  ( -1.000000000000000000, -7.304098846218135653E-16, -4.639676173203994055E-30 ) ) ;
#207445=DIRECTION ( 'NONE',  ( 1.000000000000000000, 0.000000000000000000, 0.000000000000000000 ) ) ;
#207461=ORIENTED_EDGE ( 'NONE', *, *, #232144, .T. ) ;
#207472=EDGE_CURVE ( 'NONE', #41443, #193457, #228072, .T. ) ;
#207485=CARTESIAN_POINT ( 'NONE',  ( -20.54999999999999716, 68.75000000001185185, -90.77310748452435973 ) ) ;
#207497=ORIENTED_EDGE ( 'NONE', *, *, #205819, .F. ) ;
#207544=DIRECTION ( 'NONE',  ( -1.000000000000000000, 2.952720810173289112E-16, 2.061873921506763405E-30 ) ) ;
#207611=AXIS2_PLACEMENT_3D ( 'NONE', #93833, #246491, #209954 ) ;
#207634=AXIS2_PLACEMENT_3D ( 'NONE', #191751, #74374, #153926 ) ;
#207723=CYLINDRICAL_SURFACE ( 'NONE', #169017, 0.1000000000000028644 ) ;
#207725=CARTESIAN_POINT ( 'NONE',  ( 18.51565452909439813, 85.35285933885081988, -95.82819816328898810 ) ) ;
#207745=CARTESIAN_POINT ( 'NONE',  ( 20.12481660106788439, 66.47365600773694894, -94.79696581543133505 ) ) ;
#207751=EDGE_CURVE ( 'NONE', #250150, #74197, #24852, .T. ) ;
#207793=EDGE_CURVE ( 'NONE', #222093, #101654, #251310, .T. ) ;
#207801=DIRECTION ( 'NONE',  ( 1.000000000000000000, 0.000000000000000000, 0.000000000000000000 ) ) ;
#207819=DIRECTION ( 'NONE',  ( 0.000000000000000000, 0.000000000000000000, -1.000000000000000000 ) ) ;
#207889=ORIENTED_EDGE ( 'NONE', *, *, #249193, .T. ) ;
#207942=( GEOMETRIC_REPRESENTATION_CONTEXT ( 3 ) GLOBAL_UNCERTAINTY_ASSIGNED_CONTEXT ( ( #57145 ) ) GLOBAL_UNIT_ASSIGNED_CONTEXT ( ( #185580, #123049, #220848 ) ) REPRESENTATION_CONTEXT ( 'NONE', 'WORKASPACE' ) );
#207965=CARTESIAN_POINT ( 'NONE',  ( -20.54999999999999716, 76.00000000001170974, -69.52310748452431710 ) ) ;
#207968=DIRECTION ( 'NONE',  ( -7.304098846218134667E-16, 1.000000000000000000, 6.982962677686266711E-15 ) ) ;
#207970=DIRECTION ( 'NONE',  ( 1.000000000000000000, 0.000000000000000000, 0.000000000000000000 ) ) ;
#207987=FACE_OUTER_BOUND ( 'NONE', #148035, .T. ) ;
#207994=LINE ( 'NONE', #112728, #149320 ) ;
#208003=EDGE_LOOP ( 'NONE', ( #51457, #2474, #35726, #54859 ) ) ;
#208023=CARTESIAN_POINT ( 'NONE',  ( -23.25000000000000000, 74.00000000001186606, -89.79848556176222019 ) ) ;
#208026=CARTESIAN_POINT ( 'NONE',  ( 23.25000000000000355, 98.45632476063481420, -96.22920903679255389 ) ) ;
#208027=VERTEX_POINT ( 'NONE', #27682 ) ;
#208073=DIRECTION ( 'NONE',  ( 0.000000000000000000, 0.000000000000000000, 1.000000000000000000 ) ) ;
#208090=DIRECTION ( 'NONE',  ( 0.000000000000000000, 0.000000000000000000, 1.000000000000000000 ) ) ;
#208114=FACE_OUTER_BOUND ( 'NONE', #177219, .T. ) ;
#208140=DIRECTION ( 'NONE',  ( 0.000000000000000000, 0.000000000000000000, -1.000000000000000000 ) ) ;
#208144=LINE ( 'NONE', #166463, #19217 ) ;
#208147=DIRECTION ( 'NONE',  ( 0.000000000000000000, 6.982962677686266711E-15, -1.000000000000000000 ) ) ;
#208153=DIRECTION ( 'NONE',  ( 0.000000000000000000, 6.982962677686266711E-15, -1.000000000000000000 ) ) ;
#208155=VERTEX_POINT ( 'NONE', #194443 ) ;
#208205=CARTESIAN_POINT ( 'NONE',  ( 23.15000000000000213, 88.41227409416143246, -72.62310748452421194 ) ) ;
#208207=FACE_OUTER_BOUND ( 'NONE', #5361, .T. ) ;
#208220=CYLINDRICAL_SURFACE ( 'NONE', #85062, 4.049999999999998046 ) ;
#208222=LINE ( 'NONE', #243475, #221970 ) ;
#208230=EDGE_CURVE ( 'NONE', #65772, #101606, #155684, .T. ) ;
#208239=VERTEX_POINT ( 'NONE', #172338 ) ;
#208243=CARTESIAN_POINT ( 'NONE',  ( -22.39999999999999858, 68.20922040163854660, -103.1231074845243540 ) ) ;
#208245=CARTESIAN_POINT ( 'NONE',  ( 18.59999999999997655, 76.00000000001165290, -61.62310748452430431 ) ) ;
#208259=CARTESIAN_POINT ( 'NONE',  ( -20.85000000000000142, 64.25000000001176659, -76.30697314750248950 ) ) ;
#208278=CIRCLE ( 'NONE', #195822, 0.2000000000000057288 ) ;
#208330=DIRECTION ( 'NONE',  ( -1.000000000000000000, 0.000000000000000000, -0.000000000000000000 ) ) ;
#208338=ORIENTED_EDGE ( 'NONE', *, *, #232009, .T. ) ;
#208374=ORIENTED_EDGE ( 'NONE', *, *, #87635, .F. ) ;
#208401=EDGE_CURVE ( 'NONE', #191564, #9869, #110579, .T. ) ;
#208416=CARTESIAN_POINT ( 'NONE',  ( -18.46902351632713746, 85.50947011869274661, -96.03665355026690520 ) ) ;
#208432=DIRECTION ( 'NONE',  ( 0.000000000000000000, -7.429790795770644761E-15, 1.000000000000000000 ) ) ;
#208455=AXIS2_PLACEMENT_3D ( 'NONE', #364, #137303, #196023 ) ;
#208469=CARTESIAN_POINT ( 'NONE',  ( 20.95496329884391784, 65.43256679391885200, -95.44879755223956863 ) ) ;
#208475=AXIS2_PLACEMENT_3D ( 'NONE', #124767, #225117, #24398 ) ;
#208485=CARTESIAN_POINT ( 'NONE',  ( 18.59999999999997655, 77.16412189325286874, -61.60825939895269698 ) ) ;
#208504=LINE ( 'NONE', #166823, #3420 ) ;
#208532=ORIENTED_EDGE ( 'NONE', *, *, #188927, .T. ) ;
#208538=CARTESIAN_POINT ( 'NONE',  ( -21.00023020733438628, 69.60913075474422840, -103.0231074845243597 ) ) ;
#208539=ADVANCED_FACE ( 'NONE', ( #235650 ), #101626, .T. ) ;
#208543=EDGE_CURVE ( 'NONE', #16536, #101606, #161277, .T. ) ;
#208551=CIRCLE ( 'NONE', #220983, 0.1000000000000028644 ) ;
#208573=ORIENTED_EDGE ( 'NONE', *, *, #69963, .T. ) ;
#208580=VERTEX_POINT ( 'NONE', #84228 ) ;
#208585=EDGE_LOOP ( 'NONE', ( #246717, #61084, #66313, #182026 ) ) ;
#208634=ORIENTED_EDGE ( 'NONE', *, *, #54873, .F. ) ;
#208660=CARTESIAN_POINT ( 'NONE',  ( 21.30000000000002558, 76.00000000001195133, -103.0231074845243171 ) ) ;
#208661=LINE ( 'NONE', #87396, #232041 ) ;
#208663=ORIENTED_EDGE ( 'NONE', *, *, #39020, .F. ) ;
#208668=AXIS2_PLACEMENT_3D ( 'NONE', #64904, #164025, #244826 ) ;
#208704=VERTEX_POINT ( 'NONE', #187261 ) ;
#208731=AXIS2_PLACEMENT_3D ( 'NONE', #111844, #32329, #251329 ) ;
#208734=EDGE_CURVE ( 'NONE', #174146, #223676, #1694, .T. ) ;
#208742=CARTESIAN_POINT ( 'NONE',  ( 21.05000000000000071, 87.48912529308779540, -72.52310748452423184 ) ) ;
#208755=CARTESIAN_POINT ( 'NONE',  ( -20.54999999999999716, 71.75000000001186606, -90.77310748452434552 ) ) ;
#208832=SPHERICAL_SURFACE ( 'NONE', #134949, 0.1000000000000000056 ) ;
#208838=AXIS2_PLACEMENT_3D ( 'NONE', #161670, #78244, #156544 ) ;
#208863=CARTESIAN_POINT ( 'NONE',  ( 21.04999999999999716, 67.12791932463410660, -94.50206006569311512 ) ) ;
#208930=ORIENTED_EDGE ( 'NONE', *, *, #184736, .F. ) ;
#208952=CARTESIAN_POINT ( 'NONE',  ( -21.44999999999999929, 68.85000000001186038, -90.67310748452435121 ) ) ;
#208967=ORIENTED_EDGE ( 'NONE', *, *, #183862, .F. ) ;
#208973=ORIENTED_EDGE ( 'NONE', *, *, #103269, .F. ) ;
#208982=ORIENTED_EDGE ( 'NONE', *, *, #27910, .T. ) ;
#209005=VERTEX_POINT ( 'NONE', #24573 ) ;
#209007=ORIENTED_EDGE ( 'NONE', *, *, #32463, .T. ) ;
#209009=CARTESIAN_POINT ( 'NONE',  ( 20.50589344625387156, 65.51681206853663753, -95.45011250585221774 ) ) ;
#209054=FACE_OUTER_BOUND ( 'NONE', #167084, .T. ) ;
#209074=ORIENTED_EDGE ( 'NONE', *, *, #223839, .F. ) ;
#209084=CIRCLE ( 'NONE', #79869, 0.1000000000000052097 ) ;
#209090=CARTESIAN_POINT ( 'NONE',  ( 21.05000000000000071, 76.00000000001192291, -98.72310748452429152 ) ) ;
#209104=DIRECTION ( 'NONE',  ( 0.000000000000000000, -6.454785026890406770E-15, 1.000000000000000000 ) ) ;
#209106=DIRECTION ( 'NONE',  ( -0.8660254037844653530, 0.000000000000000000, -0.4999999999999539257 ) ) ;
#209120=VERTEX_POINT ( 'NONE', #212187 ) ;
#209127=LINE ( 'NONE', #30521, #243121 ) ;
#209171=VECTOR ( 'NONE', #207372, 1000.000000000000000 ) ;
#209175=VECTOR ( 'NONE', #177968, 1000.000000000000000 ) ;
#209177=ORIENTED_EDGE ( 'NONE', *, *, #96771, .F. ) ;
#209207=CARTESIAN_POINT ( 'NONE',  ( -20.54999999999999716, 76.00000000001170974, -69.52310748452431710 ) ) ;
#209209=LINE ( 'NONE', #113961, #220251 ) ;
#209239=CARTESIAN_POINT ( 'NONE',  ( -20.54999999999999361, 64.35000000001180354, -81.67310748452439384 ) ) ;
#209249=CARTESIAN_POINT ( 'NONE',  ( 21.07928932188134397, 69.67148334361864670, -103.1220026301787414 ) ) ;
#209251=CARTESIAN_POINT ( 'NONE',  ( 21.30000000000002558, 76.00000000001195133, -103.0231074845243171 ) ) ;
#209270=DIRECTION ( 'NONE',  ( 1.000000000000000000, -2.952720810173289112E-16, -2.061873921506763405E-30 ) ) ;
#209277=DIRECTION ( 'NONE',  ( 0.000000000000000000, 0.1568667991644355497, -0.9876197685951332295 ) ) ;
#209285=AXIS2_PLACEMENT_3D ( 'NONE', #20600, #173294, #178399 ) ;
#209310=VERTEX_POINT ( 'NONE', #101151 ) ;
#209313=CARTESIAN_POINT ( 'NONE',  ( 20.94999999999999929, 84.66355140188105111, -93.49900636645693908 ) ) ;
#209337=VECTOR ( 'NONE', #99225, 1000.000000000000000 ) ;
#209347=DIRECTION ( 'NONE',  ( 0.000000000000000000, -6.938893903907222067E-15, 1.000000000000000000 ) ) ;
#209359=CIRCLE ( 'NONE', #5335, 0.1000000000000028644 ) ;
#209390=DIRECTION ( 'NONE',  ( -1.000000000000000000, 0.000000000000000000, 0.000000000000000000 ) ) ;
#209391=ADVANCED_FACE ( 'NONE', ( #64642 ), #166349, .T. ) ;
#209401=AXIS2_PLACEMENT_3D ( 'NONE', #107085, #186648, #8010 ) ;
#209403=CYLINDRICAL_SURFACE ( 'NONE', #247043, 0.09999999999999939493 ) ;
#209444=UNCERTAINTY_MEASURE_WITH_UNIT (LENGTH_MEASURE( 1.000000000000000082E-05 ), #178879, 'distance_accuracy_value', 'NONE');
#209462=EDGE_LOOP ( 'NONE', ( #18369, #90281, #247829, #12935 ) ) ;
#209486=CARTESIAN_POINT ( 'NONE',  ( -20.94999999999999929, 76.00000000001170974, -69.52310748452431710 ) ) ;
#209489=ORIENTED_EDGE ( 'NONE', *, *, #137203, .F. ) ;
#209537=ORIENTED_EDGE ( 'NONE', *, *, #180633, .F. ) ;
#209539=DIRECTION ( 'NONE',  ( 0.000000000000000000, -6.853228547068871147E-15, 1.000000000000000000 ) ) ;
#209544=CARTESIAN_POINT ( 'NONE',  ( -22.39999999999999858, 64.25000000001195133, -103.0231074845244024 ) ) ;
#209545=ORIENTED_EDGE ( 'NONE', *, *, #70547, .T. ) ;
#209547=EDGE_CURVE ( 'NONE', #61112, #175899, #48574, .T. ) ;
#209606=ORIENTED_EDGE ( 'NONE', *, *, #6896, .T. ) ;
#209615=LINE ( 'NONE', #27161, #222078 ) ;
#209645=EDGE_LOOP ( 'NONE', ( #217854, #239300, #160221, #31659, #37712 ) ) ;
#209647=ORIENTED_EDGE ( 'NONE', *, *, #156567, .F. ) ;
#209651=DIRECTION ( 'NONE',  ( 0.000000000000000000, 1.000000000000000000, 6.938893903907222067E-15 ) ) ;
#209677=AXIS2_PLACEMENT_3D ( 'NONE', #173213, #54489, #213560 ) ;
#209700=DIRECTION ( 'NONE',  ( 0.000000000000000000, 0.000000000000000000, -1.000000000000000000 ) ) ;
#209714=CARTESIAN_POINT ( 'NONE',  ( 23.24999999999999289, 71.85000000001194564, -103.0231074845243455 ) ) ;
#209729=EDGE_CURVE ( 'NONE', #40263, #108305, #203543, .T. ) ;
#209755=CARTESIAN_POINT ( 'NONE',  ( -20.94999999999999929, 87.48912529308779540, -72.52310748452423184 ) ) ;
#209767=CARTESIAN_POINT ( 'NONE',  ( 23.14999999999999503, 64.35000000001186038, -90.87310748452438247 ) ) ;
#209772=EDGE_CURVE ( 'NONE', #35900, #183385, #4047, .T. ) ;
#209809=CARTESIAN_POINT ( 'NONE',  ( 21.14999999999999503, 87.65000000001192859, -100.1231074845242262 ) ) ;
#209842=VECTOR ( 'NONE', #154500, 1000.000000000000000 ) ;
#209844=CIRCLE ( 'NONE', #184874, 0.1000000000000028644 ) ;
#209942=ORIENTED_EDGE ( 'NONE', *, *, #57217, .T. ) ;
#209948=ORIENTED_EDGE ( 'NONE', *, *, #169063, .T. ) ;
#209952=CYLINDRICAL_SURFACE ( 'NONE', #215903, 0.1000000000000028644 ) ;
#209954=DIRECTION ( 'NONE',  ( 0.000000000000000000, 0.000000000000000000, 1.000000000000000000 ) ) ;
#209981=CYLINDRICAL_SURFACE ( 'NONE', #4033, 0.5000000000000004441 ) ;
#210006=CARTESIAN_POINT ( 'NONE',  ( -22.49533356619863156, 64.34999999370783996, -103.0882300648471528 ) ) ;
#210039=DIRECTION ( 'NONE',  ( 1.000000000000000000, 0.000000000000000000, 0.000000000000000000 ) ) ;
#210041=AXIS2_PLACEMENT_3D ( 'NONE', #98165, #115201, #55189 ) ;
#210069=ORIENTED_EDGE ( 'NONE', *, *, #174193, .T. ) ;
#210070=EDGE_LOOP ( 'NONE', ( #165205, #40519, #73904, #130263 ) ) ;
#210072=CIRCLE ( 'NONE', #181027, 0.1000000000000028644 ) ;
#210092=DIRECTION ( 'NONE',  ( 1.000000000000000000, 0.000000000000000000, 0.000000000000000000 ) ) ;
#210118=CARTESIAN_POINT ( 'NONE',  ( -23.25000000000000000, 84.59626168225486254, -93.57297996737396772 ) ) ;
#210127=EDGE_CURVE ( 'NONE', #116639, #192753, #61156, .T. ) ;
#210136=ORIENTED_EDGE ( 'NONE', *, *, #54620, .F. ) ;
#210139=EDGE_LOOP ( 'NONE', ( #216868, #198507, #94092 ) ) ;
#210168=ADVANCED_FACE ( 'NONE', ( #80697 ), #160288, .F. ) ;
#210288=CARTESIAN_POINT ( 'NONE',  ( 18.43473516226078956, 85.49494228277008290, -95.97720880117476838 ) ) ;
#210298=CARTESIAN_POINT ( 'NONE',  ( -23.15000000000000213, 85.60000000001203091, -114.7731074845242460 ) ) ;
#210306=CARTESIAN_POINT ( 'NONE',  ( 20.96937028524354929, 65.37553062838524909, -95.53168138335472293 ) ) ;
#210358=AXIS2_PLACEMENT_3D ( 'NONE', #238184, #161244, #23032 ) ;
#210363=CYLINDRICAL_SURFACE ( 'NONE', #1959, 12.87499999999999822 ) ;
#210369=ORIENTED_EDGE ( 'NONE', *, *, #197470, .F. ) ;
#210386=AXIS2_PLACEMENT_3D ( 'NONE', #249841, #35946, #11233 ) ;
#210406=ORIENTED_EDGE ( 'NONE', *, *, #165950, .F. ) ;
#210428=EDGE_CURVE ( 'NONE', #135352, #233834, #64585, .T. ) ;
#210462=CARTESIAN_POINT ( 'NONE',  ( -23.15000000000000213, 87.65000000001204228, -114.7731074845242318 ) ) ;
#210465=CARTESIAN_POINT ( 'NONE',  ( -18.50000000000000000, 85.42129027953507148, -62.69922530549790451 ) ) ;
#210474=CIRCLE ( 'NONE', #127076, 0.09999999999999939493 ) ;
#210493=CARTESIAN_POINT ( 'NONE',  ( 20.94403535211772294, 65.69367753730635684, -64.01892380663480253 ) ) ;
#210503=EDGE_LOOP ( 'NONE', ( #172881, #33631, #164938, #229951 ) ) ;
#210519=ORIENTED_EDGE ( 'NONE', *, *, #237094, .T. ) ;
#210538=DIRECTION ( 'NONE',  ( 0.000000000000000000, -6.608470384673558123E-15, 1.000000000000000000 ) ) ;
#210543=ADVANCED_FACE ( 'NONE', ( #28169 ), #157530, .T. ) ;
#210570=LINE ( 'NONE', #11087, #67157 ) ;
#210571=EDGE_LOOP ( 'NONE', ( #240651, #217185, #32431, #12610 ) ) ;
#210572=CARTESIAN_POINT ( 'NONE',  ( -23.25000000000000000, 77.25000000001165290, -61.72262673010922640 ) ) ;
#210577=DIRECTION ( 'NONE',  ( 1.000000000000000000, -7.304098846218134667E-16, -5.100424963727255829E-30 ) ) ;
#210589=ORIENTED_EDGE ( 'NONE', *, *, #173958, .F. ) ;
#210596=FACE_OUTER_BOUND ( 'NONE', #29994, .T. ) ;
#210627=CIRCLE ( 'NONE', #110668, 0.5000000000000004441 ) ;
#210628=DIRECTION ( 'NONE',  ( 0.000000000000000000, 0.000000000000000000, -1.000000000000000000 ) ) ;
#210647=VERTEX_POINT ( 'NONE', #111527 ) ;
#210661=CARTESIAN_POINT ( 'NONE',  ( -23.25000000000000000, 76.00000000001186606, -90.24810748452431142 ) ) ;
#210669=CARTESIAN_POINT ( 'NONE',  ( -23.15000000000000213, 74.08971962618008433, -90.39173962932538586 ) ) ;
#210673=AXIS2_PLACEMENT_3D ( 'NONE', #217101, #97131, #239265 ) ;
#210685=AXIS2_PLACEMENT_3D ( 'NONE', #220789, #186816, #203790 ) ;
#210692=CARTESIAN_POINT ( 'NONE',  ( 23.24999999999999289, 69.35000000001186038, -90.87310748452435405 ) ) ;
#210708=EDGE_CURVE ( 'NONE', #173939, #160204, #14553, .T. ) ;
#210715=ADVANCED_FACE ( 'NONE', ( #81347 ), #47822, .T. ) ;
#210754=DIRECTION ( 'NONE',  ( 1.000000000000000000, 0.000000000000000000, 0.000000000000000000 ) ) ;
#210791=ORIENTED_EDGE ( 'NONE', *, *, #42279, .T. ) ;
#210793=ADVANCED_FACE ( 'NONE', ( #98330 ), #83902, .T. ) ;
#210794=ORIENTED_EDGE ( 'NONE', *, *, #15605, .F. ) ;
#210812=ORIENTED_EDGE ( 'NONE', *, *, #88795, .T. ) ;
#210820=FACE_OUTER_BOUND ( 'NONE', #103595, .T. ) ;
#210887=CARTESIAN_POINT ( 'NONE',  ( -21.05000000000000071, 74.25000000001186606, -91.35359592662267403 ) ) ;
#210929=EDGE_LOOP ( 'NONE', ( #22182, #116979, #81895, #19118, #125345 ) ) ;
#210959=CARTESIAN_POINT ( 'NONE',  ( 18.39999999999999858, 85.50000000001189449, -95.99103808782457747 ) ) ;
#211012=DIRECTION ( 'NONE',  ( -1.000000000000000000, 0.000000000000000000, 0.000000000000000000 ) ) ;
#211026=AXIS2_PLACEMENT_3D ( 'NONE', #129626, #228744, #110055 ) ;
#211028=CIRCLE ( 'NONE', #127826, 4.000000000000003553 ) ;
#211030=CARTESIAN_POINT ( 'NONE',  ( 18.59999999999999787, 76.00000000001195133, -103.0231074845243171 ) ) ;
#211064=DIRECTION ( 'NONE',  ( 1.000000000000000000, 0.000000000000000000, 0.000000000000000000 ) ) ;
#211084=ORIENTED_EDGE ( 'NONE', *, *, #69222, .T. ) ;
#211086=ORIENTED_EDGE ( 'NONE', *, *, #125661, .F. ) ;
#211099=CYLINDRICAL_SURFACE ( 'NONE', #226813, 0.1000000000000028644 ) ;
#211112=ORIENTED_EDGE ( 'NONE', *, *, #144761, .F. ) ;
#211147=ORIENTED_EDGE ( 'NONE', *, *, #8333, .T. ) ;
#211190=FACE_OUTER_BOUND ( 'NONE', #73501, .T. ) ;
#211221=FACE_OUTER_BOUND ( 'NONE', #59649, .T. ) ;
#211226=LINE ( 'NONE', #32628, #23433 ) ;
#211274=DIRECTION ( 'NONE',  ( 0.000000000000000000, 1.000000000000000000, 6.688090509790097607E-15 ) ) ;
#211283=EDGE_CURVE ( 'NONE', #125644, #164289, #110748, .T. ) ;
#211354=DIRECTION ( 'NONE',  ( 1.000000000000000000, 0.000000000000000000, 0.000000000000000000 ) ) ;
#211374=CARTESIAN_POINT ( 'NONE',  ( 20.94999999999999574, 74.15091558138485084, -91.36709696307720208 ) ) ;
#211401=CARTESIAN_POINT ( 'NONE',  ( 18.59999999999999787, 77.83534155023627932, -91.46795619196132066 ) ) ;
#211411=DIRECTION ( 'NONE',  ( -0.000000000000000000, -0.01283462868040327436, 0.9999176327611370985 ) ) ;
#211443=TOROIDAL_SURFACE ( 'NONE', #78162, 12.97499999999999787, 0.1000000000000000056 ) ;
#211450=VERTEX_POINT ( 'NONE', #182124 ) ;
#211497=VERTEX_POINT ( 'NONE', #21773 ) ;
#211521=CIRCLE ( 'NONE', #99063, 0.1000000000000028644 ) ;
#211536=ORIENTED_EDGE ( 'NONE', *, *, #164843, .F. ) ;
#211546=ORIENTED_EDGE ( 'NONE', *, *, #215668, .F. ) ;
#211558=DIRECTION ( 'NONE',  ( 0.000000000000000000, 1.000000000000000000, 0.000000000000000000 ) ) ;
#211563=DIRECTION ( 'NONE',  ( 0.000000000000000000, -1.000000000000000000, -6.982962677686265922E-15 ) ) ;
#211571=DIRECTION ( 'NONE',  ( 1.296989514748957922E-15, 0.9887567792719351711, -0.1495327102803594987 ) ) ;
#211574=DIRECTION ( 'NONE',  ( 0.000000000000000000, 0.000000000000000000, -1.000000000000000000 ) ) ;
#211584=ORIENTED_EDGE ( 'NONE', *, *, #201559, .T. ) ;
#211596=CARTESIAN_POINT ( 'NONE',  ( 21.05000000000000071, 75.90156250001166427, -109.3223383946165939 ) ) ;
#211609=( BOUNDED_CURVE ( )  B_SPLINE_CURVE ( 3, ( #188192, #30410, #168675, #254543 ),
 .UNSPECIFIED., .F., .F. ) 
 B_SPLINE_CURVE_WITH_KNOTS ( ( 4, 4 ),
 ( 1.570796326794901665, 3.141592653589733608 ),
 .UNSPECIFIED. ) 
 CURVE ( )  GEOMETRIC_REPRESENTATION_ITEM ( )  RATIONAL_B_SPLINE_CURVE ( ( 1.000000000000000000, 0.8047378541243801475, 0.8047378541243801475, 1.000000000000000000 ) ) 
 REPRESENTATION_ITEM ( '' )  );
#211658=CARTESIAN_POINT ( 'NONE',  ( -22.50875500270927887, 76.10085791378664055, -114.7726746119221986 ) ) ;
#211713=AXIS2_PLACEMENT_3D ( 'NONE', #245116, #122622, #104296 ) ;
#211714=DIRECTION ( 'NONE',  ( 1.000000000000000000, -7.304098846218134667E-16, -5.100424963727256530E-30 ) ) ;
#211717=EDGE_LOOP ( 'NONE', ( #131752, #57273, #64160, #22723 ) ) ;
#211742=CARTESIAN_POINT ( 'NONE',  ( -23.25000000000000000, 65.66751761918648356, -63.92826094061123143 ) ) ;
#211763=ORIENTED_EDGE ( 'NONE', *, *, #137616, .F. ) ;
#211806=EDGE_CURVE ( 'NONE', #202516, #247315, #44317, .T. ) ;
#211809=ORIENTED_EDGE ( 'NONE', *, *, #187175, .T. ) ;
#211813=ORIENTED_EDGE ( 'NONE', *, *, #113980, .T. ) ;
#211825=CIRCLE ( 'NONE', #199361, 0.1999999999999987899 ) ;
#211836=DIRECTION ( 'NONE',  ( 0.000000000000000000, 6.982962677686266711E-15, -1.000000000000000000 ) ) ;
#211843=ADVANCED_FACE ( 'NONE', ( #217059 ), #48387, .T. ) ;
#211871=ADVANCED_FACE ( 'NONE', ( #39763 ), #107404, .T. ) ;
#211883=CARTESIAN_POINT ( 'NONE',  ( -18.59999999999999787, 64.35000000001187459, -90.87310748452438247 ) ) ;
#211898=CARTESIAN_POINT ( 'NONE',  ( -20.85000000000000142, 77.85161776048053639, -57.91991776492063337 ) ) ;
#211923=ORIENTED_EDGE ( 'NONE', *, *, #180459, .F. ) ;
#211958=CARTESIAN_POINT ( 'NONE',  ( -21.05000000000000071, 87.48912529308779540, -72.62310748452422615 ) ) ;
#211969=DIRECTION ( 'NONE',  ( -1.000000000000000000, 0.000000000000000000, -0.000000000000000000 ) ) ;
#211987=AXIS2_PLACEMENT_3D ( 'NONE', #213729, #135463, #113352 ) ;
#211998=EDGE_CURVE ( 'NONE', #91113, #5814, #131963, .T. ) ;
#212012=ORIENTED_EDGE ( 'NONE', *, *, #212538, .T. ) ;
#212081=EDGE_CURVE ( 'NONE', #206540, #181805, #102712, .T. ) ;
#212091=VECTOR ( 'NONE', #143731, 1000.000000000000000 ) ;
#212183=DIRECTION ( 'NONE',  ( 0.000000000000000000, 0.000000000000000000, -1.000000000000000000 ) ) ;
#212187=CARTESIAN_POINT ( 'NONE',  ( 18.59999999999999076, 64.25000000001176659, -78.17310748452439384 ) ) ;
#212209=CARTESIAN_POINT ( 'NONE',  ( -20.64999999999999858, 71.65000000001187175, -90.67310748452433700 ) ) ;
#212243=DIRECTION ( 'NONE',  ( 1.000000000000000000, 0.000000000000000000, 0.000000000000000000 ) ) ;
#212250=VERTEX_POINT ( 'NONE', #154975 ) ;
#212283=EDGE_CURVE ( 'NONE', #114552, #221948, #117111, .T. ) ;
#212308=EDGE_CURVE ( 'NONE', #232010, #8374, #119510, .T. ) ;
#212320=DIRECTION ( 'NONE',  ( 0.000000000000000000, 0.000000000000000000, 1.000000000000000000 ) ) ;
#212323=CARTESIAN_POINT ( 'NONE',  ( 21.00000000000000000, 66.25000000001179501, -81.87310748452438247 ) ) ;
#212350=DIRECTION ( 'NONE',  ( -1.000000000000000000, 0.000000000000000000, 0.000000000000000000 ) ) ;
#212396=LINE ( 'NONE', #113278, #152188 ) ;
#212429=DIRECTION ( 'NONE',  ( 0.000000000000000000, 0.000000000000000000, 1.000000000000000000 ) ) ;
#212436=ADVANCED_FACE ( 'NONE', ( #200494 ), #102905, .F. ) ;
#212455=DIRECTION ( 'NONE',  ( -1.000000000000000000, 0.000000000000000000, 0.000000000000000000 ) ) ;
#212485=EDGE_LOOP ( 'NONE', ( #206103, #191876, #250447, #121694, #184580 ) ) ;
#212522=CARTESIAN_POINT ( 'NONE',  ( -20.94999999999999929, 70.15000000001192859, -92.89061026024637613 ) ) ;
#212537=CARTESIAN_POINT ( 'NONE',  ( 18.59999999999999787, 77.85102823015273543, -91.36919421510179973 ) ) ;
#212538=EDGE_CURVE ( 'NONE', #127173, #87867, #132157, .T. ) ;
#212543=DIRECTION ( 'NONE',  ( 0.000000000000000000, 1.000000000000000000, 6.982962677686266711E-15 ) ) ;
#212562=CARTESIAN_POINT ( 'NONE',  ( -20.54999999999999716, 74.00000000001180922, -82.74772940728641402 ) ) ;
#212585=AXIS2_PLACEMENT_3D ( 'NONE', #121189, #3771, #22069 ) ;
#212588=VECTOR ( 'NONE', #78748, 1000.000000000000000 ) ;
#212599=AXIS2_PLACEMENT_3D ( 'NONE', #95690, #155711, #56542 ) ;
#212600=CARTESIAN_POINT ( 'NONE',  ( -18.59999999999999787, 64.35000000001190301, -96.00830171387039513 ) ) ;
#212601=CARTESIAN_POINT ( 'NONE',  ( -18.50000000000000355, 85.40000000001187175, -95.72584772486095517 ) ) ;
#212635=CARTESIAN_POINT ( 'NONE',  ( -21.05000000000000071, 69.65527659592170551, -103.0378253410479203 ) ) ;
#212702=LINE ( 'NONE', #34093, #23182 ) ;
#212725=AXIS2_PLACEMENT_3D ( 'NONE', #174592, #92415, #251491 ) ;
#212732=TOROIDAL_SURFACE ( 'NONE', #33698, 0.2000000000000000111, 0.1000000000000000056 ) ;
#212754=DIRECTION ( 'NONE',  ( -1.000000000000000000, 0.000000000000000000, -0.000000000000000000 ) ) ;
#212796=CIRCLE ( 'NONE', #83743, 0.09999999999999939493 ) ;
#212814=CARTESIAN_POINT ( 'NONE',  ( -23.15000000000000213, 84.66355140188093742, -79.04720860259155302 ) ) ;
#212836=EDGE_CURVE ( 'NONE', #603, #89644, #240661, .T. ) ;
#212852=ORIENTED_EDGE ( 'NONE', *, *, #49968, .T. ) ;
#212874=CIRCLE ( 'NONE', #58715, 2.000000000000001776 ) ;
#212889=AXIS2_PLACEMENT_3D ( 'NONE', #125072, #122507, #203321 ) ;
#212934=AXIS2_PLACEMENT_3D ( 'NONE', #37257, #17656, #97157 ) ;
#212937=ORIENTED_EDGE ( 'NONE', *, *, #188632, .F. ) ;
#212941=EDGE_CURVE ( 'NONE', #143163, #142060, #15842, .T. ) ;
#212946=ORIENTED_EDGE ( 'NONE', *, *, #59171, .F. ) ;
#212952=EDGE_CURVE ( 'NONE', #243017, #11996, #107377, .T. ) ;
#212954=CARTESIAN_POINT ( 'NONE',  ( 23.14999999999999858, 70.10000000001177511, -79.74220724918072278 ) ) ;
#212961=CARTESIAN_POINT ( 'NONE',  ( 21.07964655665547582, 67.22511038503330383, -90.80119090156031803 ) ) ;
#212976=CARTESIAN_POINT ( 'NONE',  ( -18.50000000000000000, 69.15387683765909799, -65.78538121767449809 ) ) ;
#212987=DIRECTION ( 'NONE',  ( -1.000000000000000000, 0.000000000000000000, -0.000000000000000000 ) ) ;
#212999=EDGE_CURVE ( 'NONE', #25605, #148456, #128059, .T. ) ;
#213002=DIRECTION ( 'NONE',  ( 0.000000000000000000, -6.661338147750933721E-15, 1.000000000000000000 ) ) ;
#213013=ADVANCED_FACE ( 'NONE', ( #29292 ), #198961, .F. ) ;
#213016=CARTESIAN_POINT ( 'NONE',  ( 18.59999999999999432, 77.29973367124280514, -112.9949779616549108 ) ) ;
#213018=ORIENTED_EDGE ( 'NONE', *, *, #235606, .F. ) ;
#213083=ORIENTED_EDGE ( 'NONE', *, *, #206134, .T. ) ;
#213089=ADVANCED_FACE ( 'NONE', ( #196036 ), #214310, .F. ) ;
#213109=ADVANCED_FACE ( 'NONE', ( #255944 ), #32639, .T. ) ;
#213111=AXIS2_PLACEMENT_3D ( 'NONE', #50321, #129868, #150733 ) ;
#213158=DIRECTION ( 'NONE',  ( 0.000000000000000000, 0.000000000000000000, -1.000000000000000000 ) ) ;
#213202=CARTESIAN_POINT ( 'NONE',  ( 20.94999999999999574, 87.65000000001192859, -100.1231074845242262 ) ) ;
#213211=DIRECTION ( 'NONE',  ( 1.000000000000000000, 0.000000000000000000, 0.000000000000000000 ) ) ;
#213212=CARTESIAN_POINT ( 'NONE',  ( -18.59999999999999787, 64.35000000001187459, -90.87310748452438247 ) ) ;
#213233=EDGE_CURVE ( 'NONE', #225625, #8311, #194894, .T. ) ;
#213255=CARTESIAN_POINT ( 'NONE',  ( 18.46163235739473407, 85.48015080692994161, -62.86549694464678595 ) ) ;
#213262=AXIS2_PLACEMENT_3D ( 'NONE', #208205, #131212, #227743 ) ;
#213285=CARTESIAN_POINT ( 'NONE',  ( 18.49999999999999289, 64.25000000001188027, -94.92310748452439384 ) ) ;
#213288=EDGE_CURVE ( 'NONE', #102678, #18466, #182428, .T. ) ;
#213309=CARTESIAN_POINT ( 'NONE',  ( -22.49436431346200038, 64.35004905235850003, -103.0900110142466417 ) ) ;
#213321=CARTESIAN_POINT ( 'NONE',  ( -18.59999999999999787, 74.16465844978745281, -91.46795619196133487 ) ) ;
#213331=DIRECTION ( 'NONE',  ( 0.000000000000000000, -6.982962677686266711E-15, 1.000000000000000000 ) ) ;
#213342=ORIENTED_EDGE ( 'NONE', *, *, #77677, .F. ) ;
#213413=ORIENTED_EDGE ( 'NONE', *, *, #70226, .F. ) ;
#213415=CIRCLE ( 'NONE', #246739, 0.1000000000000043771 ) ;
#213420=CARTESIAN_POINT ( 'NONE',  ( 21.05000000000000071, 76.00000000001186606, -90.87310748452429721 ) ) ;
#213460=ORIENTED_EDGE ( 'NONE', *, *, #38576, .T. ) ;
#213486=DIRECTION ( 'NONE',  ( -0.7071067811865389130, 4.937700262164590641E-15, -0.7071067811865561215 ) ) ;
#213527=ORIENTED_EDGE ( 'NONE', *, *, #11670, .T. ) ;
#213532=AXIS2_PLACEMENT_3D ( 'NONE', #73747, #95828, #32057 ) ;
#213539=CARTESIAN_POINT ( 'NONE',  ( -21.05000000000000071, 69.74218538953583391, -103.1208977758331571 ) ) ;
#213541=ADVANCED_FACE ( 'NONE', ( #216569 ), #62303, .T. ) ;
#213554=LINE ( 'NONE', #34968, #16320 ) ;
#213560=DIRECTION ( 'NONE',  ( 0.000000000000000000, -6.454785026890510900E-15, 1.000000000000000000 ) ) ;
#213582=ORIENTED_EDGE ( 'NONE', *, *, #101820, .T. ) ;
#213583=FACE_OUTER_BOUND ( 'NONE', #112844, .T. ) ;
#213584=DIRECTION ( 'NONE',  ( -0.000000000000000000, 1.000000000000000000, 6.982962677686266711E-15 ) ) ;
#213589=CARTESIAN_POINT ( 'NONE',  ( 21.14999999999999858, 65.28660755661196902, -90.77310748452438816 ) ) ;
#213613=CARTESIAN_POINT ( 'NONE',  ( 21.05000000000000071, 69.74218538953581970, -103.1208977758331429 ) ) ;
#213615=ORIENTED_EDGE ( 'NONE', *, *, #236349, .F. ) ;
#213636=EDGE_CURVE ( 'NONE', #111193, #4968, #28697, .T. ) ;
#213672=ORIENTED_EDGE ( 'NONE', *, *, #207751, .T. ) ;
#213696=VERTEX_POINT ( 'NONE', #144722 ) ;
#213721=CARTESIAN_POINT ( 'NONE',  ( 23.14999999999998792, 64.35000000001195986, -103.0231074845244024 ) ) ;
#213722=DIRECTION ( 'NONE',  ( 0.000000000000000000, -0.4999999999999689138, 0.8660254037844565822 ) ) ;
#213728=DIRECTION ( 'NONE',  ( 0.000000000000000000, 6.982962677686266711E-15, -1.000000000000000000 ) ) ;
#213729=CARTESIAN_POINT ( 'NONE',  ( -20.64999999999999858, 71.65000000001180069, -81.87310748452433984 ) ) ;
#213739=CIRCLE ( 'NONE', #101259, 0.1000000000000028644 ) ;
#213743=VERTEX_POINT ( 'NONE', #34759 ) ;
#213745=ORIENTED_EDGE ( 'NONE', *, *, #179060, .T. ) ;
#213759=CARTESIAN_POINT ( 'NONE',  ( -21.14999999999999858, 75.90220970870321082, -109.2809220950004203 ) ) ;
#213767=CIRCLE ( 'NONE', #105401, 0.1000000000000067224 ) ;
#213780=DIRECTION ( 'NONE',  ( 0.000000000000000000, 0.9893560106964510714, -0.1455152366551481502 ) ) ;
#213794=ORIENTED_EDGE ( 'NONE', *, *, #249193, .F. ) ;
#213829=DIRECTION ( 'NONE',  ( 1.000000000000000000, 0.000000000000000000, 0.000000000000000000 ) ) ;
#213850=CIRCLE ( 'NONE', #255302, 0.5000000000000004441 ) ;
#213853=CIRCLE ( 'NONE', #55590, 0.6000000000000033085 ) ;
#213855=CARTESIAN_POINT ( 'NONE',  ( 18.59999999999999432, 85.48068669529062902, -62.58199231576638510 ) ) ;
#213882=CARTESIAN_POINT ( 'NONE',  ( -21.93642651522410247, 68.67283376068614587, -103.0231074845243739 ) ) ;
#213885=CARTESIAN_POINT ( 'NONE',  ( -21.45000000000000284, 68.29142135624910281, -81.87310748452436826 ) ) ;
#213892=CIRCLE ( 'NONE', #222238, 4.000000000000003553 ) ;
#213898=CARTESIAN_POINT ( 'NONE',  ( -20.54999999999999716, 76.00000000001172396, -71.52310748452431710 ) ) ;
#213900=CARTESIAN_POINT ( 'NONE',  ( -18.59999999999999787, 65.66751761918648356, -63.92826094061123143 ) ) ;
#213908=CARTESIAN_POINT ( 'NONE',  ( -20.94999999999999929, 77.83585931145526615, -58.01866831572577610 ) ) ;
#213922=PLANE ( 'NONE',  #57586 ) ;
#213923=AXIS2_PLACEMENT_3D ( 'NONE', #193914, #171807, #253855 ) ;
#213924=CIRCLE ( 'NONE', #76551, 0.1000000000000028644 ) ;
#213932=DIRECTION ( 'NONE',  ( 0.000000000000000000, 0.9908441862701605762, 0.1350103645451835310 ) ) ;
#213933=DIRECTION ( 'NONE',  ( -5.603264701231743991E-32, -7.172728831056617961E-15, 1.000000000000000000 ) ) ;
#214007=CARTESIAN_POINT ( 'NONE',  ( 21.05000000000000071, 67.22371710471941242, -94.46447848938342418 ) ) ;
#214032=CARTESIAN_POINT ( 'NONE',  ( -20.54999999999999716, 76.00000000001170974, -69.52310748452431710 ) ) ;
#214040=AXIS2_PLACEMENT_3D ( 'NONE', #102405, #21634, #5892 ) ;
#214060=VERTEX_POINT ( 'NONE', #189650 ) ;
#214066=EDGE_CURVE ( 'NONE', #152778, #134706, #190601, .T. ) ;
#214077=FACE_OUTER_BOUND ( 'NONE', #112132, .T. ) ;
#214116=TOROIDAL_SURFACE ( 'NONE', #168371, 12.77499999999999858, 0.1000000000000000056 ) ;
#214133=AXIS2_PLACEMENT_3D ( 'NONE', #31497, #11924, #32786 ) ;
#214174=DIRECTION ( 'NONE',  ( 1.000000000000000000, 0.000000000000000000, 0.000000000000000000 ) ) ;
#214176=VERTEX_POINT ( 'NONE', #151829 ) ;
#214231=CIRCLE ( 'NONE', #101751, 11.80000000000000426 ) ;
#214275=CARTESIAN_POINT ( 'NONE',  ( -23.25000000000000000, 76.00000000001195133, -103.0231074845243171 ) ) ;
#214310=CYLINDRICAL_SURFACE ( 'NONE', #128421, 0.09999999999999867328 ) ;
#214315=DIRECTION ( 'NONE',  ( 1.000000000000000000, 0.000000000000000000, 0.000000000000000000 ) ) ;
#214353=ORIENTED_EDGE ( 'NONE', *, *, #143159, .F. ) ;
#214358=ORIENTED_EDGE ( 'NONE', *, *, #15857, .F. ) ;
#214362=DIRECTION ( 'NONE',  ( 1.000000000000000000, 0.000000000000000000, 0.000000000000000000 ) ) ;
#214372=ORIENTED_EDGE ( 'NONE', *, *, #21357, .F. ) ;
#214432=ORIENTED_EDGE ( 'NONE', *, *, #187950, .F. ) ;
#214436=FACE_OUTER_BOUND ( 'NONE', #20279, .T. ) ;
#214479=CARTESIAN_POINT ( 'NONE',  ( -21.14999999999999858, 76.10000000001203091, -114.6726782920691079 ) ) ;
#214486=CARTESIAN_POINT ( 'NONE',  ( -21.05000000000000071, 87.29603075034701476, -72.57100664418810254 ) ) ;
#214521=AXIS2_PLACEMENT_3D ( 'NONE', #53132, #153573, #132683 ) ;
#214528=TOROIDAL_SURFACE ( 'NONE', #2144, 2.100000000000002309, 0.1000000000000000056 ) ;
#214544=CARTESIAN_POINT ( 'NONE',  ( 18.31572054635706692, 85.54847543579069225, -62.67253731977577758 ) ) ;
#214549=CARTESIAN_POINT ( 'NONE',  ( 20.94999999999999929, 64.35000000001176090, -76.36470817442145176 ) ) ;
#214566=CIRCLE ( 'NONE', #52249, 0.1000000000000028644 ) ;
#214573=EDGE_CURVE ( 'NONE', #192382, #116639, #203429, .T. ) ;
#214603=ORIENTED_EDGE ( 'NONE', *, *, #31641, .T. ) ;
#214645=DIRECTION ( 'NONE',  ( -2.561896900575096011E-15, 0.5907332058517336115, -0.8068669527896984439 ) ) ;
#214654=AXIS2_PLACEMENT_3D ( 'NONE', #38285, #117809, #43416 ) ;
#214678=DIRECTION ( 'NONE',  ( 0.000000000000000000, 1.000000000000000000, 0.000000000000000000 ) ) ;
#214693=ORIENTED_EDGE ( 'NONE', *, *, #35488, .T. ) ;
#214697=DIRECTION ( 'NONE',  ( 0.000000000000000000, 0.000000000000000000, -1.000000000000000000 ) ) ;
#214709=AXIS2_PLACEMENT_3D ( 'NONE', #9070, #226832, #29946 ) ;
#214725=DIRECTION ( 'NONE',  ( 7.589415207398576792E-15, 1.000000000000000000, 6.982962677686266711E-15 ) ) ;
#214783=CIRCLE ( 'NONE', #31660, 0.1000000000000028644 ) ;
#214794=DIRECTION ( 'NONE',  ( -0.000000000000000000, 0.8660254037844377084, 0.5000000000000016653 ) ) ;
#214824=FACE_OUTER_BOUND ( 'NONE', #25520, .T. ) ;
#214844=TOROIDAL_SURFACE ( 'NONE', #60704, 7.800000000000000711, 0.1000000000000000056 ) ;
#214872=DIRECTION ( 'NONE',  ( 1.000000000000000000, 0.000000000000000000, 0.000000000000000000 ) ) ;
#214873=CARTESIAN_POINT ( 'NONE',  ( -18.59999999999999787, 66.75000000001179501, -81.87310748452438247 ) ) ;
#214900=CARTESIAN_POINT ( 'NONE',  ( 21.14999999999999858, 69.45934304831071415, -103.0231074845243597 ) ) ;
#214913=AXIS2_PLACEMENT_3D ( 'NONE', #79321, #122324, #140589 ) ;
#214916=CARTESIAN_POINT ( 'NONE',  ( -21.05000000000000071, 87.65000000001172964, -72.62310748452422615 ) ) ;
#214963=ORIENTED_EDGE ( 'NONE', *, *, #227153, .F. ) ;
#214966=CARTESIAN_POINT ( 'NONE',  ( 18.49999999999999289, 65.79142135624907439, -78.37310748452438247 ) ) ;
#214977=EDGE_CURVE ( 'NONE', #10839, #74222, #116131, .T. ) ;
#214993=ORIENTED_EDGE ( 'NONE', *, *, #248794, .T. ) ;
#214994=VERTEX_POINT ( 'NONE', #50781 ) ;
#215002=DIRECTION ( 'NONE',  ( -1.000000000000000000, 0.000000000000000000, -0.000000000000000000 ) ) ;
#215026=VERTEX_POINT ( 'NONE', #173374 ) ;
#215095=ADVANCED_FACE ( 'NONE', ( #141890 ), #100170, .F. ) ;
#215115=DIRECTION ( 'NONE',  ( 0.000000000000000000, 0.000000000000000000, 1.000000000000000000 ) ) ;
#215159=ORIENTED_EDGE ( 'NONE', *, *, #22895, .F. ) ;
#215187=DIRECTION ( 'NONE',  ( 1.000000000000000000, 0.000000000000000000, 0.000000000000000000 ) ) ;
#215237=CIRCLE ( 'NONE', #186393, 0.1000000000000028644 ) ;
#215266=CARTESIAN_POINT ( 'NONE',  ( -22.39999999999999858, 75.90000000001199965, -110.8138870828977218 ) ) ;
#215273=AXIS2_PLACEMENT_3D ( 'NONE', #250676, #211571, #171199 ) ;
#215314=CARTESIAN_POINT ( 'NONE',  ( 20.94999999999999574, 64.37928932189309705, -76.39152413686537102 ) ) ;
#215322=DIRECTION ( 'NONE',  ( 0.000000000000000000, -1.000000000000000000, -6.982962677686266711E-15 ) ) ;
#215336=EDGE_LOOP ( 'NONE', ( #64468, #164259, #186932, #114400 ) ) ;
#215370=VERTEX_POINT ( 'NONE', #207008 ) ;
#215402=FACE_OUTER_BOUND ( 'NONE', #78804, .T. ) ;
#215417=DIRECTION ( 'NONE',  ( -1.836970198721029934E-16, -1.000000000000000000, -6.982962677686266711E-15 ) ) ;
#215439=DIRECTION ( 'NONE',  ( 0.000000000000000000, 0.000000000000000000, -1.000000000000000000 ) ) ;
#215468=CIRCLE ( 'NONE', #136328, 0.1000000000000028644 ) ;
#215502=ORIENTED_EDGE ( 'NONE', *, *, #177493, .F. ) ;
#215505=DIRECTION ( 'NONE',  ( 0.000000000000000000, -1.000000000000000000, -6.982962677686265922E-15 ) ) ;
#215507=DIRECTION ( 'NONE',  ( 1.000000000000000000, 0.000000000000000000, 0.000000000000000000 ) ) ;
#215545=DIRECTION ( 'NONE',  ( 0.000000000000000000, -6.853228547068871147E-15, 1.000000000000000000 ) ) ;
#215574=CIRCLE ( 'NONE', #44897, 0.1000000000000028644 ) ;
#215579=CYLINDRICAL_SURFACE ( 'NONE', #174877, 4.049999999999998046 ) ;
#215600=AXIS2_PLACEMENT_3D ( 'NONE', #229238, #70179, #31062 ) ;
#215612=ORIENTED_EDGE ( 'NONE', *, *, #188632, .T. ) ;
#215613=ADVANCED_FACE ( 'NONE', ( #188101 ), #87709, .T. ) ;
#215622=VERTEX_POINT ( 'NONE', #185531 ) ;
#215668=EDGE_CURVE ( 'NONE', #116663, #132890, #165998, .T. ) ;
#215704=VECTOR ( 'NONE', #231592, 1000.000000000000000 ) ;
#215775=LINE ( 'NONE', #95824, #209175 ) ;
#215806=DIRECTION ( 'NONE',  ( -1.000000000000000000, -0.000000000000000000, -0.000000000000000000 ) ) ;
#215833=ORIENTED_EDGE ( 'NONE', *, *, #151337, .T. ) ;
#215843=EDGE_CURVE ( 'NONE', #161543, #185034, #137779, .T. ) ;
#215849=CARTESIAN_POINT ( 'NONE',  ( -18.42637059832564361, 85.49694546190137601, -62.91403017472440951 ) ) ;
#215898=ORIENTED_EDGE ( 'NONE', *, *, #170471, .T. ) ;
#215901=AXIS2_PLACEMENT_3D ( 'NONE', #251944, #73344, #155461 ) ;
#215903=AXIS2_PLACEMENT_3D ( 'NONE', #131678, #192946, #115984 ) ;
#215945=VERTEX_POINT ( 'NONE', #214966 ) ;
#215962=FACE_OUTER_BOUND ( 'NONE', #220969, .T. ) ;
#215975=LINE ( 'NONE', #96034, #63560 ) ;
#215983=VERTEX_POINT ( 'NONE', #134137 ) ;
#216005=VECTOR ( 'NONE', #106777, 1000.000000000000000 ) ;
#216009=CIRCLE ( 'NONE', #249362, 0.1000000000000028644 ) ;
#216019=CARTESIAN_POINT ( 'NONE',  ( 18.59999999999999432, 74.27191306321758191, -116.1386724793565577 ) ) ;
#216056=FACE_OUTER_BOUND ( 'NONE', #122746, .T. ) ;
#216063=VERTEX_POINT ( 'NONE', #4872 ) ;
#216069=AXIS2_PLACEMENT_3D ( 'NONE', #250011, #94780, #16550 ) ;
#216113=VERTEX_POINT ( 'NONE', #166576 ) ;
#216172=CARTESIAN_POINT ( 'NONE',  ( -23.25000000000000000, 87.75000000001202238, -114.7731074845242318 ) ) ;
#216201=LINE ( 'NONE', #81801, #192596 ) ;
#216229=DIRECTION ( 'NONE',  ( -1.000000000000000000, 2.952720810173289112E-16, 2.061873921506763405E-30 ) ) ;
#216255=TOROIDAL_SURFACE ( 'NONE', #128799, 0.2000000000000000111, 0.1000000000000000056 ) ;
#216260=AXIS2_PLACEMENT_3D ( 'NONE', #25352, #65735, #8345 ) ;
#216267=AXIS2_PLACEMENT_3D ( 'NONE', #249418, #27825, #229843 ) ;
#216276=CARTESIAN_POINT ( 'NONE',  ( 18.49999999999999289, 68.87972903831409610, -65.86354444268503983 ) ) ;
#216293=DIRECTION ( 'NONE',  ( 0.000000000000000000, -0.4930308989875170078, -0.8700118002898356018 ) ) ;
#216303=VERTEX_POINT ( 'NONE', #180674 ) ;
#216305=DIRECTION ( 'NONE',  ( -1.000000000000000000, -0.000000000000000000, 0.000000000000000000 ) ) ;
#216319=AXIS2_PLACEMENT_3D ( 'NONE', #12919, #247647, #33782 ) ;
#216347=DIRECTION ( 'NONE',  ( 0.000000000000000000, 0.000000000000000000, -1.000000000000000000 ) ) ;
#216351=VECTOR ( 'NONE', #17487, 1000.000000000000000 ) ;
#216405=DIRECTION ( 'NONE',  ( 1.000000000000000000, -7.304098846218134667E-16, -5.100424963727255829E-30 ) ) ;
#216406=DIRECTION ( 'NONE',  ( 0.000000000000000000, -6.938893903907222067E-15, 1.000000000000000000 ) ) ;
#216411=CARTESIAN_POINT ( 'NONE',  ( 21.05000000000000071, 85.40000000001188596, -93.12913836187179584 ) ) ;
#216427=SHAPE_DEFINITION_REPRESENTATION ( #184567, #178537 ) ;
#216446=DIRECTION ( 'NONE',  ( 0.000000000000000000, -6.454785026890510900E-15, 1.000000000000000000 ) ) ;
#216467=EDGE_CURVE ( 'NONE', #87934, #158368, #134510, .T. ) ;
#216482=AXIS2_PLACEMENT_3D ( 'NONE', #58211, #159925, #76502 ) ;
#216503=CARTESIAN_POINT ( 'NONE',  ( -20.85000000000000142, 76.00000000001165290, -61.62310748452430431 ) ) ;
#216516=ORIENTED_EDGE ( 'NONE', *, *, #33500, .F. ) ;
#216567=EDGE_CURVE ( 'NONE', #53558, #51895, #235917, .T. ) ;
#216569=FACE_OUTER_BOUND ( 'NONE', #125495, .T. ) ;
#216580=TOROIDAL_SURFACE ( 'NONE', #8317, 2.100000000000002309, 0.1000000000000000056 ) ;
#216583=ORIENTED_EDGE ( 'NONE', *, *, #233382, .T. ) ;
#216595=AXIS2_PLACEMENT_3D ( 'NONE', #75250, #192607, #212183 ) ;
#216606=CARTESIAN_POINT ( 'NONE',  ( 23.14999999999999503, 64.35000000001186038, -90.87310748452438247 ) ) ;
#216625=VERTEX_POINT ( 'NONE', #198315 ) ;
#216630=EDGE_CURVE ( 'NONE', #96528, #237868, #9808, .T. ) ;
#216667=AXIS2_PLACEMENT_3D ( 'NONE', #79729, #98006, #58880 ) ;
#216696=CARTESIAN_POINT ( 'NONE',  ( -20.64999999999999858, 84.66355140188105111, -93.49900636645693908 ) ) ;
#216710=EDGE_CURVE ( 'NONE', #12008, #416, #148984, .T. ) ;
#216717=AXIS2_PLACEMENT_3D ( 'NONE', #35848, #114069, #120225 ) ;
#216752=VECTOR ( 'NONE', #80052, 1000.000000000000000 ) ;
#216778=EDGE_CURVE ( 'NONE', #206570, #215370, #5510, .T. ) ;
#216818=CIRCLE ( 'NONE', #208475, 0.1000000000000028644 ) ;
#216868=ORIENTED_EDGE ( 'NONE', *, *, #80247, .T. ) ;
#216904=CARTESIAN_POINT ( 'NONE',  ( -23.15000000000000213, 73.50000000001180922, -82.74772940728642823 ) ) ;
#217019=CARTESIAN_POINT ( 'NONE',  ( 18.49999999999999645, 77.16412189325286874, -61.60825939895269698 ) ) ;
#217029=DIRECTION ( 'NONE',  ( 0.000000000000000000, -1.000000000000000000, -8.717686153663073805E-15 ) ) ;
#217035=CYLINDRICAL_SURFACE ( 'NONE', #138570, 0.09999999999999939493 ) ;
#217058=DIRECTION ( 'NONE',  ( 0.000000000000000000, 1.000000000000000000, 6.982962677686266711E-15 ) ) ;
#217059=FACE_OUTER_BOUND ( 'NONE', #171187, .T. ) ;
#217066=CARTESIAN_POINT ( 'NONE',  ( 18.59999999999998721, 69.15387683765909799, -65.78538121767449809 ) ) ;
#217068=ORIENTED_EDGE ( 'NONE', *, *, #101678, .T. ) ;
#217096=CARTESIAN_POINT ( 'NONE',  ( -20.94999999999999929, 76.00000000001179501, -81.32310748452431426 ) ) ;
#217101=CARTESIAN_POINT ( 'NONE',  ( -21.05000000000000071, 74.16465844978745281, -91.46795619196133487 ) ) ;
#217129=CARTESIAN_POINT ( 'NONE',  ( 20.94999999999999929, 70.60000000001178933, -79.41707660717679573 ) ) ;
#217149=AXIS2_PLACEMENT_3D ( 'NONE', #126295, #20808, #165445 ) ;
#217157=ORIENTED_EDGE ( 'NONE', *, *, #185848, .F. ) ;
#217169=ADVANCED_FACE ( 'NONE', ( #131307 ), #8803, .F. ) ;
#217172=EDGE_LOOP ( 'NONE', ( #215502, #128124, #212012, #21009 ) ) ;
#217185=ORIENTED_EDGE ( 'NONE', *, *, #14869, .F. ) ;
#217351=CARTESIAN_POINT ( 'NONE',  ( 21.05000000000000071, 71.14953271029224879, -90.98884007552265984 ) ) ;
#217360=DIRECTION ( 'NONE',  ( 0.000000000000000000, -6.938893903907222067E-15, 1.000000000000000000 ) ) ;
#217364=DIRECTION ( 'NONE',  ( 1.000000000000000000, 0.000000000000000000, 0.000000000000000000 ) ) ;
#217387=ORIENTED_EDGE ( 'NONE', *, *, #41375, .F. ) ;
#217404=LINE ( 'NONE', #118336, #245119 ) ;
#217418=DIRECTION ( 'NONE',  ( 1.000000000000000000, 0.000000000000000000, 0.000000000000000000 ) ) ;
#217491=DIRECTION ( 'NONE',  ( 1.000000000000000000, 0.000000000000000000, 0.000000000000000000 ) ) ;
#217500=CARTESIAN_POINT ( 'NONE',  ( 22.39999999999999503, 76.10085836911075319, -114.7726746080137019 ) ) ;
#217521=ORIENTED_EDGE ( 'NONE', *, *, #160921, .T. ) ;
#217550=CARTESIAN_POINT ( 'NONE',  ( -23.15000000000000213, 85.00000000001179501, -79.41707660717668205 ) ) ;
#217556=DIRECTION ( 'NONE',  ( 0.000000000000000000, 6.982962677686266711E-15, -1.000000000000000000 ) ) ;
#217569=DIRECTION ( 'NONE',  ( 1.000000000000000000, 0.000000000000000000, 0.000000000000000000 ) ) ;
#217576=ORIENTED_EDGE ( 'NONE', *, *, #15101, .F. ) ;
#217599=EDGE_CURVE ( 'NONE', #206540, #159653, #60060, .T. ) ;
#217640=ORIENTED_EDGE ( 'NONE', *, *, #164172, .F. ) ;
#217644=ORIENTED_EDGE ( 'NONE', *, *, #128742, .F. ) ;
#217653=CARTESIAN_POINT ( 'NONE',  ( -20.64999999999999858, 68.75000000001185185, -90.77310748452435973 ) ) ;
#217654=TOROIDAL_SURFACE ( 'NONE', #1361, 11.65000000000000036, 0.1000000000000000056 ) ;
#217659=PLANE ( 'NONE',  #129190 ) ;
#217660=DIRECTION ( 'NONE',  ( 1.000000000000000000, 0.000000000000000000, 0.000000000000000000 ) ) ;
#217665=EDGE_CURVE ( 'NONE', #24108, #189878, #176791, .T. ) ;
#217667=CARTESIAN_POINT ( 'NONE',  ( -1.739115166359751801E-14, 64.35000000001181775, -81.67310748452439384 ) ) ;
#217674=CARTESIAN_POINT ( 'NONE',  ( 23.14999999999999503, 69.55000000001179217, -81.87310748452435405 ) ) ;
#217686=( BOUNDED_CURVE ( )  B_SPLINE_CURVE ( 3, ( #69342, #28966, #189281, #19633 ),
 .UNSPECIFIED., .F., .F. ) 
 B_SPLINE_CURVE_WITH_KNOTS ( ( 4, 4 ),
 ( 0.06456096931748350753, 3.077031684272309775 ),
 .UNSPECIFIED. ) 
 CURVE ( )  GEOMETRIC_REPRESENTATION_ITEM ( )  RATIONAL_B_SPLINE_CURVE ( ( 1.000000000000000000, 0.3763440860215095940, 0.3763440860215095940, 1.000000000000000000 ) ) 
 REPRESENTATION_ITEM ( '' )  );
#217689=VECTOR ( 'NONE', #73721, 1000.000000000000000 ) ;
#217693=CARTESIAN_POINT ( 'NONE',  ( -18.54159361262954775, 85.46313213550493515, -95.97398526823127440 ) ) ;
#217707=CARTESIAN_POINT ( 'NONE',  ( -22.39999999999999858, 76.10085836911075319, -114.7726746080137019 ) ) ;
#217710=AXIS2_PLACEMENT_3D ( 'NONE', #224715, #164764, #223432 ) ;
#217742=VECTOR ( 'NONE', #16783, 999.9999999999998863 ) ;
#217744=ORIENTED_EDGE ( 'NONE', *, *, #154628, .F. ) ;
#217823=ORIENTED_EDGE ( 'NONE', *, *, #200492, .F. ) ;
#217854=ORIENTED_EDGE ( 'NONE', *, *, #212999, .T. ) ;
#217882=ORIENTED_EDGE ( 'NONE', *, *, #246602, .F. ) ;
#217927=ADVANCED_FACE ( 'NONE', ( #82551 ), #81274, .F. ) ;
#217933=DIRECTION ( 'NONE',  ( -1.000000000000000000, 0.000000000000000000, 0.000000000000000000 ) ) ;
#218117=CARTESIAN_POINT ( 'NONE',  ( -20.54999999999999716, 85.00000000001188027, -93.62913836187181005 ) ) ;
#218119=CARTESIAN_POINT ( 'NONE',  ( 22.50000000000000000, 64.35042919246716053, -103.1231074845243825 ) ) ;
#218126=VERTEX_POINT ( 'NONE', #13335 ) ;
#218174=CARTESIAN_POINT ( 'NONE',  ( -23.25000000000000000, 64.35000000001180354, -81.67310748452439384 ) ) ;
#218198=CARTESIAN_POINT ( 'NONE',  ( -20.64999999999999858, 74.00000000001180922, -82.34772940728642254 ) ) ;
#218208=ADVANCED_FACE ( 'NONE', ( #234950 ), #155448, .T. ) ;
#218211=DIRECTION ( 'NONE',  ( 0.000000000000000000, 6.982962677686266711E-15, -1.000000000000000000 ) ) ;
#218216=DIRECTION ( 'NONE',  ( -1.000000000000000000, 3.265361837132813093E-16, 2.280189983783949500E-30 ) ) ;
#218253=ORIENTED_EDGE ( 'NONE', *, *, #169580, .T. ) ;
#218314=EDGE_LOOP ( 'NONE', ( #56271, #99090, #186260, #129941 ) ) ;
#218341=ORIENTED_EDGE ( 'NONE', *, *, #108712, .T. ) ;
#218352=ORIENTED_EDGE ( 'NONE', *, *, #169322, .F. ) ;
#218379=DIRECTION ( 'NONE',  ( 0.000000000000000000, -0.1350103645451807555, -0.9908441862701610203 ) ) ;
#218386=EDGE_CURVE ( 'NONE', #46226, #227104, #97432, .T. ) ;
#218388=ORIENTED_EDGE ( 'NONE', *, *, #50153, .F. ) ;
#218394=DIRECTION ( 'NONE',  ( 1.000000000000000000, -0.000000000000000000, 0.000000000000000000 ) ) ;
#218400=CARTESIAN_POINT ( 'NONE',  ( 21.05000000000000071, 76.00000000001173817, -72.42310748452430857 ) ) ;
#218417=CYLINDRICAL_SURFACE ( 'NONE', #222688, 0.1000000000000028644 ) ;
#218440=EDGE_CURVE ( 'NONE', #37642, #196167, #205799, .T. ) ;
#218468=AXIS2_PLACEMENT_3D ( 'NONE', #153, #122711, #100517 ) ;
#218479=CARTESIAN_POINT ( 'NONE',  ( -18.50000000000000000, 76.00000000001195133, -103.0231074845243171 ) ) ;
#218485=VERTEX_POINT ( 'NONE', #131351 ) ;
#218519=DIRECTION ( 'NONE',  ( -5.603264701231743991E-32, -7.172728831056617961E-15, 1.000000000000000000 ) ) ;
#218539=AXIS2_PLACEMENT_3D ( 'NONE', #257207, #99445, #179047 ) ;
#218546=ORIENTED_EDGE ( 'NONE', *, *, #213233, .T. ) ;
#218596=DIRECTION ( 'NONE',  ( 0.000000000000000000, -6.352154140967427193E-15, 1.000000000000000000 ) ) ;
#218676=DIRECTION ( 'NONE',  ( 0.000000000000000000, 6.938893903907222067E-15, -1.000000000000000000 ) ) ;
#218715=CIRCLE ( 'NONE', #139604, 2.100000000000004530 ) ;
#218743=TOROIDAL_SURFACE ( 'NONE', #52158, 0.2000000000000000111, 0.1000000000000000056 ) ;
#218765=DIRECTION ( 'NONE',  ( 0.000000000000000000, -6.982962677686266711E-15, 1.000000000000000000 ) ) ;
#218778=CYLINDRICAL_SURFACE ( 'NONE', #190769, 0.1000000000000028644 ) ;
#218779=AXIS2_PLACEMENT_3D ( 'NONE', #195094, #114248, #213331 ) ;
#218811=DIRECTION ( 'NONE',  ( 0.000000000000000000, 6.982962677686266711E-15, -1.000000000000000000 ) ) ;
#218814=DIRECTION ( 'NONE',  ( 0.000000000000000000, 6.982962677686267499E-15, -1.000000000000000000 ) ) ;
#218843=CARTESIAN_POINT ( 'NONE',  ( 23.24999999999999289, 69.55000000001203375, -114.7731074845243455 ) ) ;
#218844=DIRECTION ( 'NONE',  ( -1.000000000000000000, -9.012599976027990443E-15, -6.882867235861669241E-14 ) ) ;
#218848=VECTOR ( 'NONE', #195014, 1000.000000000000000 ) ;
#218871=ADVANCED_FACE ( 'NONE', ( #198720 ), #85134, .T. ) ;
#218881=DIRECTION ( 'NONE',  ( 0.000000000000000000, -6.467318590049456648E-15, 1.000000000000000000 ) ) ;
#218884=ORIENTED_EDGE ( 'NONE', *, *, #84584, .F. ) ;
#218907=CARTESIAN_POINT ( 'NONE',  ( -18.58735405345342429, 85.56647862034827767, -62.70039283825828846 ) ) ;
#218925=VECTOR ( 'NONE', #104243, 1000.000000000000000 ) ;
#218946=LINE ( 'NONE', #237242, #39776 ) ;
#218968=DIRECTION ( 'NONE',  ( 1.000000000000000000, 0.000000000000000000, 0.000000000000000000 ) ) ;
#218976=EDGE_CURVE ( 'NONE', #123658, #167394, #81061, .T. ) ;
#218994=PRODUCT_CONTEXT ( 'NONE', #230605, 'mechanical' ) ;
#218997=ORIENTED_EDGE ( 'NONE', *, *, #58654, .T. ) ;
#219009=LINE ( 'NONE', #202031, #13896 ) ;
#219018=ADVANCED_FACE ( 'NONE', ( #103453 ), #205122, .F. ) ;
#219037=CIRCLE ( 'NONE', #65107, 0.09999999999999939493 ) ;
#219054=CARTESIAN_POINT ( 'NONE',  ( 18.59999999999997655, 64.25000000001170974, -69.52310748452438816 ) ) ;
#219058=DIRECTION ( 'NONE',  ( -1.000000000000000000, 0.000000000000000000, 0.000000000000000000 ) ) ;
#219079=DIRECTION ( 'NONE',  ( 1.000000000000000000, 0.000000000000000000, 0.000000000000000000 ) ) ;
#219092=ORIENTED_EDGE ( 'NONE', *, *, #139230, .T. ) ;
#219117=CARTESIAN_POINT ( 'NONE',  ( -21.64999999999999858, 68.65000000001187175, -90.67310748452436542 ) ) ;
#219152=TOROIDAL_SURFACE ( 'NONE', #111026, 11.65000000000000036, 0.1000000000000000056 ) ;
#219178=ORIENTED_EDGE ( 'NONE', *, *, #81043, .T. ) ;
#219188=DIRECTION ( 'NONE',  ( -1.000000000000000000, 0.000000000000000000, -0.000000000000000000 ) ) ;
#219201=ADVANCED_FACE ( 'NONE', ( #47335 ), #8244, .T. ) ;
#219251=ADVANCED_FACE ( 'NONE', ( #82156 ), #26081, .F. ) ;
#219285=CARTESIAN_POINT ( 'NONE',  ( -22.47071067811865319, 75.90090754530939421, -110.7431822290223806 ) ) ;
#219286=ADVANCED_FACE ( 'NONE', ( #46894 ), #123896, .F. ) ;
#219314=CARTESIAN_POINT ( 'NONE',  ( -20.54999999999999716, 66.65000000001180069, -81.87310748452438247 ) ) ;
#219343=CIRCLE ( 'NONE', #177694, 0.1000000000000028644 ) ;
#219385=DIRECTION ( 'NONE',  ( -1.000000000000000000, -0.000000000000000000, -0.000000000000000000 ) ) ;
#219398=CIRCLE ( 'NONE', #106980, 0.1000000000000028644 ) ;
#219431=EDGE_CURVE ( 'NONE', #111551, #81780, #93736, .T. ) ;
#219474=EDGE_CURVE ( 'NONE', #165247, #233834, #131323, .T. ) ;
#219494=CYLINDRICAL_SURFACE ( 'NONE', #131584, 11.80000000000000426 ) ;
#219495=ORIENTED_EDGE ( 'NONE', *, *, #136107, .T. ) ;
#219563=DIRECTION ( 'NONE',  ( 1.000000000000000000, 0.000000000000000000, 0.000000000000000000 ) ) ;
#219568=CARTESIAN_POINT ( 'NONE',  ( 20.75572585718184726, 67.11768327161587422, -94.52584908581822276 ) ) ;
#219571=ORIENTED_EDGE ( 'NONE', *, *, #47644, .T. ) ;
#219605=CARTESIAN_POINT ( 'NONE',  ( -18.59999999999999787, 74.13328508995456900, -91.27043223824230722 ) ) ;
#219664=AXIS2_PLACEMENT_3D ( 'NONE', #256113, #16311, #78802 ) ;
#219668=ORIENTED_EDGE ( 'NONE', *, *, #236990, .T. ) ;
#219682=EDGE_CURVE ( 'NONE', #107353, #39176, #31090, .T. ) ;
#219689=PLANE ( 'NONE',  #187804 ) ;
#219799=AXIS2_PLACEMENT_3D ( 'NONE', #127675, #104230, #45563 ) ;
#219814=EDGE_CURVE ( 'NONE', #86681, #201690, #106545, .T. ) ;
#219822=FACE_OUTER_BOUND ( 'NONE', #28838, .T. ) ;
#219839=ORIENTED_EDGE ( 'NONE', *, *, #257376, .F. ) ;
#219857=ORIENTED_EDGE ( 'NONE', *, *, #75332, .F. ) ;
#219877=ORIENTED_EDGE ( 'NONE', *, *, #207793, .T. ) ;
#219900=ORIENTED_EDGE ( 'NONE', *, *, #229993, .T. ) ;
#219902=CARTESIAN_POINT ( 'NONE',  ( 18.49999999999999289, 64.35000000001201670, -114.7731074845243882 ) ) ;
#219921=ADVANCED_FACE ( 'NONE', ( #77858 ), #156505, .T. ) ;
#219939=ADVANCED_FACE ( 'NONE', ( #209054 ), #6993, .T. ) ;
#219943=AXIS2_PLACEMENT_3D ( 'NONE', #5894, #204101, #104970 ) ;
#219948=CARTESIAN_POINT ( 'NONE',  ( -20.94999999999999929, 77.84915357198768504, -57.91714086472724432 ) ) ;
#219958=CIRCLE ( 'NONE', #111821, 0.1999999999999987899 ) ;
#219965=DIRECTION ( 'NONE',  ( 0.000000000000000000, 1.000000000000000000, 6.982962677686266711E-15 ) ) ;
#219968=CARTESIAN_POINT ( 'NONE',  ( -20.85000000000000142, 77.83585931145526615, -58.01866831572577610 ) ) ;
#219988=DIRECTION ( 'NONE',  ( -1.000000000000000000, -0.000000000000000000, -0.000000000000000000 ) ) ;
#219998=FACE_OUTER_BOUND ( 'NONE', #46791, .T. ) ;
#220004=LINE ( 'NONE', #145591, #200073 ) ;
#220008=CYLINDRICAL_SURFACE ( 'NONE', #234635, 0.1000000000000052097 ) ;
#220014=DIRECTION ( 'NONE',  ( -1.000000000000000000, -0.000000000000000000, -0.000000000000000000 ) ) ;
#220058=EDGE_CURVE ( 'NONE', #179506, #29920, #210627, .T. ) ;
#220094=DIRECTION ( 'NONE',  ( 1.000000000000000000, -2.952720810173289112E-16, -2.061873921506763405E-30 ) ) ;
#220095=ORIENTED_EDGE ( 'NONE', *, *, #18017, .F. ) ;
#220104=CARTESIAN_POINT ( 'NONE',  ( 18.39999999999999858, 85.40000000001204228, -114.7731074845242460 ) ) ;
#220117=DIRECTION ( 'NONE',  ( 0.000000000000000000, -6.467318590049456648E-15, 1.000000000000000000 ) ) ;
#220124=CIRCLE ( 'NONE', #174572, 0.2000000000000057288 ) ;
#220165=CARTESIAN_POINT ( 'NONE',  ( -23.25000000000000000, 85.60000000001188880, -93.12913836187179584 ) ) ;
#220192=EDGE_LOOP ( 'NONE', ( #154, #189496, #114047, #94296 ) ) ;
#220251=VECTOR ( 'NONE', #31894, 1000.000000000000000 ) ;
#220283=CYLINDRICAL_SURFACE ( 'NONE', #135294, 2.000000000000001776 ) ;
#220318=CARTESIAN_POINT ( 'NONE',  ( -23.15000000000000213, 87.65000000001172964, -72.62310748452422615 ) ) ;
#220338=LINE ( 'NONE', #121272, #1591 ) ;
#220340=ADVANCED_FACE ( 'NONE', ( #238896 ), #60237, .F. ) ;
#220345=AXIS2_PLACEMENT_3D ( 'NONE', #88516, #168129, #243767 ) ;
#220364=CARTESIAN_POINT ( 'NONE',  ( -20.64999999999999858, 73.60000000001180354, -82.74772940728642823 ) ) ;
#220373=LINE ( 'NONE', #22180, #180807 ) ;
#220394=FACE_OUTER_BOUND ( 'NONE', #124448, .T. ) ;
#220416=EDGE_CURVE ( 'NONE', #203922, #20026, #69365, .T. ) ;
#220417=DIRECTION ( 'NONE',  ( 0.000000000000000000, -6.467318590049456648E-15, 1.000000000000000000 ) ) ;
#220424=ADVANCED_FACE ( 'NONE', ( #69254 ), #203610, .F. ) ;
#220443=TOROIDAL_SURFACE ( 'NONE', #174519, 0.2000000000000000111, 0.1000000000000000056 ) ;
#220505=CIRCLE ( 'NONE', #37345, 0.09999999999999939493 ) ;
#220516=VERTEX_POINT ( 'NONE', #153963 ) ;
#220540=CARTESIAN_POINT ( 'NONE',  ( -23.25000000000000000, 77.85161776048053639, -57.91991776492063337 ) ) ;
#220548=LINE ( 'NONE', #241403, #41475 ) ;
#220571=EDGE_CURVE ( 'NONE', #3343, #42984, #248582, .T. ) ;
#220583=CIRCLE ( 'NONE', #8206, 11.70000000000000284 ) ;
#220588=DIRECTION ( 'NONE',  ( 0.000000000000000000, 0.000000000000000000, 1.000000000000000000 ) ) ;
#220604=AXIS2_PLACEMENT_3D ( 'NONE', #168289, #185237, #148694 ) ;
#220644=TOROIDAL_SURFACE ( 'NONE', #104083, 0.9750000000000019762, 0.1000000000000000056 ) ;
#220648=EDGE_LOOP ( 'NONE', ( #139845, #109522, #134119, #71761 ) ) ;
#220660=CARTESIAN_POINT ( 'NONE',  ( -22.39999999999999858, 76.00000000001195133, -103.1231074845243114 ) ) ;
#220661=LINE ( 'NONE', #22479, #12287 ) ;
#220666=CARTESIAN_POINT ( 'NONE',  ( 23.24999999999999645, 70.40000000001187175, -90.61784146561124942 ) ) ;
#220675=CARTESIAN_POINT ( 'NONE',  ( -21.14999999999999858, 76.00000000001195133, -103.0231074845243171 ) ) ;
#220677=EDGE_CURVE ( 'NONE', #146049, #16439, #231864, .T. ) ;
#220681=ORIENTED_EDGE ( 'NONE', *, *, #251367, .F. ) ;
#220767=FACE_OUTER_BOUND ( 'NONE', #147978, .T. ) ;
#220778=ORIENTED_EDGE ( 'NONE', *, *, #219474, .T. ) ;
#220789=CARTESIAN_POINT ( 'NONE',  ( -20.85000000000000142, 76.00000000001170974, -69.52310748452431710 ) ) ;
#220795=CIRCLE ( 'NONE', #54384, 0.09999999999999739653 ) ;
#220802=LINE ( 'NONE', #42184, #98459 ) ;
#220838=LINE ( 'NONE', #181728, #252598 ) ;
#220848=( NAMED_UNIT ( * ) SI_UNIT ( $, .STERADIAN. ) SOLID_ANGLE_UNIT ( ) );
#220862=EDGE_CURVE ( 'NONE', #21614, #136482, #165477, .T. ) ;
#220901=EDGE_CURVE ( 'NONE', #216625, #208580, #61155, .T. ) ;
#220927=AXIS2_PLACEMENT_3D ( 'NONE', #196496, #17856, #97368 ) ;
#220941=CYLINDRICAL_SURFACE ( 'NONE', #116159, 0.09999999999999939493 ) ;
#220943=CARTESIAN_POINT ( 'NONE',  ( 18.59999999999999076, 65.50857864377445594, -78.17310748452437963 ) ) ;
#220945=CARTESIAN_POINT ( 'NONE',  ( -20.85000000000000142, 87.75000000001173817, -72.42310748452422331 ) ) ;
#220952=CARTESIAN_POINT ( 'NONE',  ( -23.25000000000000000, 68.97833521811159585, -65.68954208262705663 ) ) ;
#220967=DIRECTION ( 'NONE',  ( -0.000000000000000000, -6.982962677686266711E-15, 1.000000000000000000 ) ) ;
#220969=EDGE_LOOP ( 'NONE', ( #91567, #83504, #86061, #156193 ) ) ;
#220978=DIRECTION ( 'NONE',  ( -4.336808689941751890E-15, -0.8660254037844445918, -0.4999999999999897304 ) ) ;
#220980=AXIS2_PLACEMENT_3D ( 'NONE', #233656, #156708, #35477 ) ;
#220981=ORIENTED_EDGE ( 'NONE', *, *, #133496, .F. ) ;
#220983=AXIS2_PLACEMENT_3D ( 'NONE', #30066, #225637, #109556 ) ;
#220995=FACE_OUTER_BOUND ( 'NONE', #251648, .T. ) ;
#221012=CARTESIAN_POINT ( 'NONE',  ( -20.85000000000000142, 69.15387683765909799, -65.78538121767449809 ) ) ;
#221033=EDGE_CURVE ( 'NONE', #96528, #55246, #190346, .T. ) ;
#221059=ORIENTED_EDGE ( 'NONE', *, *, #143010, .T. ) ;
#221064=CARTESIAN_POINT ( 'NONE',  ( -21.07954763557533084, 75.93412408139347747, -109.3523984745629463 ) ) ;
#221070=ORIENTED_EDGE ( 'NONE', *, *, #212836, .T. ) ;
#221085=CIRCLE ( 'NONE', #75388, 0.1000000000000028644 ) ;
#221124=CARTESIAN_POINT ( 'NONE',  ( -21.12757541349819590, 75.99483878420227256, -109.4964880557758704 ) ) ;
#221143=DIRECTION ( 'NONE',  ( 1.000000000000000000, 0.000000000000000000, 0.000000000000000000 ) ) ;
#221144=DIRECTION ( 'NONE',  ( 0.7071067811865475727, -0.7071067811865475727, -4.937700262164531476E-15 ) ) ;
#221151=ORIENTED_EDGE ( 'NONE', *, *, #114256, .T. ) ;
#221162=DIRECTION ( 'NONE',  ( 0.000000000000000000, 6.938893903907222067E-15, -1.000000000000000000 ) ) ;
#221182=CARTESIAN_POINT ( 'NONE',  ( 21.14999999999999858, 69.45934304831071415, -103.0231074845243597 ) ) ;
#221191=CIRCLE ( 'NONE', #142083, 0.3999999999999975797 ) ;
#221200=DIRECTION ( 'NONE',  ( 0.000000000000000000, 0.000000000000000000, 1.000000000000000000 ) ) ;
#221208=AXIS2_PLACEMENT_3D ( 'NONE', #122144, #60867, #62170 ) ;
#221235=CIRCLE ( 'NONE', #212889, 11.64999999999999325 ) ;
#221237=VERTEX_POINT ( 'NONE', #242112 ) ;
#221241=EDGE_CURVE ( 'NONE', #101254, #31810, #36415, .T. ) ;
#221253=CARTESIAN_POINT ( 'NONE',  ( 18.49999999999999289, 65.70729864260985664, -64.06574559737245522 ) ) ;
#221276=CARTESIAN_POINT ( 'NONE',  ( 21.14999999999999858, 64.35000000001186038, -90.87310748452438247 ) ) ;
#221290=CARTESIAN_POINT ( 'NONE',  ( 21.14999999999999503, 76.00000000001195133, -103.0231074845243171 ) ) ;
#221339=CARTESIAN_POINT ( 'NONE',  ( -21.05000000000000071, 64.35000000001190301, -96.23924182154622997 ) ) ;
#221340=ORIENTED_EDGE ( 'NONE', *, *, #91274, .F. ) ;
#221355=VERTEX_POINT ( 'NONE', #38486 ) ;
#221359=ORIENTED_EDGE ( 'NONE', *, *, #63254, .T. ) ;
#221361=EDGE_CURVE ( 'NONE', #110160, #214060, #118014, .T. ) ;
#221385=CARTESIAN_POINT ( 'NONE',  ( 18.59999999999999787, 77.83534155023627932, -91.36795619196132634 ) ) ;
#221386=ORIENTED_EDGE ( 'NONE', *, *, #34571, .T. ) ;
#221402=CARTESIAN_POINT ( 'NONE',  ( -20.64999999999999858, 76.00000000001185185, -90.04810748452430857 ) ) ;
#221463=CARTESIAN_POINT ( 'NONE',  ( -18.39999999999999858, 85.68240343348806221, -62.86626410711144786 ) ) ;
#221492=LINE ( 'NONE', #85814, #79464 ) ;
#221502=ORIENTED_EDGE ( 'NONE', *, *, #225726, .F. ) ;
#221523=DIRECTION ( 'NONE',  ( 0.000000000000000000, 0.000000000000000000, 1.000000000000000000 ) ) ;
#221563=DIRECTION ( 'NONE',  ( -0.000000000000000000, 1.000000000000000000, 6.982962677686266711E-15 ) ) ;
#221614=CARTESIAN_POINT ( 'NONE',  ( 20.85000000000000142, 68.92903212821283887, -65.77654326265606244 ) ) ;
#221618=ORIENTED_EDGE ( 'NONE', *, *, #202215, .T. ) ;
#221629=CIRCLE ( 'NONE', #201000, 4.049999999999998046 ) ;
#221652=VERTEX_POINT ( 'NONE', #30499 ) ;
#221656=ORIENTED_EDGE ( 'NONE', *, *, #217665, .F. ) ;
#221683=CARTESIAN_POINT ( 'NONE',  ( 22.50927854361893310, 76.10085807353982545, -114.7726746105512063 ) ) ;
#221695=VERTEX_POINT ( 'NONE', #176108 ) ;
#221753=ADVANCED_FACE ( 'NONE', ( #130858, #195673 ), #213922, .T. ) ;
#221758=FACE_OUTER_BOUND ( 'NONE', #171810, .T. ) ;
#221767=DIRECTION ( 'NONE',  ( 1.000000000000000000, 0.000000000000000000, 0.000000000000000000 ) ) ;
#221777=CARTESIAN_POINT ( 'NONE',  ( -20.94999999999999929, 87.65000000001192859, -100.1231074845242262 ) ) ;
#221800=DIRECTION ( 'NONE',  ( 1.000000000000000000, 0.000000000000000000, 0.000000000000000000 ) ) ;
#221810=LINE ( 'NONE', #7941, #137227 ) ;
#221830=CARTESIAN_POINT ( 'NONE',  ( -21.00023020733502932, 76.00000000001200817, -109.4139767297926653 ) ) ;
#221863=CARTESIAN_POINT ( 'NONE',  ( -20.64999999999999858, 71.65000000001187175, -90.67310748452433700 ) ) ;
#221873=VECTOR ( 'NONE', #82378, 1000.000000000000000 ) ;
#221878=CARTESIAN_POINT ( 'NONE',  ( 22.00411653889209518, 75.90096189422524731, -110.2765503521647048 ) ) ;
#221901=VERTEX_POINT ( 'NONE', #63840 ) ;
#221945=CYLINDRICAL_SURFACE ( 'NONE', #108231, 0.09999999999999976963 ) ;
#221948=VERTEX_POINT ( 'NONE', #128953 ) ;
#221961=CARTESIAN_POINT ( 'NONE',  ( -20.85000000000000142, 77.83585931145526615, -58.01866831572577610 ) ) ;
#221970=VECTOR ( 'NONE', #29601, 999.9999999999998863 ) ;
#221981=EDGE_CURVE ( 'NONE', #194795, #64660, #208504, .T. ) ;
#222033=ORIENTED_EDGE ( 'NONE', *, *, #153268, .T. ) ;
#222037=ORIENTED_EDGE ( 'NONE', *, *, #22227, .T. ) ;
#222047=CIRCLE ( 'NONE', #251290, 0.09999999999999520384 ) ;
#222078=VECTOR ( 'NONE', #147054, 1000.000000000000000 ) ;
#222093=VERTEX_POINT ( 'NONE', #91100 ) ;
#222118=CARTESIAN_POINT ( 'NONE',  ( 23.24999999999999645, 70.40000000001180069, -81.92837350343744163 ) ) ;
#222135=CIRCLE ( 'NONE', #126306, 0.1000000000000017680 ) ;
#222143=VERTEX_POINT ( 'NONE', #111966 ) ;
#222149=VECTOR ( 'NONE', #13315, 1000.000000000000000 ) ;
#222166=AXIS2_PLACEMENT_3D ( 'NONE', #10080, #111753, #33544 ) ;
#222213=CARTESIAN_POINT ( 'NONE',  ( -20.94999999999999929, 64.25000000001190870, -96.00830171387039513 ) ) ;
#222237=EDGE_CURVE ( 'NONE', #168899, #18436, #165962, .T. ) ;
#222238=AXIS2_PLACEMENT_3D ( 'NONE', #199506, #160388, #243743 ) ;
#222252=EDGE_LOOP ( 'NONE', ( #217521, #11496, #236652, #46115 ) ) ;
#222265=CARTESIAN_POINT ( 'NONE',  ( 20.94999999999999574, 74.16465844978745281, -91.46795619196133487 ) ) ;
#222308=ORIENTED_EDGE ( 'NONE', *, *, #45806, .F. ) ;
#222310=LINE ( 'NONE', #38579, #223925 ) ;
#222312=DIRECTION ( 'NONE',  ( -1.000000000000000000, 0.000000000000000000, -0.000000000000000000 ) ) ;
#222329=CARTESIAN_POINT ( 'NONE',  ( -21.07928932188134041, 75.90110485435761234, -109.3516241409176075 ) ) ;
#222354=CARTESIAN_POINT ( 'NONE',  ( 18.59999999999999076, 65.79142135624910281, -81.77310748452437394 ) ) ;
#222360=CARTESIAN_POINT ( 'NONE',  ( -23.25000000000000000, 76.00000000001170974, -69.52310748452431710 ) ) ;
#222376=ORIENTED_EDGE ( 'NONE', *, *, #174078, .T. ) ;
#222396=ORIENTED_EDGE ( 'NONE', *, *, #231385, .T. ) ;
#222398=DIRECTION ( 'NONE',  ( 1.000000000000000000, 0.000000000000000000, 0.000000000000000000 ) ) ;
#222434=ORIENTED_EDGE ( 'NONE', *, *, #27548, .T. ) ;
#222446=DIRECTION ( 'NONE',  ( 0.000000000000000000, 0.000000000000000000, 1.000000000000000000 ) ) ;
#222471=CARTESIAN_POINT ( 'NONE',  ( 23.15000000000000213, 87.65000000001195701, -103.0231074845242318 ) ) ;
#222543=DIRECTION ( 'NONE',  ( 1.000000000000000000, 0.000000000000000000, 0.000000000000000000 ) ) ;
#222551=DIRECTION ( 'NONE',  ( 0.000000000000000000, -1.000000000000000000, -6.982962677686265922E-15 ) ) ;
#222552=DIRECTION ( 'NONE',  ( -1.000000000000000000, -0.000000000000000000, -0.000000000000000000 ) ) ;
#222620=CARTESIAN_POINT ( 'NONE',  ( -20.94999999999999929, 64.40000000001188596, -96.09490425424883142 ) ) ;
#222657=FACE_BOUND ( 'NONE', #71239, .T. ) ;
#222678=ORIENTED_EDGE ( 'NONE', *, *, #77629, .F. ) ;
#222684=DIRECTION ( 'NONE',  ( 1.000000000000000000, 0.000000000000000000, 0.000000000000000000 ) ) ;
#222688=AXIS2_PLACEMENT_3D ( 'NONE', #38527, #21540, #161049 ) ;
#222691=CARTESIAN_POINT ( 'NONE',  ( 21.05000000000000071, 87.39257802171739797, -72.59705706435616435 ) ) ;
#222704=AXIS2_PLACEMENT_3D ( 'NONE', #78742, #256054, #138692 ) ;
#222717=ORIENTED_EDGE ( 'NONE', *, *, #253503, .T. ) ;
#222718=EDGE_CURVE ( 'NONE', #195198, #232010, #59324, .T. ) ;
#222732=ORIENTED_EDGE ( 'NONE', *, *, #20308, .F. ) ;
#222763=VERTEX_POINT ( 'NONE', #196298 ) ;
#222776=EDGE_LOOP ( 'NONE', ( #45541, #142511, #53719, #6430, #136899, #156406 ) ) ;
#222800=CARTESIAN_POINT ( 'NONE',  ( -18.59999999999999787, 85.32100840337318459, -95.78716923544635620 ) ) ;
#222839=VECTOR ( 'NONE', #66742, 1000.000000000000000 ) ;
#222859=CARTESIAN_POINT ( 'NONE',  ( 20.85000000000000142, 76.00000000001170974, -69.52310748452431710 ) ) ;
#222863=CARTESIAN_POINT ( 'NONE',  ( 20.95203847575071521, 65.49893946073788698, -95.45603613590083114 ) ) ;
#222865=EDGE_CURVE ( 'NONE', #111551, #184113, #104869, .T. ) ;
#222871=ORIENTED_EDGE ( 'NONE', *, *, #50601, .F. ) ;
#222936=CARTESIAN_POINT ( 'NONE',  ( 23.24999999999999289, 69.35000000001180354, -81.67310748452436542 ) ) ;
#222969=CARTESIAN_POINT ( 'NONE',  ( 19.75857864376269291, 64.35000000001177511, -78.27310748452438816 ) ) ;
#222978=CARTESIAN_POINT ( 'NONE',  ( -23.15000000000000213, 76.00000000001195133, -103.0231074845243171 ) ) ;
#222983=ADVANCED_FACE ( 'NONE', ( #250831 ), #78240, .F. ) ;
#223003=CARTESIAN_POINT ( 'NONE',  ( 21.04999999999999716, 69.69554417806426727, -103.0020720079842391 ) ) ;
#223027=LINE ( 'NONE', #182645, #143540 ) ;
#223165=CARTESIAN_POINT ( 'NONE',  ( 20.94999999999999929, 64.35000000001170406, -69.52310748452438816 ) ) ;
#223172=DIRECTION ( 'NONE',  ( -3.265361837132813093E-16, -1.000000000000000000, -7.026728003956683390E-15 ) ) ;
#223173=AXIS2_PLACEMENT_3D ( 'NONE', #6211, #222684, #64903 ) ;
#223207=DIRECTION ( 'NONE',  ( 1.000000000000000000, 0.000000000000000000, 0.000000000000000000 ) ) ;
#223229=ADVANCED_FACE ( 'NONE', ( #189147 ), #49345, .T. ) ;
#223245=AXIS2_PLACEMENT_3D ( 'NONE', #144382, #4870, #244783 ) ;
#223251=ORIENTED_EDGE ( 'NONE', *, *, #159794, .F. ) ;
#223268=CIRCLE ( 'NONE', #123503, 0.09999999999999520384 ) ;
#223282=EDGE_CURVE ( 'NONE', #23304, #8981, #36784, .T. ) ;
#223285=CIRCLE ( 'NONE', #119263, 0.1000000000000026007 ) ;
#223293=DIRECTION ( 'NONE',  ( 0.000000000000000000, -1.000000000000000000, -6.982962677686265922E-15 ) ) ;
#223310=ADVANCED_FACE ( 'NONE', ( #135571 ), #196835, .F. ) ;
#223315=VERTEX_POINT ( 'NONE', #98998 ) ;
#223320=ADVANCED_FACE ( 'NONE', ( #58603 ), #258060, .T. ) ;
#223335=ORIENTED_EDGE ( 'NONE', *, *, #195271, .F. ) ;
#223338=FACE_OUTER_BOUND ( 'NONE', #181937, .T. ) ;
#223365=DIRECTION ( 'NONE',  ( -2.840903330521632269E-16, -0.8700118002898356018, 0.4930308989875170078 ) ) ;
#223386=AXIS2_PLACEMENT_3D ( 'NONE', #55333, #236563, #74967 ) ;
#223404=CARTESIAN_POINT ( 'NONE',  ( 22.60000000000000142, 64.25043287652255231, -103.1239658536231047 ) ) ;
#223431=DIRECTION ( 'NONE',  ( -1.000000000000000000, 0.000000000000000000, 0.000000000000000000 ) ) ;
#223432=DIRECTION ( 'NONE',  ( 0.000000000000000000, 0.8700118002898356018, -0.4930308989875170078 ) ) ;
#223433=ADVANCED_FACE ( 'NONE', ( #44998 ), #161104, .F. ) ;
#223456=CARTESIAN_POINT ( 'NONE',  ( -18.39999999999999858, 85.60000000001167564, -62.92291809330219365 ) ) ;
#223521=FACE_OUTER_BOUND ( 'NONE', #97118, .T. ) ;
#223568=DIRECTION ( 'NONE',  ( 1.000000000000000000, 0.000000000000000000, 0.000000000000000000 ) ) ;
#223570=CIRCLE ( 'NONE', #111169, 0.1000000000000026007 ) ;
#223578=ORIENTED_EDGE ( 'NONE', *, *, #165984, .F. ) ;
#223601=ORIENTED_EDGE ( 'NONE', *, *, #219814, .F. ) ;
#223676=VERTEX_POINT ( 'NONE', #73580 ) ;
#223712=ADVANCED_FACE ( 'NONE', ( #112681 ), #57927, .T. ) ;
#223747=CARTESIAN_POINT ( 'NONE',  ( 21.08078803292165659, 69.66698703557483441, -103.1022934716821311 ) ) ;
#223762=VERTEX_POINT ( 'NONE', #231356 ) ;
#223830=VECTOR ( 'NONE', #214794, 1000.000000000000000 ) ;
#223839=EDGE_CURVE ( 'NONE', #247315, #98792, #24668, .T. ) ;
#223846=AXIS2_PLACEMENT_3D ( 'NONE', #205631, #163964, #243485 ) ;
#223852=AXIS2_PLACEMENT_3D ( 'NONE', #222265, #43670, #256212 ) ;
#223871=PLANE ( 'NONE',  #130252 ) ;
#223894=EDGE_LOOP ( 'NONE', ( #226787, #39268, #198011, #251069 ) ) ;
#223902=SPHERICAL_SURFACE ( 'NONE', #42204, 0.1000000000000000056 ) ;
#223914=DIRECTION ( 'NONE',  ( -0.000000000000000000, 1.000000000000000000, 6.982962677686266711E-15 ) ) ;
#223915=AXIS2_PLACEMENT_3D ( 'NONE', #174983, #173702, #191961 ) ;
#223925=VECTOR ( 'NONE', #80226, 1000.000000000000000 ) ;
#223938=AXIS2_PLACEMENT_3D ( 'NONE', #64937, #162781, #63655 ) ;
#223939=EDGE_LOOP ( 'NONE', ( #17959, #142883, #127004, #132117, #196037 ) ) ;
#224021=VERTEX_POINT ( 'NONE', #188062 ) ;
#224035=EDGE_LOOP ( 'NONE', ( #238590, #29826, #177698, #80132 ) ) ;
#224039=FACE_OUTER_BOUND ( 'NONE', #235758, .T. ) ;
#224096=AXIS2_PLACEMENT_3D ( 'NONE', #207485, #147496, #229605 ) ;
#224098=LINE ( 'NONE', #130133, #53829 ) ;
#224162=DIRECTION ( 'NONE',  ( 0.000000000000000000, -1.000000000000000000, -6.982962677686266711E-15 ) ) ;
#224243=SPHERICAL_SURFACE ( 'NONE', #95919, 0.1000000000000000056 ) ;
#224252=ORIENTED_EDGE ( 'NONE', *, *, #144468, .T. ) ;
#224255=CARTESIAN_POINT ( 'NONE',  ( 19.80993210785464242, 64.25000000001178080, -78.25598973563708682 ) ) ;
#224267=CIRCLE ( 'NONE', #216069, 0.09999999999999939493 ) ;
#224268=VERTEX_POINT ( 'NONE', #120113 ) ;
#224273=CIRCLE ( 'NONE', #37053, 0.3999999999999975797 ) ;
#224323=ORIENTED_EDGE ( 'NONE', *, *, #173023, .T. ) ;
#224355=CARTESIAN_POINT ( 'NONE',  ( 20.94999999999999929, 70.10000000001177511, -79.74220724918072278 ) ) ;
#224387=DIRECTION ( 'NONE',  ( 1.000000000000000000, -2.952720810173289112E-16, -2.061873921506763405E-30 ) ) ;
#224413=FACE_OUTER_BOUND ( 'NONE', #190974, .T. ) ;
#224431=DIRECTION ( 'NONE',  ( -6.938893903907222856E-15, -1.000000000000000000, -7.272083257015735086E-15 ) ) ;
#224463=CARTESIAN_POINT ( 'NONE',  ( 22.47007471830798053, 76.00000000001200817, -110.7438181364507699 ) ) ;
#224470=CARTESIAN_POINT ( 'NONE',  ( -20.64999999999999858, 74.00000000001180922, -82.24772940728641402 ) ) ;
#224481=ADVANCED_FACE ( 'NONE', ( #144749 ), #154046, .T. ) ;
#224521=CIRCLE ( 'NONE', #216319, 0.1000000000000052097 ) ;
#224558=AXIS2_PLACEMENT_3D ( 'NONE', #247613, #43004, #102946 ) ;
#224571=ADVANCED_FACE ( 'NONE', ( #192895 ), #220644, .F. ) ;
#224584=CARTESIAN_POINT ( 'NONE',  ( 20.85000000000000142, 77.83585931145526615, -58.01866831572577610 ) ) ;
#224619=VERTEX_POINT ( 'NONE', #255366 ) ;
#224628=B_SPLINE_CURVE_WITH_KNOTS ( 'NONE', 3,
 ( #99211, #56237, #41855, #116249, #157973, #240040, #256971, #61392 ),
 .UNSPECIFIED., .F., .F.,
 ( 4, 2, 2, 4 ),
 ( 0.000000000000000000, 0.0002114466876442291910, 0.0003171700314663174268, 0.0004228933752884056355 ),
 .UNSPECIFIED. ) ;
#224632=VERTEX_POINT ( 'NONE', #20689 ) ;
#224648=AXIS2_PLACEMENT_3D ( 'NONE', #8648, #186002, #86872 ) ;
#224649=DIRECTION ( 'NONE',  ( 0.000000000000000000, -6.982962677686266711E-15, 1.000000000000000000 ) ) ;
#224675=CARTESIAN_POINT ( 'NONE',  ( 23.15000000000000213, 85.00000000001179501, -79.41707660717668205 ) ) ;
#224694=FILL_AREA_STYLE_COLOUR ( '', #170566 ) ;
#224703=FACE_OUTER_BOUND ( 'NONE', #189482, .T. ) ;
#224715=CARTESIAN_POINT ( 'NONE',  ( -23.25000000000000000, 69.01799029515524353, -65.82695536626808064 ) ) ;
#224746=DIRECTION ( 'NONE',  ( 1.000000000000000000, 0.000000000000000000, 0.000000000000000000 ) ) ;
#224796=FACE_OUTER_BOUND ( 'NONE', #228878, .T. ) ;
#224804=VERTEX_POINT ( 'NONE', #45362 ) ;
#224809=ORIENTED_EDGE ( 'NONE', *, *, #5446, .T. ) ;
#224812=CARTESIAN_POINT ( 'NONE',  ( -23.25000000000000000, 64.25000000001203659, -114.7731074845243882 ) ) ;
#224822=EDGE_CURVE ( 'NONE', #21472, #2690, #245756, .T. ) ;
#224827=ADVANCED_FACE ( 'NONE', ( #145733 ), #29557, .T. ) ;
#224835=CIRCLE ( 'NONE', #20873, 4.099999999999992539 ) ;
#224838=AXIS2_PLACEMENT_3D ( 'NONE', #127017, #187013, #15763 ) ;
#224869=CIRCLE ( 'NONE', #112482, 0.09999999999999520384 ) ;
#224894=TOROIDAL_SURFACE ( 'NONE', #241666, 7.800000000000000711, 0.1000000000000000056 ) ;
#224913=CARTESIAN_POINT ( 'NONE',  ( -21.04999999999999005, 75.90156250001201954, -109.3223383946111653 ) ) ;
#224924=EDGE_CURVE ( 'NONE', #11015, #229726, #158307, .T. ) ;
#224949=CARTESIAN_POINT ( 'NONE',  ( -20.64999999999999858, 74.07476635515205032, -90.29286395139820343 ) ) ;
#225003=CARTESIAN_POINT ( 'NONE',  ( -21.05000000000000071, 76.00000000001170974, -69.52310748452431710 ) ) ;
#225017=ADVANCED_FACE ( 'NONE', ( #25192 ), #158482, .T. ) ;
#225030=ORIENTED_EDGE ( 'NONE', *, *, #126646, .F. ) ;
#225043=FACE_OUTER_BOUND ( 'NONE', #2163, .T. ) ;
#225057=CARTESIAN_POINT ( 'NONE',  ( 18.59999999999999076, 65.79142135624910281, -81.67310748452439384 ) ) ;
#225072=FACE_OUTER_BOUND ( 'NONE', #44181, .T. ) ;
#225075=EDGE_LOOP ( 'NONE', ( #103761, #15977, #71020, #26359 ) ) ;
#225085=CARTESIAN_POINT ( 'NONE',  ( -23.25000000000000000, 64.25000000001195133, -103.0231074845244024 ) ) ;
#225117=DIRECTION ( 'NONE',  ( 0.000000000000000000, 1.000000000000000000, 6.982962677686266711E-15 ) ) ;
#225142=AXIS2_PLACEMENT_3D ( 'NONE', #225057, #46432, #26912 ) ;
#225163=ORIENTED_EDGE ( 'NONE', *, *, #47264, .F. ) ;
#225203=DIRECTION ( 'NONE',  ( 1.000000000000000000, 0.000000000000000000, 0.000000000000000000 ) ) ;
#225208=FACE_OUTER_BOUND ( 'NONE', #89340, .T. ) ;
#225219=LINE ( 'NONE', #23227, #241993 ) ;
#225248=LINE ( 'NONE', #186150, #132035 ) ;
#225257=CARTESIAN_POINT ( 'NONE',  ( -20.99551997958379701, 64.25000000001176659, -76.37144834683515171 ) ) ;
#225261=EDGE_CURVE ( 'NONE', #41443, #6405, #50285, .T. ) ;
#225271=ORIENTED_EDGE ( 'NONE', *, *, #56179, .F. ) ;
#225286=DIRECTION ( 'NONE',  ( -0.7071067811865214825, -0.7071067811865735520, 0.000000000000000000 ) ) ;
#225296=EDGE_CURVE ( 'NONE', #185475, #203922, #114978, .T. ) ;
#225318=( NAMED_UNIT ( * ) PLANE_ANGLE_UNIT ( ) SI_UNIT ( $, .RADIAN. ) );
#225321=VERTEX_POINT ( 'NONE', #133261 ) ;
#225380=EDGE_LOOP ( 'NONE', ( #138113, #213413, #45130, #3011 ) ) ;
#225382=DIRECTION ( 'NONE',  ( 2.952720810173289112E-16, 1.000000000000000000, 6.982962677686266711E-15 ) ) ;
#225410=CARTESIAN_POINT ( 'NONE',  ( -21.64999999999999858, 68.65000000001187175, -90.77310748452435973 ) ) ;
#225415=DIRECTION ( 'NONE',  ( -0.000000000000000000, 6.982962677686266711E-15, -1.000000000000000000 ) ) ;
#225423=ORIENTED_EDGE ( 'NONE', *, *, #1783, .F. ) ;
#225468=DIRECTION ( 'NONE',  ( 1.000000000000000000, 0.000000000000000000, 0.000000000000000000 ) ) ;
#225496=EDGE_CURVE ( 'NONE', #254433, #237868, #100155, .T. ) ;
#225518=CARTESIAN_POINT ( 'NONE',  ( 19.87657994472052181, 64.25000000001176659, -78.25731935989793442 ) ) ;
#225543=ORIENTED_EDGE ( 'NONE', *, *, #228316, .T. ) ;
#225545=VERTEX_POINT ( 'NONE', #10450 ) ;
#225571=EDGE_CURVE ( 'NONE', #16721, #191564, #221629, .T. ) ;
#225591=DIRECTION ( 'NONE',  ( 0.000000000000000000, -4.562560375171877784E-14, 1.000000000000000000 ) ) ;
#225619=EDGE_CURVE ( 'NONE', #14256, #11996, #48279, .T. ) ;
#225625=VERTEX_POINT ( 'NONE', #106958 ) ;
#225637=DIRECTION ( 'NONE',  ( -0.000000000000000000, 1.000000000000000000, 6.982962677686267499E-15 ) ) ;
#225684=CIRCLE ( 'NONE', #238171, 0.2000000000000057288 ) ;
#225702=VECTOR ( 'NONE', #36545, 999.9999999999998863 ) ;
#225726=EDGE_CURVE ( 'NONE', #180772, #246470, #32614, .T. ) ;
#225749=ADVANCED_FACE ( 'NONE', ( #155125 ), #190385, .T. ) ;
#225754=DIRECTION ( 'NONE',  ( 1.000000000000000000, 0.000000000000000000, 0.000000000000000000 ) ) ;
#225783=LINE ( 'NONE', #70618, #222839 ) ;
#225821=FACE_OUTER_BOUND ( 'NONE', #114328, .T. ) ;
#225851=ORIENTED_EDGE ( 'NONE', *, *, #89929, .T. ) ;
#225881=AXIS2_PLACEMENT_3D ( 'NONE', #167826, #46544, #145649 ) ;
#225903=CARTESIAN_POINT ( 'NONE',  ( 23.14999999999999858, 69.35000000001186038, -90.67310748452435121 ) ) ;
#225906=FACE_OUTER_BOUND ( 'NONE', #198995, .T. ) ;
#225956=CARTESIAN_POINT ( 'NONE',  ( -23.25000000000000000, 87.75000000001173817, -72.62310748452422615 ) ) ;
#225963=CARTESIAN_POINT ( 'NONE',  ( 20.74897398619119215, 65.40430697834545981, -95.34379602826817290 ) ) ;
#226005=DIRECTION ( 'NONE',  ( 0.000000000000000000, 0.9915357197604892647, -0.1298341882519715440 ) ) ;
#226013=DIRECTION ( 'NONE',  ( 1.000000000000000000, 0.000000000000000000, 0.000000000000000000 ) ) ;
#226014=SPHERICAL_SURFACE ( 'NONE', #206938, 0.1000000000000000056 ) ;
#226034=CARTESIAN_POINT ( 'NONE',  ( 20.94999999999999929, 70.50000000001185185, -90.61784146561124942 ) ) ;
#226057=EDGE_CURVE ( 'NONE', #80064, #101254, #152242, .T. ) ;
#226104=AXIS2_PLACEMENT_3D ( 'NONE', #203028, #24430, #243443 ) ;
#226109=EDGE_LOOP ( 'NONE', ( #147599, #181817, #106188, #118266 ) ) ;
#226122=LINE ( 'NONE', #21545, #177739 ) ;
#226125=VERTEX_POINT ( 'NONE', #193919 ) ;
#226144=EDGE_CURVE ( 'NONE', #21468, #239334, #53102, .T. ) ;
#226147=VERTEX_POINT ( 'NONE', #55637 ) ;
#226149=DIRECTION ( 'NONE',  ( 2.952720810173289112E-16, 1.000000000000000000, 6.467318590049456648E-15 ) ) ;
#226173=EDGE_LOOP ( 'NONE', ( #230300, #146360, #89345, #154512 ) ) ;
#226177=ORIENTED_EDGE ( 'NONE', *, *, #216710, .F. ) ;
#226181=CIRCLE ( 'NONE', #159588, 4.099999999999992539 ) ;
#226255=CARTESIAN_POINT ( 'NONE',  ( -20.94999999999999929, 74.83729825007388570, -95.02310748452431710 ) ) ;
#226263=DIRECTION ( 'NONE',  ( 0.000000000000000000, -0.4999999999999689138, -0.8660254037844565822 ) ) ;
#226275=EDGE_CURVE ( 'NONE', #129128, #51208, #226181, .T. ) ;
#226323=CARTESIAN_POINT ( 'NONE',  ( 18.47688499308725341, 85.46485595029577098, -62.82175973138684810 ) ) ;
#226363=LINE ( 'NONE', #205530, #42789 ) ;
#226374=ORIENTED_EDGE ( 'NONE', *, *, #34571, .F. ) ;
#226388=AXIS2_PLACEMENT_3D ( 'NONE', #166131, #198162, #76928 ) ;
#226408=DIRECTION ( 'NONE',  ( 0.000000000000000000, 1.000000000000000000, 6.982962677686266711E-15 ) ) ;
#226433=CARTESIAN_POINT ( 'NONE',  ( -20.05000000000000426, 66.75000000001179501, -81.77310748452437394 ) ) ;
#226437=CARTESIAN_POINT ( 'NONE',  ( 20.94999999999999929, 67.22371710471941242, -94.46447848938342418 ) ) ;
#226586=CARTESIAN_POINT ( 'NONE',  ( -20.54999999999999716, 74.00000000001180922, -82.74772940728641402 ) ) ;
#226597=FACE_OUTER_BOUND ( 'NONE', #250465, .T. ) ;
#226626=ORIENTED_EDGE ( 'NONE', *, *, #184275, .T. ) ;
#226659=CARTESIAN_POINT ( 'NONE',  ( -18.50000000000000000, 77.86671491006917734, -91.27043223824227880 ) ) ;
#226660=EDGE_CURVE ( 'NONE', #37771, #204044, #59782, .T. ) ;
#226666=DIRECTION ( 'NONE',  ( -6.938893903907222067E-15, -1.000000000000000000, -7.272083257015735086E-15 ) ) ;
#226674=ORIENTED_EDGE ( 'NONE', *, *, #247000, .F. ) ;
#226679=VECTOR ( 'NONE', #23918, 1000.000000000000000 ) ;
#226698=AXIS2_PLACEMENT_3D ( 'NONE', #133472, #34397, #213002 ) ;
#226736=AXIS2_PLACEMENT_3D ( 'NONE', #117125, #136664, #58395 ) ;
#226739=CARTESIAN_POINT ( 'NONE',  ( 20.94999999999999929, 85.40000000001178648, -79.41707660717668205 ) ) ;
#226753=TOROIDAL_SURFACE ( 'NONE', #68556, 0.2000000000000000111, 0.1000000000000000056 ) ;
#226767=EDGE_LOOP ( 'NONE', ( #165978, #37384, #2613, #14250 ) ) ;
#226777=VECTOR ( 'NONE', #70313, 1000.000000000000000 ) ;
#226787=ORIENTED_EDGE ( 'NONE', *, *, #224822, .T. ) ;
#226804=ORIENTED_EDGE ( 'NONE', *, *, #118850, .T. ) ;
#226806=DIRECTION ( 'NONE',  ( 0.000000000000000000, -0.1575844902526579161, -0.9875055080513779338 ) ) ;
#226813=AXIS2_PLACEMENT_3D ( 'NONE', #36001, #127719, #115512 ) ;
#226816=CIRCLE ( 'NONE', #206155, 0.1000000000000028644 ) ;
#226832=DIRECTION ( 'NONE',  ( -1.000000000000000000, 0.000000000000000000, -0.000000000000000000 ) ) ;
#226842=AXIS2_PLACEMENT_3D ( 'NONE', #46020, #79988, #145113 ) ;
#226850=CIRCLE ( 'NONE', #114432, 0.2000000000000057288 ) ;
#226866=DIRECTION ( 'NONE',  ( -1.000000000000000000, 0.000000000000000000, 0.000000000000000000 ) ) ;
#226887=ORIENTED_EDGE ( 'NONE', *, *, #111377, .T. ) ;
#226900=CARTESIAN_POINT ( 'NONE',  ( -23.25000000000000000, 76.00000000001195133, -103.0231074845243171 ) ) ;
#226911=AXIS2_PLACEMENT_3D ( 'NONE', #155811, #239174, #181772 ) ;
#226927=DIRECTION ( 'NONE',  ( 1.000000000000000000, 0.000000000000000000, 0.000000000000000000 ) ) ;
#226932=ADVANCED_FACE ( 'NONE', ( #92131 ), #247423, .T. ) ;
#226984=EDGE_CURVE ( 'NONE', #4874, #108089, #32187, .T. ) ;
#227022=EDGE_CURVE ( 'NONE', #174346, #18466, #234790, .T. ) ;
#227038=ORIENTED_EDGE ( 'NONE', *, *, #254506, .T. ) ;
#227050=CARTESIAN_POINT ( 'NONE',  ( 21.05000000000000071, 65.57661458509899433, -95.53105556065429482 ) ) ;
#227104=VERTEX_POINT ( 'NONE', #174292 ) ;
#227118=AXIS2_PLACEMENT_3D ( 'NONE', #25069, #207544, #28941 ) ;
#227140=CIRCLE ( 'NONE', #243715, 11.80000000000000426 ) ;
#227153=EDGE_CURVE ( 'NONE', #43410, #134789, #76401, .T. ) ;
#227172=ORIENTED_EDGE ( 'NONE', *, *, #250632, .T. ) ;
#227203=CARTESIAN_POINT ( 'NONE',  ( 23.24999999999999289, 80.15000000001194280, -103.0231074845242887 ) ) ;
#227204=ADVANCED_FACE ( 'NONE', ( #158868 ), #136698, .F. ) ;
#227222=FACE_OUTER_BOUND ( 'NONE', #144739, .T. ) ;
#227225=DIRECTION ( 'NONE',  ( 1.000000000000000000, 0.000000000000000000, 0.000000000000000000 ) ) ;
#227233=ORIENTED_EDGE ( 'NONE', *, *, #118604, .F. ) ;
#227279=EDGE_LOOP ( 'NONE', ( #178419, #243845, #134758, #792 ) ) ;
#227300=VERTEX_POINT ( 'NONE', #197959 ) ;
#227369=CIRCLE ( 'NONE', #106540, 4.000000000000003553 ) ;
#227390=CARTESIAN_POINT ( 'NONE',  ( -20.94999999999999929, 77.83534155023627932, -91.36795619196131213 ) ) ;
#227480=DIRECTION ( 'NONE',  ( 7.304098846218134667E-16, 1.000000000000000000, 6.982962677686266711E-15 ) ) ;
#227481=CARTESIAN_POINT ( 'NONE',  ( 23.15000000000000213, 87.65000000001172964, -72.52310748452423184 ) ) ;
#227493=DIRECTION ( 'NONE',  ( 0.000000000000000000, -7.272083257015735086E-15, 1.000000000000000000 ) ) ;
#227520=DIRECTION ( 'NONE',  ( 0.000000000000000000, 0.000000000000000000, -1.000000000000000000 ) ) ;
#227536=ORIENTED_EDGE ( 'NONE', *, *, #226057, .F. ) ;
#227567=DIRECTION ( 'NONE',  ( 0.000000000000000000, 0.000000000000000000, 1.000000000000000000 ) ) ;
#227568=DIRECTION ( 'NONE',  ( -0.000000000000000000, 0.9876197685951241256, 0.1568667991644932258 ) ) ;
#227569=EDGE_CURVE ( 'NONE', #190290, #65545, #135095, .T. ) ;
#227587=CARTESIAN_POINT ( 'NONE',  ( 21.05000000000000071, 70.60000000001180354, -81.92837350343744163 ) ) ;
#227612=CARTESIAN_POINT ( 'NONE',  ( 18.59999999999999076, 76.00000000001170974, -69.52310748452431710 ) ) ;
#227634=DIRECTION ( 'NONE',  ( 0.000000000000000000, 0.000000000000000000, -1.000000000000000000 ) ) ;
#227679=EDGE_CURVE ( 'NONE', #171936, #140343, #139455, .T. ) ;
#227693=EDGE_LOOP ( 'NONE', ( #23876, #136257, #45009, #68140 ) ) ;
#227712=DIRECTION ( 'NONE',  ( 0.000000000000000000, -6.938893903907222067E-15, 1.000000000000000000 ) ) ;
#227716=EDGE_LOOP ( 'NONE', ( #142720, #8553, #244103, #50842 ) ) ;
#227741=CARTESIAN_POINT ( 'NONE',  ( 21.03675099975491136, 67.12481996722705446, -90.69756534774630552 ) ) ;
#227743=DIRECTION ( 'NONE',  ( 1.000000000000000000, 0.000000000000000000, 0.000000000000000000 ) ) ;
#227761=DIRECTION ( 'NONE',  ( 0.000000000000000000, 0.000000000000000000, -1.000000000000000000 ) ) ;
#227764=CARTESIAN_POINT ( 'NONE',  ( -23.25000000000000000, 76.00000000001195133, -103.0231074845243171 ) ) ;
#227767=DIRECTION ( 'NONE',  ( 1.000000000000000000, 0.000000000000000000, 0.000000000000000000 ) ) ;
#227791=ORIENTED_EDGE ( 'NONE', *, *, #226057, .T. ) ;
#227808=ADVANCED_FACE ( 'NONE', ( #206644 ), #218743, .F. ) ;
#227828=ORIENTED_EDGE ( 'NONE', *, *, #94254, .F. ) ;
#227843=ORIENTED_EDGE ( 'NONE', *, *, #93179, .F. ) ;
#227848=ORIENTED_EDGE ( 'NONE', *, *, #26493, .T. ) ;
#227862=ORIENTED_EDGE ( 'NONE', *, *, #65537, .T. ) ;
#227866=AXIS2_PLACEMENT_3D ( 'NONE', #164136, #29786, #166724 ) ;
#227871=DIRECTION ( 'NONE',  ( 1.000000000000000000, 0.000000000000000000, 0.000000000000000000 ) ) ;
#227881=VERTEX_POINT ( 'NONE', #216904 ) ;
#227932=EDGE_LOOP ( 'NONE', ( #99671, #164094, #37406, #226674 ) ) ;
#227939=DIRECTION ( 'NONE',  ( 0.000000000000000000, -0.8700118002898357128, 0.4930308989875170633 ) ) ;
#227940=ORIENTED_EDGE ( 'NONE', *, *, #90879, .T. ) ;
#228026=CARTESIAN_POINT ( 'NONE',  ( -21.14999999999999858, 76.00000000001200817, -109.5637644362255543 ) ) ;
#228072=LINE ( 'NONE', #110680, #84496 ) ;
#228163=DIRECTION ( 'NONE',  ( 0.000000000000000000, 6.938893903907222067E-15, -1.000000000000000000 ) ) ;
#228168=ADVANCED_FACE ( 'NONE', ( #48548 ), #87662, .T. ) ;
#228197=CYLINDRICAL_SURFACE ( 'NONE', #36538, 0.5000000000000004441 ) ;
#228238=AXIS2_PLACEMENT_3D ( 'NONE', #38141, #117659, #237616 ) ;
#228257=CARTESIAN_POINT ( 'NONE',  ( -22.39999999999999858, 75.90000000001199965, -110.8138870828977218 ) ) ;
#228316=EDGE_CURVE ( 'NONE', #142551, #118009, #100157, .T. ) ;
#228333=ORIENTED_EDGE ( 'NONE', *, *, #86590, .T. ) ;
#228342=CARTESIAN_POINT ( 'NONE',  ( -21.05000000000000071, 69.74115727647277652, -103.0551211777124507 ) ) ;
#228365=DIRECTION ( 'NONE',  ( -1.000000000000000000, -0.000000000000000000, -0.000000000000000000 ) ) ;
#228392=FACE_OUTER_BOUND ( 'NONE', #127424, .T. ) ;
#228406=CARTESIAN_POINT ( 'NONE',  ( 20.87155475150661132, 64.25000000001175238, -76.42752095536712886 ) ) ;
#228444=CYLINDRICAL_SURFACE ( 'NONE', #242796, 0.1000000000000028644 ) ;
#228478=AXIS2_PLACEMENT_3D ( 'NONE', #178599, #174768, #18215 ) ;
#228507=CARTESIAN_POINT ( 'NONE',  ( -23.25000000000000000, 77.16412189325286874, -61.60825939895269698 ) ) ;
#228512=VECTOR ( 'NONE', #74429, 1000.000000000000000 ) ;
#228529=DIRECTION ( 'NONE',  ( 0.000000000000000000, -6.938893903907222067E-15, 1.000000000000000000 ) ) ;
#228530=CIRCLE ( 'NONE', #120226, 0.09999999999999939493 ) ;
#228545=FACE_OUTER_BOUND ( 'NONE', #43805, .T. ) ;
#228552=ORIENTED_EDGE ( 'NONE', *, *, #239821, .T. ) ;
#228565=FACE_OUTER_BOUND ( 'NONE', #220648, .T. ) ;
#228567=CARTESIAN_POINT ( 'NONE',  ( 18.51997666896863137, 85.39233213153069357, -95.87970129704063993 ) ) ;
#228569=DIRECTION ( 'NONE',  ( 1.000000000000000000, 0.000000000000000000, 0.000000000000000000 ) ) ;
#228585=CARTESIAN_POINT ( 'NONE',  ( 20.22483756094572271, 66.49809532114012711, -94.88356835580994186 ) ) ;
#228599=AXIS2_PLACEMENT_3D ( 'NONE', #220318, #242426, #63802 ) ;
#228609=DIRECTION ( 'NONE',  ( 0.000000000000000000, -6.982962677686266711E-15, 1.000000000000000000 ) ) ;
#228657=DIRECTION ( 'NONE',  ( 0.000000000000000000, 0.000000000000000000, 1.000000000000000000 ) ) ;
#228658=DIRECTION ( 'NONE',  ( -3.469446951953515108E-14, -1.000000000000000000, 0.000000000000000000 ) ) ;
#228679=EDGE_CURVE ( 'NONE', #157975, #53997, #99845, .T. ) ;
#228690=ORIENTED_EDGE ( 'NONE', *, *, #43332, .T. ) ;
#228744=DIRECTION ( 'NONE',  ( 0.000000000000000000, -6.982962677686266711E-15, 1.000000000000000000 ) ) ;
#228766=ORIENTED_EDGE ( 'NONE', *, *, #205198, .F. ) ;
#228777=CARTESIAN_POINT ( 'NONE',  ( 20.92356734117541706, 65.68026841930881687, -63.97257401318893955 ) ) ;
#228781=CIRCLE ( 'NONE', #66463, 0.09999999999999939493 ) ;
#228865=DIRECTION ( 'NONE',  ( -0.000000000000000000, 6.982962677686266711E-15, -1.000000000000000000 ) ) ;
#228878=EDGE_LOOP ( 'NONE', ( #100120, #248311, #104333, #132040 ) ) ;
#228887=DIRECTION ( 'NONE',  ( 1.000000000000000000, 0.000000000000000000, 0.000000000000000000 ) ) ;
#228904=DIRECTION ( 'NONE',  ( -1.000000000000000000, 0.000000000000000000, 0.000000000000000000 ) ) ;
#228946=CARTESIAN_POINT ( 'NONE',  ( 23.14999999999999858, 76.00000000001170974, -69.52310748452431710 ) ) ;
#228968=AXIS2_PLACEMENT_3D ( 'NONE', #205429, #221144, #4656 ) ;
#228973=DIRECTION ( 'NONE',  ( -1.000000000000000000, 0.000000000000000000, 0.000000000000000000 ) ) ;
#229032=CARTESIAN_POINT ( 'NONE',  ( 20.94999999999999929, 77.83534155023627932, -91.46795619196132066 ) ) ;
#229035=ORIENTED_EDGE ( 'NONE', *, *, #229545, .F. ) ;
#229046=FACE_OUTER_BOUND ( 'NONE', #168908, .T. ) ;
#229055=ORIENTED_EDGE ( 'NONE', *, *, #229156, .T. ) ;
#229058=CIRCLE ( 'NONE', #108259, 0.09999999999999939493 ) ;
#229074=AXIS2_PLACEMENT_3D ( 'NONE', #114352, #214725, #13979 ) ;
#229078=DIRECTION ( 'NONE',  ( 0.000000000000000000, 2.362176648138631684E-15, 1.000000000000000000 ) ) ;
#229080=ORIENTED_EDGE ( 'NONE', *, *, #248014, .T. ) ;
#229084=CARTESIAN_POINT ( 'NONE',  ( 23.14999999999999858, 76.00000000001170974, -69.52310748452431710 ) ) ;
#229104=DIRECTION ( 'NONE',  ( 0.000000000000000000, -1.000000000000000000, -6.982962677686265922E-15 ) ) ;
#229111=LINE ( 'NONE', #209544, #6600 ) ;
#229114=AXIS2_PLACEMENT_3D ( 'NONE', #237324, #215187, #36588 ) ;
#229139=ORIENTED_EDGE ( 'NONE', *, *, #166306, .F. ) ;
#229156=EDGE_CURVE ( 'NONE', #159228, #231733, #220802, .T. ) ;
#229204=CARTESIAN_POINT ( 'NONE',  ( -23.25000000000000000, 71.65000000001187175, -90.77310748452434552 ) ) ;
#229229=EDGE_CURVE ( 'NONE', #20238, #199047, #244231, .T. ) ;
#229238=CARTESIAN_POINT ( 'NONE',  ( 23.15000000000000213, 85.00000000001179501, -79.41707660717668205 ) ) ;
#229242=EDGE_LOOP ( 'NONE', ( #225851, #131639, #168207, #182860 ) ) ;
#229275=EDGE_LOOP ( 'NONE', ( #20829, #43091, #90205, #83202 ) ) ;
#229289=ADVANCED_FACE ( 'NONE', ( #227222 ), #231802, .T. ) ;
#229294=ORIENTED_EDGE ( 'NONE', *, *, #166920, .F. ) ;
#229298=CARTESIAN_POINT ( 'NONE',  ( -21.12230431290520016, 69.54243334671895127, -103.0283173362133624 ) ) ;
#229319=AXIS2_PLACEMENT_3D ( 'NONE', #185314, #47065, #168365 ) ;
#229321=DIRECTION ( 'NONE',  ( 0.000000000000000000, 0.000000000000000000, 1.000000000000000000 ) ) ;
#229339=DIRECTION ( 'NONE',  ( -1.000000000000000000, 0.000000000000000000, 0.000000000000000000 ) ) ;
#229413=DIRECTION ( 'NONE',  ( 3.265361837132813093E-16, 1.000000000000000000, 6.982962677686266711E-15 ) ) ;
#229446=ORIENTED_EDGE ( 'NONE', *, *, #195271, .T. ) ;
#229447=ORIENTED_EDGE ( 'NONE', *, *, #33500, .T. ) ;
#229449=ADVANCED_FACE ( 'NONE', ( #138376 ), #52887, .T. ) ;
#229463=ADVANCED_FACE ( 'NONE', ( #137123 ), #74618, .T. ) ;
#229489=VECTOR ( 'NONE', #155291, 1000.000000000000000 ) ;
#229509=DIRECTION ( 'NONE',  ( -0.000000000000000000, 1.000000000000000000, 6.982962677686266711E-15 ) ) ;
#229510=CYLINDRICAL_SURFACE ( 'NONE', #199230, 0.1000000000000028644 ) ;
#229512=DIRECTION ( 'NONE',  ( 0.000000000000000000, 0.000000000000000000, -1.000000000000000000 ) ) ;
#229535=DIRECTION ( 'NONE',  ( 1.000000000000000000, 0.000000000000000000, 0.000000000000000000 ) ) ;
#229545=EDGE_CURVE ( 'NONE', #108305, #34745, #36362, .T. ) ;
#229546=LINE ( 'NONE', #169610, #61315 ) ;
#229567=EDGE_CURVE ( 'NONE', #51895, #36183, #123990, .T. ) ;
#229569=CARTESIAN_POINT ( 'NONE',  ( -22.50014994444008565, 64.25028026811963855, -103.1061876412435936 ) ) ;
#229575=FACE_OUTER_BOUND ( 'NONE', #56819, .T. ) ;
#229584=CARTESIAN_POINT ( 'NONE',  ( 18.59999999999999432, 74.83729825007388570, -94.92310748452432279 ) ) ;
#229593=DIRECTION ( 'NONE',  ( 0.000000000000000000, -6.938893903907222067E-15, 1.000000000000000000 ) ) ;
#229605=DIRECTION ( 'NONE',  ( 0.000000000000000000, -6.982962677686266711E-15, 1.000000000000000000 ) ) ;
#229606=AXIS2_PLACEMENT_3D ( 'NONE', #137829, #178288, #217364 ) ;
#229624=FACE_OUTER_BOUND ( 'NONE', #40892, .T. ) ;
#229669=VERTEX_POINT ( 'NONE', #48289 ) ;
#229681=CARTESIAN_POINT ( 'NONE',  ( 20.94999999999999929, 64.36312671090729509, -76.34486669784918433 ) ) ;
#229682=DIRECTION ( 'NONE',  ( 1.000000000000000000, 0.000000000000000000, 0.000000000000000000 ) ) ;
#229713=CARTESIAN_POINT ( 'NONE',  ( 20.94999999999999929, 67.07338541492478612, -94.55142446530125255 ) ) ;
#229726=VERTEX_POINT ( 'NONE', #148693 ) ;
#229751=ORIENTED_EDGE ( 'NONE', *, *, #131915, .F. ) ;
#229799=VERTEX_POINT ( 'NONE', #129117 ) ;
#229834=CARTESIAN_POINT ( 'NONE',  ( 22.59999999999999787, 64.35042919246716053, -103.1231074845243825 ) ) ;
#229843=DIRECTION ( 'NONE',  ( 0.000000000000000000, -6.938893903907222067E-15, 1.000000000000000000 ) ) ;
#229859=CARTESIAN_POINT ( 'NONE',  ( 20.53930447208010790, 67.02285131248687833, -94.58060034294609864 ) ) ;
#229866=ADVANCED_FACE ( 'NONE', ( #198065 ), #134231, .F. ) ;
#229949=VERTEX_POINT ( 'NONE', #92539 ) ;
#229950=CARTESIAN_POINT ( 'NONE',  ( 23.14999999999999503, 69.55000000001203375, -114.7731074845243455 ) ) ;
#229951=ORIENTED_EDGE ( 'NONE', *, *, #243088, .F. ) ;
#229978=CARTESIAN_POINT ( 'NONE',  ( 22.39999999999999503, 76.00000000001203659, -114.6726782920691221 ) ) ;
#229985=DIRECTION ( 'NONE',  ( -2.915501640297152804E-16, -1.000000000000000000, -6.997203936713167125E-15 ) ) ;
#229993=EDGE_CURVE ( 'NONE', #253445, #11088, #173942, .T. ) ;
#230056=CARTESIAN_POINT ( 'NONE',  ( -21.14999999999999858, 64.35000000001190301, -96.23924182154622997 ) ) ;
#230085=CARTESIAN_POINT ( 'NONE',  ( -18.54148534481894117, 65.67467670974396299, -63.95317318268840978 ) ) ;
#230089=CIRCLE ( 'NONE', #13442, 0.09999999999999799327 ) ;
#230100=DIRECTION ( 'NONE',  ( -1.000000000000000000, 7.304098846218134667E-16, 5.100424963727256530E-30 ) ) ;
#230144=CARTESIAN_POINT ( 'NONE',  ( 20.85000000000000142, 87.75000000001172396, -72.52310748452423184 ) ) ;
#230166=FACE_OUTER_BOUND ( 'NONE', #102384, .T. ) ;
#230219=DIRECTION ( 'NONE',  ( -1.000000000000000000, 0.000000000000000000, -0.000000000000000000 ) ) ;
#230223=DIRECTION ( 'NONE',  ( 0.000000000000000000, 0.000000000000000000, -1.000000000000000000 ) ) ;
#230225=CYLINDRICAL_SURFACE ( 'NONE', #213532, 0.09999999999999939493 ) ;
#230239=DIRECTION ( 'NONE',  ( 0.000000000000000000, 7.056502275159890832E-15, -1.000000000000000000 ) ) ;
#230253=CARTESIAN_POINT ( 'NONE',  ( 18.59999996954842771, 85.52320413787062137, -62.64006577260797570 ) ) ;
#230300=ORIENTED_EDGE ( 'NONE', *, *, #27769, .T. ) ;
#230361=CIRCLE ( 'NONE', #155395, 0.1000000000000021289 ) ;
#230450=EDGE_CURVE ( 'NONE', #74222, #97650, #220838, .T. ) ;
#230461=AXIS2_PLACEMENT_3D ( 'NONE', #71856, #211354, #27612 ) ;
#230576=ORIENTED_EDGE ( 'NONE', *, *, #126807, .F. ) ;
#230605=APPLICATION_CONTEXT ( 'automotive_design' ) ;
#230607=ORIENTED_EDGE ( 'NONE', *, *, #255155, .T. ) ;
#230612=EDGE_CURVE ( 'NONE', #146049, #121066, #251966, .T. ) ;
#230622=CARTESIAN_POINT ( 'NONE',  ( -18.50000000000000000, 64.35000000001203091, -114.7731074845243882 ) ) ;
#230643=DIRECTION ( 'NONE',  ( 0.000000000000000000, -6.982962677686266711E-15, 1.000000000000000000 ) ) ;
#230652=LINE ( 'NONE', #67717, #48029 ) ;
#230703=DIRECTION ( 'NONE',  ( 0.000000000000000000, -1.000000000000000000, 0.000000000000000000 ) ) ;
#230719=LINE ( 'NONE', #152484, #158294 ) ;
#230721=DIRECTION ( 'NONE',  ( 0.000000000000000000, -6.982962677686266711E-15, 1.000000000000000000 ) ) ;
#230798=ORIENTED_EDGE ( 'NONE', *, *, #236990, .F. ) ;
#230805=CARTESIAN_POINT ( 'NONE',  ( -18.59999999999999787, 74.83729825007388570, -94.92310748452432279 ) ) ;
#230887=CARTESIAN_POINT ( 'NONE',  ( -20.94403535211772294, 65.69367753730635684, -64.01892380663480253 ) ) ;
#230889=AXIS2_PLACEMENT_3D ( 'NONE', #52931, #172934, #227712 ) ;
#230900=AXIS2_PLACEMENT_3D ( 'NONE', #65136, #45585, #164263 ) ;
#230904=CARTESIAN_POINT ( 'NONE',  ( -21.70464131381649509, 68.90464198104409377, -103.0231074845243739 ) ) ;
#230923=DIRECTION ( 'NONE',  ( -1.000000000000000000, -0.000000000000000000, -0.000000000000000000 ) ) ;
#230945=DIRECTION ( 'NONE',  ( 0.000000000000000000, -6.938893903907222067E-15, 1.000000000000000000 ) ) ;
#230964=CARTESIAN_POINT ( 'NONE',  ( 18.49999999999999289, 65.65621891165865520, -78.19466220664698142 ) ) ;
#230973=DIRECTION ( 'NONE',  ( 0.000000000000000000, 0.000000000000000000, -1.000000000000000000 ) ) ;
#230977=AXIS2_PLACEMENT_3D ( 'NONE', #7522, #83173, #242271 ) ;
#230982=DIRECTION ( 'NONE',  ( -4.701977403289178058E-30, -2.433019743745433765E-14, 1.000000000000000000 ) ) ;
#231022=CYLINDRICAL_SURFACE ( 'NONE', #35251, 0.1000000000000028644 ) ;
#231045=ORIENTED_EDGE ( 'NONE', *, *, #246271, .T. ) ;
#231060=DIRECTION ( 'NONE',  ( -1.836970198721029934E-16, -1.000000000000000000, -6.982962677686266711E-15 ) ) ;
#231088=DIRECTION ( 'NONE',  ( 1.000000000000000000, 0.000000000000000000, 0.000000000000000000 ) ) ;
#231098=ORIENTED_EDGE ( 'NONE', *, *, #257625, .T. ) ;
#231132=DIRECTION ( 'NONE',  ( -1.000000000000000000, 0.000000000000000000, -0.000000000000000000 ) ) ;
#231167=CARTESIAN_POINT ( 'NONE',  ( 20.51284917709620359, 65.68911337716723153, -95.35063429893224907 ) ) ;
#231171=CARTESIAN_POINT ( 'NONE',  ( -23.25000000000000000, 77.25000000001165290, -61.72262673010922640 ) ) ;
#231182=AXIS2_PLACEMENT_3D ( 'NONE', #94905, #253977, #191487 ) ;
#231186=ORIENTED_EDGE ( 'NONE', *, *, #90950, .T. ) ;
#231191=CARTESIAN_POINT ( 'NONE',  ( -20.54999999999999716, 73.60000000001180354, -82.74772940728642823 ) ) ;
#231235=ADVANCED_FACE ( 'NONE', ( #211190 ), #228197, .F. ) ;
#231244=CIRCLE ( 'NONE', #210386, 0.5000000000000004441 ) ;
#231263=EDGE_LOOP ( 'NONE', ( #57021, #24955, #158733, #138677 ) ) ;
#231312=CARTESIAN_POINT ( 'NONE',  ( -22.39999999999999858, 76.00000000001203659, -114.6726782920691221 ) ) ;
#231319=DIRECTION ( 'NONE',  ( 0.000000000000000000, -6.982962677686266711E-15, 1.000000000000000000 ) ) ;
#231320=FACE_OUTER_BOUND ( 'NONE', #6769, .T. ) ;
#231322=DIRECTION ( 'NONE',  ( 0.000000000000000000, 0.8660254037844377084, 0.5000000000000016653 ) ) ;
#231348=DIRECTION ( 'NONE',  ( -1.000000000000000000, 2.952720810173289112E-16, 2.061873921506763405E-30 ) ) ;
#231355=ORIENTED_EDGE ( 'NONE', *, *, #177783, .F. ) ;
#231356=CARTESIAN_POINT ( 'NONE',  ( -20.94999999999999929, 74.14897176987101091, -91.36919421510182815 ) ) ;
#231385=EDGE_CURVE ( 'NONE', #239900, #252190, #253150, .T. ) ;
#231388=CIRCLE ( 'NONE', #102338, 4.000000000000003553 ) ;
#231400=DIRECTION ( 'NONE',  ( 0.000000000000000000, 7.056502275159890832E-15, -1.000000000000000000 ) ) ;
#231412=CIRCLE ( 'NONE', #127343, 0.6000000000000033085 ) ;
#231416=AXIS2_PLACEMENT_3D ( 'NONE', #94001, #251802, #73202 ) ;
#231444=EDGE_CURVE ( 'NONE', #161481, #252623, #65723, .T. ) ;
#231459=ORIENTED_EDGE ( 'NONE', *, *, #176634, .T. ) ;
#231464=AXIS2_PLACEMENT_3D ( 'NONE', #96914, #60387, #255975 ) ;
#231486=DIRECTION ( 'NONE',  ( -1.000000000000000000, -7.304098846218135653E-16, -5.100424963727256530E-30 ) ) ;
#231489=CARTESIAN_POINT ( 'NONE',  ( -20.85000000000000142, 77.16412189325286874, -61.60825939895269698 ) ) ;
#231508=VECTOR ( 'NONE', #207060, 1000.000000000000000 ) ;
#231513=DIRECTION ( 'NONE',  ( 2.952720810173289112E-16, 1.000000000000000000, -6.088138035986627436E-46 ) ) ;
#231583=CIRCLE ( 'NONE', #135879, 7.800000000000001599 ) ;
#231592=DIRECTION ( 'NONE',  ( 0.000000000000000000, 1.000000000000000000, 6.982962677686266711E-15 ) ) ;
#231634=DIRECTION ( 'NONE',  ( 1.000000000000000000, -0.000000000000000000, 0.000000000000000000 ) ) ;
#231693=CARTESIAN_POINT ( 'NONE',  ( 21.30000000000002558, 76.00000000001197975, -107.0731074845243143 ) ) ;
#231733=VERTEX_POINT ( 'NONE', #38661 ) ;
#231757=LINE ( 'NONE', #135190, #105561 ) ;
#231776=CIRCLE ( 'NONE', #69469, 0.2000000000000057288 ) ;
#231802=TOROIDAL_SURFACE ( 'NONE', #11212, 3.899999999999999467, 0.1000000000000000056 ) ;
#231836=DIRECTION ( 'NONE',  ( -4.408576920032448588E-17, -0.1350103645451807555, -0.9908441862701609093 ) ) ;
#231837=CIRCLE ( 'NONE', #90334, 0.1000000000000016431 ) ;
#231864=CIRCLE ( 'NONE', #57020, 0.5000000000000004441 ) ;
#231867=LINE ( 'NONE', #192728, #62095 ) ;
#231877=LINE ( 'NONE', #70244, #34167 ) ;
#231881=CARTESIAN_POINT ( 'NONE',  ( 20.94999999999999574, 65.57661458509899433, -95.53105556065429482 ) ) ;
#231896=DIRECTION ( 'NONE',  ( 0.000000000000000000, -7.487053152578127080E-15, 1.000000000000000000 ) ) ;
#231908=ORIENTED_EDGE ( 'NONE', *, *, #139499, .T. ) ;
#231910=EDGE_CURVE ( 'NONE', #23326, #51672, #40985, .T. ) ;
#231923=VERTEX_POINT ( 'NONE', #56299 ) ;
#231945=AXIS2_PLACEMENT_3D ( 'NONE', #62706, #83511, #142232 ) ;
#231956=CARTESIAN_POINT ( 'NONE',  ( -21.05000000000000071, 70.10000000001193143, -92.80400771986793984 ) ) ;
#232009=EDGE_CURVE ( 'NONE', #110239, #145746, #65901, .T. ) ;
#232010=VERTEX_POINT ( 'NONE', #101831 ) ;
#232014=CIRCLE ( 'NONE', #48642, 0.09999999999999939493 ) ;
#232027=AXIS2_PLACEMENT_3D ( 'NONE', #38976, #239733, #55926 ) ;
#232028=DIRECTION ( 'NONE',  ( -1.000000000000000000, 0.000000000000000000, 0.000000000000000000 ) ) ;
#232041=VECTOR ( 'NONE', #166989, 1000.000000000000227 ) ;
#232059=CARTESIAN_POINT ( 'NONE',  ( -23.25000000000000000, 87.65000000001172964, -72.62310748452422615 ) ) ;
#232074=CARTESIAN_POINT ( 'NONE',  ( -18.59999999999999787, 77.83585931145526615, -57.91866831572577468 ) ) ;
#232075=DIRECTION ( 'NONE',  ( 0.7071067811865127117, 0.7071067811865821007, 0.000000000000000000 ) ) ;
#232087=EDGE_CURVE ( 'NONE', #127648, #202516, #245157, .T. ) ;
#232090=CARTESIAN_POINT ( 'NONE',  ( 21.07888907270776002, 65.27493078649663971, -90.80191389769119326 ) ) ;
#232098=ORIENTED_EDGE ( 'NONE', *, *, #107701, .T. ) ;
#232105=ORIENTED_EDGE ( 'NONE', *, *, #57925, .T. ) ;
#232137=CIRCLE ( 'NONE', #153051, 11.74999999999999645 ) ;
#232143=DIRECTION ( 'NONE',  ( 0.000000000000000000, 0.9908441862701605762, 0.1350103645451835310 ) ) ;
#232144=EDGE_CURVE ( 'NONE', #201306, #50342, #157718, .T. ) ;
#232169=CARTESIAN_POINT ( 'NONE',  ( -18.41799967126739901, 85.50000000001189449, -95.99103767126818809 ) ) ;
#232189=CARTESIAN_POINT ( 'NONE',  ( -21.29999999999995808, 76.00000000001197975, -107.0731074845243143 ) ) ;
#232200=CARTESIAN_POINT ( 'NONE',  ( -20.85000000000000142, 76.00000000001170974, -69.52310748452431710 ) ) ;
#232211=CIRCLE ( 'NONE', #48825, 0.09999999999999939493 ) ;
#232256=ORIENTED_EDGE ( 'NONE', *, *, #110712, .T. ) ;
#232273=CIRCLE ( 'NONE', #40570, 6.329289321881356400 ) ;
#232327=CARTESIAN_POINT ( 'NONE',  ( 21.12642695952774119, 75.90109671682263581, -109.3987674065594859 ) ) ;
#232355=ORIENTED_EDGE ( 'NONE', *, *, #108021, .F. ) ;
#232369=DIRECTION ( 'NONE',  ( 0.000000000000000000, 0.000000000000000000, 1.000000000000000000 ) ) ;
#232395=AXIS2_PLACEMENT_3D ( 'NONE', #184645, #105072, #208090 ) ;
#232473=CARTESIAN_POINT ( 'NONE',  ( -21.45000000000000284, 68.29142135624910281, -81.87310748452436826 ) ) ;
#232484=DIRECTION ( 'NONE',  ( 1.000000000000000000, 0.000000000000000000, 0.000000000000000000 ) ) ;
#232543=SPHERICAL_SURFACE ( 'NONE', #49136, 0.1000000000000000056 ) ;
#232575=CIRCLE ( 'NONE', #207611, 0.2000000000000057288 ) ;
#232637=ORIENTED_EDGE ( 'NONE', *, *, #151471, .F. ) ;
#232638=VERTEX_POINT ( 'NONE', #252605 ) ;
#232716=DIRECTION ( 'NONE',  ( -0.000000000000000000, -6.982962677686266711E-15, 1.000000000000000000 ) ) ;
#232720=EDGE_LOOP ( 'NONE', ( #602, #218341, #222678 ) ) ;
#232729=DIRECTION ( 'NONE',  ( 1.000000000000000000, 0.000000000000000000, 0.000000000000000000 ) ) ;
#232777=EDGE_CURVE ( 'NONE', #171947, #9869, #62360, .T. ) ;
#232801=CIRCLE ( 'NONE', #62096, 0.6000000000000033085 ) ;
#232826=DIRECTION ( 'NONE',  ( -0.000000000000000000, -1.000000000000000000, -7.272083257015735086E-15 ) ) ;
#232850=DIRECTION ( 'NONE',  ( 0.000000000000000000, 0.000000000000000000, 1.000000000000000000 ) ) ;
#232933=ORIENTED_EDGE ( 'NONE', *, *, #222718, .F. ) ;
#232937=CIRCLE ( 'NONE', #237209, 0.1000000000000028644 ) ;
#232946=CARTESIAN_POINT ( 'NONE',  ( 22.39999999999999858, 75.90000000001199965, -110.8138870828976934 ) ) ;
#232947=ORIENTED_EDGE ( 'NONE', *, *, #69272, .F. ) ;
#232948=DIRECTION ( 'NONE',  ( 0.000000000000000000, -6.982962677686266711E-15, 1.000000000000000000 ) ) ;
#232966=EDGE_LOOP ( 'NONE', ( #109807, #230607, #91545, #104377 ) ) ;
#232980=DIRECTION ( 'NONE',  ( -1.000000000000000000, 0.000000000000000000, -0.000000000000000000 ) ) ;
#232991=CARTESIAN_POINT ( 'NONE',  ( -23.25000000000000000, 85.60000000001177511, -79.41707660717668205 ) ) ;
#232994=VECTOR ( 'NONE', #180712, 1000.000000000000000 ) ;
#233014=ORIENTED_EDGE ( 'NONE', *, *, #49690, .F. ) ;
#233020=DIRECTION ( 'NONE',  ( -1.000000000000000000, 0.000000000000000000, 0.000000000000000000 ) ) ;
#233062=DIRECTION ( 'NONE',  ( 1.000000000000000000, -0.000000000000000000, 0.000000000000000000 ) ) ;
#233084=CARTESIAN_POINT ( 'NONE',  ( -18.59999999999999787, 77.83534155023627932, -91.36795619196132634 ) ) ;
#233146=DIRECTION ( 'NONE',  ( 0.000000000000000000, 6.608470384673558123E-15, -1.000000000000000000 ) ) ;
#233149=DIRECTION ( 'NONE',  ( 1.000000000000000000, -7.304098846218133681E-16, -4.639676173203992654E-30 ) ) ;
#233155=DIRECTION ( 'NONE',  ( -0.000000000000000000, 0.1350103645451974088, -0.9908441862701587999 ) ) ;
#233176=AXIS2_PLACEMENT_3D ( 'NONE', #120595, #116718, #39787 ) ;
#233189=DIRECTION ( 'NONE',  ( 0.000000000000000000, -1.565658005757035267E-14, 1.000000000000000000 ) ) ;
#233211=CARTESIAN_POINT ( 'NONE',  ( 21.04999999999999716, 69.69981666374559381, -103.0744349168653571 ) ) ;
#233240=CARTESIAN_POINT ( 'NONE',  ( 20.84999999999999432, 77.16412189325286874, -61.60825939895269698 ) ) ;
#233246=ADVANCED_FACE ( 'NONE', ( #200045 ), #1817, .T. ) ;
#233257=DIRECTION ( 'NONE',  ( 0.000000000000000000, 6.982962677686266711E-15, -1.000000000000000000 ) ) ;
#233260=FACE_OUTER_BOUND ( 'NONE', #849, .T. ) ;
#233262=CARTESIAN_POINT ( 'NONE',  ( 20.94999999999999574, 87.41227409416161720, -100.1231074845242262 ) ) ;
#233299=VERTEX_POINT ( 'NONE', #89064 ) ;
#233317=DIRECTION ( 'NONE',  ( 0.000000000000000000, 0.000000000000000000, 1.000000000000000000 ) ) ;
#233363=AXIS2_PLACEMENT_3D ( 'NONE', #15005, #115363, #116652 ) ;
#233372=CARTESIAN_POINT ( 'NONE',  ( 21.00000000000000000, 66.25000000001186606, -90.77310748452438816 ) ) ;
#233382=EDGE_CURVE ( 'NONE', #603, #183504, #151653, .T. ) ;
#233384=CARTESIAN_POINT ( 'NONE',  ( 21.10642757222115407, 65.27684371085327086, -90.78240996073918723 ) ) ;
#233406=EDGE_CURVE ( 'NONE', #82775, #12289, #58602, .T. ) ;
#233427=EDGE_CURVE ( 'NONE', #142820, #3343, #73399, .T. ) ;
#233455=ORIENTED_EDGE ( 'NONE', *, *, #175080, .F. ) ;
#233467=ORIENTED_EDGE ( 'NONE', *, *, #134772, .T. ) ;
#233472=CARTESIAN_POINT ( 'NONE',  ( -20.85000000000000142, 76.00000000001170974, -69.52310748452431710 ) ) ;
#233484=DIRECTION ( 'NONE',  ( 0.000000000000000000, 7.147358527629766941E-15, -1.000000000000000000 ) ) ;
#233520=ORIENTED_EDGE ( 'NONE', *, *, #93236, .T. ) ;
#233541=CARTESIAN_POINT ( 'NONE',  ( 23.15000000000000213, 87.65000000001172964, -72.62310748452422615 ) ) ;
#233560=DIRECTION ( 'NONE',  ( 2.259780016855445309E-14, -0.9875055080513764905, 0.1575844902526679359 ) ) ;
#233582=ORIENTED_EDGE ( 'NONE', *, *, #135771, .T. ) ;
#233641=EDGE_CURVE ( 'NONE', #76960, #170856, #83289, .T. ) ;
#233656=CARTESIAN_POINT ( 'NONE',  ( -20.64999999999999858, 73.60000000001184617, -89.79848556176223440 ) ) ;
#233663=DIRECTION ( 'NONE',  ( 1.000000000000000000, -3.265361837132813093E-16, -2.280189983783949500E-30 ) ) ;
#233692=ORIENTED_EDGE ( 'NONE', *, *, #247000, .T. ) ;
#233744=DIRECTION ( 'NONE',  ( 0.000000000000000000, -6.982962677686266711E-15, 1.000000000000000000 ) ) ;
#233768=DIRECTION ( 'NONE',  ( 0.000000000000000000, -6.982962677686266711E-15, 1.000000000000000000 ) ) ;
#233834=VERTEX_POINT ( 'NONE', #120883 ) ;
#233851=EDGE_CURVE ( 'NONE', #32631, #129506, #158604, .T. ) ;
#233871=CYLINDRICAL_SURFACE ( 'NONE', #91443, 0.1000000000000028644 ) ;
#233874=VECTOR ( 'NONE', #232826, 1000.000000000000000 ) ;
#233882=VERTEX_POINT ( 'NONE', #76583 ) ;
#233891=DIRECTION ( 'NONE',  ( 0.000000000000000000, 1.000000000000000000, 6.352154140967427193E-15 ) ) ;
#233942=DIRECTION ( 'NONE',  ( 0.000000000000000000, 0.000000000000000000, -1.000000000000000000 ) ) ;
#233945=CIRCLE ( 'NONE', #242130, 0.8750000000000007772 ) ;
#233964=CYLINDRICAL_SURFACE ( 'NONE', #248477, 0.09999999999999939493 ) ;
#233979=ORIENTED_EDGE ( 'NONE', *, *, #122832, .T. ) ;
#233986=CARTESIAN_POINT ( 'NONE',  ( 21.14999999999999858, 65.28660755661196902, -90.67310748452437963 ) ) ;
#234023=DIRECTION ( 'NONE',  ( 0.000000000000000000, 0.000000000000000000, 1.000000000000000000 ) ) ;
#234026=CARTESIAN_POINT ( 'NONE',  ( -20.85000000000000142, 64.25000000001170974, -69.52310748452438816 ) ) ;
#234040=DIRECTION ( 'NONE',  ( 0.000000000000000000, 6.982962677686266711E-15, -1.000000000000000000 ) ) ;
#234057=DIRECTION ( 'NONE',  ( 2.659396599871503635E-15, -0.6132151058540604716, 0.7899159663865477077 ) ) ;
#234079=DIRECTION ( 'NONE',  ( 1.000000000000000000, 0.000000000000000000, 0.000000000000000000 ) ) ;
#234105=CARTESIAN_POINT ( 'NONE',  ( 18.50000000000001421, 85.48068669529062902, -62.58199231576637800 ) ) ;
#234107=CARTESIAN_POINT ( 'NONE',  ( 20.85000000000000142, 76.00000000001165290, -61.62310748452430431 ) ) ;
#234110=ADVANCED_FACE ( 'NONE', ( #150687 ), #192113, .F. ) ;
#234157=CIRCLE ( 'NONE', #159187, 0.1000000000000028644 ) ;
#234165=CARTESIAN_POINT ( 'NONE',  ( -20.94999999999999929, 75.74389420791972327, -103.0580039261966050 ) ) ;
#234181=TOROIDAL_SURFACE ( 'NONE', #151013, 12.97499999999999787, 0.1000000000000000056 ) ;
#234261=CARTESIAN_POINT ( 'NONE',  ( 23.15000000000000213, 84.66355140188105111, -93.49900636645693908 ) ) ;
#234285=AXIS2_PLACEMENT_3D ( 'NONE', #21425, #40988, #65651 ) ;
#234310=ORIENTED_EDGE ( 'NONE', *, *, #128009, .T. ) ;
#234347=CIRCLE ( 'NONE', #209401, 0.09999999999999939493 ) ;
#234371=DIRECTION ( 'NONE',  ( 1.000000000000000000, -3.265361837132813093E-16, -2.280189983783949500E-30 ) ) ;
#234410=DIRECTION ( 'NONE',  ( 0.000000000000000000, -0.4999999999999689138, 0.8660254037844565822 ) ) ;
#234432=DIRECTION ( 'NONE',  ( 0.000000000000000000, 0.8700118002898393765, -0.4930308989875104575 ) ) ;
#234495=SPHERICAL_SURFACE ( 'NONE', #212725, 0.1000000000000000056 ) ;
#234508=CIRCLE ( 'NONE', #9655, 0.1000000000000028644 ) ;
#234516=EDGE_CURVE ( 'NONE', #186482, #199102, #238043, .T. ) ;
#234579=CARTESIAN_POINT ( 'NONE',  ( -23.25000000000000000, 69.01799029515524353, -65.82695536626808064 ) ) ;
#234583=CIRCLE ( 'NONE', #188802, 0.1999999999999987899 ) ;
#234587=CARTESIAN_POINT ( 'NONE',  ( 23.15000000000000213, 85.50000000001179501, -79.41707660717668205 ) ) ;
#234603=DIRECTION ( 'NONE',  ( 0.000000000000000000, -0.9998779222360097974, 0.01562500000000363945 ) ) ;
#234635=AXIS2_PLACEMENT_3D ( 'NONE', #182178, #100033, #179622 ) ;
#234667=EDGE_LOOP ( 'NONE', ( #232098, #145663, #49806, #34686 ) ) ;
#234705=VECTOR ( 'NONE', #152176, 1000.000000000000000 ) ;
#234721=FACE_OUTER_BOUND ( 'NONE', #247334, .T. ) ;
#234750=FACE_OUTER_BOUND ( 'NONE', #207334, .T. ) ;
#234790=CIRCLE ( 'NONE', #9920, 0.1000000000000028644 ) ;
#234809=ORIENTED_EDGE ( 'NONE', *, *, #178742, .T. ) ;
#234872=AXIS2_PLACEMENT_3D ( 'NONE', #253633, #158440, #234079 ) ;
#234878=CARTESIAN_POINT ( 'NONE',  ( 20.85000000000000142, 77.83585931145526615, -58.01866831572577610 ) ) ;
#234899=DIRECTION ( 'NONE',  ( -1.000000000000000000, 0.000000000000000000, 0.000000000000000000 ) ) ;
#234903=EDGE_CURVE ( 'NONE', #246385, #67031, #163595, .T. ) ;
#234933=DIRECTION ( 'NONE',  ( 0.000000000000000000, 0.000000000000000000, 1.000000000000000000 ) ) ;
#234950=FACE_OUTER_BOUND ( 'NONE', #254381, .T. ) ;
#234955=AXIS2_PLACEMENT_3D ( 'NONE', #158891, #20656, #169166 ) ;
#234975=DIRECTION ( 'NONE',  ( -1.000000000000000000, -1.387778780781454006E-13, 0.000000000000000000 ) ) ;
#234983=CIRCLE ( 'NONE', #151613, 11.74999999999999645 ) ;
#234984=CARTESIAN_POINT ( 'NONE',  ( -20.54999999999999716, 85.40000000001188596, -93.12913836187179584 ) ) ;
#234990=VECTOR ( 'NONE', #157485, 1000.000000000000000 ) ;
#235042=CIRCLE ( 'NONE', #122634, 0.1000000000000033223 ) ;
#235049=FACE_OUTER_BOUND ( 'NONE', #206093, .T. ) ;
#235054=EDGE_LOOP ( 'NONE', ( #123958, #68503, #53418, #37750 ) ) ;
#235059=EDGE_LOOP ( 'NONE', ( #57472, #226887, #80514, #74590 ) ) ;
#235076=ORIENTED_EDGE ( 'NONE', *, *, #90412, .F. ) ;
#235081=DIRECTION ( 'NONE',  ( 0.000000000000000000, -1.000000000000000000, 0.000000000000000000 ) ) ;
#235087=DIRECTION ( 'NONE',  ( 0.000000000000000000, 0.000000000000000000, 1.000000000000000000 ) ) ;
#235099=LINE ( 'NONE', #16074, #60685 ) ;
#235128=ADVANCED_FACE ( 'NONE', ( #36954 ), #116464, .F. ) ;
#235138=FACE_OUTER_BOUND ( 'NONE', #146676, .T. ) ;
#235180=CIRCLE ( 'NONE', #56089, 0.1000000000000028644 ) ;
#235248=ORIENTED_EDGE ( 'NONE', *, *, #133522, .F. ) ;
#235269=TOROIDAL_SURFACE ( 'NONE', #181144, 1.900000000000002576, 0.1000000000000000056 ) ;
#235297=CARTESIAN_POINT ( 'NONE',  ( -20.94999999999999929, 87.48912529308798014, -99.92310748452423752 ) ) ;
#235304=EDGE_LOOP ( 'NONE', ( #124210, #37648, #40430 ) ) ;
#235332=DIRECTION ( 'NONE',  ( 0.000000000000000000, 0.000000000000000000, -1.000000000000000000 ) ) ;
#235348=DIRECTION ( 'NONE',  ( -0.000000000000000000, -6.982962677686266711E-15, 1.000000000000000000 ) ) ;
#235432=ORIENTED_EDGE ( 'NONE', *, *, #161025, .T. ) ;
#235442=DIRECTION ( 'NONE',  ( 0.000000000000000000, -0.9908441862701605762, -0.1350103645451835310 ) ) ;
#235464=FACE_OUTER_BOUND ( 'NONE', #47814, .T. ) ;
#235470=VERTEX_POINT ( 'NONE', #95295 ) ;
#235473=AXIS2_PLACEMENT_3D ( 'NONE', #174625, #254086, #75494 ) ;
#235494=ORIENTED_EDGE ( 'NONE', *, *, #91534, .T. ) ;
#235495=DIRECTION ( 'NONE',  ( 0.000000000000000000, 0.000000000000000000, 1.000000000000000000 ) ) ;
#235550=DIRECTION ( 'NONE',  ( -1.000000000000000000, 2.952720810173289112E-16, 2.061873921506763405E-30 ) ) ;
#235566=ORIENTED_EDGE ( 'NONE', *, *, #108841, .T. ) ;
#235596=CIRCLE ( 'NONE', #181464, 0.1000000000000043771 ) ;
#235606=EDGE_CURVE ( 'NONE', #206437, #83423, #67637, .T. ) ;
#235639=EDGE_CURVE ( 'NONE', #59214, #37771, #51037, .T. ) ;
#235641=CARTESIAN_POINT ( 'NONE',  ( 21.05000000000000071, 76.00000000001173817, -73.52310748452431710 ) ) ;
#235650=FACE_OUTER_BOUND ( 'NONE', #227932, .T. ) ;
#235654=CARTESIAN_POINT ( 'NONE',  ( -18.59999999999999787, 74.25000000001186606, -91.35359592662267403 ) ) ;
#235740=PLANE ( 'NONE',  #102680 ) ;
#235758=EDGE_LOOP ( 'NONE', ( #211084, #127070, #20265 ) ) ;
#235759=ORIENTED_EDGE ( 'NONE', *, *, #158015, .F. ) ;
#235774=DIRECTION ( 'NONE',  ( 1.000000000000000000, 0.000000000000000000, 0.000000000000000000 ) ) ;
#235783=DIRECTION ( 'NONE',  ( 0.000000000000000000, 0.000000000000000000, 1.000000000000000000 ) ) ;
#235795=AXIS2_PLACEMENT_3D ( 'NONE', #37222, #617, #80141 ) ;
#235829=DIRECTION ( 'NONE',  ( 0.000000000000000000, 0.000000000000000000, -1.000000000000000000 ) ) ;
#235834=DIRECTION ( 'NONE',  ( 1.000000000000000000, 0.000000000000000000, 0.000000000000000000 ) ) ;
#235864=VERTEX_POINT ( 'NONE', #84675 ) ;
#235883=CARTESIAN_POINT ( 'NONE',  ( 21.05000000000000071, 76.00000000001170974, -69.52310748452431710 ) ) ;
#235914=EDGE_CURVE ( 'NONE', #8981, #160733, #180266, .T. ) ;
#235917=( BOUNDED_CURVE ( )  B_SPLINE_CURVE ( 3, ( #2674, #215314, #77084, #18399 ),
 .UNSPECIFIED., .F., .F. ) 
 B_SPLINE_CURVE_WITH_KNOTS ( ( 4, 4 ),
 ( 4.712388980384689674, 6.283185307179586232 ),
 .UNSPECIFIED. ) 
 CURVE ( )  GEOMETRIC_REPRESENTATION_ITEM ( )  RATIONAL_B_SPLINE_CURVE ( ( 1.000000000000000000, 0.8047378541243649375, 0.8047378541243649375, 1.000000000000000000 ) ) 
 REPRESENTATION_ITEM ( '' )  );
#235921=AXIS2_PLACEMENT_3D ( 'NONE', #127197, #227568, #85456 ) ;
#235935=DIRECTION ( 'NONE',  ( -1.000000000000000000, -0.000000000000000000, -0.000000000000000000 ) ) ;
#235956=CARTESIAN_POINT ( 'NONE',  ( 23.24999999999999645, 76.00000000001195133, -103.0231074845243171 ) ) ;
#235982=DIRECTION ( 'NONE',  ( 0.000000000000000000, -6.769652589177795712E-15, 1.000000000000000000 ) ) ;
#235984=( BOUNDED_SURFACE ( )  B_SPLINE_SURFACE ( 3, 2, ( 
 ( #188147, #87737, #149037 ),
 ( #128174, #207725, #9496 ),
 ( #89029, #228567, #49909 ),
 ( #189437, #51166, #130733 ),
 ( #171196, #129455, #106007 ),
 ( #210288, #31670, #91611 ),
 ( #185571, #166037, #250672 ),
 ( #245558, #172484, #115028 ) ),
 .UNSPECIFIED., .F., .F., .F. ) 
 B_SPLINE_SURFACE_WITH_KNOTS ( ( 4, 2, 2, 4 ),
 ( 3, 3 ),
 ( 0.0001704874539069995342, 0.0003809798300636783679, 0.0004862260181420178119, 0.0005914722062203572016 ),
 ( 0.000000000000000000, 1.000000000000000000 ),
 .UNSPECIFIED. ) 
 GEOMETRIC_REPRESENTATION_ITEM ( )  RATIONAL_B_SPLINE_SURFACE ( (
 ( 1.000000000000000000, 0.7071067811864699681, 1.000000000000000000),
 ( 1.000000000000000000, 0.7670648383568722251, 1.000000000000000000),
 ( 1.000000000000000000, 0.8204820770262503116, 1.000000000000000000),
 ( 1.000000000000000000, 0.8877218296108694284, 1.000000000000000000),
 ( 1.000000000000000000, 0.9080815932666681523, 1.000000000000000000),
 ( 1.000000000000000000, 0.9395541505860662834, 1.000000000000000000),
 ( 1.000000000000000000, 0.9506520335379859965, 1.000000000000000000),
 ( 1.000000000000000000, 0.9504532311154701985, 1.000000000000000000) ) ) 
 REPRESENTATION_ITEM ( '' )  SURFACE ( )  );
#236006=CARTESIAN_POINT ( 'NONE',  ( 21.05000000000000071, 85.00000000001179501, -79.41707660717668205 ) ) ;
#236007=EDGE_CURVE ( 'NONE', #235470, #201306, #118410, .T. ) ;
#236022=DIRECTION ( 'NONE',  ( -0.7071067811865127117, -0.7071067811865821007, 0.000000000000000000 ) ) ;
#236041=B_SPLINE_CURVE_WITH_KNOTS ( 'NONE', 3,
 ( #31514, #13217, #53615, #111018 ),
 .UNSPECIFIED., .F., .F.,
 ( 4, 4 ),
 ( 0.000000000000000000, 0.001767853679387101484 ),
 .UNSPECIFIED. ) ;
#236062=VERTEX_POINT ( 'NONE', #58391 ) ;
#236071=DIRECTION ( 'NONE',  ( 1.000000000000000000, -0.000000000000000000, 0.000000000000000000 ) ) ;
#236079=EDGE_LOOP ( 'NONE', ( #227233, #104301, #219178, #222396 ) ) ;
#236087=EDGE_CURVE ( 'NONE', #54475, #192857, #9896, .T. ) ;
#236165=ORIENTED_EDGE ( 'NONE', *, *, #143138, .T. ) ;
#236205=ADVANCED_FACE ( 'NONE', ( #204336 ), #147457, .T. ) ;
#236225=ORIENTED_EDGE ( 'NONE', *, *, #176634, .F. ) ;
#236238=SURFACE_STYLE_FILL_AREA ( #240105 ) ;
#236306=EDGE_CURVE ( 'NONE', #189878, #102088, #197328, .T. ) ;
#236318=CARTESIAN_POINT ( 'NONE',  ( 18.59999999999999076, 74.16465844978745281, -91.46795619196133487 ) ) ;
#236322=CARTESIAN_POINT ( 'NONE',  ( 21.06089410995835109, 65.27470446788827019, -90.82072675348118196 ) ) ;
#236323=ADVANCED_FACE ( 'NONE', ( #75142 ), #208220, .F. ) ;
#236349=EDGE_CURVE ( 'NONE', #167256, #206918, #185050, .T. ) ;
#236359=EDGE_LOOP ( 'NONE', ( #70710, #251407 ) ) ;
#236371=CARTESIAN_POINT ( 'NONE',  ( 21.07199075132371746, 67.22505500089579300, -90.80957532291151324 ) ) ;
#236427=CYLINDRICAL_SURFACE ( 'NONE', #210041, 0.09999999999999939493 ) ;
#236428=CARTESIAN_POINT ( 'NONE',  ( -18.59999999999999787, 85.48068669529064323, -62.58199231576639932 ) ) ;
#236440=CIRCLE ( 'NONE', #49004, 0.1999999999999987899 ) ;
#236485=ORIENTED_EDGE ( 'NONE', *, *, #83244, .F. ) ;
#236494=LINE ( 'NONE', #81255, #6678 ) ;
#236538=LINE ( 'NONE', #154485, #32939 ) ;
#236563=DIRECTION ( 'NONE',  ( -1.000000000000000000, 2.952720810173289112E-16, 2.061873921506763405E-30 ) ) ;
#236595=CARTESIAN_POINT ( 'NONE',  ( -22.37643362114956957, 75.90091862633062192, -110.6488974784827093 ) ) ;
#236597=CIRCLE ( 'NONE', #124204, 0.1000000000000055705 ) ;
#236600=ADVANCED_FACE ( 'NONE', ( #194466 ), #231022, .T. ) ;
#236623=DIRECTION ( 'NONE',  ( 9.044546369203337730E-15, 0.7397360091702647189, 0.6728971962616949742 ) ) ;
#236624=EDGE_CURVE ( 'NONE', #156778, #118009, #89184, .T. ) ;
#236626=CARTESIAN_POINT ( 'NONE',  ( -18.59999999999999787, 64.35000000001190301, -96.00830171387039513 ) ) ;
#236652=ORIENTED_EDGE ( 'NONE', *, *, #61673, .F. ) ;
#236673=FACE_OUTER_BOUND ( 'NONE', #163338, .T. ) ;
#236690=VECTOR ( 'NONE', #73172, 1000.000000000000000 ) ;
#236705=CARTESIAN_POINT ( 'NONE',  ( -23.25000000000000000, 76.00000000001195133, -103.0231074845243171 ) ) ;
#236706=DIRECTION ( 'NONE',  ( -0.000000000000000000, 1.000000000000000000, 6.982962677686266711E-15 ) ) ;
#236719=CARTESIAN_POINT ( 'NONE',  ( -22.48660254037843487, 64.35000000001195986, -103.0731074845243711 ) ) ;
#236734=CARTESIAN_POINT ( 'NONE',  ( 23.14999999999999858, 76.00000000001195133, -103.0231074845243171 ) ) ;
#236738=ADVANCED_FACE ( 'NONE', ( #182597 ), #39244, .T. ) ;
#236746=CYLINDRICAL_SURFACE ( 'NONE', #175707, 0.09999999999999939493 ) ;
#236758=CIRCLE ( 'NONE', #124358, 0.1000000000000028644 ) ;
#236774=ORIENTED_EDGE ( 'NONE', *, *, #109462, .F. ) ;
#236837=ORIENTED_EDGE ( 'NONE', *, *, #251367, .T. ) ;
#236842=EDGE_CURVE ( 'NONE', #182384, #46212, #197691, .T. ) ;
#236867=CIRCLE ( 'NONE', #86826, 0.1000000000000021289 ) ;
#236880=ORIENTED_EDGE ( 'NONE', *, *, #27090, .F. ) ;
#236906=CARTESIAN_POINT ( 'NONE',  ( -21.05000000000000071, 74.25000000001186606, -91.35359592662267403 ) ) ;
#236981=DIRECTION ( 'NONE',  ( -1.000000000000000000, -0.000000000000000000, -0.000000000000000000 ) ) ;
#236986=AXIS2_PLACEMENT_3D ( 'NONE', #9020, #49429, #51977 ) ;
#236990=EDGE_CURVE ( 'NONE', #216113, #171759, #181162, .T. ) ;
#237057=AXIS2_PLACEMENT_3D ( 'NONE', #187823, #10456, #9166 ) ;
#237061=VERTEX_POINT ( 'NONE', #132886 ) ;
#237065=CIRCLE ( 'NONE', #203745, 0.3999999999999975797 ) ;
#237089=DIRECTION ( 'NONE',  ( -0.000000000000000000, 1.000000000000000000, 7.525063763929033127E-15 ) ) ;
#237094=EDGE_CURVE ( 'NONE', #96528, #35640, #89734, .T. ) ;
#237145=DIRECTION ( 'NONE',  ( 1.000000000000000000, 0.000000000000000000, 0.000000000000000000 ) ) ;
#237151=AXIS2_PLACEMENT_3D ( 'NONE', #235883, #177237, #218881 ) ;
#237156=CARTESIAN_POINT ( 'NONE',  ( -18.59999999999999787, 77.25000000001189449, -95.02310748452430289 ) ) ;
#237159=CARTESIAN_POINT ( 'NONE',  ( -18.50000000000000000, 66.65000000001187175, -90.67310748452437963 ) ) ;
#237161=ORIENTED_EDGE ( 'NONE', *, *, #254398, .F. ) ;
#237206=DIRECTION ( 'NONE',  ( 0.000000000000000000, -7.109473446599835262E-15, 1.000000000000000000 ) ) ;
#237209=AXIS2_PLACEMENT_3D ( 'NONE', #219968, #243379, #180855 ) ;
#237214=CARTESIAN_POINT ( 'NONE',  ( -18.59999999999999787, 85.52395432076444592, -62.64109042769693048 ) ) ;
#237242=CARTESIAN_POINT ( 'NONE',  ( -20.07928932188135107, 66.77928932189314537, -81.77310748452437394 ) ) ;
#237292=CARTESIAN_POINT ( 'NONE',  ( -18.50000000000001066, 85.42130820975087602, -95.78074427047334893 ) ) ;
#237324=CARTESIAN_POINT ( 'NONE',  ( 21.05000000000000071, 71.00000000001186606, -90.61784146561124942 ) ) ;
#237341=DIRECTION ( 'NONE',  ( -1.000000000000000000, 0.000000000000000000, 0.000000000000000000 ) ) ;
#237342=VECTOR ( 'NONE', #75262, 1000.000000000000000 ) ;
#237361=DIRECTION ( 'NONE',  ( 0.000000000000000000, -6.982962677686266711E-15, 1.000000000000000000 ) ) ;
#237377=ORIENTED_EDGE ( 'NONE', *, *, #152471, .T. ) ;
#237388=LINE ( 'NONE', #99132, #4774 ) ;
#237419=DIRECTION ( 'NONE',  ( 0.000000000000000000, -0.4999999999999689138, -0.8660254037844565822 ) ) ;
#237421=VERTEX_POINT ( 'NONE', #63594 ) ;
#237438=CARTESIAN_POINT ( 'NONE',  ( 22.24259225415828567, 75.90093411655917066, -110.5150453550897254 ) ) ;
#237484=CARTESIAN_POINT ( 'NONE',  ( 20.94999999999999929, 77.83534155023627932, -91.46795619196132066 ) ) ;
#237493=ADVANCED_FACE ( 'NONE', ( #253770 ), #51706, .T. ) ;
#237495=CIRCLE ( 'NONE', #12653, 12.97499999999999964 ) ;
#237521=ORIENTED_EDGE ( 'NONE', *, *, #150235, .T. ) ;
#237534=ORIENTED_EDGE ( 'NONE', *, *, #154673, .F. ) ;
#237542=ORIENTED_EDGE ( 'NONE', *, *, #120368, .F. ) ;
#237545=CARTESIAN_POINT ( 'NONE',  ( 22.39999999999999858, 68.20922040163857503, -103.1231074845243540 ) ) ;
#237576=ORIENTED_EDGE ( 'NONE', *, *, #89868, .T. ) ;
#237595=EDGE_CURVE ( 'NONE', #154058, #22444, #10824, .T. ) ;
#237613=CIRCLE ( 'NONE', #95934, 0.5000000000000004441 ) ;
#237615=AXIS2_PLACEMENT_3D ( 'NONE', #65660, #228609, #245596 ) ;
#237616=DIRECTION ( 'NONE',  ( 0.000000000000000000, 0.000000000000000000, 1.000000000000000000 ) ) ;
#237620=CARTESIAN_POINT ( 'NONE',  ( 21.05000000000000071, 85.40000000001178648, -79.41707660717668205 ) ) ;
#237625=AXIS2_PLACEMENT_3D ( 'NONE', #151702, #192097, #228657 ) ;
#237676=ORIENTED_EDGE ( 'NONE', *, *, #241836, .T. ) ;
#237692=AXIS2_PLACEMENT_3D ( 'NONE', #79215, #80479, #101309 ) ;
#237701=CARTESIAN_POINT ( 'NONE',  ( 23.15000000000000213, 87.48912529308779540, -72.62310748452422615 ) ) ;
#237708=ORIENTED_EDGE ( 'NONE', *, *, #252701, .F. ) ;
#237711=CARTESIAN_POINT ( 'NONE',  ( 22.49999999999999645, 64.35023708198002623, -103.1119174609113145 ) ) ;
#237712=DIRECTION ( 'NONE',  ( 0.000000000000000000, -0.9274965247785555977, 0.3738317757009190223 ) ) ;
#237723=EDGE_CURVE ( 'NONE', #7823, #134789, #40994, .T. ) ;
#237741=ORIENTED_EDGE ( 'NONE', *, *, #99690, .F. ) ;
#237752=CIRCLE ( 'NONE', #183590, 0.1000000000000028644 ) ;
#237766=DIRECTION ( 'NONE',  ( -0.000000000000000000, 0.7397360091702708251, 0.6728971962616883129 ) ) ;
#237767=ORIENTED_EDGE ( 'NONE', *, *, #35913, .T. ) ;
#237782=VERTEX_POINT ( 'NONE', #250903 ) ;
#237789=DIRECTION ( 'NONE',  ( -0.000000000000000000, 1.000000000000000000, 6.982962677686266711E-15 ) ) ;
#237802=FACE_OUTER_BOUND ( 'NONE', #16037, .T. ) ;
#237824=ORIENTED_EDGE ( 'NONE', *, *, #41725, .T. ) ;
#237868=VERTEX_POINT ( 'NONE', #185367 ) ;
#237875=FACE_OUTER_BOUND ( 'NONE', #117282, .T. ) ;
#237877=DIRECTION ( 'NONE',  ( 0.000000000000000000, 1.000000000000000000, 7.272083257015735086E-15 ) ) ;
#237891=CARTESIAN_POINT ( 'NONE',  ( -22.47071067811865319, 75.90090754530939421, -110.7431822290223806 ) ) ;
#237905=CARTESIAN_POINT ( 'NONE',  ( 20.94999999999999929, 77.83534155023627932, -91.46795619196132066 ) ) ;
#237924=VERTEX_POINT ( 'NONE', #204917 ) ;
#237941=CARTESIAN_POINT ( 'NONE',  ( -22.39999999999999858, 76.00000000001200817, -110.8138870828977218 ) ) ;
#237952=CARTESIAN_POINT ( 'NONE',  ( -20.94999999999999929, 64.30000000001176375, -76.27810563404301547 ) ) ;
#237967=DIRECTION ( 'NONE',  ( 0.000000000000000000, 0.8777080977375072424, -0.4791956752371691608 ) ) ;
#237977=EDGE_LOOP ( 'NONE', ( #205000, #85672, #152848, #205255 ) ) ;
#238040=CARTESIAN_POINT ( 'NONE',  ( 23.14999999999999503, 64.35000000001176090, -76.53791325517833855 ) ) ;
#238043=CIRCLE ( 'NONE', #208838, 0.1000000000000028644 ) ;
#238047=VECTOR ( 'NONE', #235935, 1000.000000000000000 ) ;
#238065=DIRECTION ( 'NONE',  ( 0.000000000000000000, -6.853228547068871147E-15, 1.000000000000000000 ) ) ;
#238071=DIRECTION ( 'NONE',  ( 0.000000000000000000, -1.000000000000000000, -8.717686153663073805E-15 ) ) ;
#238162=ADVANCED_FACE ( 'NONE', ( #180510 ), #129312, .F. ) ;
#238166=CARTESIAN_POINT ( 'NONE',  ( -22.50000000000000000, 64.25000000001195133, -103.0231074845244024 ) ) ;
#238171=AXIS2_PLACEMENT_3D ( 'NONE', #92496, #72977, #149933 ) ;
#238184=CARTESIAN_POINT ( 'NONE',  ( -21.05000000000000071, 87.48912529308779540, -72.42310748452423752 ) ) ;
#238188=AXIS2_PLACEMENT_3D ( 'NONE', #204875, #165790, #127932 ) ;
#238219=DIRECTION ( 'NONE',  ( 1.000000000000000000, 0.000000000000000000, 0.000000000000000000 ) ) ;
#238221=DIRECTION ( 'NONE',  ( 0.000000000000000000, -7.116814260417668513E-15, 1.000000000000000000 ) ) ;
#238238=ORIENTED_EDGE ( 'NONE', *, *, #182641, .T. ) ;
#238250=CARTESIAN_POINT ( 'NONE',  ( -20.64999999999999858, 85.40000000001188596, -93.12913836187179584 ) ) ;
#238286=CARTESIAN_POINT ( 'NONE',  ( -18.59999999999999787, 74.16465844978745281, -91.36795619196134055 ) ) ;
#238316=ORIENTED_EDGE ( 'NONE', *, *, #140784, .F. ) ;
#238369=DIRECTION ( 'NONE',  ( 0.000000000000000000, 6.982962677686266711E-15, -1.000000000000000000 ) ) ;
#238380=VECTOR ( 'NONE', #95540, 1000.000000000000000 ) ;
#238399=AXIS2_PLACEMENT_3D ( 'NONE', #67255, #248467, #205472 ) ;
#238417=FACE_OUTER_BOUND ( 'NONE', #73012, .T. ) ;
#238429=ORIENTED_EDGE ( 'NONE', *, *, #198986, .F. ) ;
#238446=DIRECTION ( 'NONE',  ( 0.000000000000000000, 0.000000000000000000, -1.000000000000000000 ) ) ;
#238540=DIRECTION ( 'NONE',  ( -7.304098846218134667E-16, -1.000000000000000000, -6.982962677686267499E-15 ) ) ;
#238560=DIRECTION ( 'NONE',  ( 0.000000000000000000, 0.000000000000000000, -1.000000000000000000 ) ) ;
#238563=CARTESIAN_POINT ( 'NONE',  ( -18.60000000000000142, 85.32100840337318459, -95.78716923544635620 ) ) ;
#238576=TOROIDAL_SURFACE ( 'NONE', #167871, 7.800000000000000711, 0.1000000000000000056 ) ;
#238590=ORIENTED_EDGE ( 'NONE', *, *, #23549, .F. ) ;
#238591=ORIENTED_EDGE ( 'NONE', *, *, #194030, .F. ) ;
#238624=EDGE_CURVE ( 'NONE', #242308, #5184, #141076, .T. ) ;
#238630=LINE ( 'NONE', #2567, #140707 ) ;
#238694=EDGE_CURVE ( 'NONE', #160189, #213743, #81109, .T. ) ;
#238725=EDGE_LOOP ( 'NONE', ( #239188, #36789, #97474 ) ) ;
#238742=CARTESIAN_POINT ( 'NONE',  ( 21.14999999999999858, 76.10000000001203091, -114.6726782920691079 ) ) ;
#238825=ORIENTED_EDGE ( 'NONE', *, *, #226984, .F. ) ;
#238836=DIRECTION ( 'NONE',  ( 0.000000000000000000, 0.1298341882519953583, 0.9915357197604861561 ) ) ;
#238866=ORIENTED_EDGE ( 'NONE', *, *, #238624, .T. ) ;
#238870=DIRECTION ( 'NONE',  ( 1.000000000000000000, -0.000000000000000000, 0.000000000000000000 ) ) ;
#238872=CIRCLE ( 'NONE', #26498, 0.1000000000000028644 ) ;
#238896=FACE_OUTER_BOUND ( 'NONE', #103961, .T. ) ;
#238920=CARTESIAN_POINT ( 'NONE',  ( -20.85000000000000142, 87.75000000001172396, -69.52310748452423184 ) ) ;
#238983=EDGE_CURVE ( 'NONE', #226125, #196796, #24046, .T. ) ;
#238985=CIRCLE ( 'NONE', #150927, 0.09999999999999520384 ) ;
#239008=CARTESIAN_POINT ( 'NONE',  ( -18.33682934331525161, 85.51118559110511796, -62.61745271585106565 ) ) ;
#239019=EDGE_CURVE ( 'NONE', #252190, #239900, #57322, .T. ) ;
#239039=ADVANCED_FACE ( 'NONE', ( #161637 ), #140528, .T. ) ;
#239134=DIRECTION ( 'NONE',  ( -0.9880948137434723000, -0.1538461538461483591, -1.074301950413233512E-15 ) ) ;
#239136=EDGE_CURVE ( 'NONE', #160189, #229726, #68459, .T. ) ;
#239174=DIRECTION ( 'NONE',  ( -1.836970198721029934E-16, -1.000000000000000000, -6.982962677686266711E-15 ) ) ;
#239188=ORIENTED_EDGE ( 'NONE', *, *, #142649, .F. ) ;
#239194=AXIS2_PLACEMENT_3D ( 'NONE', #85690, #218811, #179715 ) ;
#239201=ORIENTED_EDGE ( 'NONE', *, *, #201735, .F. ) ;
#239208=ORIENTED_EDGE ( 'NONE', *, *, #58431, .F. ) ;
#239265=DIRECTION ( 'NONE',  ( 0.000000000000000000, 0.000000000000000000, 1.000000000000000000 ) ) ;
#239276=LINE ( 'NONE', #141447, #97405 ) ;
#239282=VECTOR ( 'NONE', #53934, 1000.000000000000000 ) ;
#239300=ORIENTED_EDGE ( 'NONE', *, *, #167423, .T. ) ;
#239310=CARTESIAN_POINT ( 'NONE',  ( -22.49231231312463208, 64.35001509633467265, -103.0841603721257513 ) ) ;
#239334=VERTEX_POINT ( 'NONE', #19224 ) ;
#239339=DIRECTION ( 'NONE',  ( 1.000000000000000000, 0.000000000000000000, 0.000000000000000000 ) ) ;
#239345=EDGE_CURVE ( 'NONE', #103624, #162117, #90134, .T. ) ;
#239350=DIRECTION ( 'NONE',  ( 0.000000000000000000, 0.000000000000000000, 1.000000000000000000 ) ) ;
#239353=CARTESIAN_POINT ( 'NONE',  ( 20.94999999999999929, 76.00000000001172396, -71.52310748452431710 ) ) ;
#239375=DIRECTION ( 'NONE',  ( -1.000000000000000000, 1.836970198721029934E-16, 1.601412966608202925E-30 ) ) ;
#239383=CIRCLE ( 'NONE', #156207, 0.1000000000000028644 ) ;
#239386=VECTOR ( 'NONE', #82421, 1000.000000000000000 ) ;
#239418=AXIS2_PLACEMENT_3D ( 'NONE', #208485, #29855, #36267 ) ;
#239422=LINE ( 'NONE', #213420, #69903 ) ;
#239427=VERTEX_POINT ( 'NONE', #212954 ) ;
#239430=CARTESIAN_POINT ( 'NONE',  ( -21.10320863425827298, 75.97497774878489452, -109.4233848709835542 ) ) ;
#239443=ORIENTED_EDGE ( 'NONE', *, *, #154282, .T. ) ;
#239457=DIRECTION ( 'NONE',  ( 0.000000000000000000, -6.769652589177795712E-15, 1.000000000000000000 ) ) ;
#239497=AXIS2_PLACEMENT_3D ( 'NONE', #173333, #130290, #48189 ) ;
#239514=ADVANCED_FACE ( 'NONE', ( #91720 ), #232543, .T. ) ;
#239550=AXIS2_PLACEMENT_3D ( 'NONE', #252198, #193538, #174010 ) ;
#239555=ORIENTED_EDGE ( 'NONE', *, *, #195745, .T. ) ;
#239574=DIRECTION ( 'NONE',  ( -1.000000000000000000, 0.000000000000000000, -0.000000000000000000 ) ) ;
#239635=DIRECTION ( 'NONE',  ( -1.000000000000000000, 0.000000000000000000, 0.000000000000000000 ) ) ;
#239645=FACE_OUTER_BOUND ( 'NONE', #44780, .T. ) ;
#239647=TOROIDAL_SURFACE ( 'NONE', #43830, 0.2000000000000000111, 0.1000000000000000056 ) ;
#239649=DIRECTION ( 'NONE',  ( 0.000000000000000000, 1.000000000000000000, 0.000000000000000000 ) ) ;
#239662=FACE_OUTER_BOUND ( 'NONE', #240115, .T. ) ;
#239675=ORIENTED_EDGE ( 'NONE', *, *, #111053, .T. ) ;
#239688=ORIENTED_EDGE ( 'NONE', *, *, #170055, .T. ) ;
#239693=TOROIDAL_SURFACE ( 'NONE', #61193, 4.149999999999999467, 0.1000000000000000056 ) ;
#239707=CARTESIAN_POINT ( 'NONE',  ( 21.05000000000000071, 65.51540711881665402, -95.56639391393910898 ) ) ;
#239725=ORIENTED_EDGE ( 'NONE', *, *, #77821, .T. ) ;
#239733=DIRECTION ( 'NONE',  ( 0.000000000000000000, -1.000000000000000000, -6.982962677686265922E-15 ) ) ;
#239742=DIRECTION ( 'NONE',  ( 0.000000000000000000, 7.026728003956683390E-15, -1.000000000000000000 ) ) ;
#239795=DIRECTION ( 'NONE',  ( 1.000000000000000000, 0.000000000000000000, 0.000000000000000000 ) ) ;
#239821=EDGE_CURVE ( 'NONE', #9918, #81803, #78550, .T. ) ;
#239837=AXIS2_PLACEMENT_3D ( 'NONE', #151139, #70343, #53314 ) ;
#239857=DIRECTION ( 'NONE',  ( 0.000000000000000000, 0.000000000000000000, 1.000000000000000000 ) ) ;
#239900=VERTEX_POINT ( 'NONE', #70597 ) ;
#239921=CARTESIAN_POINT ( 'NONE',  ( 18.59999999999999432, 77.16270174994990327, -94.92310748452430857 ) ) ;
#239931=DIRECTION ( 'NONE',  ( 1.000000000000000000, 0.000000000000000000, 0.000000000000000000 ) ) ;
#239957=DIRECTION ( 'NONE',  ( -1.000000000000000000, 0.000000000000000000, 0.000000000000000000 ) ) ;
#239987=DIRECTION ( 'NONE',  ( 0.000000000000000000, 7.086529944415894657E-15, -1.000000000000000000 ) ) ;
#239998=CARTESIAN_POINT ( 'NONE',  ( 22.45463910399147522, 76.00000000001291767, -114.6726782947074383 ) ) ;
#240036=AXIS2_PLACEMENT_3D ( 'NONE', #165033, #145456, #144163 ) ;
#240040=CARTESIAN_POINT ( 'NONE',  ( 18.46921299892755997, 85.50937817783569983, -96.03652877515386876 ) ) ;
#240077=DIRECTION ( 'NONE',  ( 1.000000000000000000, 0.000000000000000000, 0.000000000000000000 ) ) ;
#240105=FILL_AREA_STYLE ('',( #200968 ) ) ;
#240115=EDGE_LOOP ( 'NONE', ( #81361, #157089, #32005, #211086 ) ) ;
#240162=AXIS2_PLACEMENT_3D ( 'NONE', #100829, #37085, #1760 ) ;
#240180=ORIENTED_EDGE ( 'NONE', *, *, #152785, .T. ) ;
#240183=CARTESIAN_POINT ( 'NONE',  ( -21.12642695952773764, 69.62434007797678248, -103.1220107677137179 ) ) ;
#240191=DIRECTION ( 'NONE',  ( 1.000000000000000000, 0.000000000000000000, 0.000000000000000000 ) ) ;
#240202=DIRECTION ( 'NONE',  ( 0.000000000000000000, -6.982962677686266711E-15, 1.000000000000000000 ) ) ;
#240227=CARTESIAN_POINT ( 'NONE',  ( 20.85000000000000142, 77.16412189325286874, -61.60825939895269698 ) ) ;
#240239=ORIENTED_EDGE ( 'NONE', *, *, #82692, .F. ) ;
#240252=DIRECTION ( 'NONE',  ( -0.000000000000000000, 1.000000000000000000, 7.272083257015735086E-15 ) ) ;
#240297=CARTESIAN_POINT ( 'NONE',  ( -18.40904629823846861, 85.50000000001168132, -62.92291792204296286 ) ) ;
#240368=ORIENTED_EDGE ( 'NONE', *, *, #139781, .F. ) ;
#240371=VERTEX_POINT ( 'NONE', #36282 ) ;
#240484=ORIENTED_EDGE ( 'NONE', *, *, #138006, .F. ) ;
#240488=CARTESIAN_POINT ( 'NONE',  ( 21.14999999999999858, 64.35000000001195986, -102.9231074845243938 ) ) ;
#240497=DIRECTION ( 'NONE',  ( 0.000000000000000000, -7.487053152578127080E-15, 1.000000000000000000 ) ) ;
#240534=CYLINDRICAL_SURFACE ( 'NONE', #46566, 0.1000000000000028644 ) ;
#240538=ADVANCED_FACE ( 'NONE', ( #60943 ), #70000, .T. ) ;
#240553=CARTESIAN_POINT ( 'NONE',  ( -18.59999999999999787, 69.15387683765909799, -65.78538121767449809 ) ) ;
#240605=( BOUNDED_SURFACE ( )  B_SPLINE_SURFACE ( 3, 2, ( 
 ( #30192, #189253, #31487 ),
 ( #110993, #165849, #171018 ),
 ( #146252, #185394, #250490 ),
 ( #71880, #151420, #230964 ),
 ( #52278, #131834, #245379 ),
 ( #54847, #116139, #17042 ) ),
 .UNSPECIFIED., .F., .F., .F. ) 
 B_SPLINE_SURFACE_WITH_KNOTS ( ( 4, 2, 4 ),
 ( 3, 3 ),
 ( 3.141592653589783346, 3.926990816987233845, 4.712388980384684345 ),
 ( 0.000000000000000000, 1.000000000000000000 ),
 .UNSPECIFIED. ) 
 GEOMETRIC_REPRESENTATION_ITEM ( )  RATIONAL_B_SPLINE_SURFACE ( (
 ( 1.000000000000000000, 0.9238795325112774126, 1.000000000000000000),
 ( 1.000000000000000000, 0.9240297172247110558, 1.000000000000000000),
 ( 1.000000000000000000, 0.9038128468034775098, 1.000000000000000000),
 ( 1.000000000000000000, 0.8282379607654114517, 1.000000000000000000),
 ( 1.000000000000000000, 0.7727932973487930957, 1.000000000000000000),
 ( 1.000000000000000000, 0.7071067811865352493, 1.000000000000000000) ) ) 
 REPRESENTATION_ITEM ( '' )  SURFACE ( )  );
#240607=ORIENTED_EDGE ( 'NONE', *, *, #217599, .F. ) ;
#240651=ORIENTED_EDGE ( 'NONE', *, *, #104557, .T. ) ;
#240661=CIRCLE ( 'NONE', #48934, 0.1000000000000028644 ) ;
#240683=AXIS2_PLACEMENT_3D ( 'NONE', #6243, #181068, #121108 ) ;
#240700=EDGE_LOOP ( 'NONE', ( #43768, #90442, #209606, #43146 ) ) ;
#240718=CARTESIAN_POINT ( 'NONE',  ( -23.25000000000000000, 85.68240343348806221, -62.86626410711144786 ) ) ;
#240727=EDGE_LOOP ( 'NONE', ( #103035, #854, #217640, #58186 ) ) ;
#240741=EDGE_CURVE ( 'NONE', #24156, #21614, #153376, .T. ) ;
#240743=ORIENTED_EDGE ( 'NONE', *, *, #77821, .F. ) ;
#240758=ORIENTED_EDGE ( 'NONE', *, *, #219431, .T. ) ;
#240770=CARTESIAN_POINT ( 'NONE',  ( 22.14074124539698829, 68.60992214896820940, -103.1221603803684417 ) ) ;
#240779=AXIS2_PLACEMENT_3D ( 'NONE', #181253, #161692, #15 ) ;
#240780=DIRECTION ( 'NONE',  ( -1.000000000000000000, -9.012599976027990443E-15, -6.882867235861669241E-14 ) ) ;
#240815=CYLINDRICAL_SURFACE ( 'NONE', #195969, 0.1000000000000028644 ) ;
#240825=CARTESIAN_POINT ( 'NONE',  ( 20.94999999999999574, 74.73821383144687047, -94.93660852097883662 ) ) ;
#240847=CARTESIAN_POINT ( 'NONE',  ( -20.94999999999999929, 77.83534155023627932, -91.46795619196130644 ) ) ;
#240849=CARTESIAN_POINT ( 'NONE',  ( 22.47071067811865319, 76.00000000001195133, -103.0231074845243171 ) ) ;
#240859=DIRECTION ( 'NONE',  ( 0.000000000000000000, 0.000000000000000000, 1.000000000000000000 ) ) ;
#240867=SPHERICAL_SURFACE ( 'NONE', #39019, 0.1000000000000000056 ) ;
#240893=ORIENTED_EDGE ( 'NONE', *, *, #107567, .F. ) ;
#240968=CARTESIAN_POINT ( 'NONE',  ( 21.05000000000000071, 77.36087058720393372, -94.95010955743333625 ) ) ;
#240979=DIRECTION ( 'NONE',  ( -1.000000000000000000, 0.000000000000000000, -0.000000000000000000 ) ) ;
#240988=CARTESIAN_POINT ( 'NONE',  ( 20.95262331984812221, 65.49584273722207683, -95.46221915493103438 ) ) ;
#241017=DIRECTION ( 'NONE',  ( 0.000000000000000000, 0.000000000000000000, 1.000000000000000000 ) ) ;
#241043=CARTESIAN_POINT ( 'NONE',  ( -20.64999999999999858, 84.66355140188093742, -79.04720860259155302 ) ) ;
#241047=AXIS2_PLACEMENT_3D ( 'NONE', #130436, #146144, #10508 ) ;
#241060=ORIENTED_EDGE ( 'NONE', *, *, #11089, .F. ) ;
#241073=ORIENTED_EDGE ( 'NONE', *, *, #123838, .F. ) ;
#241085=CARTESIAN_POINT ( 'NONE',  ( -23.25000000000000000, 87.75000000001173817, -72.62310748452422615 ) ) ;
#241111=DIRECTION ( 'NONE',  ( -0.000000000000000000, -6.982962677686266711E-15, 1.000000000000000000 ) ) ;
#241113=CARTESIAN_POINT ( 'NONE',  ( -23.15000000000000213, 76.00000000001170974, -69.52310748452431710 ) ) ;
#241145=DIRECTION ( 'NONE',  ( 0.000000000000000000, 0.000000000000000000, -1.000000000000000000 ) ) ;
#241150=CARTESIAN_POINT ( 'NONE',  ( 21.05000000000000071, 65.27628289530434813, -90.87310748452438247 ) ) ;
#241153=DIRECTION ( 'NONE',  ( 0.000000000000000000, -6.982962677686266711E-15, 1.000000000000000000 ) ) ;
#241157=CARTESIAN_POINT ( 'NONE',  ( -18.59999999999999787, 77.16412189325286874, -61.60825939895269698 ) ) ;
#241186=DIRECTION ( 'NONE',  ( 1.000000000000000000, 0.000000000000000000, 0.000000000000000000 ) ) ;
#241201=EDGE_LOOP ( 'NONE', ( #224252, #113654, #3039, #189070, #109419, #186056 ) ) ;
#241208=LINE ( 'NONE', #101642, #170922 ) ;
#241233=ORIENTED_EDGE ( 'NONE', *, *, #243441, .T. ) ;
#241245=CYLINDRICAL_SURFACE ( 'NONE', #156429, 7.900000000000003908 ) ;
#241255=CARTESIAN_POINT ( 'NONE',  ( 20.94999999999999929, 74.16465844978745281, -91.46795619196133487 ) ) ;
#241257=CARTESIAN_POINT ( 'NONE',  ( 23.14999999999999503, 69.45000000001181206, -81.87310748452435405 ) ) ;
#241270=ORIENTED_EDGE ( 'NONE', *, *, #205993, .T. ) ;
#241279=EDGE_LOOP ( 'NONE', ( #131442, #121644, #21934, #148827 ) ) ;
#241321=ORIENTED_EDGE ( 'NONE', *, *, #246893, .F. ) ;
#241390=ADVANCED_FACE ( 'NONE', ( #207261 ), #186411, .F. ) ;
#241394=( NAMED_UNIT ( * ) SI_UNIT ( $, .STERADIAN. ) SOLID_ANGLE_UNIT ( ) );
#241399=AXIS2_PLACEMENT_3D ( 'NONE', #209767, #11582, #212350 ) ;
#241403=CARTESIAN_POINT ( 'NONE',  ( -21.14999999999999858, 64.25000000001195133, -103.0231074845244024 ) ) ;
#241437=CARTESIAN_POINT ( 'NONE',  ( -22.47007471830799119, 76.00000000001200817, -110.7438181364507983 ) ) ;
#241447=CARTESIAN_POINT ( 'NONE',  ( 23.24999999999999645, 78.10000000001171827, -69.52310748452430289 ) ) ;
#241460=CARTESIAN_POINT ( 'NONE',  ( -21.59780538579341069, 69.15290947006869260, -103.1220861541223428 ) ) ;
#241462=FACE_OUTER_BOUND ( 'NONE', #243809, .T. ) ;
#241492=ADVANCED_FACE ( 'NONE', ( #7767 ), #11928, .F. ) ;
#241511=FACE_OUTER_BOUND ( 'NONE', #210070, .T. ) ;
#241560=DIRECTION ( 'NONE',  ( -1.000000000000000000, 0.000000000000000000, 0.000000000000000000 ) ) ;
#241571=DIRECTION ( 'NONE',  ( 0.000000000000000000, 0.000000000000000000, 1.000000000000000000 ) ) ;
#241577=VECTOR ( 'NONE', #241186, 1000.000000000000000 ) ;
#241624=CARTESIAN_POINT ( 'NONE',  ( 20.94999999999999929, 77.16412189325286874, -61.60825939895269698 ) ) ;
#241631=EDGE_CURVE ( 'NONE', #131489, #233299, #161949, .T. ) ;
#241653=DIRECTION ( 'NONE',  ( -1.000000000000000000, 0.000000000000000000, 0.000000000000000000 ) ) ;
#241666=AXIS2_PLACEMENT_3D ( 'NONE', #82307, #161904, #62781 ) ;
#241699=DIRECTION ( 'NONE',  ( 0.000000000000000000, 6.997203936713167125E-15, -1.000000000000000000 ) ) ;
#241711=EDGE_LOOP ( 'NONE', ( #180973, #11642, #177597, #73058, #220681 ) ) ;
#241722=ORIENTED_EDGE ( 'NONE', *, *, #58431, .T. ) ;
#241752=CARTESIAN_POINT ( 'NONE',  ( 21.05000000000000071, 67.22371711014413620, -90.84689234345620434 ) ) ;
#241778=DIRECTION ( 'NONE',  ( 1.000000000000000000, -2.952720810173289112E-16, -2.061873921506763405E-30 ) ) ;
#241800=EDGE_CURVE ( 'NONE', #17324, #152778, #89124, .T. ) ;
#241809=ORIENTED_EDGE ( 'NONE', *, *, #158484, .F. ) ;
#241836=EDGE_CURVE ( 'NONE', #218126, #10704, #107941, .T. ) ;
#241852=DIRECTION ( 'NONE',  ( 0.000000000000000000, 6.982962677686266711E-15, -1.000000000000000000 ) ) ;
#241871=CARTESIAN_POINT ( 'NONE',  ( 21.05000000000000071, 71.18691588786226987, -81.46462524104816794 ) ) ;
#241900=AXIS2_PLACEMENT_3D ( 'NONE', #4446, #3152, #82673 ) ;
#241922=AXIS2_PLACEMENT_3D ( 'NONE', #70823, #29146, #111206 ) ;
#241972=EDGE_CURVE ( 'NONE', #31606, #111418, #178978, .T. ) ;
#241980=ORIENTED_EDGE ( 'NONE', *, *, #199612, .F. ) ;
#241993=VECTOR ( 'NONE', #122301, 1000.000000000000000 ) ;
#241998=CARTESIAN_POINT ( 'NONE',  ( -23.15000000000000213, 87.75000000001202238, -114.7731074845242318 ) ) ;
#242014=VERTEX_POINT ( 'NONE', #78539 ) ;
#242019=DIRECTION ( 'NONE',  ( -1.000000000000000000, 0.000000000000000000, -0.000000000000000000 ) ) ;
#242050=VERTEX_POINT ( 'NONE', #56401 ) ;
#242057=ORIENTED_EDGE ( 'NONE', *, *, #127501, .F. ) ;
#242101=VECTOR ( 'NONE', #27040, 1000.000000000000000 ) ;
#242112=CARTESIAN_POINT ( 'NONE',  ( 18.52928932188133970, 65.72071067813043044, -78.37310748452438247 ) ) ;
#242123=CYLINDRICAL_SURFACE ( 'NONE', #128676, 0.1000000000000028644 ) ;
#242130=AXIS2_PLACEMENT_3D ( 'NONE', #35064, #154997, #177128 ) ;
#242151=DIRECTION ( 'NONE',  ( 0.000000000000000000, 0.000000000000000000, 1.000000000000000000 ) ) ;
#242158=CARTESIAN_POINT ( 'NONE',  ( -23.15000000000000213, 76.00000000001170974, -69.52310748452431710 ) ) ;
#242185=DIRECTION ( 'NONE',  ( -3.265361837132813093E-16, -1.000000000000000000, 7.445645354460596589E-46 ) ) ;
#242206=ORIENTED_EDGE ( 'NONE', *, *, #50092, .T. ) ;
#242233=CIRCLE ( 'NONE', #13307, 0.1000000000000028644 ) ;
#242237=AXIS2_PLACEMENT_3D ( 'NONE', #228946, #131115, #69888 ) ;
#242271=DIRECTION ( 'NONE',  ( 0.000000000000000000, 0.9908441862701605762, -0.1350103645451835310 ) ) ;
#242289=DIRECTION ( 'NONE',  ( 0.000000000000000000, 0.6728971962616412394, -0.7397360091703134577 ) ) ;
#242308=VERTEX_POINT ( 'NONE', #213900 ) ;
#242339=CARTESIAN_POINT ( 'NONE',  ( 23.14999999999999858, 64.35000000001176090, -76.53791325517833855 ) ) ;
#242392=DIRECTION ( 'NONE',  ( -0.000000000000000000, 6.982962677686266711E-15, -1.000000000000000000 ) ) ;
#242417=DIRECTION ( 'NONE',  ( 0.000000000000000000, -6.938893903907222067E-15, 1.000000000000000000 ) ) ;
#242426=DIRECTION ( 'NONE',  ( 0.000000000000000000, -1.000000000000000000, -6.982962677686265922E-15 ) ) ;
#242435=CARTESIAN_POINT ( 'NONE',  ( -18.50000000000000000, 68.97833521811159585, -65.88954208262707368 ) ) ;
#242444=EDGE_LOOP ( 'NONE', ( #248868, #174771, #147479, #76688 ) ) ;
#242488=CARTESIAN_POINT ( 'NONE',  ( -20.64999999999999858, 76.00000000001195133, -103.0231074845243171 ) ) ;
#242497=ADVANCED_FACE ( 'NONE', ( #234750 ), #183325, .F. ) ;
#242512=EDGE_CURVE ( 'NONE', #239334, #61048, #203331, .T. ) ;
#242519=DIRECTION ( 'NONE',  ( 0.000000000000000000, -0.9875055080513754913, 0.1575844902526733482 ) ) ;
#242531=CARTESIAN_POINT ( 'NONE',  ( -18.50000000000000000, 85.40000000001167280, -62.60844914155458696 ) ) ;
#242549=ORIENTED_EDGE ( 'NONE', *, *, #169552, .T. ) ;
#242563=EDGE_CURVE ( 'NONE', #201392, #192753, #108325, .T. ) ;
#242583=VECTOR ( 'NONE', #167592, 1000.000000000000000 ) ;
#242612=DIRECTION ( 'NONE',  ( 1.000000000000000000, 0.000000000000000000, 0.000000000000000000 ) ) ;
#242628=CARTESIAN_POINT ( 'NONE',  ( 20.95000000000000284, 64.40000000001175806, -76.45131071479988805 ) ) ;
#242634=ADVANCED_FACE ( 'NONE', ( #152366 ), #71544, .F. ) ;
#242641=ORIENTED_EDGE ( 'NONE', *, *, #47843, .F. ) ;
#242645=LINE ( 'NONE', #64021, #128567 ) ;
#242671=ORIENTED_EDGE ( 'NONE', *, *, #244249, .F. ) ;
#242676=CYLINDRICAL_SURFACE ( 'NONE', #257737, 0.1000000000000064587 ) ;
#242687=EDGE_CURVE ( 'NONE', #82068, #243292, #237495, .T. ) ;
#242700=ORIENTED_EDGE ( 'NONE', *, *, #122832, .F. ) ;
#242781=ORIENTED_EDGE ( 'NONE', *, *, #27279, .F. ) ;
#242796=AXIS2_PLACEMENT_3D ( 'NONE', #114900, #31548, #169776 ) ;
#242805=EDGE_CURVE ( 'NONE', #5347, #37627, #250149, .T. ) ;
#242831=LINE ( 'NONE', #218117, #212091 ) ;
#242832=ORIENTED_EDGE ( 'NONE', *, *, #219682, .T. ) ;
#242838=EDGE_CURVE ( 'NONE', #146605, #256668, #95998, .T. ) ;
#242842=VERTEX_POINT ( 'NONE', #919 ) ;
#242851=DIRECTION ( 'NONE',  ( 0.000000000000000000, -7.304098846218139203E-15, 1.000000000000000000 ) ) ;
#242870=CARTESIAN_POINT ( 'NONE',  ( 18.49999999999999645, 77.86671491006917734, -91.27043223824227880 ) ) ;
#242871=ORIENTED_EDGE ( 'NONE', *, *, #272, .T. ) ;
#242895=EDGE_LOOP ( 'NONE', ( #106215, #237521, #5208 ) ) ;
#242912=CARTESIAN_POINT ( 'NONE',  ( -21.14999999999999858, 64.35000000001195986, -102.9231074845243938 ) ) ;
#242955=ORIENTED_EDGE ( 'NONE', *, *, #245356, .F. ) ;
#242963=DIRECTION ( 'NONE',  ( 1.000000000000000000, 0.000000000000000000, 0.000000000000000000 ) ) ;
#242968=DIRECTION ( 'NONE',  ( -1.000000000000000000, 0.000000000000000000, 0.000000000000000000 ) ) ;
#242978=FILL_AREA_STYLE ('',( #224694 ) ) ;
#243010=EDGE_CURVE ( 'NONE', #221695, #56583, #220004, .T. ) ;
#243016=EDGE_CURVE ( 'NONE', #7336, #71686, #216818, .T. ) ;
#243017=VERTEX_POINT ( 'NONE', #243417 ) ;
#243049=EDGE_CURVE ( 'NONE', #196167, #37642, #100082, .T. ) ;
#243088=EDGE_CURVE ( 'NONE', #140889, #61685, #188575, .T. ) ;
#243108=VECTOR ( 'NONE', #46806, 1000.000000000000000 ) ;
#243117=EDGE_CURVE ( 'NONE', #92109, #153564, #166484, .T. ) ;
#243121=VECTOR ( 'NONE', #90459, 1000.000000000000000 ) ;
#243143=DIRECTION ( 'NONE',  ( 0.000000000000000000, 1.000000000000000000, 6.938893903907222067E-15 ) ) ;
#243147=CIRCLE ( 'NONE', #230889, 4.000000000000003553 ) ;
#243171=FACE_OUTER_BOUND ( 'NONE', #27333, .T. ) ;
#243172=FACE_OUTER_BOUND ( 'NONE', #94151, .T. ) ;
#243192=DIRECTION ( 'NONE',  ( 1.000000000000000000, -7.304098846218134667E-16, -5.100424963727256530E-30 ) ) ;
#243255=CARTESIAN_POINT ( 'NONE',  ( -21.14999999999999858, 76.00000000001200817, -109.5637644362255543 ) ) ;
#243276=AXIS2_PLACEMENT_3D ( 'NONE', #170363, #226408, #47774 ) ;
#243291=EDGE_CURVE ( 'NONE', #80949, #255841, #221085, .T. ) ;
#243292=VERTEX_POINT ( 'NONE', #119324 ) ;
#243320=CARTESIAN_POINT ( 'NONE',  ( 22.50014994444006788, 64.25028026811989434, -103.1061876412436504 ) ) ;
#243331=VERTEX_POINT ( 'NONE', #176740 ) ;
#243359=DIRECTION ( 'NONE',  ( 0.000000000000000000, 0.000000000000000000, -1.000000000000000000 ) ) ;
#243361=FACE_OUTER_BOUND ( 'NONE', #128696, .T. ) ;
#243366=CARTESIAN_POINT ( 'NONE',  ( -21.55000000000000071, 68.65000000001187175, -90.67310748452436542 ) ) ;
#243376=DIRECTION ( 'NONE',  ( 1.000000000000000000, -2.952720810173289112E-16, -2.061873921506763405E-30 ) ) ;
#243379=DIRECTION ( 'NONE',  ( 1.000000000000000000, 0.000000000000000000, -0.000000000000000000 ) ) ;
#243388=ADVANCED_FACE ( 'NONE', ( #80151 ), #83990, .F. ) ;
#243400=ADVANCED_FACE ( 'NONE', ( #184422 ), #219689, .T. ) ;
#243409=CARTESIAN_POINT ( 'NONE',  ( -18.59999999999999787, 66.65000000001187175, -90.67310748452437963 ) ) ;
#243417=CARTESIAN_POINT ( 'NONE',  ( -22.39999999999999858, 64.25000000001195133, -102.9231074845243938 ) ) ;
#243419=DIRECTION ( 'NONE',  ( 0.000000000000000000, -1.000000000000000000, -6.982962677686265922E-15 ) ) ;
#243421=CARTESIAN_POINT ( 'NONE',  ( -21.05000000000000071, 76.00000000001170974, -69.52310748452431710 ) ) ;
#243441=EDGE_CURVE ( 'NONE', #156778, #20503, #127024, .T. ) ;
#243443=DIRECTION ( 'NONE',  ( 1.000000000000000000, 0.000000000000000000, 0.000000000000000000 ) ) ;
#243460=CARTESIAN_POINT ( 'NONE',  ( 21.05000000000000071, 69.74218538953583391, -103.1208977758331571 ) ) ;
#243469=ORIENTED_EDGE ( 'NONE', *, *, #115650, .F. ) ;
#243474=AXIS2_PLACEMENT_3D ( 'NONE', #240553, #118029, #237967 ) ;
#243475=CARTESIAN_POINT ( 'NONE',  ( -20.94999999999999929, 77.25000000001189449, -95.02310748452430289 ) ) ;
#243479=ORIENTED_EDGE ( 'NONE', *, *, #178633, .T. ) ;
#243485=DIRECTION ( 'NONE',  ( 1.000000000000000000, 0.000000000000000000, 0.000000000000000000 ) ) ;
#243487=FACE_OUTER_BOUND ( 'NONE', #40561, .T. ) ;
#243572=EDGE_CURVE ( 'NONE', #120661, #65772, #34073, .T. ) ;
#243582=CARTESIAN_POINT ( 'NONE',  ( 20.04142135623730070, 64.35000000001180354, -81.67310748452439384 ) ) ;
#243614=DIRECTION ( 'NONE',  ( 1.000000000000000000, 0.000000000000000000, 0.000000000000000000 ) ) ;
#243659=DIRECTION ( 'NONE',  ( 0.000000000000000000, -6.982962677686266711E-15, 1.000000000000000000 ) ) ;
#243661=DIRECTION ( 'NONE',  ( -0.7071067811865474617, 0.7071067811865474617, 4.937700262164531476E-15 ) ) ;
#243663=DIRECTION ( 'NONE',  ( -0.000000000000000000, 6.982962677686266711E-15, -1.000000000000000000 ) ) ;
#243711=CARTESIAN_POINT ( 'NONE',  ( -21.05000000000000071, 64.35000000001176090, -76.53791325517833855 ) ) ;
#243715=AXIS2_PLACEMENT_3D ( 'NONE', #26712, #25416, #185758 ) ;
#243716=CARTESIAN_POINT ( 'NONE',  ( 22.50000000000000000, 76.00000000001195133, -103.0231074845243171 ) ) ;
#243743=DIRECTION ( 'NONE',  ( 0.000000000000000000, 1.000000000000000000, 6.938893903907222067E-15 ) ) ;
#243767=DIRECTION ( 'NONE',  ( 0.000000000000000000, 0.000000000000000000, 1.000000000000000000 ) ) ;
#243794=CARTESIAN_POINT ( 'NONE',  ( -22.47007471830798409, 68.27928934808545591, -103.0231074845243597 ) ) ;
#243809=EDGE_LOOP ( 'NONE', ( #181912, #202360, #205274 ) ) ;
#243822=CARTESIAN_POINT ( 'NONE',  ( 19.96984138294275013, 64.25000000001176659, -78.29853541332350630 ) ) ;
#243845=ORIENTED_EDGE ( 'NONE', *, *, #88504, .T. ) ;
#243857=AXIS2_PLACEMENT_3D ( 'NONE', #158565, #95980, #238065 ) ;
#243880=ORIENTED_EDGE ( 'NONE', *, *, #106259, .F. ) ;
#243914=VECTOR ( 'NONE', #104275, 1000.000000000000000 ) ;
#243925=ORIENTED_EDGE ( 'NONE', *, *, #252435, .F. ) ;
#243928=DIRECTION ( 'NONE',  ( -1.000000000000000000, 1.836970198721029934E-16, 1.282749433769087757E-30 ) ) ;
#243931=EDGE_CURVE ( 'NONE', #155591, #92348, #67163, .T. ) ;
#243939=AXIS2_PLACEMENT_3D ( 'NONE', #163511, #98674, #195284 ) ;
#243950=ORIENTED_EDGE ( 'NONE', *, *, #38387, .F. ) ;
#243988=ORIENTED_EDGE ( 'NONE', *, *, #44649, .F. ) ;
#243993=FACE_OUTER_BOUND ( 'NONE', #117943, .T. ) ;
#244048=CIRCLE ( 'NONE', #194194, 12.87499999999999822 ) ;
#244053=CARTESIAN_POINT ( 'NONE',  ( -20.54999999999999716, 74.07476635515205032, -90.29286395139820343 ) ) ;
#244078=AXIS2_PLACEMENT_3D ( 'NONE', #13914, #111723, #93428 ) ;
#244092=LINE ( 'NONE', #184119, #143351 ) ;
#244094=CARTESIAN_POINT ( 'NONE',  ( -20.64999999999999858, 76.00000000001170974, -69.52310748452431710 ) ) ;
#244103=ORIENTED_EDGE ( 'NONE', *, *, #197470, .T. ) ;
#244131=VERTEX_POINT ( 'NONE', #127371 ) ;
#244149=ADVANCED_FACE ( 'NONE', ( #85631 ), #161374, .T. ) ;
#244169=ORIENTED_EDGE ( 'NONE', *, *, #154720, .T. ) ;
#244189=EDGE_CURVE ( 'NONE', #43410, #3957, #107800, .T. ) ;
#244199=CARTESIAN_POINT ( 'NONE',  ( -22.59999999999999787, 76.00000000001195133, -103.0231074845243171 ) ) ;
#244221=ADVANCED_FACE ( 'NONE', ( #112945 ), #52954, .T. ) ;
#244223=AXIS2_PLACEMENT_3D ( 'NONE', #123323, #89307, #69779 ) ;
#244231=CIRCLE ( 'NONE', #86005, 0.09999999999999939493 ) ;
#244249=EDGE_CURVE ( 'NONE', #56290, #196101, #167332, .T. ) ;
#244250=CARTESIAN_POINT ( 'NONE',  ( -20.94999999999999929, 64.40000000001177227, -76.45131071479988805 ) ) ;
#244272=CIRCLE ( 'NONE', #169328, 11.74999999999999645 ) ;
#244274=ADVANCED_FACE ( 'NONE', ( #229046 ), #150782, .T. ) ;
#244293=ORIENTED_EDGE ( 'NONE', *, *, #134961, .F. ) ;
#244299=VECTOR ( 'NONE', #225415, 1000.000000000000000 ) ;
#244395=AXIS2_PLACEMENT_3D ( 'NONE', #152527, #132944, #175935 ) ;
#244418=DIRECTION ( 'NONE',  ( -1.000000000000000000, 0.000000000000000000, -0.000000000000000000 ) ) ;
#244423=SPHERICAL_SURFACE ( 'NONE', #60202, 0.1000000000000000056 ) ;
#244427=FACE_OUTER_BOUND ( 'NONE', #227716, .T. ) ;
#244432=VECTOR ( 'NONE', #103105, 1000.000000000000000 ) ;
#244473=EDGE_CURVE ( 'NONE', #92498, #128191, #62760, .T. ) ;
#244475=VECTOR ( 'NONE', #69155, 1000.000000000000000 ) ;
#244492=DIRECTION ( 'NONE',  ( -1.000000000000000000, -0.000000000000000000, -0.000000000000000000 ) ) ;
#244499=CARTESIAN_POINT ( 'NONE',  ( -21.05000000000000071, 77.26178616857691850, -94.93660852097882241 ) ) ;
#244568=CARTESIAN_POINT ( 'NONE',  ( -22.59999999999999787, 75.90000000001202807, -114.6726782920691221 ) ) ;
#244602=CARTESIAN_POINT ( 'NONE',  ( 21.14250536705908345, 69.48182782313122630, -103.0231074845243597 ) ) ;
#244607=EDGE_LOOP ( 'NONE', ( #257491, #205004, #86254, #238825 ) ) ;
#244621=DIRECTION ( 'NONE',  ( 0.000000000000000000, 6.982962677686266711E-15, -1.000000000000000000 ) ) ;
#244639=CARTESIAN_POINT ( 'NONE',  ( -20.54999999999999716, 85.00000000001179501, -79.41707660717668205 ) ) ;
#244650=VECTOR ( 'NONE', #99749, 999.9999999999998863 ) ;
#244690=ORIENTED_EDGE ( 'NONE', *, *, #167428, .F. ) ;
#244696=VECTOR ( 'NONE', #233257, 1000.000000000000000 ) ;
#244707=ADVANCED_FACE ( 'NONE', ( #107492 ), #130911, .T. ) ;
#244738=AXIS2_PLACEMENT_3D ( 'NONE', #128358, #27999, #167501 ) ;
#244762=CARTESIAN_POINT ( 'NONE',  ( -21.05000000000000071, 64.25000000001189449, -96.23924182154622997 ) ) ;
#244772=ORIENTED_EDGE ( 'NONE', *, *, #199864, .T. ) ;
#244779=ADVANCED_FACE ( 'NONE', ( #67088 ), #68379, .T. ) ;
#244783=DIRECTION ( 'NONE',  ( 1.000000000000000000, 0.000000000000000000, 0.000000000000000000 ) ) ;
#244805=EDGE_LOOP ( 'NONE', ( #179160, #34706, #208973, #146325 ) ) ;
#244812=DIRECTION ( 'NONE',  ( 0.000000000000000000, -0.9274965247785323941, -0.3738317757009769760 ) ) ;
#244826=DIRECTION ( 'NONE',  ( 0.000000000000000000, 0.000000000000000000, 1.000000000000000000 ) ) ;
#244840=ORIENTED_EDGE ( 'NONE', *, *, #127696, .F. ) ;
#244843=ADVANCED_FACE ( 'NONE', ( #133482 ), #236427, .T. ) ;
#244880=CARTESIAN_POINT ( 'NONE',  ( -18.50000000000000000, 64.35000000001195986, -102.9231074845243938 ) ) ;
#244894=DIRECTION ( 'NONE',  ( 1.000000000000000000, 0.000000000000000000, 0.000000000000000000 ) ) ;
#244912=DIRECTION ( 'NONE',  ( 0.000000000000000000, -6.982962677686266711E-15, 1.000000000000000000 ) ) ;
#244915=ORIENTED_EDGE ( 'NONE', *, *, #73169, .T. ) ;
#244945=CARTESIAN_POINT ( 'NONE',  ( -23.15000000000000213, 71.85000000001178933, -81.87310748452433984 ) ) ;
#244967=VECTOR ( 'NONE', #190926, 1000.000000000000000 ) ;
#244969=ORIENTED_EDGE ( 'NONE', *, *, #128903, .F. ) ;
#245025=LINE ( 'NONE', #209755, #138700 ) ;
#245070=CIRCLE ( 'NONE', #28450, 0.1000000000000028644 ) ;
#245094=CARTESIAN_POINT ( 'NONE',  ( 21.93642651522410603, 68.67283376068616008, -103.0231074845243739 ) ) ;
#245095=DIRECTION ( 'NONE',  ( 0.000000000000000000, 1.000000000000000000, 0.000000000000000000 ) ) ;
#245107=ADVANCED_FACE ( 'NONE', ( #225821 ), #90174, .T. ) ;
#245116=CARTESIAN_POINT ( 'NONE',  ( 23.14999999999999503, 69.35000000001180354, -81.87310748452435405 ) ) ;
#245119=VECTOR ( 'NONE', #197849, 1000.000000000000000 ) ;
#245125=DIRECTION ( 'NONE',  ( 0.000000000000000000, 0.000000000000000000, 1.000000000000000000 ) ) ;
#245157=CIRCLE ( 'NONE', #124353, 4.049999999999998046 ) ;
#245178=VECTOR ( 'NONE', #203604, 1000.000000000000114 ) ;
#245205=CIRCLE ( 'NONE', #132793, 0.09999999999999939493 ) ;
#245225=AXIS2_PLACEMENT_3D ( 'NONE', #67922, #109607, #7964 ) ;
#245232=ORIENTED_EDGE ( 'NONE', *, *, #29780, .F. ) ;
#245252=VERTEX_POINT ( 'NONE', #186303 ) ;
#245254=DIRECTION ( 'NONE',  ( 1.000000000000000000, 0.000000000000000000, 0.000000000000000000 ) ) ;
#245290=DIRECTION ( 'NONE',  ( 1.000000000000000000, 0.000000000000000000, 0.000000000000000000 ) ) ;
#245350=DIRECTION ( 'NONE',  ( -0.000000000000000000, -6.982962677686266711E-15, 1.000000000000000000 ) ) ;
#245356=EDGE_CURVE ( 'NONE', #121066, #66860, #56057, .T. ) ;
#245366=EDGE_CURVE ( 'NONE', #254886, #181805, #207148, .T. ) ;
#245379=CARTESIAN_POINT ( 'NONE',  ( 18.49999999999999289, 65.58283456529535727, -78.17310748510507779 ) ) ;
#245381=VERTEX_POINT ( 'NONE', #15373 ) ;
#245398=CARTESIAN_POINT ( 'NONE',  ( 20.99780126800921209, 64.39461131213516865, -76.43575491281889356 ) ) ;
#245453=AXIS2_PLACEMENT_3D ( 'NONE', #116059, #74387, #16959 ) ;
#245503=ORIENTED_EDGE ( 'NONE', *, *, #18236, .F. ) ;
#245528=ORIENTED_EDGE ( 'NONE', *, *, #250446, .T. ) ;
#245534=ORIENTED_EDGE ( 'NONE', *, *, #100, .T. ) ;
#245536=CIRCLE ( 'NONE', #129021, 0.1000000000000011990 ) ;
#245544=EDGE_CURVE ( 'NONE', #235470, #108747, #151396, .T. ) ;
#245553=ORIENTED_EDGE ( 'NONE', *, *, #202811, .T. ) ;
#245558=CARTESIAN_POINT ( 'NONE',  ( 18.39999999999999858, 85.50000000001189449, -95.99103808782457747 ) ) ;
#245570=LINE ( 'NONE', #225956, #121488 ) ;
#245596=DIRECTION ( 'NONE',  ( -1.000000000000000000, -0.000000000000000000, 0.000000000000000000 ) ) ;
#245756=CIRCLE ( 'NONE', #91813, 12.87499999999999822 ) ;
#245785=ORIENTED_EDGE ( 'NONE', *, *, #190924, .T. ) ;
#245859=LINE ( 'NONE', #230144, #90803 ) ;
#245880=AXIS2_PLACEMENT_3D ( 'NONE', #92374, #191518, #254012 ) ;
#245914=DIRECTION ( 'NONE',  ( 0.000000000000000000, 6.982962677686266711E-15, -1.000000000000000000 ) ) ;
#245918=ORIENTED_EDGE ( 'NONE', *, *, #196381, .F. ) ;
#245919=DIRECTION ( 'NONE',  ( 1.000000000000000000, 0.000000000000000000, 0.000000000000000000 ) ) ;
#245920=ORIENTED_EDGE ( 'NONE', *, *, #197809, .F. ) ;
#245921=DIRECTION ( 'NONE',  ( -1.000000000000000000, 0.000000000000000000, 0.000000000000000000 ) ) ;
#245947=CARTESIAN_POINT ( 'NONE',  ( -21.05000000000000071, 88.41227409416141825, -72.42310748452422331 ) ) ;
#245955=SPHERICAL_SURFACE ( 'NONE', #21514, 0.1000000000000000056 ) ;
#246146=AXIS2_PLACEMENT_3D ( 'NONE', #119083, #138602, #40854 ) ;
#246178=ORIENTED_EDGE ( 'NONE', *, *, #238983, .F. ) ;
#246221=CARTESIAN_POINT ( 'NONE',  ( 18.50000000000000000, 85.40000000001190017, -96.02382180668539036 ) ) ;
#246239=CARTESIAN_POINT ( 'NONE',  ( -18.39999999999999858, 85.51932773110434027, -96.05013110796491560 ) ) ;
#246241=DIRECTION ( 'NONE',  ( 0.000000000000000000, 1.000000000000000000, 6.982962677686266711E-15 ) ) ;
#246270=DIRECTION ( 'NONE',  ( 2.694716079187273439E-16, 1.000000000000000000, 6.467318590049456648E-15 ) ) ;
#246271=EDGE_CURVE ( 'NONE', #99793, #190048, #114908, .T. ) ;
#246290=CARTESIAN_POINT ( 'NONE',  ( -21.07946286933444568, 69.67096268100424084, -103.0997913277807498 ) ) ;
#246306=EDGE_CURVE ( 'NONE', #97650, #43089, #153928, .T. ) ;
#246371=ORIENTED_EDGE ( 'NONE', *, *, #245544, .T. ) ;
#246381=ORIENTED_EDGE ( 'NONE', *, *, #46038, .T. ) ;
#246385=VERTEX_POINT ( 'NONE', #51859 ) ;
#246390=EDGE_LOOP ( 'NONE', ( #117189, #201595, #58548, #72577 ) ) ;
#246402=CARTESIAN_POINT ( 'NONE',  ( -20.64999999999999858, 71.75000000001180922, -81.87310748452433984 ) ) ;
#246409=DIRECTION ( 'NONE',  ( 0.000000000000000000, 0.000000000000000000, 1.000000000000000000 ) ) ;
#246414=AXIS2_PLACEMENT_3D ( 'NONE', #35801, #138688, #37094 ) ;
#246424=EDGE_CURVE ( 'NONE', #169820, #215622, #16624, .T. ) ;
#246461=DIRECTION ( 'NONE',  ( 0.000000000000000000, 1.000000000000000000, 0.000000000000000000 ) ) ;
#246470=VERTEX_POINT ( 'NONE', #140387 ) ;
#246473=ORIENTED_EDGE ( 'NONE', *, *, #100, .F. ) ;
#246491=DIRECTION ( 'NONE',  ( 1.000000000000000000, 0.000000000000000000, 0.000000000000000000 ) ) ;
#246499=VERTEX_POINT ( 'NONE', #235641 ) ;
#246515=DIRECTION ( 'NONE',  ( 0.000000000000000000, -6.982962677686266711E-15, 1.000000000000000000 ) ) ;
#246527=EDGE_CURVE ( 'NONE', #190040, #138100, #83087, .T. ) ;
#246544=TOROIDAL_SURFACE ( 'NONE', #109164, 11.65000000000000036, 0.1000000000000000056 ) ;
#246550=DIRECTION ( 'NONE',  ( 0.000000000000000000, 6.982962677686267499E-15, -1.000000000000000000 ) ) ;
#246587=CARTESIAN_POINT ( 'NONE',  ( -20.85000000000000142, 68.97833521811159585, -65.78954208262706516 ) ) ;
#246602=EDGE_CURVE ( 'NONE', #242014, #218485, #33470, .T. ) ;
#246612=CARTESIAN_POINT ( 'NONE',  ( 21.05000000000000071, 65.51556651037016366, -95.56630168303246364 ) ) ;
#246623=DIRECTION ( 'NONE',  ( 0.000000000000000000, 6.769652589177795712E-15, -1.000000000000000000 ) ) ;
#246633=DIRECTION ( 'NONE',  ( 0.000000000000000000, 0.000000000000000000, -1.000000000000000000 ) ) ;
#246716=LINE ( 'NONE', #249312, #197276 ) ;
#246717=ORIENTED_EDGE ( 'NONE', *, *, #35488, .F. ) ;
#246739=AXIS2_PLACEMENT_3D ( 'NONE', #214479, #89396, #174126 ) ;
#246744=AXIS2_PLACEMENT_3D ( 'NONE', #74256, #152502, #213722 ) ;
#246748=FACE_OUTER_BOUND ( 'NONE', #35351, .T. ) ;
#246786=TOROIDAL_SURFACE ( 'NONE', #84242, 0.4000000000000010214, 0.1000000000000000056 ) ;
#246830=DIRECTION ( 'NONE',  ( 0.000000000000000000, -1.000000000000000000, -6.860497997771531562E-15 ) ) ;
#246835=VECTOR ( 'NONE', #5720, 1000.000000000000000 ) ;
#246893=EDGE_CURVE ( 'NONE', #24108, #50189, #133565, .T. ) ;
#246908=ORIENTED_EDGE ( 'NONE', *, *, #203270, .T. ) ;
#246920=AXIS2_PLACEMENT_3D ( 'NONE', #187414, #27076, #166584 ) ;
#246923=ORIENTED_EDGE ( 'NONE', *, *, #108021, .T. ) ;
#246948=ORIENTED_EDGE ( 'NONE', *, *, #65620, .F. ) ;
#246966=EDGE_CURVE ( 'NONE', #199332, #165247, #50162, .T. ) ;
#247000=EDGE_CURVE ( 'NONE', #30659, #211497, #171044, .T. ) ;
#247002=ORIENTED_EDGE ( 'NONE', *, *, #147036, .T. ) ;
#247009=TOROIDAL_SURFACE ( 'NONE', #230461, 11.70000000000000107, 0.1000000000000000056 ) ;
#247043=AXIS2_PLACEMENT_3D ( 'NONE', #153331, #208147, #188558 ) ;
#247055=ORIENTED_EDGE ( 'NONE', *, *, #42049, .T. ) ;
#247059=CIRCLE ( 'NONE', #155355, 4.000000000000003553 ) ;
#247079=AXIS2_PLACEMENT_3D ( 'NONE', #18601, #79826, #40764 ) ;
#247110=EDGE_CURVE ( 'NONE', #87379, #3181, #166927, .T. ) ;
#247111=DIRECTION ( 'NONE',  ( 0.000000000000000000, 0.1298341882519953583, 0.9915357197604862671 ) ) ;
#247142=CARTESIAN_POINT ( 'NONE',  ( 18.59999999999999076, 65.79142135624910281, -81.67310748452439384 ) ) ;
#247163=DIRECTION ( 'NONE',  ( -1.000000000000000000, -0.000000000000000000, -0.000000000000000000 ) ) ;
#247166=CARTESIAN_POINT ( 'NONE',  ( 20.85000000000000142, 76.00000000001165290, -61.72310748452430573 ) ) ;
#247170=CARTESIAN_POINT ( 'NONE',  ( 22.48660254037844197, 64.35000000001194564, -103.0731074845243853 ) ) ;
#247184=ORIENTED_EDGE ( 'NONE', *, *, #140070, .T. ) ;
#247186=CARTESIAN_POINT ( 'NONE',  ( 18.44444291854882678, 85.49010118095492317, -62.89420351963329381 ) ) ;
#247212=ORIENTED_EDGE ( 'NONE', *, *, #142093, .F. ) ;
#247270=EDGE_CURVE ( 'NONE', #23758, #190290, #212874, .T. ) ;
#247304=DIRECTION ( 'NONE',  ( 0.000000000000000000, -1.000000000000000000, 0.000000000000000000 ) ) ;
#247315=VERTEX_POINT ( 'NONE', #140751 ) ;
#247334=EDGE_LOOP ( 'NONE', ( #158183, #94444, #59350 ) ) ;
#247350=CARTESIAN_POINT ( 'NONE',  ( -23.25000000000000000, 76.00000000001170974, -69.52310748452431710 ) ) ;
#247357=ORIENTED_EDGE ( 'NONE', *, *, #60540, .F. ) ;
#247401=CARTESIAN_POINT ( 'NONE',  ( -20.94560253601877164, 64.25000000001175238, -76.51302397200892358 ) ) ;
#247423=TOROIDAL_SURFACE ( 'NONE', #139067, 12.77499999999999858, 0.1000000000000000056 ) ;
#247428=ORIENTED_EDGE ( 'NONE', *, *, #214066, .T. ) ;
#247432=CARTESIAN_POINT ( 'NONE',  ( 18.52928932188133970, 65.72071067813045886, -81.67310748452439384 ) ) ;
#247439=CIRCLE ( 'NONE', #47510, 0.1000000000000028644 ) ;
#247447=DIRECTION ( 'NONE',  ( -1.000000000000000000, 1.836970198721029934E-16, 1.282749433769087582E-30 ) ) ;
#247454=( BOUNDED_CURVE ( )  B_SPLINE_CURVE ( 3, ( #192568, #115587, #51740, #175583 ),
 .UNSPECIFIED., .F., .F. ) 
 B_SPLINE_CURVE_WITH_KNOTS ( ( 4, 4 ),
 ( 3.192897208853993085, 4.712388980384689674 ),
 .UNSPECIFIED. ) 
 CURVE ( )  GEOMETRIC_REPRESENTATION_ITEM ( )  RATIONAL_B_SPLINE_CURVE ( ( 1.000000000000000000, 0.8166740347213228279, 0.8166740347213228279, 1.000000000000000000 ) ) 
 REPRESENTATION_ITEM ( '' )  );
#247457=ORIENTED_EDGE ( 'NONE', *, *, #236087, .T. ) ;
#247501=FACE_OUTER_BOUND ( 'NONE', #210503, .T. ) ;
#247546=DIRECTION ( 'NONE',  ( 1.000000000000000000, 0.000000000000000000, 0.000000000000000000 ) ) ;
#247547=CYLINDRICAL_SURFACE ( 'NONE', #156860, 4.049999999999998046 ) ;
#247561=ORIENTED_EDGE ( 'NONE', *, *, #196323, .F. ) ;
#247569=DIRECTION ( 'NONE',  ( 0.000000000000000000, 6.982962677686266711E-15, -1.000000000000000000 ) ) ;
#247580=ORIENTED_EDGE ( 'NONE', *, *, #25622, .T. ) ;
#247610=LINE ( 'NONE', #111968, #47351 ) ;
#247613=CARTESIAN_POINT ( 'NONE',  ( -18.50000000000000000, 66.65000000001187175, -90.67310748452437963 ) ) ;
#247624=AXIS2_PLACEMENT_3D ( 'NONE', #220104, #238369, #160155 ) ;
#247646=EDGE_CURVE ( 'NONE', #59214, #125644, #131457, .T. ) ;
#247647=DIRECTION ( 'NONE',  ( 2.342056488767301376E-15, 0.1350103645451835865, 0.9908441862701605762 ) ) ;
#247682=CARTESIAN_POINT ( 'NONE',  ( 20.04142135391667168, 64.25000000001176659, -78.32060061889448832 ) ) ;
#247710=EDGE_CURVE ( 'NONE', #171759, #190547, #71420, .T. ) ;
#247741=EDGE_LOOP ( 'NONE', ( #163362, #255258, #100588 ) ) ;
#247763=ORIENTED_EDGE ( 'NONE', *, *, #105086, .F. ) ;
#247766=CARTESIAN_POINT ( 'NONE',  ( -20.54999999999999716, 84.66355140188093742, -79.04720860259155302 ) ) ;
#247801=CARTESIAN_POINT ( 'NONE',  ( 18.39999999999999858, 85.60000000001166143, -62.92291809330219365 ) ) ;
#247829=ORIENTED_EDGE ( 'NONE', *, *, #138319, .F. ) ;
#247832=ADVANCED_FACE ( 'NONE', ( #82995 ), #17916, .F. ) ;
#247839=EDGE_CURVE ( 'NONE', #204044, #131489, #46441, .T. ) ;
#247840=CARTESIAN_POINT ( 'NONE',  ( 18.39999999999999858, 85.60000000001190301, -95.99103808782457747 ) ) ;
#247845=EDGE_CURVE ( 'NONE', #49226, #243331, #104671, .T. ) ;
#247856=VECTOR ( 'NONE', #213486, 1000.000000000000000 ) ;
#247858=CARTESIAN_POINT ( 'NONE',  ( -20.94788355080264353, 65.69792220476300315, -64.03355541284614105 ) ) ;
#247860=CARTESIAN_POINT ( 'NONE',  ( 21.05000000000000071, 67.18454772081435067, -94.60271493191011416 ) ) ;
#247876=DIRECTION ( 'NONE',  ( 0.000000000000000000, 6.982962677686267499E-15, -1.000000000000000000 ) ) ;
#247899=EDGE_CURVE ( 'NONE', #107353, #74147, #196468, .T. ) ;
#247900=CARTESIAN_POINT ( 'NONE',  ( 21.05000000000000426, 65.27628289530437655, -95.42869009291126758 ) ) ;
#247945=CARTESIAN_POINT ( 'NONE',  ( 21.02374657821586013, 64.39999999919189122, -76.45131071432655290 ) ) ;
#247946=DIRECTION ( 'NONE',  ( 0.000000000000000000, -1.000000000000000000, -6.982962677686265922E-15 ) ) ;
#248014=EDGE_CURVE ( 'NONE', #47226, #175899, #66032, .T. ) ;
#248022=EDGE_CURVE ( 'NONE', #97749, #211450, #150692, .T. ) ;
#248048=ORIENTED_EDGE ( 'NONE', *, *, #149713, .F. ) ;
#248049=DIRECTION ( 'NONE',  ( 1.000000000000000000, 0.000000000000000000, 0.000000000000000000 ) ) ;
#248067=ADVANCED_FACE ( 'NONE', ( #11207 ), #175435, .T. ) ;
#248155=EDGE_LOOP ( 'NONE', ( #191351, #35154, #143832, #4550 ) ) ;
#248188=DIRECTION ( 'NONE',  ( 1.000000000000000000, 0.000000000000000000, 0.000000000000000000 ) ) ;
#248209=DIRECTION ( 'NONE',  ( 1.000000000000000000, 0.000000000000000000, 0.000000000000000000 ) ) ;
#248231=CARTESIAN_POINT ( 'NONE',  ( -23.15000000000000213, 74.00000000001180922, -82.24772940728641402 ) ) ;
#248278=CARTESIAN_POINT ( 'NONE',  ( -20.54999999999999716, 68.85000000001186038, -90.77310748452435973 ) ) ;
#248288=CARTESIAN_POINT ( 'NONE',  ( -22.43310005002225438, 75.99436305787115487, -114.6727696116587083 ) ) ;
#248311=ORIENTED_EDGE ( 'NONE', *, *, #53149, .F. ) ;
#248373=FACE_OUTER_BOUND ( 'NONE', #142617, .T. ) ;
#248395=CIRCLE ( 'NONE', #240036, 0.1000000000000028644 ) ;
#248398=DIRECTION ( 'NONE',  ( -1.000000000000000000, 0.000000000000000000, 0.000000000000000000 ) ) ;
#248399=ORIENTED_EDGE ( 'NONE', *, *, #92532, .T. ) ;
#248414=CARTESIAN_POINT ( 'NONE',  ( 23.14999999999998437, 76.00000000001197975, -107.0731074845243143 ) ) ;
#248467=DIRECTION ( 'NONE',  ( 1.000000000000000000, -0.000000000000000000, -0.000000000000000000 ) ) ;
#248477=AXIS2_PLACEMENT_3D ( 'NONE', #54042, #133580, #33240 ) ;
#248482=CARTESIAN_POINT ( 'NONE',  ( -20.94999999999999929, 77.16270174994990327, -95.02310748452430289 ) ) ;
#248501=EDGE_CURVE ( 'NONE', #222143, #110088, #73780, .T. ) ;
#248505=DIRECTION ( 'NONE',  ( 0.000000000000000000, 0.9908441862701605762, -0.1350103645451835310 ) ) ;
#248538=CARTESIAN_POINT ( 'NONE',  ( 18.31325810956326450, 85.53638847601891371, -62.65466727821948467 ) ) ;
#248545=CIRCLE ( 'NONE', #107072, 4.049999999999998046 ) ;
#248564=AXIS2_PLACEMENT_3D ( 'NONE', #103065, #123951, #5243 ) ;
#248577=EDGE_CURVE ( 'NONE', #72649, #27688, #47119, .T. ) ;
#248582=CIRCLE ( 'NONE', #198519, 0.1000000000000028644 ) ;
#248598=CARTESIAN_POINT ( 'NONE',  ( -21.05000000000000071, 77.16270174994990327, -94.92310748452430857 ) ) ;
#248604=ORIENTED_EDGE ( 'NONE', *, *, #8307, .T. ) ;
#248704=ORIENTED_EDGE ( 'NONE', *, *, #106565, .F. ) ;
#248733=VERTEX_POINT ( 'NONE', #213589 ) ;
#248794=EDGE_CURVE ( 'NONE', #224021, #225545, #200382, .T. ) ;
#248802=DIRECTION ( 'NONE',  ( 1.000000000000000000, 0.000000000000000000, 0.000000000000000000 ) ) ;
#248814=CARTESIAN_POINT ( 'NONE',  ( 23.14999999999999503, 64.25000000001179501, -81.77310748452438816 ) ) ;
#248819=AXIS2_PLACEMENT_3D ( 'NONE', #235956, #155186, #211274 ) ;
#248841=CARTESIAN_POINT ( 'NONE',  ( -18.59999999999999787, 76.00000000001195133, -103.0231074845243171 ) ) ;
#248868=ORIENTED_EDGE ( 'NONE', *, *, #72883, .T. ) ;
#248920=AXIS2_PLACEMENT_3D ( 'NONE', #105314, #204441, #109190 ) ;
#248962=AXIS2_PLACEMENT_3D ( 'NONE', #76476, #235550, #118185 ) ;
#248976=ORIENTED_EDGE ( 'NONE', *, *, #171576, .F. ) ;
#248989=CARTESIAN_POINT ( 'NONE',  ( -23.15000000000000213, 85.60000000001188880, -93.12913836187179584 ) ) ;
#249003=ORIENTED_EDGE ( 'NONE', *, *, #94254, .T. ) ;
#249010=ORIENTED_EDGE ( 'NONE', *, *, #97194, .T. ) ;
#249026=ORIENTED_EDGE ( 'NONE', *, *, #92230, .T. ) ;
#249059=ORIENTED_EDGE ( 'NONE', *, *, #99131, .F. ) ;
#249145=DIRECTION ( 'NONE',  ( 1.000000000000000000, 0.000000000000000000, 0.000000000000000000 ) ) ;
#249173=DIRECTION ( 'NONE',  ( 1.000000000000000000, 0.000000000000000000, 0.000000000000000000 ) ) ;
#249193=EDGE_CURVE ( 'NONE', #193967, #83423, #245570, .T. ) ;
#249207=VERTEX_POINT ( 'NONE', #185582 ) ;
#249212=DIRECTION ( 'NONE',  ( 0.000000000000000000, 0.000000000000000000, 1.000000000000000000 ) ) ;
#249249=CARTESIAN_POINT ( 'NONE',  ( 21.04386569057603751, 64.25000000001175238, -76.38027013274417243 ) ) ;
#249267=AXIS2_PLACEMENT_3D ( 'NONE', #50402, #70019, #229078 ) ;
#249276=ADVANCED_FACE ( 'NONE', ( #107714 ), #245955, .T. ) ;
#249288=CLOSED_SHELL ( 'NONE', ( #128286, #89925, #123142, #135905, #59366, #76957, #129688, #160040, #205158, #153352, #222983, #25086, #180013, #204756, #84553, #251173, #185422, #74529, #211843, #21475, #229289, #253945, #180509, #182411, #164085, #54797, #4715, #90982, #51609, #63186, #257239, #219939, #170874, #65638, #20291, #193036, #4151, #3694, #76515, #156902, #38805, #151847, #61622, #63825, #9828, #159280, #203306, #96852, #210793, #16048, #50702, #163870, #155644, #36498, #75400, #236323, #1634, #147366, #49276, #118345, #133558, #221753, #92009, #112551, #181580, #251520, #155624, #243388, #219251, #217169, #108155, #146877, #34760, #143025, #200697, #149260, #244779, #54449, #202441, #122994, #256008, #63908, #51346, #61803, #235128, #215095, #88118, #218208, #5418, #104693, #186141, #177371, #191717, #223433, #71741, #188689, #97238, #12879, #92614, #52651, #127339, #102318, #99664, #77074, #193554, #176865, #68413, #193349, #219018, #94532, #172303, #138051, #198050, #229463, #2160, #104728, #95947, #55780, #219286, #183709, #231235, #124037, #66406, #44283, #63819, #100704, #243400, #88339, #52372, #184431, #130716, #87587, #151155, #100258, #217927, #43690, #124715, #9382, #248067, #241390, #247832, #196580, #12835, #25448, #128906, #150934, #124049, #209391, #28950, #123267, #7137, #46353, #197802, #131207, #110874, #83946, #81707, #181495, #109041, #242634, #237493, #113038, #122210, #164086, #184859, #193647, #210168, #156892, #145249, #11301, #34782, #35907, #71179, #87904, #165425, #171347, #236738, #87618, #175221, #53426, #195339, #211871, #224827, #131878, #121215, #38129, #155423, #244843, #220340, #64838, #165869, #19710, #54949, #200310, #233246, #198908, #133641, #8254, #5344, #225017, #91179, #130929, #250782, #85196, #31531, #108201, #81687, #137084, #74212, #179718, #161035, #223320, #244707, #125736, #129740, #126854, #64599, #197442, #168318, #234110, #151646, #142722, #5130, #29007, #170953, #68282, #47480, #73875, #157184, #22637, #170168, #129173, #199442, #96007, #80081, #27366, #178641, #133975, #110971, #244221, #103775, #101441, #239039, #49173, #89520, #166846, #41206, #191673, #7578, #80557, #63112, #66012, #256517, #582, #101352, #68110, #140438, #104779, #111199, #72498, #194203, #127368, #88527, #111623, #74239, #118079, #198910, #133921, #164291, #71236, #137828, #113699, #225749, #13508, #136513, #147627, #18637, #128021, #39961, #16868, #224571, #141564, #192723, #107310, #1422, #244149, #166265, #210715, #54492, #46941, #192879, #135290, #215613, #238162, #165601, #110281, #52078, #173484, #12865, #219921, #160633, #111393, #33488, #143590, #202696, #25868, #161464, #36745, #104857, #187759, #245107, #70194, #229866, #161330, #6051, #84774, #236205, #64724, #125308, #105652, #34086, #4291, #13166, #218871, #236600, #89668, #95711, #50331, #223310, #86640, #213109, #150090, #92080, #213089, #252264, #75453, #251280, #94422, #206599, #193050, #123108, #200172, #147594, #227808, #254915, #113500, #50420, #26582, #140302, #63446, #52392, #97394, #155866, #112419, #227204, #111661, #5198, #40411, #181659, #205373, #131369, #44265, #168117, #220424, #96074, #229449, #6814, #244274, #206976, #7120, #74666, #3519, #86428, #40696, #16671, #30267, #54350, #174800, #178620, #148874, #68281, #99630, #255097, #160324, #253180, #190620, #55425, #47540, #191223, #208539, #205016, #302, #213013, #44481, #169842, #204909, #124175, #165655, #15220, #157082, #166291, #48418, #40585, #212436, #176388, #111447, #8382, #242497, #241492, #120701, #76750, #114286, #93065, #39057, #88356, #254649, #162653, #240538, #226932, #64719, #191358, #143891, #219201, #143280, #1380, #144306, #15969, #223712, #19529, #139647, #204499, #41420, #166059, #56888, #179586, #89906, #122618, #133312, #174895, #87599, #2, #99911, #200748, #123213, #203422, #26960, #181471, #46718, #61174, #79685, #135061, #84827, #72515, #40506, #46184, #19183, #223229, #224481, #86570, #239514, #122956, #15395, #22287, #252857, #25023, #205990, #181345, #17548, #249276, #228168, #213541, #142188, #210543, #58825, #9127, #94650, #154303, #13215 ) ) ;
#249312=CARTESIAN_POINT ( 'NONE',  ( -21.37071067811865532, 67.92928932189320790, -90.77310748452437394 ) ) ;
#249343=ORIENTED_EDGE ( 'NONE', *, *, #239345, .F. ) ;
#249353=DIRECTION ( 'NONE',  ( 0.000000000000000000, 0.1350103645451807832, 0.9908441862701610203 ) ) ;
#249362=AXIS2_PLACEMENT_3D ( 'NONE', #147808, #52534, #70859 ) ;
#249402=AXIS2_PLACEMENT_3D ( 'NONE', #199515, #177396, #59956 ) ;
#249407=DIRECTION ( 'NONE',  ( 0.000000000000000000, 0.000000000000000000, 1.000000000000000000 ) ) ;
#249410=DIRECTION ( 'NONE',  ( -1.000000000000000000, 0.000000000000000000, -0.000000000000000000 ) ) ;
#249412=DIRECTION ( 'NONE',  ( 0.000000000000000000, -0.9908441862701605762, 0.1350103645451835310 ) ) ;
#249418=CARTESIAN_POINT ( 'NONE',  ( 20.94999999999999929, 76.00000000001170974, -69.52310748452431710 ) ) ;
#249425=VECTOR ( 'NONE', #245914, 1000.000000000000000 ) ;
#249429=CIRCLE ( 'NONE', #216260, 0.1000000000000009492 ) ;
#249433=CARTESIAN_POINT ( 'NONE',  ( 20.11144452914043868, 66.06638914889192904, -95.13281403056952001 ) ) ;
#249436=EDGE_CURVE ( 'NONE', #129734, #81780, #150700, .T. ) ;
#249482=CARTESIAN_POINT ( 'NONE',  ( 20.85000000000000142, 77.85161776048053639, -57.91991776492063337 ) ) ;
#249521=EDGE_CURVE ( 'NONE', #14237, #71369, #39768, .T. ) ;
#249536=CARTESIAN_POINT ( 'NONE',  ( 22.57320508075688537, 64.35000000001195986, -103.0231074845244024 ) ) ;
#249550=AXIS2_PLACEMENT_3D ( 'NONE', #105127, #204259, #83005 ) ;
#249584=CARTESIAN_POINT ( 'NONE',  ( 20.94999999999999929, 87.65000000001170122, -69.52310748452423184 ) ) ;
#249594=DIRECTION ( 'NONE',  ( 0.000000000000000000, -7.086529944415894657E-15, 1.000000000000000000 ) ) ;
#249684=VERTEX_POINT ( 'NONE', #141396 ) ;
#249685=ORIENTED_EDGE ( 'NONE', *, *, #39151, .T. ) ;
#249784=AXIS2_PLACEMENT_3D ( 'NONE', #227612, #188490, #28170 ) ;
#249841=CARTESIAN_POINT ( 'NONE',  ( 23.14999999999999858, 71.00000000001180922, -81.92837350343744163 ) ) ;
#249860=CARTESIAN_POINT ( 'NONE',  ( -18.50000000000000000, 85.50000000001189449, -94.92310748452425173 ) ) ;
#249875=AXIS2_PLACEMENT_3D ( 'NONE', #164594, #5478, #83719 ) ;
#249907=EDGE_LOOP ( 'NONE', ( #153836, #239555, #13978, #171294, #120731 ) ) ;
#249939=ORIENTED_EDGE ( 'NONE', *, *, #84312, .T. ) ;
#249945=DIRECTION ( 'NONE',  ( 1.000000000000000000, 0.000000000000000000, 0.000000000000000000 ) ) ;
#249952=CARTESIAN_POINT ( 'NONE',  ( -21.29999999999995808, 76.00000000001195133, -103.0231074845243171 ) ) ;
#250011=CARTESIAN_POINT ( 'NONE',  ( -20.64999999999999858, 85.40000000001178648, -79.41707660717668205 ) ) ;
#250019=CARTESIAN_POINT ( 'NONE',  ( 20.94999999999999929, 87.65000000001172964, -72.52310748452423184 ) ) ;
#250024=DIRECTION ( 'NONE',  ( 0.000000000000000000, 0.4930308989875575865, 0.8700118002898125091 ) ) ;
#250025=ORIENTED_EDGE ( 'NONE', *, *, #201137, .F. ) ;
#250061=ORIENTED_EDGE ( 'NONE', *, *, #44649, .T. ) ;
#250081=DIRECTION ( 'NONE',  ( 0.7071067811865474617, -0.7071067811865474617, -4.937700262164531476E-15 ) ) ;
#250089=AXIS2_PLACEMENT_3D ( 'NONE', #66739, #86265, #146253 ) ;
#250105=ORIENTED_EDGE ( 'NONE', *, *, #181980, .F. ) ;
#250125=EDGE_CURVE ( 'NONE', #178001, #200940, #21862, .T. ) ;
#250127=DIRECTION ( 'NONE',  ( -1.000000000000000000, 0.000000000000000000, -0.000000000000000000 ) ) ;
#250133=EDGE_CURVE ( 'NONE', #237782, #208580, #70582, .T. ) ;
#250137=CARTESIAN_POINT ( 'NONE',  ( -20.94999999999999929, 87.48912529308779540, -72.62310748452422615 ) ) ;
#250143=CARTESIAN_POINT ( 'NONE',  ( 20.95561247346651967, 65.40499263480833747, -95.42932471754275525 ) ) ;
#250149=CIRCLE ( 'NONE', #108488, 0.09999999999999939493 ) ;
#250150=VERTEX_POINT ( 'NONE', #69282 ) ;
#250158=DIRECTION ( 'NONE',  ( 1.000000000000000000, 0.000000000000000000, 0.000000000000000000 ) ) ;
#250255=ORIENTED_EDGE ( 'NONE', *, *, #209547, .T. ) ;
#250268=VECTOR ( 'NONE', #4431, 1000.000000000000000 ) ;
#250333=DIRECTION ( 'NONE',  ( -1.000000000000000000, -7.304098846218105085E-16, -4.217023435051676515E-16 ) ) ;
#250360=EDGE_CURVE ( 'NONE', #8981, #10090, #47146, .T. ) ;
#250390=EDGE_CURVE ( 'NONE', #246470, #134706, #128264, .T. ) ;
#250420=CARTESIAN_POINT ( 'NONE',  ( -20.94999999999999929, 65.70711192142346135, -64.06510546851221477 ) ) ;
#250422=CARTESIAN_POINT ( 'NONE',  ( -18.46946985241255845, 85.50931722872357454, -96.03644491902473135 ) ) ;
#250446=EDGE_CURVE ( 'NONE', #91291, #135352, #245025, .T. ) ;
#250447=ORIENTED_EDGE ( 'NONE', *, *, #6896, .F. ) ;
#250449=EDGE_LOOP ( 'NONE', ( #47743, #47921, #22504, #122704 ) ) ;
#250465=EDGE_LOOP ( 'NONE', ( #239201, #142803, #32903, #113669, #153641 ) ) ;
#250475=DIRECTION ( 'NONE',  ( 0.000000000000000000, -1.000000000000000000, -6.352154140967427193E-15 ) ) ;
#250481=CARTESIAN_POINT ( 'NONE',  ( -23.25000000000000000, 64.25000000001176659, -76.53791325517833855 ) ) ;
#250486=EDGE_LOOP ( 'NONE', ( #192247, #68948, #63375, #101633 ) ) ;
#250490=CARTESIAN_POINT ( 'NONE',  ( 18.49999999999999289, 65.76093837589027657, -78.26871004992719350 ) ) ;
#250514=CARTESIAN_POINT ( 'NONE',  ( -20.64999999999999858, 71.65000000001180069, -81.87310748452433984 ) ) ;
#250548=CARTESIAN_POINT ( 'NONE',  ( 21.05000000000000071, 67.12338541492479749, -94.63802700567968884 ) ) ;
#250550=CARTESIAN_POINT ( 'NONE',  ( -23.25000000000000000, 77.83585931145526615, -58.01866831572577610 ) ) ;
#250584=ADVANCED_BREP_SHAPE_REPRESENTATION ( '', ( #111872, #2425 ), #185415 ) ;
#250593=CARTESIAN_POINT ( 'NONE',  ( 20.95429693346636313, 65.45669512011612312, -95.46222494621135013 ) ) ;
#250603=EDGE_LOOP ( 'NONE', ( #164265, #84742, #44356, #226626, #113025 ) ) ;
#250632=EDGE_CURVE ( 'NONE', #84368, #132438, #16700, .T. ) ;
#250642=EDGE_CURVE ( 'NONE', #61685, #82775, #38802, .T. ) ;
#250648=ORIENTED_EDGE ( 'NONE', *, *, #226984, .T. ) ;
#250654=DIRECTION ( 'NONE',  ( 1.000000000000000000, 0.000000000000000000, 0.000000000000000000 ) ) ;
#250662=CARTESIAN_POINT ( 'NONE',  ( 23.24999999999999289, 64.25000000001193712, -102.9231074845243938 ) ) ;
#250672=CARTESIAN_POINT ( 'NONE',  ( 18.43579564894459111, 85.51932753530431341, -96.05013084066375484 ) ) ;
#250676=CARTESIAN_POINT ( 'NONE',  ( -23.15000000000000213, 74.08971962618002749, -82.15447533972326255 ) ) ;
#250677=AXIS2_PLACEMENT_3D ( 'NONE', #93227, #114071, #234023 ) ;
#250746=EDGE_CURVE ( 'NONE', #196101, #156778, #120946, .T. ) ;
#250759=DIRECTION ( 'NONE',  ( -0.000000000000000000, 1.000000000000000000, 6.982962677686266711E-15 ) ) ;
#250782=ADVANCED_FACE ( 'NONE', ( #200454 ), #122190, .F. ) ;
#250825=EDGE_LOOP ( 'NONE', ( #256470, #221386, #24191, #194522, #5013, #189633 ) ) ;
#250831=FACE_OUTER_BOUND ( 'NONE', #74242, .T. ) ;
#250838=CARTESIAN_POINT ( 'NONE',  ( -22.49510344025093644, 75.93287232181778279, -114.6730775896385524 ) ) ;
#250845=CARTESIAN_POINT ( 'NONE',  ( 21.14999999999999858, 76.00000000001186606, -90.87310748452429721 ) ) ;
#250857=CIRCLE ( 'NONE', #63424, 0.09999999999999939493 ) ;
#250864=LINE ( 'NONE', #196050, #161034 ) ;
#250900=CIRCLE ( 'NONE', #201034, 0.3999999999999975797 ) ;
#250903=CARTESIAN_POINT ( 'NONE',  ( 20.94999999999999574, 77.16270174994990327, -95.02310748452430289 ) ) ;
#250928=EDGE_CURVE ( 'NONE', #119060, #23607, #163882, .T. ) ;
#250979=EDGE_LOOP ( 'NONE', ( #96360, #30033, #97370 ) ) ;
#251008=LINE ( 'NONE', #151960, #38052 ) ;
#251029=CARTESIAN_POINT ( 'NONE',  ( -20.64999999999999858, 85.00000000001179501, -78.91707660717668205 ) ) ;
#251036=AXIS2_PLACEMENT_3D ( 'NONE', #205345, #67137, #8458 ) ;
#251054=ORIENTED_EDGE ( 'NONE', *, *, #20308, .T. ) ;
#251068=VECTOR ( 'NONE', #217029, 1000.000000000000000 ) ;
#251069=ORIENTED_EDGE ( 'NONE', *, *, #99719, .F. ) ;
#251091=FACE_OUTER_BOUND ( 'NONE', #69474, .T. ) ;
#251093=DIRECTION ( 'NONE',  ( 1.000000000000000000, 7.304098846218135653E-16, 5.311601492717085047E-30 ) ) ;
#251101=DIRECTION ( 'NONE',  ( 0.000000000000000000, 0.8700118002898356018, -0.4930308989875170078 ) ) ;
#251126=CARTESIAN_POINT ( 'NONE',  ( 21.14999999999999858, 64.35000000001186038, -90.87310748452438247 ) ) ;
#251131=CARTESIAN_POINT ( 'NONE',  ( 20.94999999999999929, 76.00000000001170974, -69.52310748452431710 ) ) ;
#251155=EDGE_CURVE ( 'NONE', #82161, #85086, #247439, .T. ) ;
#251173=ADVANCED_FACE ( 'NONE', ( #146264 ), #18314, .F. ) ;
#251182=VECTOR ( 'NONE', #120455, 1000.000000000000000 ) ;
#251220=FACE_OUTER_BOUND ( 'NONE', #222252, .T. ) ;
#251249=DIRECTION ( 'NONE',  ( 0.000000000000000000, 1.000000000000000000, 6.982962677686266711E-15 ) ) ;
#251260=DIRECTION ( 'NONE',  ( 1.000000000000000000, 0.000000000000000000, 0.000000000000000000 ) ) ;
#251270=CARTESIAN_POINT ( 'NONE',  ( 20.94999999999999929, 69.45000000001188312, -93.00608031408432907 ) ) ;
#251279=VERTEX_POINT ( 'NONE', #210118 ) ;
#251280=ADVANCED_FACE ( 'NONE', ( #228392 ), #49741, .T. ) ;
#251290=AXIS2_PLACEMENT_3D ( 'NONE', #147522, #31462, #167119 ) ;
#251310=CIRCLE ( 'NONE', #5592, 0.09999999999999939493 ) ;
#251329=DIRECTION ( 'NONE',  ( 0.000000000000000000, 0.5000000000000729417, 0.8660254037843965191 ) ) ;
#251367=EDGE_CURVE ( 'NONE', #45676, #158833, #105764, .T. ) ;
#251407=ORIENTED_EDGE ( 'NONE', *, *, #157422, .T. ) ;
#251437=CARTESIAN_POINT ( 'NONE',  ( 20.94999999999999929, 76.00000000001170974, -69.52310748452431710 ) ) ;
#251491=DIRECTION ( 'NONE',  ( 1.000000000000000000, 0.000000000000000000, 0.000000000000000000 ) ) ;
#251515=CARTESIAN_POINT ( 'NONE',  ( 20.94999999999999929, 77.36242903720497566, -61.63422623660309796 ) ) ;
#251520=ADVANCED_FACE ( 'NONE', ( #105517 ), #24768, .F. ) ;
#251525=DIRECTION ( 'NONE',  ( 0.000000000000000000, 1.000000000000000000, 6.938893903907222067E-15 ) ) ;
#251531=ORIENTED_EDGE ( 'NONE', *, *, #118928, .T. ) ;
#251538=ORIENTED_EDGE ( 'NONE', *, *, #183247, .T. ) ;
#251544=DIRECTION ( 'NONE',  ( 0.000000000000000000, -0.4999999999999689138, -0.8660254037844565822 ) ) ;
#251547=ORIENTED_EDGE ( 'NONE', *, *, #110011, .T. ) ;
#251555=ORIENTED_EDGE ( 'NONE', *, *, #52883, .T. ) ;
#251562=DIRECTION ( 'NONE',  ( 1.000000000000000000, 0.000000000000000000, 0.000000000000000000 ) ) ;
#251563=CARTESIAN_POINT ( 'NONE',  ( -22.39999999999999858, 76.00000000001203659, -114.6726782920691221 ) ) ;
#251576=ORIENTED_EDGE ( 'NONE', *, *, #90443, .F. ) ;
#251582=VECTOR ( 'NONE', #174515, 1000.000000000000000 ) ;
#251622=CARTESIAN_POINT ( 'NONE',  ( -20.64999999999999858, 73.50000000001186606, -89.79848556176223440 ) ) ;
#251627=EDGE_CURVE ( 'NONE', #208155, #114552, #71589, .T. ) ;
#251636=DIRECTION ( 'NONE',  ( -1.000000000000000000, -0.000000000000000000, -0.000000000000000000 ) ) ;
#251638=CIRCLE ( 'NONE', #26802, 4.049999999999998046 ) ;
#251648=EDGE_LOOP ( 'NONE', ( #255771, #30010, #112325, #236225 ) ) ;
#251672=CARTESIAN_POINT ( 'NONE',  ( -20.64999999999999858, 68.85000000001186038, -90.67310748452435121 ) ) ;
#251680=VECTOR ( 'NONE', #203230, 1000.000000000000000 ) ;
#251685=CARTESIAN_POINT ( 'NONE',  ( -22.59066674512261486, 64.25000000001193712, -103.0536116081548101 ) ) ;
#251702=ORIENTED_EDGE ( 'NONE', *, *, #19022, .F. ) ;
#251703=FACE_OUTER_BOUND ( 'NONE', #20992, .T. ) ;
#251710=EDGE_CURVE ( 'NONE', #74147, #237782, #51789, .T. ) ;
#251714=EDGE_LOOP ( 'NONE', ( #252095, #189981, #155492, #164367 ) ) ;
#251725=AXIS2_PLACEMENT_3D ( 'NONE', #220952, #21504, #85279 ) ;
#251729=PLANE ( 'NONE',  #224096 ) ;
#251774=LINE ( 'NONE', #250481, #236690 ) ;
#251792=DIRECTION ( 'NONE',  ( 0.000000000000000000, -1.000000000000000000, -6.982962677686266711E-15 ) ) ;
#251802=DIRECTION ( 'NONE',  ( -0.000000000000000000, 1.000000000000000000, 6.982962677686266711E-15 ) ) ;
#251822=VECTOR ( 'NONE', #144910, 1000.000000000000000 ) ;
#251841=ORIENTED_EDGE ( 'NONE', *, *, #168600, .T. ) ;
#251851=EDGE_LOOP ( 'NONE', ( #109193, #140793, #104829, #246371 ) ) ;
#251853=ORIENTED_EDGE ( 'NONE', *, *, #100919, .T. ) ;
#251873=ORIENTED_EDGE ( 'NONE', *, *, #94339, .T. ) ;
#251879=CARTESIAN_POINT ( 'NONE',  ( 22.48660254037844197, 64.35000000001194564, -103.0731074845243853 ) ) ;
#251944=CARTESIAN_POINT ( 'NONE',  ( -23.15000000000000213, 76.00000000001192291, -98.87310748452431142 ) ) ;
#251966=LINE ( 'NONE', #152906, #182067 ) ;
#251970=CARTESIAN_POINT ( 'NONE',  ( 18.59999999999999076, 69.55000000001179217, -81.77310748452434552 ) ) ;
#251990=CARTESIAN_POINT ( 'NONE',  ( 21.14999999999999503, 76.00000000001199396, -109.5637644362255543 ) ) ;
#251991=TOROIDAL_SURFACE ( 'NONE', #43895, 0.2000000000000000111, 0.1000000000000000056 ) ;
#251995=EDGE_CURVE ( 'NONE', #8175, #98180, #118658, .T. ) ;
#252016=DIRECTION ( 'NONE',  ( 0.000000000000000000, 0.000000000000000000, 1.000000000000000000 ) ) ;
#252079=CARTESIAN_POINT ( 'NONE',  ( 21.05995757104869526, 67.22461075529059826, -90.82820236153315818 ) ) ;
#252095=ORIENTED_EDGE ( 'NONE', *, *, #105274, .T. ) ;
#252098=DIRECTION ( 'NONE',  ( -0.000000000000000000, 0.2605042016806385363, 0.9654727137038795481 ) ) ;
#252121=ORIENTED_EDGE ( 'NONE', *, *, #58639, .T. ) ;
#252123=CARTESIAN_POINT ( 'NONE',  ( -20.64999999999999858, 85.00000000001179501, -79.41707660717668205 ) ) ;
#252129=CARTESIAN_POINT ( 'NONE',  ( -22.49756042579671700, 75.92195366299485215, -114.6729724456266268 ) ) ;
#252163=CARTESIAN_POINT ( 'NONE',  ( 20.93975676684922504, 65.68895814178220860, -64.00265578621380769 ) ) ;
#252165=ORIENTED_EDGE ( 'NONE', *, *, #194834, .F. ) ;
#252190=VERTEX_POINT ( 'NONE', #97182 ) ;
#252198=CARTESIAN_POINT ( 'NONE',  ( 23.14999999999999858, 70.40000000001187175, -90.61784146561124942 ) ) ;
#252205=ORIENTED_EDGE ( 'NONE', *, *, #200979, .T. ) ;
#252219=CARTESIAN_POINT ( 'NONE',  ( -21.05000000000000071, 87.65000000001195701, -103.0231074845242318 ) ) ;
#252253=DIRECTION ( 'NONE',  ( -2.557131231893037478E-16, -0.8660254037844420383, 0.4999999999999941713 ) ) ;
#252264=ADVANCED_FACE ( 'NONE', ( #58079 ), #196322, .F. ) ;
#252315=VERTEX_POINT ( 'NONE', #241871 ) ;
#252333=CARTESIAN_POINT ( 'NONE',  ( -23.15000000000000213, 74.00000000001186606, -89.79848556176222019 ) ) ;
#252336=CARTESIAN_POINT ( 'NONE',  ( -20.64999999999999858, 68.75000000001179501, -81.87310748452436826 ) ) ;
#252338=DIRECTION ( 'NONE',  ( 0.000000000000000000, 0.000000000000000000, 1.000000000000000000 ) ) ;
#252348=AXIS2_PLACEMENT_3D ( 'NONE', #75901, #53765, #36810 ) ;
#252389=ORIENTED_EDGE ( 'NONE', *, *, #116300, .F. ) ;
#252435=EDGE_CURVE ( 'NONE', #20503, #236062, #227140, .T. ) ;
#252475=CIRCLE ( 'NONE', #235921, 0.09999999999999938105 ) ;
#252527=CIRCLE ( 'NONE', #77733, 11.80000000000000426 ) ;
#252544=DIRECTION ( 'NONE',  ( -0.000000000000000000, -6.982962677686266711E-15, 1.000000000000000000 ) ) ;
#252551=CARTESIAN_POINT ( 'NONE',  ( 20.04142135623730070, 64.25000000001176659, -78.37310748452439668 ) ) ;
#252562=DIRECTION ( 'NONE',  ( 0.000000000000000000, 0.000000000000000000, -1.000000000000000000 ) ) ;
#252564=CARTESIAN_POINT ( 'NONE',  ( -20.94999999999999929, 77.73625713160926409, -91.45445515550680682 ) ) ;
#252598=VECTOR ( 'NONE', #3063, 1000.000000000000000 ) ;
#252605=CARTESIAN_POINT ( 'NONE',  ( 18.59999999999999432, 74.73821383144687047, -94.93660852097883662 ) ) ;
#252609=CARTESIAN_POINT ( 'NONE',  ( -20.54999999999999716, 71.65000000001180069, -81.77310748452433131 ) ) ;
#252612=AXIS2_PLACEMENT_3D ( 'NONE', #192288, #153188, #115297 ) ;
#252620=DIRECTION ( 'NONE',  ( 0.000000000000000000, -7.116814260417668513E-15, 1.000000000000000000 ) ) ;
#252623=VERTEX_POINT ( 'NONE', #161926 ) ;
#252628=EDGE_LOOP ( 'NONE', ( #202708, #160512, #10168, #62041 ) ) ;
#252633=DIRECTION ( 'NONE',  ( 0.000000000000000000, 1.000000000000000000, 6.982962677686266711E-15 ) ) ;
#252652=CIRCLE ( 'NONE', #165179, 0.1000000000000055705 ) ;
#252667=EDGE_CURVE ( 'NONE', #94746, #85340, #144890, .T. ) ;
#252671=AXIS2_PLACEMENT_3D ( 'NONE', #42828, #143192, #198036 ) ;
#252672=LINE ( 'NONE', #132762, #192451 ) ;
#252673=ORIENTED_EDGE ( 'NONE', *, *, #237723, .T. ) ;
#252688=CARTESIAN_POINT ( 'NONE',  ( -20.94999999999999929, 77.16412189325286874, -61.60825939895269698 ) ) ;
#252691=CARTESIAN_POINT ( 'NONE',  ( -20.64999999999999858, 68.85000000001180354, -81.87310748452436826 ) ) ;
#252701=EDGE_CURVE ( 'NONE', #80661, #87379, #14957, .T. ) ;
#252703=CARTESIAN_POINT ( 'NONE',  ( 23.24999999999999289, 64.35000000001178933, -81.67310748452439384 ) ) ;
#252731=DIRECTION ( 'NONE',  ( -1.836970198721029934E-16, -1.000000000000000000, -6.982962677686266711E-15 ) ) ;
#252732=ORIENTED_EDGE ( 'NONE', *, *, #257903, .F. ) ;
#252748=VECTOR ( 'NONE', #231836, 1000.000000000000114 ) ;
#252754=ORIENTED_EDGE ( 'NONE', *, *, #69466, .T. ) ;
#252774=LINE ( 'NONE', #135392, #244696 ) ;
#252780=CARTESIAN_POINT ( 'NONE',  ( 23.14999999999999858, 71.00000000001180922, -81.42837350343744163 ) ) ;
#252794=ORIENTED_EDGE ( 'NONE', *, *, #105274, .F. ) ;
#252818=DIRECTION ( 'NONE',  ( 1.000000000000000000, 0.000000000000000000, 0.000000000000000000 ) ) ;
#252837=DIRECTION ( 'NONE',  ( 1.734723475976817507E-14, -6.982962677686266711E-15, 1.000000000000000000 ) ) ;
#252842=CARTESIAN_POINT ( 'NONE',  ( 23.14999999999999503, 64.35000000001178933, -81.67310748452439384 ) ) ;
#252848=DIRECTION ( 'NONE',  ( 1.000000000000000000, 0.000000000000000000, 0.000000000000000000 ) ) ;
#252857=ADVANCED_FACE ( 'NONE', ( #234721 ), #255508, .T. ) ;
#252922=CARTESIAN_POINT ( 'NONE',  ( -22.50000000000000000, 76.00000000001199396, -109.2731074845243171 ) ) ;
#252955=CIRCLE ( 'NONE', #140511, 0.1000000000000028644 ) ;
#252961=CARTESIAN_POINT ( 'NONE',  ( 18.59999999999999432, 74.83729825007388570, -94.92310748452432279 ) ) ;
#253018=VECTOR ( 'NONE', #230100, 1000.000000000000000 ) ;
#253044=EDGE_CURVE ( 'NONE', #22444, #154058, #135912, .T. ) ;
#253048=DIRECTION ( 'NONE',  ( 0.000000000000000000, -0.8660254037844377084, -0.5000000000000016653 ) ) ;
#253109=DIRECTION ( 'NONE',  ( 0.000000000000000000, 0.000000000000000000, 1.000000000000000000 ) ) ;
#253121=CIRCLE ( 'NONE', #165680, 0.2000000000000057288 ) ;
#253126=EDGE_CURVE ( 'NONE', #216303, #167394, #169300, .T. ) ;
#253136=DIRECTION ( 'NONE',  ( 0.000000000000000000, 0.000000000000000000, 1.000000000000000000 ) ) ;
#253140=CYLINDRICAL_SURFACE ( 'NONE', #72563, 2.000000000000001776 ) ;
#253150=CIRCLE ( 'NONE', #170012, 2.000000000000001776 ) ;
#253167=EDGE_LOOP ( 'NONE', ( #173699, #207497, #132152, #32101 ) ) ;
#253180=ADVANCED_FACE ( 'NONE', ( #158577 ), #98524, .T. ) ;
#253193=ORIENTED_EDGE ( 'NONE', *, *, #194030, .T. ) ;
#253198=EDGE_LOOP ( 'NONE', ( #229447, #28330 ) ) ;
#253200=CARTESIAN_POINT ( 'NONE',  ( -20.94999999999999929, 76.00000000001195133, -103.0231074845243171 ) ) ;
#253211=DIRECTION ( 'NONE',  ( -1.000000000000000000, 0.000000000000000000, 0.000000000000000000 ) ) ;
#253217=ORIENTED_EDGE ( 'NONE', *, *, #51991, .T. ) ;
#253310=AXIS2_PLACEMENT_3D ( 'NONE', #251970, #14680, #158062 ) ;
#253322=DIRECTION ( 'NONE',  ( 1.000000000000000000, 0.000000000000000000, 0.000000000000000000 ) ) ;
#253441=DIRECTION ( 'NONE',  ( 0.000000000000000000, 0.000000000000000000, -1.000000000000000000 ) ) ;
#253445=VERTEX_POINT ( 'NONE', #31911 ) ;
#253503=EDGE_CURVE ( 'NONE', #76480, #41443, #48064, .T. ) ;
#253505=CARTESIAN_POINT ( 'NONE',  ( -18.59999999999999787, 66.65000000001187175, -90.67310748452437963 ) ) ;
#253506=LINE ( 'NONE', #170181, #3199 ) ;
#253512=AXIS2_PLACEMENT_3D ( 'NONE', #41918, #197100, #178874 ) ;
#253513=VECTOR ( 'NONE', #84916, 1000.000000000000000 ) ;
#253592=ORIENTED_EDGE ( 'NONE', *, *, #165950, .T. ) ;
#253594=DIRECTION ( 'NONE',  ( 1.000000000000000000, 0.000000000000000000, 0.000000000000000000 ) ) ;
#253617=DIRECTION ( 'NONE',  ( 0.000000000000000000, 6.982962677686267499E-15, -1.000000000000000000 ) ) ;
#253633=CARTESIAN_POINT ( 'NONE',  ( 18.59999999999999432, 74.83729825007388570, -94.92310748452432279 ) ) ;
#253656=CIRCLE ( 'NONE', #57840, 0.1000000000000028644 ) ;
#253690=STYLED_ITEM ( 'NONE', ( #3070 ), #111872 ) ;
#253693=EDGE_CURVE ( 'NONE', #81780, #37627, #26454, .T. ) ;
#253694=VECTOR ( 'NONE', #105331, 1000.000000000000000 ) ;
#253711=CARTESIAN_POINT ( 'NONE',  ( 18.49999999999999645, 77.63717271298224887, -91.44095411905229298 ) ) ;
#253733=EDGE_CURVE ( 'NONE', #97650, #254207, #5566, .T. ) ;
#253754=ORIENTED_EDGE ( 'NONE', *, *, #83079, .T. ) ;
#253761=ORIENTED_EDGE ( 'NONE', *, *, #193734, .F. ) ;
#253770=FACE_OUTER_BOUND ( 'NONE', #54178, .T. ) ;
#253801=VECTOR ( 'NONE', #149731, 1000.000000000000000 ) ;
#253855=DIRECTION ( 'NONE',  ( 1.000000000000000000, 0.000000000000000000, 0.000000000000000000 ) ) ;
#253866=DIRECTION ( 'NONE',  ( -1.000000000000000000, 0.000000000000000000, -0.000000000000000000 ) ) ;
#253903=ORIENTED_EDGE ( 'NONE', *, *, #46841, .F. ) ;
#253910=VERTEX_POINT ( 'NONE', #227203 ) ;
#253931=LINE ( 'NONE', #92299, #252748 ) ;
#253945=ADVANCED_FACE ( 'NONE', ( #139635 ), #19729, .F. ) ;
#253957=DIRECTION ( 'NONE',  ( -0.000000000000000000, -1.000000000000000000, -6.982962677686266711E-15 ) ) ;
#253973=CARTESIAN_POINT ( 'NONE',  ( -23.25000000000000000, 76.00000000001192291, -98.97310748452431994 ) ) ;
#253977=DIRECTION ( 'NONE',  ( -1.000000000000000000, 0.000000000000000000, -0.000000000000000000 ) ) ;
#253998=ORIENTED_EDGE ( 'NONE', *, *, #41956, .F. ) ;
#254012=DIRECTION ( 'NONE',  ( -4.448008912761042820E-16, -1.000000000000000000, -7.116814260417668513E-15 ) ) ;
#254021=DIRECTION ( 'NONE',  ( 1.000000000000000000, 0.000000000000000000, 0.000000000000000000 ) ) ;
#254043=SPHERICAL_SURFACE ( 'NONE', #209285, 0.1000000000000000056 ) ;
#254054=DIRECTION ( 'NONE',  ( 1.000000000000000000, 0.000000000000000000, 0.000000000000000000 ) ) ;
#254068=VECTOR ( 'NONE', #181153, 1000.000000000000114 ) ;
#254086=DIRECTION ( 'NONE',  ( -0.000000000000000000, 0.1298341882519668811, 0.9915357197604899309 ) ) ;
#254110=VERTEX_POINT ( 'NONE', #2703 ) ;
#254119=CIRCLE ( 'NONE', #216717, 0.1000000000000028644 ) ;
#254175=CARTESIAN_POINT ( 'NONE',  ( -20.54999999999999716, 85.50000000001179501, -79.41707660717668205 ) ) ;
#254180=CARTESIAN_POINT ( 'NONE',  ( 21.05193202509564543, 65.27606398031468871, -90.85057288119861596 ) ) ;
#254198=DIRECTION ( 'NONE',  ( 0.000000000000000000, -6.982962677686266711E-15, 1.000000000000000000 ) ) ;
#254207=VERTEX_POINT ( 'NONE', #50805 ) ;
#254259=CARTESIAN_POINT ( 'NONE',  ( -18.52186455168995494, 85.48101848145434190, -95.99809100660965555 ) ) ;
#254381=EDGE_LOOP ( 'NONE', ( #251576, #241270, #79548, #5001, #211813, #135967, #142473, #161540 ) ) ;
#254398=EDGE_CURVE ( 'NONE', #201799, #224021, #155101, .T. ) ;
#254420=EDGE_LOOP ( 'NONE', ( #69062, #174427, #142507, #193500 ) ) ;
#254425=VERTEX_POINT ( 'NONE', #81580 ) ;
#254426=EDGE_CURVE ( 'NONE', #94746, #157975, #109967, .T. ) ;
#254433=VERTEX_POINT ( 'NONE', #184557 ) ;
#254470=CARTESIAN_POINT ( 'NONE',  ( 23.15000000000000213, 87.65000000001202807, -114.7731074845242318 ) ) ;
#254491=DIRECTION ( 'NONE',  ( 0.000000000000000000, -0.2605042016806740079, 0.9654727137038698892 ) ) ;
#254494=DIRECTION ( 'NONE',  ( 0.7071067811865474617, -0.7071067811865474617, -5.142139384388980375E-15 ) ) ;
#254497=CARTESIAN_POINT ( 'NONE',  ( -21.05000000000000071, 87.48912529308779540, -72.62310748452422615 ) ) ;
#254506=EDGE_CURVE ( 'NONE', #20503, #142551, #169280, .T. ) ;
#254508=ORIENTED_EDGE ( 'NONE', *, *, #247110, .F. ) ;
#254515=AXIS2_PLACEMENT_3D ( 'NONE', #2231, #220014, #143020 ) ;
#254520=CARTESIAN_POINT ( 'NONE',  ( 22.41477678272288188, 75.99917613424908325, -114.6726927690397133 ) ) ;
#254543=CARTESIAN_POINT ( 'NONE',  ( 18.49999999999999289, 65.79142135624907439, -78.37310748452438247 ) ) ;
#254546=FACE_OUTER_BOUND ( 'NONE', #203636, .T. ) ;
#254550=CARTESIAN_POINT ( 'NONE',  ( -20.64999999999999858, 85.00000000001188027, -93.62913836187181005 ) ) ;
#254556=CYLINDRICAL_SURFACE ( 'NONE', #205260, 0.1000000000000028644 ) ;
#254583=EDGE_CURVE ( 'NONE', #86349, #204570, #198455, .T. ) ;
#254597=DIRECTION ( 'NONE',  ( 0.000000000000000000, -2.910293365522255334E-14, 1.000000000000000000 ) ) ;
#254620=DIRECTION ( 'NONE',  ( 1.000000000000000000, 0.000000000000000000, 0.000000000000000000 ) ) ;
#254625=DIRECTION ( 'NONE',  ( 1.000000000000000000, 0.000000000000000000, 0.000000000000000000 ) ) ;
#254642=AXIS2_PLACEMENT_3D ( 'NONE', #16286, #76215, #51501 ) ;
#254644=ORIENTED_EDGE ( 'NONE', *, *, #435, .F. ) ;
#254649=ADVANCED_FACE ( 'NONE', ( #98266 ), #176582, .T. ) ;
#254667=FACE_OUTER_BOUND ( 'NONE', #37957, .T. ) ;
#254739=AXIS2_PLACEMENT_3D ( 'NONE', #67417, #83090, #7437 ) ;
#254759=ORIENTED_EDGE ( 'NONE', *, *, #241836, .F. ) ;
#254844=CARTESIAN_POINT ( 'NONE',  ( -23.25000000000000000, 71.65000000001180069, -81.67310748452435121 ) ) ;
#254886=VERTEX_POINT ( 'NONE', #189411 ) ;
#254912=DIRECTION ( 'NONE',  ( 0.000000000000000000, 0.000000000000000000, -1.000000000000000000 ) ) ;
#254915=ADVANCED_FACE ( 'NONE', ( #228545 ), #178873, .T. ) ;
#254945=ORIENTED_EDGE ( 'NONE', *, *, #234903, .F. ) ;
#254957=EDGE_CURVE ( 'NONE', #114552, #197574, #177819, .T. ) ;
#254964=CARTESIAN_POINT ( 'NONE',  ( 18.59999999999999787, 77.25000000001165290, -61.72262673010922640 ) ) ;
#254974=DIRECTION ( 'NONE',  ( 1.000000000000000000, 0.000000000000000000, 0.000000000000000000 ) ) ;
#254994=ORIENTED_EDGE ( 'NONE', *, *, #103197, .T. ) ;
#255019=EDGE_CURVE ( 'NONE', #200905, #192753, #11205, .T. ) ;
#255039=AXIS2_PLACEMENT_3D ( 'NONE', #36451, #152552, #232075 ) ;
#255097=ADVANCED_FACE ( 'NONE', ( #66596 ), #3644, .T. ) ;
#255144=ORIENTED_EDGE ( 'NONE', *, *, #47644, .F. ) ;
#255155=EDGE_CURVE ( 'NONE', #96147, #183416, #242645, .T. ) ;
#255253=AXIS2_PLACEMENT_3D ( 'NONE', #20318, #99801, #239350 ) ;
#255258=ORIENTED_EDGE ( 'NONE', *, *, #63486, .F. ) ;
#255267=TOROIDAL_SURFACE ( 'NONE', #192795, 0.2000000000000000111, 0.1000000000000000056 ) ;
#255268=CARTESIAN_POINT ( 'NONE',  ( -20.00857864376270001, 66.65000000001187175, -90.67310748452437963 ) ) ;
#255302=AXIS2_PLACEMENT_3D ( 'NONE', #133501, #98186, #197313 ) ;
#255316=CYLINDRICAL_SURFACE ( 'NONE', #51085, 0.1000000000000028644 ) ;
#255325=VERTEX_POINT ( 'NONE', #212537 ) ;
#255330=EDGE_CURVE ( 'NONE', #16439, #152113, #127857, .T. ) ;
#255366=CARTESIAN_POINT ( 'NONE',  ( 23.14999999999999858, 70.50000000001185185, -90.61784146561124942 ) ) ;
#255382=ORIENTED_EDGE ( 'NONE', *, *, #242512, .T. ) ;
#255461=DIRECTION ( 'NONE',  ( 2.710505431213777355E-16, 1.000000000000000000, 6.982962677686266711E-15 ) ) ;
#255469=DIRECTION ( 'NONE',  ( 0.000000000000000000, 6.982962677686266711E-15, -1.000000000000000000 ) ) ;
#255481=CIRCLE ( 'NONE', #143076, 0.1000000000000028644 ) ;
#255502=DIRECTION ( 'NONE',  ( -0.7071067811865127117, -0.7071067811865821007, 0.000000000000000000 ) ) ;
#255508=SPHERICAL_SURFACE ( 'NONE', #143931, 0.1000000000000000056 ) ;
#255511=CARTESIAN_POINT ( 'NONE',  ( 21.05000000000000071, 76.00000000001170974, -69.52310748452431710 ) ) ;
#255515=ORIENTED_EDGE ( 'NONE', *, *, #8496, .T. ) ;
#255524=CARTESIAN_POINT ( 'NONE',  ( 18.55857864376268296, 65.63284271248636514, -78.27310748452438816 ) ) ;
#255526=DIRECTION ( 'NONE',  ( 0.000000000000000000, -1.411300455031978166E-14, 1.000000000000000000 ) ) ;
#255531=ORIENTED_EDGE ( 'NONE', *, *, #23806, .F. ) ;
#255534=DIRECTION ( 'NONE',  ( -0.7071067811865475727, 0.7071067811865475727, 4.937700262164531476E-15 ) ) ;
#255560=FACE_OUTER_BOUND ( 'NONE', #92903, .T. ) ;
#255591=CIRCLE ( 'NONE', #226388, 4.150000000000001243 ) ;
#255605=AXIS2_PLACEMENT_3D ( 'NONE', #218400, #256192, #21525 ) ;
#255608=VECTOR ( 'NONE', #223568, 1000.000000000000000 ) ;
#255663=VERTEX_POINT ( 'NONE', #167982 ) ;
#255730=FACE_OUTER_BOUND ( 'NONE', #157577, .T. ) ;
#255745=AXIS2_PLACEMENT_3D ( 'NONE', #91260, #14312, #190372 ) ;
#255753=ORIENTED_EDGE ( 'NONE', *, *, #91534, .F. ) ;
#255755=CARTESIAN_POINT ( 'NONE',  ( 20.04142135623730070, 64.35000000001180354, -81.67310748452439384 ) ) ;
#255765=CARTESIAN_POINT ( 'NONE',  ( -22.57320508075687115, 64.25000000001195133, -103.0231074845244024 ) ) ;
#255768=ORIENTED_EDGE ( 'NONE', *, *, #19474, .F. ) ;
#255771=ORIENTED_EDGE ( 'NONE', *, *, #168600, .F. ) ;
#255789=CARTESIAN_POINT ( 'NONE',  ( 22.49436431346199683, 75.93309647028976883, -114.6730584321777684 ) ) ;
#255827=LINE ( 'NONE', #57656, #245178 ) ;
#255841=VERTEX_POINT ( 'NONE', #38712 ) ;
#255844=CARTESIAN_POINT ( 'NONE',  ( -23.25000000000000000, 64.35000000001187459, -90.87310748452438247 ) ) ;
#255850=DIRECTION ( 'NONE',  ( 1.000000000000000000, 0.000000000000000000, 0.000000000000000000 ) ) ;
#255882=CARTESIAN_POINT ( 'NONE',  ( 21.14999999999999858, 67.21339244341174890, -90.77310748452437394 ) ) ;
#255917=DIRECTION ( 'NONE',  ( 0.000000000000000000, -0.3738317757008748909, -0.9274965247785733613 ) ) ;
#255944=FACE_OUTER_BOUND ( 'NONE', #173275, .T. ) ;
#255946=CARTESIAN_POINT ( 'NONE',  ( 22.39999999999999147, 68.20922040163857503, -103.0231074845243597 ) ) ;
#255964=CARTESIAN_POINT ( 'NONE',  ( -20.00857864376270001, 66.65000000001187175, -90.77310748452437394 ) ) ;
#255975=DIRECTION ( 'NONE',  ( 0.000000000000000000, 0.4999999999999689138, -0.8660254037844565822 ) ) ;
#255980=DIRECTION ( 'NONE',  ( -1.000000000000000000, 2.952720810173289112E-16, 2.061873921506763405E-30 ) ) ;
#255994=AXIS2_PLACEMENT_3D ( 'NONE', #210298, #31681, #186889 ) ;
#256008=ADVANCED_FACE ( 'NONE', ( #185912 ), #146755, .F. ) ;
#256013=TOROIDAL_SURFACE ( 'NONE', #6451, 12.77499999999999858, 0.1000000000000000056 ) ;
#256021=LINE ( 'NONE', #157002, #163976 ) ;
#256054=DIRECTION ( 'NONE',  ( 1.000000000000000000, -2.952720810173289112E-16, -2.061873921506763405E-30 ) ) ;
#256057=ORIENTED_EDGE ( 'NONE', *, *, #27910, .F. ) ;
#256072=ORIENTED_EDGE ( 'NONE', *, *, #100825, .F. ) ;
#256113=CARTESIAN_POINT ( 'NONE',  ( 20.85000000000000142, 87.65000000001172964, -72.42310748452422331 ) ) ;
#256125=CARTESIAN_POINT ( 'NONE',  ( 21.14999999999999858, 64.25000000001185185, -90.87310748452438247 ) ) ;
#256131=CARTESIAN_POINT ( 'NONE',  ( -20.00857864376270001, 66.85000000001186038, -90.67310748452436542 ) ) ;
#256174=CARTESIAN_POINT ( 'NONE',  ( -22.50000000000000000, 76.00000000001203659, -114.6726782920691221 ) ) ;
#256189=FACE_OUTER_BOUND ( 'NONE', #47188, .T. ) ;
#256192=DIRECTION ( 'NONE',  ( 0.000000000000000000, 1.000000000000000000, 6.982962677686266711E-15 ) ) ;
#256206=CYLINDRICAL_SURFACE ( 'NONE', #212934, 0.1000000000000028644 ) ;
#256207=CARTESIAN_POINT ( 'NONE',  ( -18.50000000000000000, 85.41908450282495835, -62.69319967749883915 ) ) ;
#256210=FACE_OUTER_BOUND ( 'NONE', #111411, .T. ) ;
#256212=DIRECTION ( 'NONE',  ( 0.000000000000000000, 0.9908441862701605762, 0.1350103645451835310 ) ) ;
#256249=PLANE ( 'NONE',  #218779 ) ;
#256265=DIRECTION ( 'NONE',  ( -0.000000000000000000, 6.982962677686266711E-15, -1.000000000000000000 ) ) ;
#256274=DIRECTION ( 'NONE',  ( 0.000000000000000000, 6.997203936713167125E-15, -1.000000000000000000 ) ) ;
#256283=AXIS2_PLACEMENT_3D ( 'NONE', #186798, #86360, #107239 ) ;
#256285=CARTESIAN_POINT ( 'NONE',  ( -23.15000000000000213, 74.00000000001180922, -82.14772940728641970 ) ) ;
#256308=EDGE_CURVE ( 'NONE', #67031, #215026, #192866, .T. ) ;
#256320=DIRECTION ( 'NONE',  ( 1.000000000000000000, 0.000000000000000000, 0.000000000000000000 ) ) ;
#256355=CARTESIAN_POINT ( 'NONE',  ( 20.12500000000000000, 66.25000000001185185, -81.87310748452438247 ) ) ;
#256375=DIRECTION ( 'NONE',  ( 0.000000000000000000, 0.000000000000000000, 1.000000000000000000 ) ) ;
#256380=DIRECTION ( 'NONE',  ( -4.408576920032448588E-17, -0.1350103645451807832, -0.9908441862701610203 ) ) ;
#256417=ORIENTED_EDGE ( 'NONE', *, *, #112404, .F. ) ;
#256470=ORIENTED_EDGE ( 'NONE', *, *, #248577, .F. ) ;
#256502=CARTESIAN_POINT ( 'NONE',  ( 21.05000000000000071, 71.00000000001180922, -81.52837350343745015 ) ) ;
#256506=CIRCLE ( 'NONE', #89973, 0.1000000000000014488 ) ;
#256517=ADVANCED_FACE ( 'NONE', ( #19352 ), #2332, .F. ) ;
#256536=CARTESIAN_POINT ( 'NONE',  ( 21.09096482362058467, 69.63645563460745791, -103.0625557632984339 ) ) ;
#256559=ORIENTED_EDGE ( 'NONE', *, *, #188614, .T. ) ;
#256560=DIRECTION ( 'NONE',  ( 4.239556034732057360E-17, 0.1298341882519953860, 0.9915357197604862671 ) ) ;
#256577=VERTEX_POINT ( 'NONE', #7814 ) ;
#256583=AXIS2_PLACEMENT_3D ( 'NONE', #134280, #170913, #169624 ) ;
#256612=ORIENTED_EDGE ( 'NONE', *, *, #236306, .T. ) ;
#256618=CIRCLE ( 'NONE', #144231, 11.80000000000000426 ) ;
#256635=CARTESIAN_POINT ( 'NONE',  ( 21.05000000000000071, 65.37127968600755423, -95.35819391543677170 ) ) ;
#256652=CARTESIAN_POINT ( 'NONE',  ( -18.50000000000000000, 85.50000000001203659, -114.7731074845242460 ) ) ;
#256668=VERTEX_POINT ( 'NONE', #38930 ) ;
#256716=VECTOR ( 'NONE', #160805, 1000.000000000000000 ) ;
#256726=AXIS2_PLACEMENT_3D ( 'NONE', #115321, #93191, #172782 ) ;
#256754=CARTESIAN_POINT ( 'NONE',  ( -21.44999999999999929, 68.85000000001186038, -90.77310748452435973 ) ) ;
#256774=CARTESIAN_POINT ( 'NONE',  ( 18.43709777086140278, 85.68240343348807642, -62.86626410711147628 ) ) ;
#256787=CARTESIAN_POINT ( 'NONE',  ( -18.51555513499573635, 85.35265705451607232, -95.82793758882698398 ) ) ;
#256796=ORIENTED_EDGE ( 'NONE', *, *, #146236, .T. ) ;
#256800=DIRECTION ( 'NONE',  ( 0.000000000000000000, -5.551115123125777653E-14, 1.000000000000000000 ) ) ;
#256838=CIRCLE ( 'NONE', #36350, 3.900000000000000799 ) ;
#256865=DIRECTION ( 'NONE',  ( 0.000000000000000000, 0.000000000000000000, 1.000000000000000000 ) ) ;
#256895=DIRECTION ( 'NONE',  ( 1.000000000000000000, -3.265361837132813093E-16, -2.280189983783949500E-30 ) ) ;
#256898=VERTEX_POINT ( 'NONE', #199281 ) ;
#256905=AXIS2_PLACEMENT_3D ( 'NONE', #143493, #44415, #206045 ) ;
#256937=EDGE_CURVE ( 'NONE', #76326, #96909, #51752, .T. ) ;
#256946=CARTESIAN_POINT ( 'NONE',  ( 22.01447462590973458, 75.90096299995246909, -110.2869076857542154 ) ) ;
#256952=ORIENTED_EDGE ( 'NONE', *, *, #152722, .T. ) ;
#256971=CARTESIAN_POINT ( 'NONE',  ( 18.43565242384933711, 85.51932773110434027, -96.05013110796494402 ) ) ;
#256998=ORIENTED_EDGE ( 'NONE', *, *, #163797, .F. ) ;
#257007=AXIS2_PLACEMENT_3D ( 'NONE', #247166, #108942, #142919 ) ;
#257062=CARTESIAN_POINT ( 'NONE',  ( 21.05000000000000071, 84.73084112150721126, -93.42503276553991043 ) ) ;
#257085=CARTESIAN_POINT ( 'NONE',  ( -21.53699400384203599, 75.99999999999828049, -109.8108192777691414 ) ) ;
#257103=CARTESIAN_POINT ( 'NONE',  ( -23.25000000000000000, 77.83585931145526615, -58.01866831572577610 ) ) ;
#257116=CARTESIAN_POINT ( 'NONE',  ( 18.49999999999998934, 69.45000000001181206, -81.77310748452434552 ) ) ;
#257158=VECTOR ( 'NONE', #6609, 1000.000000000000000 ) ;
#257170=CARTESIAN_POINT ( 'NONE',  ( -18.59999999999999787, 77.83585931145526615, -58.01866831572577610 ) ) ;
#257207=CARTESIAN_POINT ( 'NONE',  ( -22.50000000000000000, 76.00000000001195133, -103.0231074845243171 ) ) ;
#257215=CARTESIAN_POINT ( 'NONE',  ( 22.48970261584622321, 64.35000000001195986, -103.0784769727417967 ) ) ;
#257239=ADVANCED_FACE ( 'NONE', ( #43745 ), #202812, .T. ) ;
#257247=ORIENTED_EDGE ( 'NONE', *, *, #90753, .T. ) ;
#257295=AXIS2_PLACEMENT_3D ( 'NONE', #205521, #26929, #106407 ) ;
#257296=VECTOR ( 'NONE', #195265, 1000.000000000000000 ) ;
#257307=CARTESIAN_POINT ( 'NONE',  ( -21.55000000000000071, 68.65000000001187175, -90.77310748452435973 ) ) ;
#257344=DIRECTION ( 'NONE',  ( 0.000000000000000000, 0.000000000000000000, 1.000000000000000000 ) ) ;
#257348=AXIS2_PLACEMENT_3D ( 'NONE', #85030, #125480, #108482 ) ;
#257376=EDGE_CURVE ( 'NONE', #186482, #64319, #147984, .T. ) ;
#257394=LINE ( 'NONE', #115373, #251068 ) ;
#257403=DIRECTION ( 'NONE',  ( -1.000000000000000000, 0.000000000000000000, 0.000000000000000000 ) ) ;
#257416=ORIENTED_EDGE ( 'NONE', *, *, #204189, .T. ) ;
#257423=CARTESIAN_POINT ( 'NONE',  ( 20.94999999999999929, 85.40000000001178648, -79.41707660717668205 ) ) ;
#257430=CARTESIAN_POINT ( 'NONE',  ( -23.15000000000000213, 71.65000000001180069, -81.67310748452435121 ) ) ;
#257463=CARTESIAN_POINT ( 'NONE',  ( 21.05000000000000071, 71.00000000001180922, -81.92837350343744163 ) ) ;
#257491=ORIENTED_EDGE ( 'NONE', *, *, #43565, .T. ) ;
#257503=DIRECTION ( 'NONE',  ( 1.000000000000000000, 0.000000000000000000, 0.000000000000000000 ) ) ;
#257583=ORIENTED_EDGE ( 'NONE', *, *, #169635, .T. ) ;
#257591=CARTESIAN_POINT ( 'NONE',  ( 20.95512820512820440, 67.12384868372377866, -94.46447848938342418 ) ) ;
#257596=ORIENTED_EDGE ( 'NONE', *, *, #209772, .F. ) ;
#257605=AXIS2_PLACEMENT_3D ( 'NONE', #12473, #55391, #151995 ) ;
#257622=EDGE_CURVE ( 'NONE', #22332, #53093, #223027, .T. ) ;
#257625=EDGE_CURVE ( 'NONE', #191619, #28459, #176886, .T. ) ;
#257651=CARTESIAN_POINT ( 'NONE',  ( 20.94999999999999574, 65.37642973952908676, -95.53116228129383103 ) ) ;
#257705=TOROIDAL_SURFACE ( 'NONE', #249402, 0.6000000000000017542, 0.1000000000000000056 ) ;
#257716=DIRECTION ( 'NONE',  ( -2.978066053179066272E-16, -1.000000000000000000, -7.147358527629759053E-15 ) ) ;
#257730=ORIENTED_EDGE ( 'NONE', *, *, #157365, .T. ) ;
#257737=AXIS2_PLACEMENT_3D ( 'NONE', #44500, #238836, #61485 ) ;
#257828=DIRECTION ( 'NONE',  ( 0.000000000000000000, 0.000000000000000000, 1.000000000000000000 ) ) ;
#257853=DIRECTION ( 'NONE',  ( 1.000000000000000000, 0.000000000000000000, 0.000000000000000000 ) ) ;
#257863=CARTESIAN_POINT ( 'NONE',  ( 23.14999999999999858, 74.00000000001170974, -69.52310748452431710 ) ) ;
#257903=EDGE_CURVE ( 'NONE', #157610, #242842, #218715, .T. ) ;
#257994=DIRECTION ( 'NONE',  ( 1.000000000000000000, 0.000000000000000000, 0.000000000000000000 ) ) ;
#258060=CYLINDRICAL_SURFACE ( 'NONE', #140995, 0.1000000000000028644 ) ;
#258077=ORIENTED_EDGE ( 'NONE', *, *, #179060, .F. ) ;
ENDSEC;
END-ISO-10303-21;
